ISO-10303-21;
HEADER;
/* Generated by software containing ST-Developer
 * from STEP Tools, Inc. (www.steptools.com) 
 */

FILE_DESCRIPTION(
/* description */ (''),
/* implementation_level */ '2;1');

FILE_NAME(
/* name */ '14_Cap_Screw_ISO_4762_M12x60.step',
/* time_stamp */ '2026-10-26T07:49:00-07:00',
/* author */ (''),
/* organization */ (''),
/* preprocessor_version */ 'ST-DEVELOPER v20.2',
/* originating_system */ 'Autodesk Translation Framework v15.15.0.0',
/* authorisation */ '');

FILE_SCHEMA (('AUTOMOTIVE_DESIGN { 1 0 10303 214 3 1 1 }'));
ENDSEC;

DATA;
#10=MECHANICAL_DESIGN_GEOMETRIC_PRESENTATION_REPRESENTATION('',(#190),#38507);
#160=SHAPE_REPRESENTATION_RELATIONSHIP('SRR','None',#38588,#175);
#175=ADVANCED_BREP_SHAPE_REPRESENTATION('',(#205),#38505);
#190=STYLED_ITEM('',(#38727),#205);
#205=MANIFOLD_SOLID_BREP('Body1',#15084);
#252=B_SPLINE_SURFACE_WITH_KNOTS('',3,3,((#31387,#31388,#31389,#31390,#31391,
#31392,#31393,#31394,#31395,#31396,#31397,#31398,#31399,#31400,#31401,#31402,
#31403,#31404,#31405,#31406,#31407,#31408,#31409,#31410,#31411,#31412,#31413,
#31414,#31415,#31416,#31417,#31418,#31419,#31420,#31421,#31422,#31423,#31424,
#31425,#31426,#31427,#31428,#31429,#31430,#31431,#31432,#31433,#31434,#31435,
#31436,#31437,#31438,#31439,#31440,#31441,#31442,#31443,#31444,#31445,#31446,
#31447,#31448,#31449,#31450,#31451,#31452,#31453,#31454,#31455,#31456,#31457,
#31458,#31459,#31460,#31461,#31462,#31463,#31464,#31465,#31466,#31467,#31468,
#31469,#31470,#31471,#31472,#31473,#31474,#31475,#31476,#31477,#31478,#31479,
#31480,#31481,#31482,#31483,#31484,#31485,#31486,#31487,#31488,#31489,#31490,
#31491,#31492,#31493,#31494,#31495,#31496,#31497,#31498,#31499,#31500,#31501,
#31502,#31503,#31504,#31505,#31506,#31507,#31508,#31509,#31510,#31511,#31512,
#31513,#31514,#31515,#31516,#31517,#31518,#31519,#31520,#31521,#31522,#31523,
#31524,#31525,#31526,#31527,#31528,#31529,#31530,#31531,#31532,#31533,#31534,
#31535,#31536,#31537,#31538,#31539,#31540,#31541,#31542,#31543,#31544,#31545,
#31546,#31547,#31548,#31549,#31550,#31551,#31552,#31553,#31554,#31555,#31556,
#31557,#31558,#31559,#31560,#31561,#31562,#31563,#31564,#31565,#31566,#31567,
#31568,#31569,#31570,#31571,#31572,#31573,#31574,#31575,#31576,#31577,#31578,
#31579,#31580,#31581,#31582,#31583,#31584,#31585,#31586,#31587,#31588,#31589,
#31590,#31591,#31592,#31593,#31594,#31595,#31596,#31597,#31598,#31599,#31600,
#31601,#31602,#31603,#31604,#31605,#31606,#31607,#31608,#31609,#31610,#31611,
#31612,#31613,#31614,#31615,#31616,#31617,#31618,#31619,#31620,#31621,#31622,
#31623,#31624,#31625,#31626,#31627,#31628,#31629,#31630,#31631,#31632,#31633,
#31634,#31635,#31636,#31637,#31638,#31639,#31640,#31641,#31642,#31643,#31644,
#31645,#31646,#31647,#31648,#31649,#31650,#31651,#31652,#31653,#31654,#31655,
#31656,#31657,#31658,#31659,#31660,#31661,#31662,#31663,#31664,#31665,#31666,
#31667,#31668,#31669,#31670,#31671,#31672,#31673,#31674,#31675,#31676,#31677,
#31678,#31679,#31680,#31681,#31682,#31683,#31684,#31685,#31686,#31687,#31688,
#31689,#31690,#31691,#31692,#31693,#31694,#31695,#31696,#31697,#31698,#31699,
#31700,#31701,#31702,#31703,#31704,#31705,#31706,#31707,#31708,#31709,#31710,
#31711,#31712,#31713,#31714,#31715,#31716,#31717,#31718,#31719,#31720,#31721,
#31722,#31723,#31724,#31725,#31726,#31727,#31728,#31729,#31730,#31731,#31732,
#31733,#31734,#31735,#31736,#31737,#31738,#31739,#31740,#31741,#31742,#31743,
#31744,#31745,#31746,#31747,#31748,#31749,#31750,#31751,#31752,#31753,#31754,
#31755,#31756,#31757,#31758,#31759,#31760,#31761,#31762,#31763,#31764,#31765,
#31766,#31767,#31768,#31769,#31770,#31771,#31772,#31773,#31774,#31775,#31776,
#31777,#31778,#31779,#31780,#31781,#31782,#31783,#31784,#31785,#31786,#31787,
#31788,#31789,#31790,#31791,#31792,#31793,#31794,#31795,#31796,#31797,#31798,
#31799,#31800,#31801,#31802,#31803,#31804,#31805,#31806,#31807,#31808,#31809,
#31810,#31811,#31812,#31813,#31814,#31815,#31816,#31817,#31818,#31819,#31820,
#31821),(#31822,#31823,#31824,#31825,#31826,#31827,#31828,#31829,#31830,
#31831,#31832,#31833,#31834,#31835,#31836,#31837,#31838,#31839,#31840,#31841,
#31842,#31843,#31844,#31845,#31846,#31847,#31848,#31849,#31850,#31851,#31852,
#31853,#31854,#31855,#31856,#31857,#31858,#31859,#31860,#31861,#31862,#31863,
#31864,#31865,#31866,#31867,#31868,#31869,#31870,#31871,#31872,#31873,#31874,
#31875,#31876,#31877,#31878,#31879,#31880,#31881,#31882,#31883,#31884,#31885,
#31886,#31887,#31888,#31889,#31890,#31891,#31892,#31893,#31894,#31895,#31896,
#31897,#31898,#31899,#31900,#31901,#31902,#31903,#31904,#31905,#31906,#31907,
#31908,#31909,#31910,#31911,#31912,#31913,#31914,#31915,#31916,#31917,#31918,
#31919,#31920,#31921,#31922,#31923,#31924,#31925,#31926,#31927,#31928,#31929,
#31930,#31931,#31932,#31933,#31934,#31935,#31936,#31937,#31938,#31939,#31940,
#31941,#31942,#31943,#31944,#31945,#31946,#31947,#31948,#31949,#31950,#31951,
#31952,#31953,#31954,#31955,#31956,#31957,#31958,#31959,#31960,#31961,#31962,
#31963,#31964,#31965,#31966,#31967,#31968,#31969,#31970,#31971,#31972,#31973,
#31974,#31975,#31976,#31977,#31978,#31979,#31980,#31981,#31982,#31983,#31984,
#31985,#31986,#31987,#31988,#31989,#31990,#31991,#31992,#31993,#31994,#31995,
#31996,#31997,#31998,#31999,#32000,#32001,#32002,#32003,#32004,#32005,#32006,
#32007,#32008,#32009,#32010,#32011,#32012,#32013,#32014,#32015,#32016,#32017,
#32018,#32019,#32020,#32021,#32022,#32023,#32024,#32025,#32026,#32027,#32028,
#32029,#32030,#32031,#32032,#32033,#32034,#32035,#32036,#32037,#32038,#32039,
#32040,#32041,#32042,#32043,#32044,#32045,#32046,#32047,#32048,#32049,#32050,
#32051,#32052,#32053,#32054,#32055,#32056,#32057,#32058,#32059,#32060,#32061,
#32062,#32063,#32064,#32065,#32066,#32067,#32068,#32069,#32070,#32071,#32072,
#32073,#32074,#32075,#32076,#32077,#32078,#32079,#32080,#32081,#32082,#32083,
#32084,#32085,#32086,#32087,#32088,#32089,#32090,#32091,#32092,#32093,#32094,
#32095,#32096,#32097,#32098,#32099,#32100,#32101,#32102,#32103,#32104,#32105,
#32106,#32107,#32108,#32109,#32110,#32111,#32112,#32113,#32114,#32115,#32116,
#32117,#32118,#32119,#32120,#32121,#32122,#32123,#32124,#32125,#32126,#32127,
#32128,#32129,#32130,#32131,#32132,#32133,#32134,#32135,#32136,#32137,#32138,
#32139,#32140,#32141,#32142,#32143,#32144,#32145,#32146,#32147,#32148,#32149,
#32150,#32151,#32152,#32153,#32154,#32155,#32156,#32157,#32158,#32159,#32160,
#32161,#32162,#32163,#32164,#32165,#32166,#32167,#32168,#32169,#32170,#32171,
#32172,#32173,#32174,#32175,#32176,#32177,#32178,#32179,#32180,#32181,#32182,
#32183,#32184,#32185,#32186,#32187,#32188,#32189,#32190,#32191,#32192,#32193,
#32194,#32195,#32196,#32197,#32198,#32199,#32200,#32201,#32202,#32203,#32204,
#32205,#32206,#32207,#32208,#32209,#32210,#32211,#32212,#32213,#32214,#32215,
#32216,#32217,#32218,#32219,#32220,#32221,#32222,#32223,#32224,#32225,#32226,
#32227,#32228,#32229,#32230,#32231,#32232,#32233,#32234,#32235,#32236,#32237,
#32238,#32239,#32240,#32241,#32242,#32243,#32244,#32245,#32246,#32247,#32248,
#32249,#32250,#32251,#32252,#32253,#32254,#32255,#32256),(#32257,#32258,
#32259,#32260,#32261,#32262,#32263,#32264,#32265,#32266,#32267,#32268,#32269,
#32270,#32271,#32272,#32273,#32274,#32275,#32276,#32277,#32278,#32279,#32280,
#32281,#32282,#32283,#32284,#32285,#32286,#32287,#32288,#32289,#32290,#32291,
#32292,#32293,#32294,#32295,#32296,#32297,#32298,#32299,#32300,#32301,#32302,
#32303,#32304,#32305,#32306,#32307,#32308,#32309,#32310,#32311,#32312,#32313,
#32314,#32315,#32316,#32317,#32318,#32319,#32320,#32321,#32322,#32323,#32324,
#32325,#32326,#32327,#32328,#32329,#32330,#32331,#32332,#32333,#32334,#32335,
#32336,#32337,#32338,#32339,#32340,#32341,#32342,#32343,#32344,#32345,#32346,
#32347,#32348,#32349,#32350,#32351,#32352,#32353,#32354,#32355,#32356,#32357,
#32358,#32359,#32360,#32361,#32362,#32363,#32364,#32365,#32366,#32367,#32368,
#32369,#32370,#32371,#32372,#32373,#32374,#32375,#32376,#32377,#32378,#32379,
#32380,#32381,#32382,#32383,#32384,#32385,#32386,#32387,#32388,#32389,#32390,
#32391,#32392,#32393,#32394,#32395,#32396,#32397,#32398,#32399,#32400,#32401,
#32402,#32403,#32404,#32405,#32406,#32407,#32408,#32409,#32410,#32411,#32412,
#32413,#32414,#32415,#32416,#32417,#32418,#32419,#32420,#32421,#32422,#32423,
#32424,#32425,#32426,#32427,#32428,#32429,#32430,#32431,#32432,#32433,#32434,
#32435,#32436,#32437,#32438,#32439,#32440,#32441,#32442,#32443,#32444,#32445,
#32446,#32447,#32448,#32449,#32450,#32451,#32452,#32453,#32454,#32455,#32456,
#32457,#32458,#32459,#32460,#32461,#32462,#32463,#32464,#32465,#32466,#32467,
#32468,#32469,#32470,#32471,#32472,#32473,#32474,#32475,#32476,#32477,#32478,
#32479,#32480,#32481,#32482,#32483,#32484,#32485,#32486,#32487,#32488,#32489,
#32490,#32491,#32492,#32493,#32494,#32495,#32496,#32497,#32498,#32499,#32500,
#32501,#32502,#32503,#32504,#32505,#32506,#32507,#32508,#32509,#32510,#32511,
#32512,#32513,#32514,#32515,#32516,#32517,#32518,#32519,#32520,#32521,#32522,
#32523,#32524,#32525,#32526,#32527,#32528,#32529,#32530,#32531,#32532,#32533,
#32534,#32535,#32536,#32537,#32538,#32539,#32540,#32541,#32542,#32543,#32544,
#32545,#32546,#32547,#32548,#32549,#32550,#32551,#32552,#32553,#32554,#32555,
#32556,#32557,#32558,#32559,#32560,#32561,#32562,#32563,#32564,#32565,#32566,
#32567,#32568,#32569,#32570,#32571,#32572,#32573,#32574,#32575,#32576,#32577,
#32578,#32579,#32580,#32581,#32582,#32583,#32584,#32585,#32586,#32587,#32588,
#32589,#32590,#32591,#32592,#32593,#32594,#32595,#32596,#32597,#32598,#32599,
#32600,#32601,#32602,#32603,#32604,#32605,#32606,#32607,#32608,#32609,#32610,
#32611,#32612,#32613,#32614,#32615,#32616,#32617,#32618,#32619,#32620,#32621,
#32622,#32623,#32624,#32625,#32626,#32627,#32628,#32629,#32630,#32631,#32632,
#32633,#32634,#32635,#32636,#32637,#32638,#32639,#32640,#32641,#32642,#32643,
#32644,#32645,#32646,#32647,#32648,#32649,#32650,#32651,#32652,#32653,#32654,
#32655,#32656,#32657,#32658,#32659,#32660,#32661,#32662,#32663,#32664,#32665,
#32666,#32667,#32668,#32669,#32670,#32671,#32672,#32673,#32674,#32675,#32676,
#32677,#32678,#32679,#32680,#32681,#32682,#32683,#32684,#32685,#32686,#32687,
#32688,#32689,#32690,#32691),(#32692,#32693,#32694,#32695,#32696,#32697,
#32698,#32699,#32700,#32701,#32702,#32703,#32704,#32705,#32706,#32707,#32708,
#32709,#32710,#32711,#32712,#32713,#32714,#32715,#32716,#32717,#32718,#32719,
#32720,#32721,#32722,#32723,#32724,#32725,#32726,#32727,#32728,#32729,#32730,
#32731,#32732,#32733,#32734,#32735,#32736,#32737,#32738,#32739,#32740,#32741,
#32742,#32743,#32744,#32745,#32746,#32747,#32748,#32749,#32750,#32751,#32752,
#32753,#32754,#32755,#32756,#32757,#32758,#32759,#32760,#32761,#32762,#32763,
#32764,#32765,#32766,#32767,#32768,#32769,#32770,#32771,#32772,#32773,#32774,
#32775,#32776,#32777,#32778,#32779,#32780,#32781,#32782,#32783,#32784,#32785,
#32786,#32787,#32788,#32789,#32790,#32791,#32792,#32793,#32794,#32795,#32796,
#32797,#32798,#32799,#32800,#32801,#32802,#32803,#32804,#32805,#32806,#32807,
#32808,#32809,#32810,#32811,#32812,#32813,#32814,#32815,#32816,#32817,#32818,
#32819,#32820,#32821,#32822,#32823,#32824,#32825,#32826,#32827,#32828,#32829,
#32830,#32831,#32832,#32833,#32834,#32835,#32836,#32837,#32838,#32839,#32840,
#32841,#32842,#32843,#32844,#32845,#32846,#32847,#32848,#32849,#32850,#32851,
#32852,#32853,#32854,#32855,#32856,#32857,#32858,#32859,#32860,#32861,#32862,
#32863,#32864,#32865,#32866,#32867,#32868,#32869,#32870,#32871,#32872,#32873,
#32874,#32875,#32876,#32877,#32878,#32879,#32880,#32881,#32882,#32883,#32884,
#32885,#32886,#32887,#32888,#32889,#32890,#32891,#32892,#32893,#32894,#32895,
#32896,#32897,#32898,#32899,#32900,#32901,#32902,#32903,#32904,#32905,#32906,
#32907,#32908,#32909,#32910,#32911,#32912,#32913,#32914,#32915,#32916,#32917,
#32918,#32919,#32920,#32921,#32922,#32923,#32924,#32925,#32926,#32927,#32928,
#32929,#32930,#32931,#32932,#32933,#32934,#32935,#32936,#32937,#32938,#32939,
#32940,#32941,#32942,#32943,#32944,#32945,#32946,#32947,#32948,#32949,#32950,
#32951,#32952,#32953,#32954,#32955,#32956,#32957,#32958,#32959,#32960,#32961,
#32962,#32963,#32964,#32965,#32966,#32967,#32968,#32969,#32970,#32971,#32972,
#32973,#32974,#32975,#32976,#32977,#32978,#32979,#32980,#32981,#32982,#32983,
#32984,#32985,#32986,#32987,#32988,#32989,#32990,#32991,#32992,#32993,#32994,
#32995,#32996,#32997,#32998,#32999,#33000,#33001,#33002,#33003,#33004,#33005,
#33006,#33007,#33008,#33009,#33010,#33011,#33012,#33013,#33014,#33015,#33016,
#33017,#33018,#33019,#33020,#33021,#33022,#33023,#33024,#33025,#33026,#33027,
#33028,#33029,#33030,#33031,#33032,#33033,#33034,#33035,#33036,#33037,#33038,
#33039,#33040,#33041,#33042,#33043,#33044,#33045,#33046,#33047,#33048,#33049,
#33050,#33051,#33052,#33053,#33054,#33055,#33056,#33057,#33058,#33059,#33060,
#33061,#33062,#33063,#33064,#33065,#33066,#33067,#33068,#33069,#33070,#33071,
#33072,#33073,#33074,#33075,#33076,#33077,#33078,#33079,#33080,#33081,#33082,
#33083,#33084,#33085,#33086,#33087,#33088,#33089,#33090,#33091,#33092,#33093,
#33094,#33095,#33096,#33097,#33098,#33099,#33100,#33101,#33102,#33103,#33104,
#33105,#33106,#33107,#33108,#33109,#33110,#33111,#33112,#33113,#33114,#33115,
#33116,#33117,#33118,#33119,#33120,#33121,#33122,#33123,#33124,#33125,#33126)),
 .UNSPECIFIED.,.F.,.F.,.F.,(4,4),(4,1,1,1,1,1,1,1,1,1,1,1,1,1,1,1,1,1,1,
1,1,1,1,1,1,1,1,1,1,1,1,1,1,1,1,1,1,1,1,1,1,1,1,1,1,1,1,1,1,1,1,1,1,1,1,
1,1,1,1,1,1,1,1,1,1,1,1,1,1,1,1,1,1,1,1,1,1,1,1,1,1,1,1,1,1,1,1,1,1,1,1,
1,1,1,1,1,1,1,1,1,1,1,1,1,1,1,1,1,1,1,1,1,1,1,1,1,1,1,1,1,1,1,1,1,1,1,1,
1,1,1,1,1,1,1,1,1,1,1,1,1,1,1,1,1,1,1,1,1,1,1,1,1,1,1,1,1,1,1,1,1,1,1,1,
1,1,1,1,1,1,1,1,1,1,1,1,1,1,1,1,1,1,1,1,1,1,1,1,1,1,1,1,1,1,1,1,1,1,1,1,
1,1,1,1,1,1,1,1,1,1,1,1,1,1,1,1,1,1,1,1,1,1,1,1,1,1,1,1,1,1,1,1,1,1,1,1,
1,1,1,1,1,1,1,1,1,1,1,1,1,1,1,1,1,1,1,1,1,1,1,1,1,1,1,1,1,1,1,1,1,1,1,1,
1,1,1,1,1,1,1,1,1,1,1,1,1,1,1,1,1,1,1,1,1,1,1,1,1,1,1,1,1,1,1,1,1,1,1,1,
1,1,1,1,1,1,1,1,1,1,1,1,1,1,1,1,1,1,1,1,1,1,1,1,1,1,1,1,1,1,1,1,1,1,1,1,
1,1,1,1,1,1,1,1,1,1,1,1,1,1,1,1,1,1,1,1,1,1,1,1,1,1,1,1,1,1,1,1,1,1,1,1,
1,1,1,1,1,1,1,1,1,1,1,1,1,1,1,1,1,1,1,1,1,1,1,1,1,1,1,1,1,1,1,1,1,1,1,1,
1,1,1,1,1,1,1,1,1,1,1,1,1,1,1,1,1,4),(0.,0.115296848757168),(8.30592286723195,
8.80591593374569,9.30590900025942,9.80590206677316,10.3058951332869,10.8058881998006,
11.3058812663144,11.8058743328281,12.3058673993418,12.8058604658556,13.3058535323693,
13.805846598883,14.3058396653968,14.8058327319105,15.3058257984242,15.805818864938,
16.3058119314517,16.8058049979655,17.3057980644792,17.8057911309929,18.3057841975067,
18.8057772640204,19.3057703305341,19.8057633970479,20.3057564635616,20.8057495300753,
21.3057425965891,21.8057356631028,22.3057287296165,22.8057217961303,23.305714862644,
23.8057079291577,24.3057009956715,24.8056940621852,25.305687128699,25.8056801952127,
26.3056732617264,26.8056663282402,27.3056593947539,27.8056524612676,28.3056455277814,
28.8056385942951,29.3056316608088,29.8056247273226,30.3056177938363,30.80561086035,
31.3056039268638,31.8055969933775,32.3055900598912,32.805583126405,33.3055761929187,
33.8055692594324,34.3055623259462,34.8055553924599,35.3055484589737,35.8055415254874,
36.3055345920011,36.8055276585149,37.3055207250286,37.8055137915423,38.3055068580561,
38.8054999245698,39.3054929910835,39.8054860575973,40.305479124111,40.8054721906247,
41.3054652571385,41.8054583236522,42.305451390166,42.8054444566797,43.3054375231934,
43.8054305897072,44.3054236562209,44.8054167227346,45.3054097892484,45.8054028557621,
46.3053959222758,46.8053889887896,47.3053820553033,47.805375121817,48.3053681883308,
48.8053612548445,49.3053543213582,49.805347387872,50.3053404543857,50.8053335208995,
51.3053265874132,51.8053196539269,52.3053127204407,52.8053057869544,53.3052988534681,
53.8052919199819,54.3052849864956,54.8052780530093,55.3052711195231,55.8052641860368,
56.3052572525505,56.8052503190643,57.305243385578,57.8052364520917,58.3052295186055,
58.8052225851192,59.3052156516329,59.8052087181467,60.3052017846604,60.8051948511742,
61.3051879176879,61.8051809842016,62.3051740507154,62.8051671172291,63.3051601837428,
63.8051532502566,64.3051463167703,64.805139383284,65.3051324497978,65.8051255163115,
66.3051185828252,66.805111649339,67.3051047158527,67.8050977823664,68.3050908488802,
68.8050839153939,69.3050769819077,69.8050700484214,70.3050631149351,70.8050561814489,
71.3050492479626,71.8050423144763,72.3050353809901,72.8050284475038,73.3050215140175,
73.8050145805313,74.305007647045,74.8050007135587,75.3049937800725,75.8049868465862,
76.3049799131,76.8049729796137,77.3049660461274,77.8049591126412,78.3049521791549,
78.8049452456686,79.3049383121824,79.8049313786961,80.3049244452098,80.8049175117236,
81.3049105782373,81.804903644751,82.3048967112648,82.8048897777785,83.3048828442923,
83.804875910806,84.3048689773197,84.8048620438335,85.3048551103472,85.8048481768609,
86.3048412433747,86.8048343098884,87.3048273764021,87.8048204429159,88.3048135094296,
88.8048065759433,89.3047996424571,89.8047927089708,90.3047857754845,90.8047788419983,
91.304771908512,91.8047649750257,92.3047580415395,92.8047511080532,93.3047441745669,
93.8047372410807,94.3047303075944,94.8047233741082,95.3047164406219,95.8047095071356,
96.3047025736494,96.8046956401631,97.3046887066768,97.8046817731906,98.3046748397043,
98.804667906218,99.3046609727318,99.8046540392455,100.304647105759,100.804640172273,
101.304633238787,101.8046263053,102.304619371814,102.804612438328,103.304605504842,
103.804598571355,104.304591637869,104.804584704383,105.304577770897,105.80457083741,
106.304563903924,106.804556970438,107.304550036952,107.804543103465,108.304536169979,
108.804529236493,109.304522303006,109.80451536952,110.304508436034,110.804501502548,
111.304494569061,111.804487635575,112.304480702089,112.804473768603,113.304466835116,
113.80445990163,114.304452968144,114.804446034658,115.304439101171,115.804432167685,
116.304425234199,116.804418300713,117.304411367226,117.80440443374,118.304397500254,
118.804390566767,119.304383633281,119.804376699795,120.304369766309,120.804362832822,
121.304355899336,121.80434896585,122.304342032364,122.804335098877,123.304328165391,
123.804321231905,124.304314298419,124.804307364932,125.304300431446,125.80429349796,
126.304286564473,126.804279630987,127.304272697501,127.804265764015,128.304258830528,
128.804251897042,129.304244963556,129.80423803007,130.304231096583,130.804224163097,
131.304217229611,131.804210296125,132.304203362638,132.804196429152,133.304189495666,
133.80418256218,134.304175628693,134.804168695207,135.304161761721,135.804154828234,
136.304147894748,136.804140961262,137.304134027776,137.804127094289,138.304120160803,
138.804113227317,139.304106293831,139.804099360344,140.304092426858,140.804085493372,
141.304078559886,141.804071626399,142.304064692913,142.804057759427,143.30405082594,
143.804043892454,144.304036958968,144.804030025482,145.304023091995,145.804016158509,
146.304009225023,146.804002291537,147.30399535805,147.803988424564,148.303981491078,
148.803974557592,149.303967624105,149.803960690619,150.303953757133,150.803946823646,
151.30393989016,151.803932956674,152.303926023188,152.803919089701,153.303912156215,
153.803905222729,154.303898289243,154.803891355756,155.30388442227,155.803877488784,
156.303870555298,156.803863621811,157.303856688325,157.803849754839,158.303842821353,
158.803835887866,159.30382895438,159.803822020894,160.303815087407,160.803808153921,
161.303801220435,161.803794286949,162.303787353462,162.803780419976,163.30377348649,
163.803766553004,164.303759619517,164.803752686031,165.303745752545,165.803738819059,
166.303731885572,166.803724952086,167.3037180186,167.803711085113,168.303704151627,
168.803697218141,169.303690284655,169.803683351168,170.303676417682,170.803669484196,
171.30366255071,171.803655617223,172.303648683737,172.803641750251,173.303634816765,
173.803627883278,174.303620949792,174.803614016306,175.30360708282,175.803600149333,
176.303593215847,176.803586282361,177.303579348874,177.803572415388,178.303565481902,
178.803558548416,179.303551614929,179.803544681443,180.303537747957,180.803530814471,
181.303523880984,181.803516947498,182.303510014012,182.803503080526,183.303496147039,
183.803489213553,184.303482280067,184.803475346581,185.303468413094,185.803461479608,
186.303454546122,186.803447612635,187.303440679149,187.803433745663,188.303426812177,
188.80341987869,189.303412945204,189.803406011718,190.303399078232,190.803392144745,
191.303385211259,191.803378277773,192.303371344287,192.8033644108,193.303357477314,
193.803350543828,194.303343610341,194.803336676855,195.303329743369,195.803322809883,
196.303315876396,196.80330894291,197.303302009424,197.803295075938,198.303288142451,
198.803281208965,199.303274275479,199.803267341993,200.303260408506,200.80325347502,
201.303246541534,201.803239608047,202.303232674561,202.803225741075,203.303218807589,
203.803211874102,204.303204940616,204.80319800713,205.303191073644,205.803184140157,
206.303177206671,206.803170273185,207.303163339699,207.803156406212,208.303149472726,
208.80314253924,209.303135605754,209.803128672267,210.303121738781,210.803114805295,
211.303107871808,211.803100938322,212.303094004836,212.80308707135,213.303080137863,
213.803073204377,214.303066270891,214.803059337405,215.303052403918,215.803045470432,
216.303038536946,216.80303160346,217.303024669973,217.803017736487,218.303010803001,
218.803003869514,219.302996936028,219.802990002542,220.302983069056,220.802976135569,
221.302969202083,221.802962268597,222.302955335111,222.802948401624,223.302941468138,
223.802934534652,224.302927601166),.UNSPECIFIED.);
#253=B_SPLINE_SURFACE_WITH_KNOTS('',3,3,((#33529,#33530,#33531,#33532,#33533,
#33534,#33535,#33536,#33537,#33538,#33539,#33540,#33541,#33542,#33543,#33544,
#33545,#33546,#33547,#33548,#33549,#33550,#33551,#33552,#33553,#33554,#33555,
#33556,#33557,#33558,#33559,#33560,#33561,#33562,#33563,#33564,#33565,#33566,
#33567,#33568,#33569,#33570,#33571,#33572,#33573,#33574,#33575,#33576,#33577,
#33578,#33579,#33580,#33581,#33582,#33583,#33584,#33585,#33586,#33587,#33588,
#33589,#33590,#33591,#33592,#33593,#33594,#33595,#33596,#33597,#33598,#33599,
#33600,#33601,#33602,#33603,#33604,#33605,#33606,#33607,#33608,#33609,#33610,
#33611,#33612,#33613,#33614,#33615,#33616,#33617,#33618,#33619,#33620,#33621,
#33622,#33623,#33624,#33625,#33626,#33627,#33628,#33629,#33630,#33631,#33632,
#33633,#33634,#33635,#33636,#33637,#33638,#33639,#33640,#33641,#33642,#33643,
#33644,#33645,#33646,#33647,#33648,#33649,#33650,#33651,#33652,#33653,#33654,
#33655,#33656,#33657,#33658,#33659,#33660,#33661,#33662,#33663,#33664,#33665,
#33666,#33667,#33668,#33669,#33670,#33671,#33672,#33673,#33674,#33675,#33676,
#33677,#33678,#33679,#33680,#33681,#33682,#33683,#33684,#33685,#33686,#33687,
#33688,#33689,#33690,#33691,#33692,#33693,#33694,#33695,#33696,#33697,#33698,
#33699,#33700,#33701,#33702,#33703,#33704,#33705,#33706,#33707,#33708,#33709,
#33710,#33711,#33712,#33713,#33714,#33715,#33716,#33717,#33718,#33719,#33720,
#33721,#33722,#33723,#33724,#33725,#33726,#33727,#33728,#33729,#33730,#33731,
#33732,#33733,#33734,#33735,#33736,#33737,#33738,#33739,#33740,#33741,#33742,
#33743,#33744,#33745,#33746,#33747,#33748,#33749,#33750,#33751,#33752,#33753,
#33754,#33755,#33756,#33757,#33758,#33759,#33760,#33761,#33762,#33763,#33764,
#33765,#33766,#33767,#33768,#33769,#33770,#33771,#33772,#33773,#33774,#33775,
#33776,#33777,#33778,#33779,#33780,#33781,#33782,#33783,#33784,#33785,#33786,
#33787,#33788,#33789,#33790,#33791,#33792,#33793,#33794,#33795,#33796,#33797,
#33798,#33799,#33800,#33801,#33802,#33803,#33804,#33805,#33806,#33807,#33808,
#33809,#33810,#33811,#33812,#33813,#33814,#33815,#33816,#33817,#33818,#33819,
#33820,#33821,#33822,#33823,#33824,#33825,#33826,#33827,#33828,#33829,#33830,
#33831,#33832,#33833,#33834,#33835,#33836,#33837,#33838,#33839,#33840,#33841,
#33842,#33843,#33844,#33845,#33846,#33847,#33848,#33849,#33850,#33851,#33852,
#33853,#33854,#33855,#33856,#33857,#33858,#33859,#33860,#33861,#33862,#33863,
#33864,#33865,#33866,#33867,#33868,#33869,#33870,#33871,#33872,#33873,#33874,
#33875,#33876,#33877,#33878,#33879,#33880,#33881,#33882,#33883,#33884,#33885,
#33886,#33887,#33888,#33889,#33890,#33891,#33892,#33893,#33894,#33895,#33896,
#33897,#33898,#33899,#33900,#33901,#33902,#33903,#33904,#33905,#33906,#33907,
#33908,#33909,#33910,#33911,#33912,#33913,#33914,#33915,#33916,#33917,#33918,
#33919,#33920,#33921,#33922,#33923,#33924,#33925,#33926,#33927,#33928,#33929,
#33930,#33931,#33932,#33933,#33934,#33935,#33936,#33937,#33938,#33939,#33940,
#33941,#33942,#33943,#33944,#33945,#33946,#33947,#33948,#33949,#33950,#33951,
#33952,#33953,#33954,#33955,#33956,#33957,#33958,#33959,#33960,#33961,#33962,
#33963),(#33964,#33965,#33966,#33967,#33968,#33969,#33970,#33971,#33972,
#33973,#33974,#33975,#33976,#33977,#33978,#33979,#33980,#33981,#33982,#33983,
#33984,#33985,#33986,#33987,#33988,#33989,#33990,#33991,#33992,#33993,#33994,
#33995,#33996,#33997,#33998,#33999,#34000,#34001,#34002,#34003,#34004,#34005,
#34006,#34007,#34008,#34009,#34010,#34011,#34012,#34013,#34014,#34015,#34016,
#34017,#34018,#34019,#34020,#34021,#34022,#34023,#34024,#34025,#34026,#34027,
#34028,#34029,#34030,#34031,#34032,#34033,#34034,#34035,#34036,#34037,#34038,
#34039,#34040,#34041,#34042,#34043,#34044,#34045,#34046,#34047,#34048,#34049,
#34050,#34051,#34052,#34053,#34054,#34055,#34056,#34057,#34058,#34059,#34060,
#34061,#34062,#34063,#34064,#34065,#34066,#34067,#34068,#34069,#34070,#34071,
#34072,#34073,#34074,#34075,#34076,#34077,#34078,#34079,#34080,#34081,#34082,
#34083,#34084,#34085,#34086,#34087,#34088,#34089,#34090,#34091,#34092,#34093,
#34094,#34095,#34096,#34097,#34098,#34099,#34100,#34101,#34102,#34103,#34104,
#34105,#34106,#34107,#34108,#34109,#34110,#34111,#34112,#34113,#34114,#34115,
#34116,#34117,#34118,#34119,#34120,#34121,#34122,#34123,#34124,#34125,#34126,
#34127,#34128,#34129,#34130,#34131,#34132,#34133,#34134,#34135,#34136,#34137,
#34138,#34139,#34140,#34141,#34142,#34143,#34144,#34145,#34146,#34147,#34148,
#34149,#34150,#34151,#34152,#34153,#34154,#34155,#34156,#34157,#34158,#34159,
#34160,#34161,#34162,#34163,#34164,#34165,#34166,#34167,#34168,#34169,#34170,
#34171,#34172,#34173,#34174,#34175,#34176,#34177,#34178,#34179,#34180,#34181,
#34182,#34183,#34184,#34185,#34186,#34187,#34188,#34189,#34190,#34191,#34192,
#34193,#34194,#34195,#34196,#34197,#34198,#34199,#34200,#34201,#34202,#34203,
#34204,#34205,#34206,#34207,#34208,#34209,#34210,#34211,#34212,#34213,#34214,
#34215,#34216,#34217,#34218,#34219,#34220,#34221,#34222,#34223,#34224,#34225,
#34226,#34227,#34228,#34229,#34230,#34231,#34232,#34233,#34234,#34235,#34236,
#34237,#34238,#34239,#34240,#34241,#34242,#34243,#34244,#34245,#34246,#34247,
#34248,#34249,#34250,#34251,#34252,#34253,#34254,#34255,#34256,#34257,#34258,
#34259,#34260,#34261,#34262,#34263,#34264,#34265,#34266,#34267,#34268,#34269,
#34270,#34271,#34272,#34273,#34274,#34275,#34276,#34277,#34278,#34279,#34280,
#34281,#34282,#34283,#34284,#34285,#34286,#34287,#34288,#34289,#34290,#34291,
#34292,#34293,#34294,#34295,#34296,#34297,#34298,#34299,#34300,#34301,#34302,
#34303,#34304,#34305,#34306,#34307,#34308,#34309,#34310,#34311,#34312,#34313,
#34314,#34315,#34316,#34317,#34318,#34319,#34320,#34321,#34322,#34323,#34324,
#34325,#34326,#34327,#34328,#34329,#34330,#34331,#34332,#34333,#34334,#34335,
#34336,#34337,#34338,#34339,#34340,#34341,#34342,#34343,#34344,#34345,#34346,
#34347,#34348,#34349,#34350,#34351,#34352,#34353,#34354,#34355,#34356,#34357,
#34358,#34359,#34360,#34361,#34362,#34363,#34364,#34365,#34366,#34367,#34368,
#34369,#34370,#34371,#34372,#34373,#34374,#34375,#34376,#34377,#34378,#34379,
#34380,#34381,#34382,#34383,#34384,#34385,#34386,#34387,#34388,#34389,#34390,
#34391,#34392,#34393,#34394,#34395,#34396,#34397,#34398),(#34399,#34400,
#34401,#34402,#34403,#34404,#34405,#34406,#34407,#34408,#34409,#34410,#34411,
#34412,#34413,#34414,#34415,#34416,#34417,#34418,#34419,#34420,#34421,#34422,
#34423,#34424,#34425,#34426,#34427,#34428,#34429,#34430,#34431,#34432,#34433,
#34434,#34435,#34436,#34437,#34438,#34439,#34440,#34441,#34442,#34443,#34444,
#34445,#34446,#34447,#34448,#34449,#34450,#34451,#34452,#34453,#34454,#34455,
#34456,#34457,#34458,#34459,#34460,#34461,#34462,#34463,#34464,#34465,#34466,
#34467,#34468,#34469,#34470,#34471,#34472,#34473,#34474,#34475,#34476,#34477,
#34478,#34479,#34480,#34481,#34482,#34483,#34484,#34485,#34486,#34487,#34488,
#34489,#34490,#34491,#34492,#34493,#34494,#34495,#34496,#34497,#34498,#34499,
#34500,#34501,#34502,#34503,#34504,#34505,#34506,#34507,#34508,#34509,#34510,
#34511,#34512,#34513,#34514,#34515,#34516,#34517,#34518,#34519,#34520,#34521,
#34522,#34523,#34524,#34525,#34526,#34527,#34528,#34529,#34530,#34531,#34532,
#34533,#34534,#34535,#34536,#34537,#34538,#34539,#34540,#34541,#34542,#34543,
#34544,#34545,#34546,#34547,#34548,#34549,#34550,#34551,#34552,#34553,#34554,
#34555,#34556,#34557,#34558,#34559,#34560,#34561,#34562,#34563,#34564,#34565,
#34566,#34567,#34568,#34569,#34570,#34571,#34572,#34573,#34574,#34575,#34576,
#34577,#34578,#34579,#34580,#34581,#34582,#34583,#34584,#34585,#34586,#34587,
#34588,#34589,#34590,#34591,#34592,#34593,#34594,#34595,#34596,#34597,#34598,
#34599,#34600,#34601,#34602,#34603,#34604,#34605,#34606,#34607,#34608,#34609,
#34610,#34611,#34612,#34613,#34614,#34615,#34616,#34617,#34618,#34619,#34620,
#34621,#34622,#34623,#34624,#34625,#34626,#34627,#34628,#34629,#34630,#34631,
#34632,#34633,#34634,#34635,#34636,#34637,#34638,#34639,#34640,#34641,#34642,
#34643,#34644,#34645,#34646,#34647,#34648,#34649,#34650,#34651,#34652,#34653,
#34654,#34655,#34656,#34657,#34658,#34659,#34660,#34661,#34662,#34663,#34664,
#34665,#34666,#34667,#34668,#34669,#34670,#34671,#34672,#34673,#34674,#34675,
#34676,#34677,#34678,#34679,#34680,#34681,#34682,#34683,#34684,#34685,#34686,
#34687,#34688,#34689,#34690,#34691,#34692,#34693,#34694,#34695,#34696,#34697,
#34698,#34699,#34700,#34701,#34702,#34703,#34704,#34705,#34706,#34707,#34708,
#34709,#34710,#34711,#34712,#34713,#34714,#34715,#34716,#34717,#34718,#34719,
#34720,#34721,#34722,#34723,#34724,#34725,#34726,#34727,#34728,#34729,#34730,
#34731,#34732,#34733,#34734,#34735,#34736,#34737,#34738,#34739,#34740,#34741,
#34742,#34743,#34744,#34745,#34746,#34747,#34748,#34749,#34750,#34751,#34752,
#34753,#34754,#34755,#34756,#34757,#34758,#34759,#34760,#34761,#34762,#34763,
#34764,#34765,#34766,#34767,#34768,#34769,#34770,#34771,#34772,#34773,#34774,
#34775,#34776,#34777,#34778,#34779,#34780,#34781,#34782,#34783,#34784,#34785,
#34786,#34787,#34788,#34789,#34790,#34791,#34792,#34793,#34794,#34795,#34796,
#34797,#34798,#34799,#34800,#34801,#34802,#34803,#34804,#34805,#34806,#34807,
#34808,#34809,#34810,#34811,#34812,#34813,#34814,#34815,#34816,#34817,#34818,
#34819,#34820,#34821,#34822,#34823,#34824,#34825,#34826,#34827,#34828,#34829,
#34830,#34831,#34832,#34833),(#34834,#34835,#34836,#34837,#34838,#34839,
#34840,#34841,#34842,#34843,#34844,#34845,#34846,#34847,#34848,#34849,#34850,
#34851,#34852,#34853,#34854,#34855,#34856,#34857,#34858,#34859,#34860,#34861,
#34862,#34863,#34864,#34865,#34866,#34867,#34868,#34869,#34870,#34871,#34872,
#34873,#34874,#34875,#34876,#34877,#34878,#34879,#34880,#34881,#34882,#34883,
#34884,#34885,#34886,#34887,#34888,#34889,#34890,#34891,#34892,#34893,#34894,
#34895,#34896,#34897,#34898,#34899,#34900,#34901,#34902,#34903,#34904,#34905,
#34906,#34907,#34908,#34909,#34910,#34911,#34912,#34913,#34914,#34915,#34916,
#34917,#34918,#34919,#34920,#34921,#34922,#34923,#34924,#34925,#34926,#34927,
#34928,#34929,#34930,#34931,#34932,#34933,#34934,#34935,#34936,#34937,#34938,
#34939,#34940,#34941,#34942,#34943,#34944,#34945,#34946,#34947,#34948,#34949,
#34950,#34951,#34952,#34953,#34954,#34955,#34956,#34957,#34958,#34959,#34960,
#34961,#34962,#34963,#34964,#34965,#34966,#34967,#34968,#34969,#34970,#34971,
#34972,#34973,#34974,#34975,#34976,#34977,#34978,#34979,#34980,#34981,#34982,
#34983,#34984,#34985,#34986,#34987,#34988,#34989,#34990,#34991,#34992,#34993,
#34994,#34995,#34996,#34997,#34998,#34999,#35000,#35001,#35002,#35003,#35004,
#35005,#35006,#35007,#35008,#35009,#35010,#35011,#35012,#35013,#35014,#35015,
#35016,#35017,#35018,#35019,#35020,#35021,#35022,#35023,#35024,#35025,#35026,
#35027,#35028,#35029,#35030,#35031,#35032,#35033,#35034,#35035,#35036,#35037,
#35038,#35039,#35040,#35041,#35042,#35043,#35044,#35045,#35046,#35047,#35048,
#35049,#35050,#35051,#35052,#35053,#35054,#35055,#35056,#35057,#35058,#35059,
#35060,#35061,#35062,#35063,#35064,#35065,#35066,#35067,#35068,#35069,#35070,
#35071,#35072,#35073,#35074,#35075,#35076,#35077,#35078,#35079,#35080,#35081,
#35082,#35083,#35084,#35085,#35086,#35087,#35088,#35089,#35090,#35091,#35092,
#35093,#35094,#35095,#35096,#35097,#35098,#35099,#35100,#35101,#35102,#35103,
#35104,#35105,#35106,#35107,#35108,#35109,#35110,#35111,#35112,#35113,#35114,
#35115,#35116,#35117,#35118,#35119,#35120,#35121,#35122,#35123,#35124,#35125,
#35126,#35127,#35128,#35129,#35130,#35131,#35132,#35133,#35134,#35135,#35136,
#35137,#35138,#35139,#35140,#35141,#35142,#35143,#35144,#35145,#35146,#35147,
#35148,#35149,#35150,#35151,#35152,#35153,#35154,#35155,#35156,#35157,#35158,
#35159,#35160,#35161,#35162,#35163,#35164,#35165,#35166,#35167,#35168,#35169,
#35170,#35171,#35172,#35173,#35174,#35175,#35176,#35177,#35178,#35179,#35180,
#35181,#35182,#35183,#35184,#35185,#35186,#35187,#35188,#35189,#35190,#35191,
#35192,#35193,#35194,#35195,#35196,#35197,#35198,#35199,#35200,#35201,#35202,
#35203,#35204,#35205,#35206,#35207,#35208,#35209,#35210,#35211,#35212,#35213,
#35214,#35215,#35216,#35217,#35218,#35219,#35220,#35221,#35222,#35223,#35224,
#35225,#35226,#35227,#35228,#35229,#35230,#35231,#35232,#35233,#35234,#35235,
#35236,#35237,#35238,#35239,#35240,#35241,#35242,#35243,#35244,#35245,#35246,
#35247,#35248,#35249,#35250,#35251,#35252,#35253,#35254,#35255,#35256,#35257,
#35258,#35259,#35260,#35261,#35262,#35263,#35264,#35265,#35266,#35267,#35268)),
 .UNSPECIFIED.,.F.,.F.,.F.,(4,4),(4,1,1,1,1,1,1,1,1,1,1,1,1,1,1,1,1,1,1,
1,1,1,1,1,1,1,1,1,1,1,1,1,1,1,1,1,1,1,1,1,1,1,1,1,1,1,1,1,1,1,1,1,1,1,1,
1,1,1,1,1,1,1,1,1,1,1,1,1,1,1,1,1,1,1,1,1,1,1,1,1,1,1,1,1,1,1,1,1,1,1,1,
1,1,1,1,1,1,1,1,1,1,1,1,1,1,1,1,1,1,1,1,1,1,1,1,1,1,1,1,1,1,1,1,1,1,1,1,
1,1,1,1,1,1,1,1,1,1,1,1,1,1,1,1,1,1,1,1,1,1,1,1,1,1,1,1,1,1,1,1,1,1,1,1,
1,1,1,1,1,1,1,1,1,1,1,1,1,1,1,1,1,1,1,1,1,1,1,1,1,1,1,1,1,1,1,1,1,1,1,1,
1,1,1,1,1,1,1,1,1,1,1,1,1,1,1,1,1,1,1,1,1,1,1,1,1,1,1,1,1,1,1,1,1,1,1,1,
1,1,1,1,1,1,1,1,1,1,1,1,1,1,1,1,1,1,1,1,1,1,1,1,1,1,1,1,1,1,1,1,1,1,1,1,
1,1,1,1,1,1,1,1,1,1,1,1,1,1,1,1,1,1,1,1,1,1,1,1,1,1,1,1,1,1,1,1,1,1,1,1,
1,1,1,1,1,1,1,1,1,1,1,1,1,1,1,1,1,1,1,1,1,1,1,1,1,1,1,1,1,1,1,1,1,1,1,1,
1,1,1,1,1,1,1,1,1,1,1,1,1,1,1,1,1,1,1,1,1,1,1,1,1,1,1,1,1,1,1,1,1,1,1,1,
1,1,1,1,1,1,1,1,1,1,1,1,1,1,1,1,1,1,1,1,1,1,1,1,1,1,1,1,1,1,1,1,1,1,1,1,
1,1,1,1,1,1,1,1,1,1,1,1,1,1,1,1,1,4),(0.,0.115296848757168),(11.6154215191109,
12.1154145856246,12.6154076521384,13.1154007186521,13.6153937851658,14.1153868516796,
14.6153799181933,15.1153729847071,15.6153660512208,16.1153591177345,16.6153521842483,
17.115345250762,17.6153383172757,18.1153313837895,18.6153244503032,19.1153175168169,
19.6153105833307,20.1153036498444,20.6152967163581,21.1152897828719,21.6152828493856,
22.1152759158993,22.6152689824131,23.1152620489268,23.6152551154406,24.1152481819543,
24.615241248468,25.1152343149818,25.6152273814955,26.1152204480092,26.615213514523,
27.1152065810367,27.6151996475504,28.1151927140642,28.6151857805779,29.1151788470916,
29.6151719136054,30.1151649801191,30.6151580466328,31.1151511131466,31.6151441796603,
32.115137246174,32.6151303126878,33.1151233792015,33.6151164457153,34.115109512229,
34.6151025787427,35.1150956452565,35.6150887117702,36.1150817782839,36.6150748447977,
37.1150679113114,37.6150609778251,38.1150540443389,38.6150471108526,39.1150401773663,
39.6150332438801,40.1150263103938,40.6150193769075,41.1150124434213,41.615005509935,
42.1149985764488,42.6149916429625,43.1149847094762,43.61497777599,44.1149708425037,
44.6149639090174,45.1149569755312,45.6149500420449,46.1149431085586,46.6149361750724,
47.1149292415861,47.6149223080998,48.1149153746136,48.6149084411273,49.114901507641,
49.6148945741548,50.1148876406685,50.6148807071823,51.114873773696,51.6148668402097,
52.1148599067235,52.6148529732372,53.1148460397509,53.6148391062647,54.1148321727784,
54.6148252392921,55.1148183058059,55.6148113723196,56.1148044388333,56.6147975053471,
57.1147905718608,57.6147836383745,58.1147767048883,58.614769771402,59.1147628379157,
59.6147559044295,60.1147489709432,60.6147420374569,61.1147351039707,61.6147281704844,
62.1147212369982,62.6147143035119,63.1147073700256,63.6147004365394,64.1146935030531,
64.6146865695668,65.1146796360806,65.6146727025943,66.114665769108,66.6146588356218,
67.1146519021355,67.6146449686492,68.114638035163,68.6146311016767,69.1146241681904,
69.6146172347042,70.1146103012179,70.6146033677317,71.1145964342454,71.6145895007591,
72.1145825672729,72.6145756337866,73.1145687003003,73.6145617668141,74.1145548333278,
74.6145478998415,75.1145409663553,75.614534032869,76.1145270993827,76.6145201658965,
77.1145132324102,77.614506298924,78.1144993654377,78.6144924319514,79.1144854984652,
79.6144785649789,80.1144716314926,80.6144646980064,81.1144577645201,81.6144508310338,
82.1144438975476,82.6144369640613,83.114430030575,83.6144230970888,84.1144161636025,
84.6144092301162,85.11440229663,85.6143953631437,86.1143884296575,86.6143814961712,
87.1143745626849,87.6143676291987,88.1143606957124,88.6143537622261,89.1143468287399,
89.6143398952536,90.1143329617673,90.6143260282811,91.1143190947948,91.6143121613085,
92.1143052278223,92.614298294336,93.1142913608497,93.6142844273635,94.1142774938772,
94.6142705603909,95.1142636269047,95.6142566934184,96.1142497599322,96.6142428264459,
97.1142358929596,97.6142289594734,98.1142220259871,98.6142150925008,99.1142081590146,
99.6142012255283,100.114194292042,100.614187358556,101.11418042507,101.614173491583,
102.114166558097,102.614159624611,103.114152691124,103.614145757638,104.114138824152,
104.614131890666,105.114124957179,105.614118023693,106.114111090207,106.614104156721,
107.114097223234,107.614090289748,108.114083356262,108.614076422776,109.114069489289,
109.614062555803,110.114055622317,110.61404868883,111.114041755344,111.614034821858,
112.114027888372,112.614020954885,113.114014021399,113.614007087913,114.114000154427,
114.61399322094,115.113986287454,115.613979353968,116.113972420482,116.613965486995,
117.113958553509,117.613951620023,118.113944686536,118.61393775305,119.113930819564,
119.613923886078,120.113916952591,120.613910019105,121.113903085619,121.613896152133,
122.113889218646,122.61388228516,123.113875351674,123.613868418188,124.113861484701,
124.613854551215,125.113847617729,125.613840684243,126.113833750756,126.61382681727,
127.113819883784,127.613812950297,128.113806016811,128.613799083325,129.113792149839,
129.613785216352,130.113778282866,130.61377134938,131.113764415894,131.613757482407,
132.113750548921,132.613743615435,133.113736681949,133.613729748462,134.113722814976,
134.61371588149,135.113708948003,135.613702014517,136.113695081031,136.613688147545,
137.113681214058,137.613674280572,138.113667347086,138.6136604136,139.113653480113,
139.613646546627,140.113639613141,140.613632679655,141.113625746168,141.613618812682,
142.113611879196,142.61360494571,143.113598012223,143.613591078737,144.113584145251,
144.613577211764,145.113570278278,145.613563344792,146.113556411306,146.613549477819,
147.113542544333,147.613535610847,148.113528677361,148.613521743874,149.113514810388,
149.613507876902,150.113500943416,150.613494009929,151.113487076443,151.613480142957,
152.11347320947,152.613466275984,153.113459342498,153.613452409012,154.113445475525,
154.613438542039,155.113431608553,155.613424675067,156.11341774158,156.613410808094,
157.113403874608,157.613396941122,158.113390007635,158.613383074149,159.113376140663,
159.613369207177,160.11336227369,160.613355340204,161.113348406718,161.613341473231,
162.113334539745,162.613327606259,163.113320672773,163.613313739286,164.1133068058,
164.613299872314,165.113292938828,165.613286005341,166.113279071855,166.613272138369,
167.113265204883,167.613258271396,168.11325133791,168.613244404424,169.113237470937,
169.613230537451,170.113223603965,170.613216670479,171.113209736992,171.613202803506,
172.11319587002,172.613188936534,173.113182003047,173.613175069561,174.113168136075,
174.613161202589,175.113154269102,175.613147335616,176.11314040213,176.613133468643,
177.113126535157,177.613119601671,178.113112668185,178.613105734698,179.113098801212,
179.613091867726,180.11308493424,180.613078000753,181.113071067267,181.613064133781,
182.113057200295,182.613050266808,183.113043333322,183.613036399836,184.11302946635,
184.613022532863,185.113015599377,185.613008665891,186.113001732404,186.612994798918,
187.112987865432,187.612980931946,188.112973998459,188.612967064973,189.112960131487,
189.612953198001,190.112946264514,190.612939331028,191.112932397542,191.612925464056,
192.112918530569,192.612911597083,193.112904663597,193.61289773011,194.112890796624,
194.612883863138,195.112876929652,195.612869996165,196.112863062679,196.612856129193,
197.112849195707,197.61284226222,198.112835328734,198.612828395248,199.112821461762,
199.612814528275,200.112807594789,200.612800661303,201.112793727816,201.61278679433,
202.112779860844,202.612772927358,203.112765993871,203.612759060385,204.112752126899,
204.612745193413,205.112738259926,205.61273132644,206.112724392954,206.612717459468,
207.112710525981,207.612703592495,208.112696659009,208.612689725523,209.112682792036,
209.61267585855,210.112668925064,210.612661991577,211.112655058091,211.612648124605,
212.112641191119,212.612634257632,213.112627324146,213.61262039066,214.112613457174,
214.612606523687,215.112599590201,215.612592656715,216.112585723229,216.612578789742,
217.112571856256,217.61256492277,218.112557989284,218.612551055797,219.112544122311,
219.612537188825,220.112530255338,220.612523321852,221.112516388366,221.61250945488,
222.112502521393,222.612495587907,223.112488654421,223.612481720935,224.112474787448,
224.612467853962,225.112460920476,225.61245398699,226.112447053503,226.612440120017,
227.112433186531,227.612426253044),.UNSPECIFIED.);
#517=FACE_BOUND('',#3424,.T.);
#518=FACE_BOUND('',#3426,.T.);
#519=FACE_BOUND('',#3427,.T.);
#520=FACE_BOUND('',#3428,.T.);
#521=FACE_BOUND('',#3429,.T.);
#522=FACE_BOUND('',#3430,.T.);
#523=FACE_BOUND('',#3431,.T.);
#524=FACE_BOUND('',#3432,.T.);
#525=FACE_BOUND('',#3433,.T.);
#526=FACE_BOUND('',#3434,.T.);
#527=FACE_BOUND('',#3435,.T.);
#528=FACE_BOUND('',#3436,.T.);
#529=FACE_BOUND('',#3437,.T.);
#530=FACE_BOUND('',#3438,.T.);
#531=FACE_BOUND('',#3439,.T.);
#532=FACE_BOUND('',#3440,.T.);
#533=FACE_BOUND('',#3441,.T.);
#534=FACE_BOUND('',#3442,.T.);
#535=FACE_BOUND('',#3443,.T.);
#536=FACE_BOUND('',#3444,.T.);
#537=FACE_BOUND('',#3445,.T.);
#538=FACE_BOUND('',#3446,.T.);
#539=FACE_BOUND('',#3447,.T.);
#540=FACE_BOUND('',#3448,.T.);
#541=FACE_BOUND('',#3449,.T.);
#542=FACE_BOUND('',#3450,.T.);
#543=FACE_BOUND('',#3451,.T.);
#544=FACE_BOUND('',#3452,.T.);
#545=FACE_BOUND('',#3453,.T.);
#546=FACE_BOUND('',#3454,.T.);
#547=FACE_BOUND('',#3455,.T.);
#548=FACE_BOUND('',#3456,.T.);
#549=FACE_BOUND('',#3457,.T.);
#550=FACE_BOUND('',#3458,.T.);
#551=FACE_BOUND('',#3459,.T.);
#552=FACE_BOUND('',#3460,.T.);
#553=FACE_BOUND('',#3463,.T.);
#811=PLANE('',#16428);
#812=PLANE('',#16433);
#813=PLANE('',#16434);
#814=PLANE('',#16436);
#815=PLANE('',#16437);
#816=PLANE('',#16439);
#817=PLANE('',#16440);
#818=PLANE('',#16442);
#819=PLANE('',#16443);
#820=PLANE('',#16445);
#821=PLANE('',#16446);
#822=PLANE('',#16448);
#823=PLANE('',#16449);
#824=PLANE('',#16451);
#825=PLANE('',#16452);
#826=PLANE('',#16454);
#827=PLANE('',#16455);
#828=PLANE('',#16457);
#829=PLANE('',#16458);
#830=PLANE('',#16460);
#831=PLANE('',#16461);
#832=PLANE('',#16463);
#833=PLANE('',#16464);
#834=PLANE('',#16466);
#835=PLANE('',#16467);
#836=PLANE('',#16469);
#837=PLANE('',#16470);
#838=PLANE('',#16472);
#839=PLANE('',#16473);
#840=PLANE('',#16475);
#841=PLANE('',#16476);
#842=PLANE('',#16478);
#843=PLANE('',#16479);
#844=PLANE('',#16481);
#845=PLANE('',#16482);
#846=PLANE('',#16484);
#847=PLANE('',#16485);
#848=PLANE('',#16487);
#849=PLANE('',#16488);
#850=PLANE('',#16490);
#851=PLANE('',#16491);
#852=PLANE('',#16493);
#853=PLANE('',#16494);
#854=PLANE('',#16496);
#855=PLANE('',#16497);
#856=PLANE('',#16499);
#857=PLANE('',#16500);
#858=PLANE('',#16502);
#859=PLANE('',#16503);
#860=PLANE('',#16505);
#861=PLANE('',#16506);
#862=PLANE('',#16508);
#863=PLANE('',#16509);
#864=PLANE('',#16511);
#865=PLANE('',#16512);
#866=PLANE('',#16514);
#867=PLANE('',#16515);
#868=PLANE('',#16517);
#869=PLANE('',#16518);
#870=PLANE('',#16520);
#871=PLANE('',#16521);
#872=PLANE('',#16523);
#873=PLANE('',#16524);
#874=PLANE('',#16526);
#875=PLANE('',#16527);
#876=PLANE('',#16529);
#877=PLANE('',#16530);
#878=PLANE('',#16532);
#879=PLANE('',#16533);
#880=PLANE('',#16535);
#881=PLANE('',#16536);
#882=PLANE('',#16539);
#883=PLANE('',#16540);
#884=PLANE('',#16543);
#885=PLANE('',#16544);
#886=PLANE('',#16546);
#887=PLANE('',#16547);
#888=PLANE('',#16549);
#889=PLANE('',#16550);
#890=PLANE('',#16552);
#891=PLANE('',#16553);
#892=PLANE('',#16555);
#893=PLANE('',#16556);
#894=PLANE('',#16558);
#895=PLANE('',#16559);
#896=PLANE('',#16561);
#897=PLANE('',#16562);
#898=PLANE('',#16564);
#899=PLANE('',#16565);
#900=PLANE('',#16567);
#901=PLANE('',#16568);
#902=PLANE('',#16570);
#903=PLANE('',#16571);
#904=PLANE('',#16573);
#905=PLANE('',#16574);
#906=PLANE('',#16576);
#907=PLANE('',#16577);
#908=PLANE('',#16579);
#909=PLANE('',#16580);
#910=PLANE('',#16582);
#911=PLANE('',#16583);
#912=PLANE('',#16585);
#913=PLANE('',#16586);
#914=PLANE('',#16588);
#915=PLANE('',#16589);
#916=PLANE('',#16591);
#917=PLANE('',#16592);
#918=PLANE('',#16594);
#919=PLANE('',#16595);
#920=PLANE('',#16597);
#921=PLANE('',#16598);
#922=PLANE('',#16600);
#923=PLANE('',#16601);
#924=PLANE('',#16603);
#925=PLANE('',#16604);
#926=PLANE('',#16606);
#927=PLANE('',#16607);
#928=PLANE('',#16609);
#929=PLANE('',#16610);
#930=PLANE('',#16612);
#931=PLANE('',#16613);
#932=PLANE('',#16615);
#933=PLANE('',#16616);
#934=PLANE('',#16618);
#935=PLANE('',#16619);
#936=PLANE('',#16621);
#937=PLANE('',#16622);
#938=PLANE('',#16624);
#939=PLANE('',#16625);
#940=PLANE('',#16627);
#941=PLANE('',#16628);
#942=PLANE('',#16630);
#943=PLANE('',#16631);
#944=PLANE('',#16633);
#945=PLANE('',#16634);
#946=PLANE('',#16636);
#947=PLANE('',#16637);
#948=PLANE('',#16639);
#949=PLANE('',#16640);
#950=PLANE('',#16642);
#951=PLANE('',#16643);
#952=PLANE('',#16645);
#953=PLANE('',#16646);
#954=PLANE('',#16648);
#955=PLANE('',#16649);
#956=PLANE('',#16651);
#957=PLANE('',#16652);
#958=PLANE('',#16653);
#959=PLANE('',#16654);
#960=PLANE('',#16655);
#961=PLANE('',#16656);
#962=PLANE('',#16657);
#963=PLANE('',#16658);
#964=PLANE('',#16663);
#965=PLANE('',#16669);
#1187=B_SPLINE_CURVE_WITH_KNOTS('',3,(#27235,#27236,#27237,#27238,#27239,
#27240,#27241,#27242,#27243,#27244,#27245,#27246,#27247,#27248,#27249,#27250),
 .UNSPECIFIED.,.F.,.F.,(4,3,3,3,3,4),(-4.0925417488383,-3.99994453210988,
-3.49995146559614,-2.99995839908241,-2.49996533256868,-2.0698041887861),
 .UNSPECIFIED.);
#1188=B_SPLINE_CURVE_WITH_KNOTS('',3,(#27253,#27254,#27255,#27256,#27257,
#27258,#27259,#27260,#27261,#27262),.UNSPECIFIED.,.F.,.F.,(4,3,3,4),(0.,
0.499993066513738,0.999986133027476,1.1188550935379),.UNSPECIFIED.);
#1189=B_SPLINE_CURVE_WITH_KNOTS('',3,(#27267,#27268,#27269,#27270,#27271,
#27272,#27273,#27274,#27275,#27276,#27277,#27278,#27279,#27280,#27281,#27282,
#27283,#27284,#27285,#27286,#27287,#27288,#27289,#27290,#27291,#27292,#27293,
#27294,#27295,#27296,#27297,#27298,#27299,#27300,#27301,#27302,#27303,#27304,
#27305,#27306),.UNSPECIFIED.,.F.,.F.,(4,3,3,3,3,3,3,3,3,3,3,3,3,4),(-10.3757270560179,
-9.9998613302747,-9.49986826376097,-8.99987519724723,-8.4998821307335,-7.99988906421976,
-7.49989599770603,-6.99990293119229,-6.49990986467856,-5.99991679816482,
-5.49992373165109,-4.99993066513735,-4.49993759862362,-4.0925417488383),
 .UNSPECIFIED.);
#1190=B_SPLINE_CURVE_WITH_KNOTS('',3,(#27307,#27308,#27309,#27310,#27311,
#27312,#27313,#27314,#27315,#27316,#27317,#27318,#27319,#27320,#27321,#27322,
#27323,#27324,#27325,#27326,#27327,#27328,#27329,#27330,#27331,#27332,#27333,
#27334,#27335,#27336,#27337,#27338,#27339,#27340,#27341,#27342,#27343,#27344,
#27345,#27346),.UNSPECIFIED.,.F.,.F.,(4,3,3,3,3,3,3,3,3,3,3,3,3,4),(1.1188550935379,
1.49997919954121,1.99997226605495,2.49996533256868,2.99995839908241,3.49995146559615,
3.99994453210988,4.49993759862362,4.99993066513735,5.49992373165109,5.99991679816482,
6.49990986467855,6.99990293119229,7.40204040071747),.UNSPECIFIED.);
#1191=B_SPLINE_CURVE_WITH_KNOTS('',3,(#27351,#27352,#27353,#27354,#27355,
#27356,#27357,#27358,#27359,#27360,#27361,#27362,#27363,#27364,#27365,#27366,
#27367,#27368,#27369,#27370,#27371,#27372,#27373,#27374,#27375,#27376,#27377,
#27378,#27379,#27380,#27381,#27382,#27383,#27384,#27385,#27386,#27387,#27388,
#27389,#27390,#27391,#27392,#27393),.UNSPECIFIED.,.F.,.F.,(4,3,3,3,3,3,
3,3,3,3,3,3,3,3,4),(-16.6589123631975,-16.4997711949533,-15.9997781284395,
-15.4997850619258,-14.9997919954121,-14.4997989288983,-13.9998058623846,
-13.4998127958708,-12.9998197293571,-12.4998266628434,-11.9998335963296,
-11.4998405298159,-10.9998474633022,-10.4998543967884,-10.3757270560179),
 .UNSPECIFIED.);
#1192=B_SPLINE_CURVE_WITH_KNOTS('',3,(#27394,#27395,#27396,#27397,#27398,
#27399,#27400,#27401,#27402,#27403,#27404,#27405,#27406,#27407,#27408,#27409,
#27410,#27411,#27412,#27413,#27414,#27415,#27416,#27417,#27418,#27419,#27420,
#27421,#27422,#27423,#27424,#27425,#27426,#27427,#27428,#27429,#27430,#27431,
#27432,#27433,#27434,#27435,#27436),.UNSPECIFIED.,.F.,.F.,(4,3,3,3,3,3,
3,3,3,3,3,3,3,3,4),(7.40204040071747,7.49989599770603,7.99988906421976,
8.4998821307335,8.99987519724724,9.49986826376097,9.99986133027471,10.4998543967884,
10.9998474633022,11.4998405298159,11.9998335963297,12.4998266628434,12.9998197293571,
13.4998127958709,13.6852257078971),.UNSPECIFIED.);
#1193=B_SPLINE_CURVE_WITH_KNOTS('',3,(#27441,#27442,#27443,#27444,#27445,
#27446,#27447,#27448,#27449,#27450,#27451,#27452,#27453,#27454,#27455,#27456,
#27457,#27458,#27459,#27460,#27461,#27462,#27463,#27464,#27465,#27466,#27467,
#27468,#27469,#27470,#27471,#27472,#27473,#27474,#27475,#27476,#27477,#27478,
#27479,#27480),.UNSPECIFIED.,.F.,.F.,(4,3,3,3,3,3,3,3,3,3,3,3,3,4),(-22.942097670377,
-22.4996879931181,-21.9996949266043,-21.4997018600906,-20.9997087935769,
-20.4997157270631,-19.9997226605494,-19.4997295940357,-18.9997365275219,
-18.4997434610082,-17.9997503944945,-17.4997573279807,-16.999764261467,
-16.6589123631975),.UNSPECIFIED.);
#1194=B_SPLINE_CURVE_WITH_KNOTS('',3,(#27481,#27482,#27483,#27484,#27485,
#27486,#27487,#27488,#27489,#27490,#27491,#27492,#27493,#27494,#27495,#27496,
#27497,#27498,#27499,#27500,#27501,#27502,#27503,#27504,#27505,#27506,#27507,
#27508,#27509,#27510,#27511,#27512,#27513,#27514,#27515,#27516,#27517,#27518,
#27519,#27520),.UNSPECIFIED.,.F.,.F.,(4,3,3,3,3,3,3,3,3,3,3,3,3,4),(13.6852257078971,
13.9998058623846,14.4997989288983,14.9997919954121,15.4997850619258,15.9997781284395,
16.4997711949533,16.999764261467,17.4997573279807,17.9997503944945,18.4997434610082,
18.9997365275219,19.4997295940357,19.9684110150766),.UNSPECIFIED.);
#1195=B_SPLINE_CURVE_WITH_KNOTS('',3,(#27525,#27526,#27527,#27528,#27529,
#27530,#27531,#27532,#27533,#27534,#27535,#27536,#27537,#27538,#27539,#27540,
#27541,#27542,#27543,#27544,#27545,#27546,#27547,#27548,#27549,#27550,#27551,
#27552,#27553,#27554,#27555,#27556,#27557,#27558,#27559,#27560,#27561,#27562,
#27563,#27564,#27565,#27566,#27567),.UNSPECIFIED.,.F.,.F.,(4,3,3,3,3,3,
3,3,3,3,3,3,3,3,4),(-29.2252829775567,-28.9995978577966,-28.4996047912829,
-27.9996117247692,-27.4996186582554,-26.9996255917417,-26.499632525228,
-25.9996394587142,-25.4996463922005,-24.9996533256868,-24.499660259173,
-23.9996671926593,-23.4996741261456,-22.9996810596318,-22.942097670377),
 .UNSPECIFIED.);
#1196=B_SPLINE_CURVE_WITH_KNOTS('',3,(#27568,#27569,#27570,#27571,#27572,
#27573,#27574,#27575,#27576,#27577,#27578,#27579,#27580,#27581,#27582,#27583,
#27584,#27585,#27586,#27587,#27588,#27589,#27590,#27591,#27592,#27593,#27594,
#27595,#27596,#27597,#27598,#27599,#27600,#27601,#27602,#27603,#27604,#27605,
#27606,#27607,#27608,#27609,#27610),.UNSPECIFIED.,.F.,.F.,(4,3,3,3,3,3,
3,3,3,3,3,3,3,3,4),(19.9684110150766,19.9997226605494,20.4997157270631,
20.9997087935769,21.4997018600906,21.9996949266044,22.4996879931181,22.9996810596318,
23.4996741261456,23.9996671926593,24.499660259173,24.9996533256868,25.4996463922005,
25.9996394587143,26.2515963222562),.UNSPECIFIED.);
#1197=B_SPLINE_CURVE_WITH_KNOTS('',3,(#27615,#27616,#27617,#27618,#27619,
#27620,#27621,#27622,#27623,#27624,#27625,#27626,#27627,#27628,#27629,#27630,
#27631,#27632,#27633,#27634,#27635,#27636,#27637,#27638,#27639,#27640,#27641,
#27642,#27643,#27644,#27645,#27646,#27647,#27648,#27649,#27650,#27651,#27652,
#27653,#27654,#27655,#27656,#27657),.UNSPECIFIED.,.F.,.F.,(4,3,3,3,3,3,
3,3,3,3,3,3,3,3,4),(-35.5084682847362,-35.4995077224752,-34.9995146559615,
-34.4995215894477,-33.999528522934,-33.4995354564203,-32.9995423899065,
-32.4995493233928,-31.9995562568791,-31.4995631903653,-30.9995701238516,
-30.4995770573379,-29.9995839908241,-29.4995909243104,-29.2252829775567),
 .UNSPECIFIED.);
#1198=B_SPLINE_CURVE_WITH_KNOTS('',3,(#27658,#27659,#27660,#27661,#27662,
#27663,#27664,#27665,#27666,#27667,#27668,#27669,#27670,#27671,#27672,#27673,
#27674,#27675,#27676,#27677,#27678,#27679,#27680,#27681,#27682,#27683,#27684,
#27685,#27686,#27687,#27688,#27689,#27690,#27691,#27692,#27693,#27694,#27695,
#27696,#27697,#27698,#27699,#27700),.UNSPECIFIED.,.F.,.F.,(4,3,3,3,3,3,
3,3,3,3,3,3,3,3,4),(26.2515963222562,26.499632525228,26.9996255917417,27.4996186582555,
27.9996117247692,28.4996047912829,28.9995978577967,29.4995909243104,29.9995839908241,
30.4995770573378,30.9995701238516,31.4995631903653,31.999556256879,32.4995493233928,
32.5347816294358),.UNSPECIFIED.);
#1199=B_SPLINE_CURVE_WITH_KNOTS('',3,(#27705,#27706,#27707,#27708,#27709,
#27710,#27711,#27712,#27713,#27714,#27715,#27716,#27717,#27718,#27719,#27720,
#27721,#27722,#27723,#27724,#27725,#27726,#27727,#27728,#27729,#27730,#27731,
#27732,#27733,#27734,#27735,#27736,#27737,#27738,#27739,#27740,#27741,#27742,
#27743,#27744),.UNSPECIFIED.,.F.,.F.,(4,3,3,3,3,3,3,3,3,3,3,3,3,4),(-41.7916535919158,
-41.49942452064,-40.9994314541263,-40.4994383876125,-39.9994453210988,-39.4994522545851,
-38.9994591880713,-38.4994661215576,-37.9994730550439,-37.4994799885301,
-36.9994869220164,-36.4994938555027,-35.9995007889889,-35.5084682847362),
 .UNSPECIFIED.);
#1200=B_SPLINE_CURVE_WITH_KNOTS('',3,(#27745,#27746,#27747,#27748,#27749,
#27750,#27751,#27752,#27753,#27754,#27755,#27756,#27757,#27758,#27759,#27760,
#27761,#27762,#27763,#27764,#27765,#27766,#27767,#27768,#27769,#27770,#27771,
#27772,#27773,#27774,#27775,#27776,#27777,#27778,#27779,#27780,#27781,#27782,
#27783,#27784),.UNSPECIFIED.,.F.,.F.,(4,3,3,3,3,3,3,3,3,3,3,3,3,4),(32.5347816294358,
32.9995423899065,33.4995354564203,33.999528522934,34.4995215894477,34.9995146559615,
35.4995077224752,35.999500788989,36.4994938555027,36.9994869220164,37.4994799885302,
37.9994730550439,38.4994661215576,38.8179669366154),.UNSPECIFIED.);
#1201=B_SPLINE_CURVE_WITH_KNOTS('',3,(#27789,#27790,#27791,#27792,#27793,
#27794,#27795,#27796,#27797,#27798,#27799,#27800,#27801,#27802,#27803,#27804,
#27805,#27806,#27807,#27808,#27809,#27810,#27811,#27812,#27813,#27814,#27815,
#27816,#27817,#27818,#27819,#27820,#27821,#27822,#27823,#27824,#27825,#27826,
#27827,#27828,#27829,#27830,#27831),.UNSPECIFIED.,.F.,.F.,(4,3,3,3,3,3,
3,3,3,3,3,3,3,3,4),(-48.0748388990954,-47.9993343853186,-47.4993413188049,
-46.9993482522911,-46.4993551857774,-45.9993621192636,-45.4993690527499,
-44.9993759862362,-44.4993829197224,-43.9993898532087,-43.499396786695,
-42.9994037201812,-42.4994106536675,-41.9994175871538,-41.7916535919158),
 .UNSPECIFIED.);
#1202=B_SPLINE_CURVE_WITH_KNOTS('',3,(#27832,#27833,#27834,#27835,#27836,
#27837,#27838,#27839,#27840,#27841,#27842,#27843,#27844,#27845,#27846,#27847,
#27848,#27849,#27850,#27851,#27852,#27853,#27854,#27855,#27856,#27857,#27858,
#27859,#27860,#27861,#27862,#27863,#27864,#27865,#27866,#27867,#27868,#27869,
#27870,#27871,#27872,#27873,#27874),.UNSPECIFIED.,.F.,.F.,(4,3,3,3,3,3,
3,3,3,3,3,3,3,3,4),(38.8179669366154,38.9994591880714,39.4994522545851,
39.9994453210988,40.4994383876126,40.9994314541263,41.49942452064,41.9994175871538,
42.4994106536675,42.9994037201812,43.499396786695,43.9993898532087,44.4993829197224,
44.9993759862362,45.101152243795),.UNSPECIFIED.);
#1203=B_SPLINE_CURVE_WITH_KNOTS('',3,(#27879,#27880,#27881,#27882,#27883,
#27884,#27885,#27886,#27887,#27888,#27889,#27890,#27891,#27892,#27893,#27894,
#27895,#27896,#27897,#27898,#27899,#27900,#27901,#27902,#27903,#27904,#27905,
#27906,#27907,#27908,#27909,#27910,#27911,#27912,#27913,#27914,#27915,#27916,
#27917,#27918),.UNSPECIFIED.,.F.,.F.,(4,3,3,3,3,3,3,3,3,3,3,3,3,4),(-54.358024206275,
-53.9992511834834,-53.4992581169697,-52.9992650504559,-52.4992719839422,
-51.9992789174285,-51.4992858509147,-50.999292784401,-50.4992997178873,
-49.9993066513735,-49.4993135848598,-48.999320518346,-48.4993274518323,
-48.0748388990954),.UNSPECIFIED.);
#1204=B_SPLINE_CURVE_WITH_KNOTS('',3,(#27919,#27920,#27921,#27922,#27923,
#27924,#27925,#27926,#27927,#27928,#27929,#27930,#27931,#27932,#27933,#27934,
#27935,#27936,#27937,#27938,#27939,#27940,#27941,#27942,#27943,#27944,#27945,
#27946,#27947,#27948,#27949,#27950,#27951,#27952,#27953,#27954,#27955,#27956,
#27957,#27958),.UNSPECIFIED.,.F.,.F.,(4,3,3,3,3,3,3,3,3,3,3,3,3,4),(45.101152243795,
45.4993690527499,45.9993621192636,46.4993551857774,46.9993482522911,47.4993413188049,
47.9993343853186,48.4993274518323,48.9993205183461,49.4993135848598,49.9993066513735,
50.4992997178873,50.999292784401,51.3843375509746),.UNSPECIFIED.);
#1205=B_SPLINE_CURVE_WITH_KNOTS('',3,(#27963,#27964,#27965,#27966,#27967,
#27968,#27969,#27970,#27971,#27972,#27973,#27974,#27975,#27976,#27977,#27978,
#27979,#27980,#27981,#27982,#27983,#27984,#27985,#27986,#27987,#27988,#27989,
#27990,#27991,#27992,#27993,#27994,#27995,#27996,#27997,#27998,#27999,#28000,
#28001,#28002,#28003,#28004,#28005),.UNSPECIFIED.,.F.,.F.,(4,3,3,3,3,3,
3,3,3,3,3,3,3,3,4),(-60.6412095134546,-60.499161048162,-59.9991679816482,
-59.4991749151345,-58.9991818486208,-58.499188782107,-57.9991957155933,
-57.4992026490795,-56.9992095825658,-56.4992165160521,-55.9992234495383,
-55.4992303830246,-54.9992373165109,-54.4992442499971,-54.358024206275),
 .UNSPECIFIED.);
#1206=B_SPLINE_CURVE_WITH_KNOTS('',3,(#28006,#28007,#28008,#28009,#28010,
#28011,#28012,#28013,#28014,#28015,#28016,#28017,#28018,#28019,#28020,#28021,
#28022,#28023,#28024,#28025,#28026,#28027,#28028,#28029,#28030,#28031,#28032,
#28033,#28034,#28035,#28036,#28037,#28038,#28039,#28040,#28041,#28042,#28043,
#28044,#28045,#28046,#28047,#28048),.UNSPECIFIED.,.F.,.F.,(4,3,3,3,3,3,
3,3,3,3,3,3,3,3,4),(51.3843375509746,51.4992858509148,51.9992789174285,
52.4992719839422,52.999265050456,53.4992581169697,53.9992511834834,54.4992442499972,
54.9992373165109,55.4992303830246,55.9992234495384,56.4992165160521,56.9992095825658,
57.4992026490796,57.6675228581542),.UNSPECIFIED.);
#1207=B_SPLINE_CURVE_WITH_KNOTS('',3,(#28053,#28054,#28055,#28056,#28057,
#28058,#28059,#28060,#28061,#28062,#28063,#28064,#28065,#28066,#28067,#28068,
#28069,#28070,#28071,#28072,#28073,#28074,#28075,#28076,#28077,#28078,#28079,
#28080,#28081,#28082,#28083,#28084,#28085,#28086,#28087,#28088,#28089,#28090,
#28091,#28092),.UNSPECIFIED.,.F.,.F.,(4,3,3,3,3,3,3,3,3,3,3,3,3,4),(-66.9243948206342,
-66.4990778463268,-65.999084779813,-65.4990917132993,-64.9990986467856,
-64.4991055802718,-63.9991125137581,-63.4991194472444,-62.9991263807306,
-62.4991333142169,-61.9991402477032,-61.4991471811894,-60.9991541146757,
-60.6412095134546),.UNSPECIFIED.);
#1208=B_SPLINE_CURVE_WITH_KNOTS('',3,(#28093,#28094,#28095,#28096,#28097,
#28098,#28099,#28100,#28101,#28102,#28103,#28104,#28105,#28106,#28107,#28108,
#28109,#28110,#28111,#28112,#28113,#28114,#28115,#28116,#28117,#28118,#28119,
#28120,#28121,#28122,#28123,#28124,#28125,#28126,#28127,#28128,#28129,#28130,
#28131,#28132),.UNSPECIFIED.,.F.,.F.,(4,3,3,3,3,3,3,3,3,3,3,3,3,4),(57.6675228581542,
57.9991957155933,58.499188782107,58.9991818486208,59.4991749151345,59.9991679816482,
60.499161048162,60.9991541146757,61.4991471811894,61.9991402477032,62.4991333142169,
62.9991263807307,63.4991194472444,63.9507081653338),.UNSPECIFIED.);
#1209=B_SPLINE_CURVE_WITH_KNOTS('',3,(#28137,#28138,#28139,#28140,#28141,
#28142,#28143,#28144,#28145,#28146,#28147,#28148,#28149,#28150,#28151,#28152,
#28153,#28154,#28155,#28156,#28157,#28158,#28159,#28160,#28161,#28162,#28163,
#28164,#28165,#28166,#28167,#28168,#28169,#28170,#28171,#28172,#28173,#28174,
#28175,#28176,#28177,#28178,#28179),.UNSPECIFIED.,.F.,.F.,(4,3,3,3,3,3,
3,3,3,3,3,3,3,3,4),(-73.2075801278138,-72.9989877110053,-72.4989946444916,
-71.9990015779779,-71.4990085114641,-70.9990154449504,-70.4990223784367,
-69.9990293119229,-69.4990362454092,-68.9990431788954,-68.4990501123817,
-67.999057045868,-67.4990639793542,-66.9990709128405,-66.9243948206342),
 .UNSPECIFIED.);
#1210=B_SPLINE_CURVE_WITH_KNOTS('',3,(#28180,#28181,#28182,#28183,#28184,
#28185,#28186,#28187,#28188,#28189,#28190,#28191,#28192,#28193,#28194,#28195,
#28196,#28197,#28198,#28199,#28200,#28201,#28202,#28203,#28204,#28205,#28206,
#28207,#28208,#28209,#28210,#28211,#28212,#28213,#28214,#28215,#28216,#28217,
#28218,#28219,#28220,#28221,#28222),.UNSPECIFIED.,.F.,.F.,(4,3,3,3,3,3,
3,3,3,3,3,3,3,3,4),(63.9507081653338,63.9991125137581,64.4991055802719,
64.9990986467856,65.4990917132993,65.9990847798131,66.4990778463268,66.9990709128405,
67.4990639793543,67.999057045868,68.4990501123817,68.9990431788954,69.4990362454092,
69.9990293119229,70.2338934725134),.UNSPECIFIED.);
#1211=B_SPLINE_CURVE_WITH_KNOTS('',3,(#28227,#28228,#28229,#28230,#28231,
#28232,#28233,#28234,#28235,#28236,#28237,#28238,#28239,#28240,#28241,#28242,
#28243,#28244,#28245,#28246,#28247,#28248,#28249,#28250,#28251,#28252,#28253,
#28254,#28255,#28256,#28257,#28258,#28259,#28260,#28261,#28262,#28263,#28264,
#28265,#28266),.UNSPECIFIED.,.F.,.F.,(4,3,3,3,3,3,3,3,3,3,3,3,3,4),(-79.4907654349934,
-78.9989045091702,-78.4989114426564,-77.9989183761427,-77.498925309629,
-76.9989322431152,-76.4989391766015,-75.9989461100877,-75.498953043574,
-74.9989599770603,-74.4989669105465,-73.9989738440328,-73.4989807775191,
-73.2075801278138),.UNSPECIFIED.);
#1212=B_SPLINE_CURVE_WITH_KNOTS('',3,(#28267,#28268,#28269,#28270,#28271,
#28272,#28273,#28274,#28275,#28276,#28277,#28278,#28279,#28280,#28281,#28282,
#28283,#28284,#28285,#28286,#28287,#28288,#28289,#28290,#28291,#28292,#28293,
#28294,#28295,#28296,#28297,#28298,#28299,#28300,#28301,#28302,#28303,#28304,
#28305,#28306,#28307,#28308,#28309),.UNSPECIFIED.,.F.,.F.,(4,3,3,3,3,3,
3,3,3,3,3,3,3,3,4),(70.2338934725134,70.4990223784366,70.9990154449504,
71.4990085114641,71.9990015779779,72.4989946444916,72.9989877110053,73.4989807775191,
73.9989738440328,74.4989669105466,74.9989599770603,75.498953043574,75.9989461100878,
76.4989391766015,76.517078779693),.UNSPECIFIED.);
#1213=B_SPLINE_CURVE_WITH_KNOTS('',3,(#28314,#28315,#28316,#28317,#28318,
#28319,#28320,#28321,#28322,#28323,#28324,#28325,#28326,#28327,#28328,#28329,
#28330,#28331,#28332,#28333,#28334,#28335,#28336,#28337,#28338,#28339,#28340,
#28341,#28342,#28343,#28344,#28345,#28346,#28347,#28348,#28349,#28350,#28351,
#28352,#28353,#28354,#28355,#28356),.UNSPECIFIED.,.F.,.F.,(4,3,3,3,3,3,
3,3,3,3,3,3,3,3,4),(-85.773950742173,-85.4988143738487,-84.998821307335,
-84.4988282408213,-83.9988351743075,-83.4988421077938,-82.9988490412801,
-82.4988559747663,-81.9988629082526,-81.4988698417388,-80.9988767752251,
-80.4988837087114,-79.9988906421976,-79.4988975756839,-79.4907654349934),
 .UNSPECIFIED.);
#1214=B_SPLINE_CURVE_WITH_KNOTS('',3,(#28357,#28358,#28359,#28360,#28361,
#28362,#28363,#28364,#28365,#28366,#28367,#28368,#28369,#28370,#28371,#28372,
#28373,#28374,#28375,#28376,#28377,#28378,#28379,#28380,#28381,#28382,#28383,
#28384,#28385,#28386,#28387,#28388,#28389,#28390,#28391,#28392,#28393,#28394,
#28395,#28396),.UNSPECIFIED.,.F.,.F.,(4,3,3,3,3,3,3,3,3,3,3,3,3,4),(76.517078779693,
76.9989322431153,77.498925309629,77.9989183761427,78.4989114426564,78.9989045091702,
79.4988975756839,79.9988906421977,80.4988837087114,80.9988767752251,81.4988698417389,
81.9988629082526,82.4988559747663,82.8002640868726),.UNSPECIFIED.);
#1215=B_SPLINE_CURVE_WITH_KNOTS('',3,(#28401,#28402,#28403,#28404,#28405,
#28406,#28407,#28408,#28409,#28410,#28411,#28412,#28413,#28414,#28415,#28416,
#28417,#28418,#28419,#28420,#28421,#28422,#28423,#28424,#28425,#28426,#28427,
#28428,#28429,#28430,#28431,#28432,#28433,#28434,#28435,#28436,#28437,#28438,
#28439,#28440,#28441,#28442,#28443),.UNSPECIFIED.,.F.,.F.,(4,3,3,3,3,3,
3,3,3,3,3,3,3,3,4),(-92.0571360493526,-91.9987242385273,-91.4987311720135,
-90.9987381054998,-90.4987450389861,-89.9987519724723,-89.4987589059586,
-88.9987658394449,-88.4987727729311,-87.9987797064174,-87.4987866399037,
-86.9987935733899,-86.4988005068762,-85.9988074403625,-85.773950742173),
 .UNSPECIFIED.);
#1216=B_SPLINE_CURVE_WITH_KNOTS('',3,(#28444,#28445,#28446,#28447,#28448,
#28449,#28450,#28451,#28452,#28453,#28454,#28455,#28456,#28457,#28458,#28459,
#28460,#28461,#28462,#28463,#28464,#28465,#28466,#28467,#28468,#28469,#28470,
#28471,#28472,#28473,#28474,#28475,#28476,#28477,#28478,#28479,#28480,#28481,
#28482,#28483,#28484,#28485,#28486),.UNSPECIFIED.,.F.,.F.,(4,3,3,3,3,3,
3,3,3,3,3,3,3,3,4),(82.8002640868726,82.9988490412801,83.4988421077938,
83.9988351743075,84.4988282408213,84.998821307335,85.4988143738488,85.9988074403625,
86.4988005068762,86.99879357339,87.4987866399037,87.9987797064175,88.4987727729312,
88.9987658394449,89.0834493940522),.UNSPECIFIED.);
#1217=B_SPLINE_CURVE_WITH_KNOTS('',3,(#28491,#28492,#28493,#28494,#28495,
#28496,#28497,#28498,#28499,#28500,#28501,#28502,#28503,#28504,#28505,#28506,
#28507,#28508,#28509,#28510,#28511,#28512,#28513,#28514,#28515,#28516,#28517,
#28518,#28519,#28520,#28521,#28522,#28523,#28524,#28525,#28526,#28527,#28528,
#28529,#28530),.UNSPECIFIED.,.F.,.F.,(4,3,3,3,3,3,3,3,3,3,3,3,3,4),(-98.3403213565321,
-97.9986410366921,-97.4986479701784,-96.9986549036646,-96.4986618371509,
-95.9986687706372,-95.4986757041234,-94.9986826376097,-94.4986895710959,
-93.9986965045822,-93.4987034380685,-92.9987103715547,-92.498717305041,
-92.0571360493526),.UNSPECIFIED.);
#1218=B_SPLINE_CURVE_WITH_KNOTS('',3,(#28531,#28532,#28533,#28534,#28535,
#28536,#28537,#28538,#28539,#28540,#28541,#28542,#28543,#28544,#28545,#28546,
#28547,#28548,#28549,#28550,#28551,#28552,#28553,#28554,#28555,#28556,#28557,
#28558,#28559,#28560,#28561,#28562,#28563,#28564,#28565,#28566,#28567,#28568,
#28569,#28570),.UNSPECIFIED.,.F.,.F.,(4,3,3,3,3,3,3,3,3,3,3,3,3,4),(89.0834493940522,
89.4987589059587,89.9987519724724,90.4987450389861,90.9987381054998,91.4987311720136,
91.9987242385273,92.498717305041,92.9987103715548,93.4987034380685,93.9986965045822,
94.498689571096,94.9986826376097,95.3666347012317),.UNSPECIFIED.);
#1219=B_SPLINE_CURVE_WITH_KNOTS('',3,(#28575,#28576,#28577,#28578,#28579,
#28580,#28581,#28582,#28583,#28584,#28585,#28586,#28587,#28588,#28589,#28590,
#28591,#28592,#28593,#28594,#28595,#28596,#28597,#28598,#28599,#28600,#28601,
#28602,#28603,#28604,#28605,#28606,#28607,#28608,#28609,#28610,#28611,#28612,
#28613,#28614,#28615,#28616,#28617),.UNSPECIFIED.,.F.,.F.,(4,3,3,3,3,3,
3,3,3,3,3,3,3,3,4),(-104.623506663712,-104.498550901371,-103.998557834857,
-103.498564768343,-102.998571701829,-102.498578635316,-101.998585568802,
-101.498592502288,-100.998599435775,-100.498606369261,-99.998613302747,
-99.4986202362333,-98.9986271697196,-98.4986341032058,-98.3403213565321),
 .UNSPECIFIED.);
#1220=B_SPLINE_CURVE_WITH_KNOTS('',3,(#28618,#28619,#28620,#28621,#28622,
#28623,#28624,#28625,#28626,#28627,#28628,#28629,#28630,#28631,#28632,#28633,
#28634,#28635,#28636,#28637,#28638,#28639,#28640,#28641,#28642,#28643,#28644,
#28645,#28646,#28647,#28648,#28649,#28650,#28651,#28652,#28653,#28654,#28655,
#28656,#28657,#28658,#28659,#28660),.UNSPECIFIED.,.F.,.F.,(4,3,3,3,3,3,
3,3,3,3,3,3,3,3,4),(95.3666347012317,95.4986757041234,95.9986687706372,
96.4986618371509,96.9986549036646,97.4986479701784,97.9986410366921,98.4986341032058,
98.9986271697196,99.4986202362333,99.9986133027471,100.498606369261,100.998599435775,
101.498592502288,101.649820008411),.UNSPECIFIED.);
#1221=B_SPLINE_CURVE_WITH_KNOTS('',3,(#28665,#28666,#28667,#28668,#28669,
#28670,#28671,#28672,#28673,#28674,#28675,#28676,#28677,#28678,#28679,#28680,
#28681,#28682,#28683,#28684,#28685,#28686,#28687,#28688,#28689,#28690,#28691,
#28692,#28693,#28694,#28695,#28696,#28697,#28698,#28699,#28700,#28701,#28702,
#28703,#28704),.UNSPECIFIED.,.F.,.F.,(4,3,3,3,3,3,3,3,3,3,3,3,3,4),(-110.906691970891,
-110.498467699535,-109.998474633022,-109.498481566508,-108.998488499994,
-108.498495433481,-107.998502366967,-107.498509300453,-106.998516233939,
-106.498523167426,-105.998530100912,-105.498537034398,-104.998543967884,
-104.623506663712),.UNSPECIFIED.);
#1222=B_SPLINE_CURVE_WITH_KNOTS('',3,(#28705,#28706,#28707,#28708,#28709,
#28710,#28711,#28712,#28713,#28714,#28715,#28716,#28717,#28718,#28719,#28720,
#28721,#28722,#28723,#28724,#28725,#28726,#28727,#28728,#28729,#28730,#28731,
#28732,#28733,#28734,#28735,#28736,#28737,#28738,#28739,#28740,#28741,#28742,
#28743,#28744),.UNSPECIFIED.,.F.,.F.,(4,3,3,3,3,3,3,3,3,3,3,3,3,4),(101.649820008411,
101.998585568802,102.498578635316,102.998571701829,103.498564768343,103.998557834857,
104.498550901371,104.998543967884,105.498537034398,105.998530100912,106.498523167426,
106.998516233939,107.498509300453,107.933005315591),.UNSPECIFIED.);
#1223=B_SPLINE_CURVE_WITH_KNOTS('',3,(#28749,#28750,#28751,#28752,#28753,
#28754,#28755,#28756,#28757,#28758,#28759,#28760,#28761,#28762,#28763,#28764,
#28765,#28766,#28767,#28768,#28769,#28770,#28771,#28772,#28773,#28774,#28775,
#28776,#28777,#28778,#28779,#28780,#28781,#28782,#28783,#28784,#28785,#28786,
#28787,#28788,#28789,#28790,#28791),.UNSPECIFIED.,.F.,.F.,(4,3,3,3,3,3,
3,3,3,3,3,3,3,3,4),(-117.189877278071,-116.998377564214,-116.4983844977,
-115.998391431187,-115.498398364673,-114.998405298159,-114.498412231645,
-113.998419165132,-113.498426098618,-112.998433032104,-112.49843996559,
-111.998446899077,-111.498453832563,-110.998460766049,-110.906691970891),
 .UNSPECIFIED.);
#1224=B_SPLINE_CURVE_WITH_KNOTS('',3,(#28792,#28793,#28794,#28795,#28796,
#28797,#28798,#28799,#28800,#28801,#28802,#28803,#28804,#28805,#28806,#28807,
#28808,#28809,#28810,#28811,#28812,#28813,#28814,#28815,#28816,#28817,#28818,
#28819,#28820,#28821,#28822,#28823,#28824,#28825,#28826,#28827,#28828,#28829,
#28830,#28831,#28832,#28833,#28834),.UNSPECIFIED.,.F.,.F.,(4,3,3,3,3,3,
3,3,3,3,3,3,3,3,4),(107.933005315591,107.998502366967,108.498495433481,
108.998488499994,109.498481566508,109.998474633022,110.498467699536,110.998460766049,
111.498453832563,111.998446899077,112.49843996559,112.998433032104,113.498426098618,
113.998419165132,114.216190622771),.UNSPECIFIED.);
#1225=B_SPLINE_CURVE_WITH_KNOTS('',3,(#28839,#28840,#28841,#28842,#28843,
#28844,#28845,#28846,#28847,#28848,#28849,#28850,#28851,#28852,#28853,#28854,
#28855,#28856,#28857,#28858,#28859,#28860,#28861,#28862,#28863,#28864,#28865,
#28866,#28867,#28868,#28869,#28870,#28871,#28872,#28873,#28874,#28875,#28876,
#28877,#28878),.UNSPECIFIED.,.F.,.F.,(4,3,3,3,3,3,3,3,3,3,3,3,3,4),(-123.473062585251,
-122.998294362379,-122.498301295865,-121.998308229351,-121.498315162838,
-120.998322096324,-120.49832902981,-119.998335963296,-119.498342896783,
-118.998349830269,-118.498356763755,-117.998363697241,-117.498370630728,
-117.189877278071),.UNSPECIFIED.);
#1226=B_SPLINE_CURVE_WITH_KNOTS('',3,(#28879,#28880,#28881,#28882,#28883,
#28884,#28885,#28886,#28887,#28888,#28889,#28890,#28891,#28892,#28893,#28894,
#28895,#28896,#28897,#28898,#28899,#28900,#28901,#28902,#28903,#28904,#28905,
#28906,#28907,#28908,#28909,#28910,#28911,#28912,#28913,#28914,#28915,#28916,
#28917,#28918),.UNSPECIFIED.,.F.,.F.,(4,3,3,3,3,3,3,3,3,3,3,3,3,4),(114.216190622771,
114.498412231645,114.998405298159,115.498398364673,115.998391431187,116.4983844977,
116.998377564214,117.498370630728,117.998363697242,118.498356763755,118.998349830269,
119.498342896783,119.998335963296,120.49937592995),.UNSPECIFIED.);
#1227=B_SPLINE_CURVE_WITH_KNOTS('',3,(#28923,#28924,#28925,#28926,#28927,
#28928,#28929,#28930,#28931,#28932,#28933,#28934,#28935,#28936,#28937,#28938,
#28939,#28940,#28941,#28942,#28943,#28944,#28945,#28946,#28947,#28948,#28949,
#28950,#28951,#28952,#28953,#28954,#28955,#28956,#28957,#28958,#28959,#28960,
#28961,#28962,#28963,#28964,#28965),.UNSPECIFIED.,.F.,.F.,(4,3,3,3,3,3,
3,3,3,3,3,3,3,3,4),(-129.75624789243,-129.498204227057,-128.998211160544,
-128.49821809403,-127.998225027516,-127.498231961002,-126.998238894489,
-126.498245827975,-125.998252761461,-125.498259694948,-124.998266628434,
-124.49827356192,-123.998280495406,-123.498287428893,-123.473062585251),
 .UNSPECIFIED.);
#1228=B_SPLINE_CURVE_WITH_KNOTS('',3,(#28966,#28967,#28968,#28969,#28970,
#28971,#28972,#28973,#28974,#28975,#28976,#28977,#28978,#28979,#28980,#28981,
#28982,#28983,#28984,#28985,#28986,#28987,#28988,#28989,#28990,#28991,#28992,
#28993,#28994,#28995,#28996,#28997,#28998,#28999,#29000,#29001,#29002,#29003,
#29004,#29005),.UNSPECIFIED.,.F.,.F.,(4,3,3,3,3,3,3,3,3,3,3,3,3,4),(120.49937592995,
120.998322096324,121.498315162838,121.998308229351,122.498301295865,122.998294362379,
123.498287428893,123.998280495406,124.49827356192,124.998266628434,125.498259694948,
125.998252761461,126.498245827975,126.78256123713),.UNSPECIFIED.);
#1229=B_SPLINE_CURVE_WITH_KNOTS('',3,(#29010,#29011,#29012,#29013,#29014,
#29015,#29016,#29017,#29018,#29019,#29020,#29021,#29022,#29023,#29024,#29025,
#29026,#29027,#29028,#29029,#29030,#29031,#29032,#29033,#29034,#29035,#29036,
#29037,#29038,#29039,#29040,#29041,#29042,#29043,#29044,#29045,#29046,#29047,
#29048,#29049,#29050,#29051,#29052),.UNSPECIFIED.,.F.,.F.,(4,3,3,3,3,3,
3,3,3,3,3,3,3,3,4),(-136.03943319961,-135.998114091736,-135.498121025222,
-134.998127958708,-134.498134892195,-133.998141825681,-133.498148759167,
-132.998155692654,-132.49816262614,-131.998169559626,-131.498176493112,
-130.998183426599,-130.498190360085,-129.998197293571,-129.75624789243),
 .UNSPECIFIED.);
#1230=B_SPLINE_CURVE_WITH_KNOTS('',3,(#29053,#29054,#29055,#29056,#29057,
#29058,#29059,#29060,#29061,#29062,#29063,#29064,#29065,#29066,#29067,#29068,
#29069,#29070,#29071,#29072,#29073,#29074,#29075,#29076,#29077,#29078,#29079,
#29080,#29081,#29082,#29083,#29084,#29085,#29086,#29087,#29088,#29089,#29090,
#29091,#29092,#29093,#29094,#29095),.UNSPECIFIED.,.F.,.F.,(4,3,3,3,3,3,
3,3,3,3,3,3,3,3,4),(126.78256123713,126.998238894489,127.498231961003,127.998225027516,
128.49821809403,128.998211160544,129.498204227057,129.998197293571,130.498190360085,
130.998183426599,131.498176493112,131.998169559626,132.49816262614,132.998155692654,
133.065746544309),.UNSPECIFIED.);
#1231=B_SPLINE_CURVE_WITH_KNOTS('',3,(#29100,#29101,#29102,#29103,#29104,
#29105,#29106,#29107,#29108,#29109,#29110,#29111,#29112,#29113,#29114,#29115,
#29116,#29117,#29118,#29119,#29120,#29121,#29122,#29123,#29124,#29125,#29126,
#29127,#29128,#29129,#29130,#29131,#29132,#29133,#29134,#29135,#29136,#29137,
#29138,#29139),.UNSPECIFIED.,.F.,.F.,(4,3,3,3,3,3,3,3,3,3,3,3,3,4),(-142.322618506789,
-141.998030889901,-141.498037823387,-140.998044756873,-140.49805169036,
-139.998058623846,-139.498065557332,-138.998072490818,-138.498079424305,
-137.998086357791,-137.498093291277,-136.998100224763,-136.49810715825,
-136.03943319961),.UNSPECIFIED.);
#1232=B_SPLINE_CURVE_WITH_KNOTS('',3,(#29140,#29141,#29142,#29143,#29144,
#29145,#29146,#29147,#29148,#29149,#29150,#29151,#29152,#29153,#29154,#29155,
#29156,#29157,#29158,#29159,#29160,#29161,#29162,#29163,#29164,#29165,#29166,
#29167,#29168,#29169,#29170,#29171,#29172,#29173,#29174,#29175,#29176,#29177,
#29178,#29179),.UNSPECIFIED.,.F.,.F.,(4,3,3,3,3,3,3,3,3,3,3,3,3,4),(133.065746544309,
133.498148759167,133.998141825681,134.498134892195,134.998127958709,135.498121025222,
135.998114091736,136.49810715825,136.998100224763,137.498093291277,137.998086357791,
138.498079424305,138.998072490818,139.348931851489),.UNSPECIFIED.);
#1233=B_SPLINE_CURVE_WITH_KNOTS('',3,(#29184,#29185,#29186,#29187,#29188,
#29189,#29190,#29191,#29192,#29193,#29194,#29195,#29196,#29197,#29198,#29199,
#29200,#29201,#29202,#29203,#29204,#29205,#29206,#29207,#29208,#29209,#29210,
#29211,#29212,#29213,#29214,#29215,#29216,#29217,#29218,#29219,#29220,#29221,
#29222,#29223,#29224,#29225,#29226),.UNSPECIFIED.,.F.,.F.,(4,3,3,3,3,3,
3,3,3,3,3,3,3,3,4),(-148.605803813969,-148.497940754579,-147.997947688066,
-147.497954621552,-146.997961555038,-146.497968488524,-145.997975422011,
-145.497982355497,-144.997989288983,-144.497996222469,-143.998003155956,
-143.498010089442,-142.998017022928,-142.498023956414,-142.322618506789),
 .UNSPECIFIED.);
#1234=B_SPLINE_CURVE_WITH_KNOTS('',3,(#29227,#29228,#29229,#29230,#29231,
#29232,#29233,#29234,#29235,#29236,#29237,#29238,#29239,#29240,#29241,#29242,
#29243,#29244,#29245,#29246,#29247,#29248,#29249,#29250,#29251,#29252,#29253,
#29254,#29255,#29256,#29257,#29258,#29259,#29260,#29261,#29262,#29263,#29264,
#29265,#29266,#29267,#29268,#29269),.UNSPECIFIED.,.F.,.F.,(4,3,3,3,3,3,
3,3,3,3,3,3,3,3,4),(139.348931851489,139.498065557332,139.998058623846,
140.49805169036,140.998044756873,141.498037823387,141.998030889901,142.498023956415,
142.998017022928,143.498010089442,143.998003155956,144.497996222469,144.997989288983,
145.497982355497,145.632117158668),.UNSPECIFIED.);
#1235=B_SPLINE_CURVE_WITH_KNOTS('',3,(#29274,#29275,#29276,#29277,#29278,
#29279,#29280,#29281,#29282,#29283,#29284,#29285,#29286,#29287,#29288,#29289,
#29290,#29291,#29292,#29293,#29294,#29295,#29296,#29297,#29298,#29299,#29300,
#29301,#29302,#29303,#29304,#29305,#29306,#29307,#29308,#29309,#29310,#29311,
#29312,#29313),.UNSPECIFIED.,.F.,.F.,(4,3,3,3,3,3,3,3,3,3,3,3,3,4),(-154.888989121148,
-154.497857552744,-153.99786448623,-153.497871419717,-152.997878353203,
-152.497885286689,-151.997892220175,-151.497899153662,-150.997906087148,
-150.497913020634,-149.997919954121,-149.497926887607,-148.997933821093,
-148.605803813969),.UNSPECIFIED.);
#1236=B_SPLINE_CURVE_WITH_KNOTS('',3,(#29314,#29315,#29316,#29317,#29318,
#29319,#29320,#29321,#29322,#29323,#29324,#29325,#29326,#29327,#29328,#29329,
#29330,#29331,#29332,#29333,#29334,#29335,#29336,#29337,#29338,#29339,#29340,
#29341,#29342,#29343,#29344,#29345,#29346,#29347,#29348,#29349,#29350,#29351,
#29352,#29353),.UNSPECIFIED.,.F.,.F.,(4,3,3,3,3,3,3,3,3,3,3,3,3,4),(145.632117158668,
145.997975422011,146.497968488524,146.997961555038,147.497954621552,147.997947688066,
148.497940754579,148.997933821093,149.497926887607,149.997919954121,150.497913020634,
150.997906087148,151.497899153662,151.915302465848),.UNSPECIFIED.);
#1237=B_SPLINE_CURVE_WITH_KNOTS('',3,(#29358,#29359,#29360,#29361,#29362,
#29363,#29364,#29365,#29366,#29367,#29368,#29369,#29370,#29371,#29372,#29373,
#29374,#29375,#29376,#29377,#29378,#29379,#29380,#29381,#29382,#29383,#29384,
#29385,#29386,#29387,#29388,#29389,#29390,#29391,#29392,#29393,#29394,#29395,
#29396,#29397,#29398,#29399,#29400),.UNSPECIFIED.,.F.,.F.,(4,3,3,3,3,3,
3,3,3,3,3,3,3,3,4),(-161.172174428328,-160.997767417423,-160.497774350909,
-159.997781284395,-159.497788217882,-158.997795151368,-158.497802084854,
-157.99780901834,-157.497815951827,-156.997822885313,-156.497829818799,
-155.997836752285,-155.497843685772,-154.997850619258,-154.888989121148),
 .UNSPECIFIED.);
#1238=B_SPLINE_CURVE_WITH_KNOTS('',3,(#29401,#29402,#29403,#29404,#29405,
#29406,#29407,#29408,#29409,#29410,#29411,#29412,#29413,#29414,#29415,#29416,
#29417,#29418,#29419,#29420,#29421,#29422,#29423,#29424,#29425,#29426,#29427,
#29428,#29429,#29430,#29431,#29432,#29433,#29434,#29435,#29436,#29437,#29438,
#29439,#29440,#29441,#29442,#29443),.UNSPECIFIED.,.F.,.F.,(4,3,3,3,3,3,
3,3,3,3,3,3,3,3,4),(151.915302465848,151.997892220175,152.497885286689,
152.997878353203,153.497871419717,153.99786448623,154.497857552744,154.997850619258,
155.497843685772,155.997836752285,156.497829818799,156.997822885313,157.497815951827,
157.99780901834,158.198487773028),.UNSPECIFIED.);
#1239=B_SPLINE_CURVE_WITH_KNOTS('',3,(#29448,#29449,#29450,#29451,#29452,
#29453,#29454,#29455,#29456,#29457,#29458,#29459,#29460,#29461,#29462,#29463,
#29464,#29465,#29466,#29467,#29468,#29469,#29470,#29471,#29472,#29473,#29474,
#29475,#29476,#29477,#29478,#29479,#29480,#29481,#29482,#29483,#29484,#29485,
#29486,#29487),.UNSPECIFIED.,.F.,.F.,(4,3,3,3,3,3,3,3,3,3,3,3,3,4),(-167.455359735507,
-166.997684215588,-166.497691149074,-165.99769808256,-165.497705016046,
-164.997711949533,-164.497718883019,-163.997725816505,-163.497732749991,
-162.997739683478,-162.497746616964,-161.99775355045,-161.497760483937,
-161.172174428328),.UNSPECIFIED.);
#1240=B_SPLINE_CURVE_WITH_KNOTS('',3,(#29488,#29489,#29490,#29491,#29492,
#29493,#29494,#29495,#29496,#29497,#29498,#29499,#29500,#29501,#29502,#29503,
#29504,#29505,#29506,#29507,#29508,#29509,#29510,#29511,#29512,#29513,#29514,
#29515,#29516,#29517,#29518,#29519,#29520,#29521,#29522,#29523,#29524,#29525,
#29526,#29527),.UNSPECIFIED.,.F.,.F.,(4,3,3,3,3,3,3,3,3,3,3,3,3,4),(158.198487773028,
158.497802084854,158.997795151368,159.497788217882,159.997781284395,160.497774350909,
160.997767417423,161.497760483937,161.99775355045,162.497746616964,162.997739683478,
163.497732749991,163.997725816505,164.481673080207),.UNSPECIFIED.);
#1241=B_SPLINE_CURVE_WITH_KNOTS('',3,(#29532,#29533,#29534,#29535,#29536,
#29537,#29538,#29539,#29540,#29541,#29542,#29543,#29544,#29545,#29546,#29547,
#29548,#29549,#29550,#29551,#29552,#29553,#29554,#29555,#29556,#29557,#29558,
#29559,#29560,#29561,#29562,#29563,#29564,#29565,#29566,#29567,#29568,#29569,
#29570,#29571,#29572,#29573,#29574),.UNSPECIFIED.,.F.,.F.,(4,3,3,3,3,3,
3,3,3,3,3,3,3,3,4),(-173.738545042687,-173.497594080266,-172.997601013752,
-172.497607947239,-171.997614880725,-171.497621814211,-170.997628747697,
-170.497635681184,-169.99764261467,-169.497649548156,-168.997656481642,
-168.497663415129,-167.997670348615,-167.497677282101,-167.455359735507),
 .UNSPECIFIED.);
#1242=B_SPLINE_CURVE_WITH_KNOTS('',3,(#29575,#29576,#29577,#29578,#29579,
#29580,#29581,#29582,#29583,#29584,#29585,#29586,#29587,#29588,#29589,#29590,
#29591,#29592,#29593,#29594,#29595,#29596,#29597,#29598,#29599,#29600,#29601,
#29602,#29603,#29604,#29605,#29606,#29607,#29608,#29609,#29610,#29611,#29612,
#29613,#29614,#29615,#29616,#29617),.UNSPECIFIED.,.F.,.F.,(4,3,3,3,3,3,
3,3,3,3,3,3,3,3,4),(164.481673080207,164.497718883019,164.997711949533,
165.497705016046,165.99769808256,166.497691149074,166.997684215588,167.497677282101,
167.997670348615,168.497663415129,168.997656481643,169.497649548156,169.99764261467,
170.497635681184,170.764858387387),.UNSPECIFIED.);
#1243=B_SPLINE_CURVE_WITH_KNOTS('',3,(#29622,#29623,#29624,#29625,#29626,
#29627,#29628,#29629,#29630,#29631,#29632,#29633,#29634,#29635,#29636,#29637,
#29638,#29639,#29640,#29641,#29642,#29643,#29644,#29645,#29646,#29647,#29648,
#29649,#29650,#29651,#29652,#29653,#29654,#29655,#29656,#29657,#29658,#29659,
#29660,#29661,#29662,#29663,#29664),.UNSPECIFIED.,.F.,.F.,(4,3,3,3,3,3,
3,3,3,3,3,3,3,3,4),(-180.021730349867,-179.997503944945,-179.497510878431,
-178.997517811917,-178.497524745403,-177.99753167889,-177.497538612376,
-176.997545545862,-176.497552479348,-175.997559412835,-175.497566346321,
-174.997573279807,-174.497580213294,-173.99758714678,-173.738545042687),
 .UNSPECIFIED.);
#1244=B_SPLINE_CURVE_WITH_KNOTS('',3,(#29665,#29666,#29667,#29668,#29669,
#29670,#29671,#29672,#29673,#29674,#29675,#29676,#29677,#29678,#29679,#29680,
#29681,#29682,#29683,#29684,#29685,#29686,#29687,#29688,#29689,#29690,#29691,
#29692,#29693,#29694,#29695,#29696,#29697,#29698,#29699,#29700,#29701,#29702,
#29703,#29704,#29705,#29706,#29707),.UNSPECIFIED.,.F.,.F.,(4,3,3,3,3,3,
3,3,3,3,3,3,3,3,4),(170.764858387387,170.997628747697,171.497621814211,
171.997614880725,172.497607947239,172.997601013752,173.497594080266,173.99758714678,
174.497580213294,174.997573279807,175.497566346321,175.997559412835,176.497552479349,
176.997545545862,177.048043694566),.UNSPECIFIED.);
#1245=B_SPLINE_CURVE_WITH_KNOTS('',3,(#29712,#29713,#29714,#29715,#29716,
#29717,#29718,#29719,#29720,#29721,#29722,#29723,#29724,#29725,#29726,#29727,
#29728,#29729,#29730,#29731,#29732,#29733,#29734,#29735,#29736,#29737,#29738,
#29739,#29740,#29741,#29742,#29743,#29744,#29745,#29746,#29747,#29748,#29749,
#29750,#29751),.UNSPECIFIED.,.F.,.F.,(4,3,3,3,3,3,3,3,3,3,3,3,3,4),(-186.304915657046,
-185.997420743109,-185.497427676596,-184.997434610082,-184.497441543568,
-183.997448477055,-183.497455410541,-182.997462344027,-182.497469277513,
-181.997476211,-181.497483144486,-180.997490077972,-180.497497011458,-180.021730349867),
 .UNSPECIFIED.);
#1246=B_SPLINE_CURVE_WITH_KNOTS('',3,(#29752,#29753,#29754,#29755,#29756,
#29757,#29758,#29759,#29760,#29761,#29762,#29763,#29764,#29765,#29766,#29767,
#29768,#29769,#29770,#29771,#29772,#29773,#29774,#29775,#29776,#29777,#29778,
#29779,#29780,#29781,#29782,#29783,#29784,#29785,#29786,#29787,#29788,#29789,
#29790,#29791),.UNSPECIFIED.,.F.,.F.,(4,3,3,3,3,3,3,3,3,3,3,3,3,4),(177.048043694566,
177.497538612376,177.99753167889,178.497524745403,178.997517811917,179.497510878431,
179.997503944945,180.497497011458,180.997490077972,181.497483144486,181.997476211,
182.497469277513,182.997462344027,183.331229001746),.UNSPECIFIED.);
#1247=B_SPLINE_CURVE_WITH_KNOTS('',3,(#29796,#29797,#29798,#29799,#29800,
#29801,#29802,#29803,#29804,#29805,#29806,#29807,#29808,#29809,#29810,#29811,
#29812,#29813,#29814,#29815,#29816,#29817,#29818,#29819,#29820,#29821,#29822,
#29823,#29824,#29825,#29826,#29827,#29828,#29829,#29830,#29831,#29832,#29833,
#29834,#29835,#29836,#29837,#29838),.UNSPECIFIED.,.F.,.F.,(4,3,3,3,3,3,
3,3,3,3,3,3,3,3,4),(-192.588100964226,-192.497330607788,-191.997337541274,
-191.497344474761,-190.997351408247,-190.497358341733,-189.997365275219,
-189.497372208706,-188.997379142192,-188.497386075678,-187.997393009164,
-187.497399942651,-186.997406876137,-186.497413809623,-186.304915657046),
 .UNSPECIFIED.);
#1248=B_SPLINE_CURVE_WITH_KNOTS('',3,(#29839,#29840,#29841,#29842,#29843,
#29844,#29845,#29846,#29847,#29848,#29849,#29850,#29851,#29852,#29853,#29854,
#29855,#29856,#29857,#29858,#29859,#29860,#29861,#29862,#29863,#29864,#29865,
#29866,#29867,#29868,#29869,#29870,#29871,#29872,#29873,#29874,#29875,#29876,
#29877,#29878,#29879,#29880,#29881),.UNSPECIFIED.,.F.,.F.,(4,3,3,3,3,3,
3,3,3,3,3,3,3,3,4),(183.331229001746,183.497455410541,183.997448477055,
184.497441543568,184.997434610082,185.497427676596,185.99742074311,186.497413809623,
186.997406876137,187.497399942651,187.997393009164,188.497386075678,188.997379142192,
189.497372208706,189.614414308925),.UNSPECIFIED.);
#1249=B_SPLINE_CURVE_WITH_KNOTS('',3,(#29886,#29887,#29888,#29889,#29890,
#29891,#29892,#29893,#29894,#29895,#29896,#29897,#29898,#29899,#29900,#29901,
#29902,#29903,#29904,#29905,#29906,#29907,#29908,#29909,#29910,#29911,#29912,
#29913,#29914,#29915,#29916,#29917,#29918,#29919,#29920,#29921,#29922,#29923,
#29924,#29925),.UNSPECIFIED.,.F.,.F.,(4,3,3,3,3,3,3,3,3,3,3,3,3,4),(-198.871286271405,
-198.497247405953,-197.997254339439,-197.497261272925,-196.997268206412,
-196.497275139898,-195.997282073384,-195.49728900687,-194.997295940357,
-194.497302873843,-193.997309807329,-193.497316740816,-192.997323674302,
-192.588100964226),.UNSPECIFIED.);
#1250=B_SPLINE_CURVE_WITH_KNOTS('',3,(#29926,#29927,#29928,#29929,#29930,
#29931,#29932,#29933,#29934,#29935,#29936,#29937,#29938,#29939,#29940,#29941,
#29942,#29943,#29944,#29945,#29946,#29947,#29948,#29949,#29950,#29951,#29952,
#29953,#29954,#29955,#29956,#29957,#29958,#29959,#29960,#29961,#29962,#29963,
#29964,#29965),.UNSPECIFIED.,.F.,.F.,(4,3,3,3,3,3,3,3,3,3,3,3,3,4),(189.614414308925,
189.997365275219,190.497358341733,190.997351408247,191.497344474761,191.997337541274,
192.497330607788,192.997323674302,193.497316740816,193.997309807329,194.497302873843,
194.997295940357,195.49728900687,195.897599616105),.UNSPECIFIED.);
#1251=B_SPLINE_CURVE_WITH_KNOTS('',3,(#29970,#29971,#29972,#29973,#29974,
#29975,#29976,#29977,#29978,#29979,#29980,#29981,#29982,#29983,#29984,#29985,
#29986,#29987,#29988,#29989,#29990,#29991,#29992,#29993,#29994,#29995,#29996,
#29997,#29998,#29999,#30000,#30001,#30002,#30003,#30004,#30005,#30006,#30007,
#30008,#30009,#30010,#30011,#30012),.UNSPECIFIED.,.F.,.F.,(4,3,3,3,3,3,
3,3,3,3,3,3,3,3,4),(-205.154471578585,-204.997157270631,-204.497164204118,
-203.997171137604,-203.49717807109,-202.997185004576,-202.497191938063,
-201.997198871549,-201.497205805035,-200.997212738522,-200.497219672008,
-199.997226605494,-199.49723353898,-198.997240472467,-198.871286271405),
 .UNSPECIFIED.);
#1252=B_SPLINE_CURVE_WITH_KNOTS('',3,(#30013,#30014,#30015,#30016,#30017,
#30018,#30019,#30020,#30021,#30022,#30023,#30024,#30025,#30026,#30027,#30028,
#30029,#30030,#30031,#30032,#30033,#30034,#30035,#30036,#30037,#30038,#30039,
#30040,#30041,#30042,#30043,#30044,#30045,#30046,#30047,#30048,#30049,#30050,
#30051,#30052,#30053,#30054,#30055),.UNSPECIFIED.,.F.,.F.,(4,3,3,3,3,3,
3,3,3,3,3,3,3,3,4),(195.897599616105,195.997282073384,196.497275139898,
196.997268206412,197.497261272925,197.997254339439,198.497247405953,198.997240472467,
199.49723353898,199.997226605494,200.497219672008,200.997212738522,201.497205805035,
201.997198871549,202.180784923285),.UNSPECIFIED.);
#1253=B_SPLINE_CURVE_WITH_KNOTS('',3,(#30060,#30061,#30062,#30063,#30064,
#30065,#30066,#30067,#30068,#30069,#30070,#30071,#30072,#30073,#30074,#30075,
#30076,#30077,#30078,#30079,#30080,#30081,#30082,#30083,#30084,#30085,#30086,
#30087,#30088,#30089,#30090,#30091,#30092,#30093,#30094,#30095,#30096,#30097,
#30098,#30099),.UNSPECIFIED.,.F.,.F.,(4,3,3,3,3,3,3,3,3,3,3,3,3,4),(-211.437656885764,
-210.997074068796,-210.497081002283,-209.997087935769,-209.497094869255,
-208.997101802741,-208.497108736228,-207.997115669714,-207.4971226032,-206.997129536686,
-206.497136470173,-205.997143403659,-205.497150337145,-205.154471578585),
 .UNSPECIFIED.);
#1254=B_SPLINE_CURVE_WITH_KNOTS('',3,(#30100,#30101,#30102,#30103,#30104,
#30105,#30106,#30107,#30108,#30109,#30110,#30111,#30112,#30113,#30114,#30115,
#30116,#30117,#30118,#30119,#30120,#30121,#30122,#30123,#30124,#30125,#30126,
#30127,#30128,#30129,#30130,#30131,#30132,#30133,#30134,#30135,#30136,#30137,
#30138,#30139),.UNSPECIFIED.,.F.,.F.,(4,3,3,3,3,3,3,3,3,3,3,3,3,4),(202.180784923285,
202.497191938063,202.997185004576,203.49717807109,203.997171137604,204.497164204118,
204.997157270631,205.497150337145,205.997143403659,206.497136470173,206.997129536686,
207.4971226032,207.997115669714,208.463970230464),.UNSPECIFIED.);
#1255=B_SPLINE_CURVE_WITH_KNOTS('',3,(#30145,#30146,#30147,#30148,#30149,
#30150,#30151,#30152,#30153),.UNSPECIFIED.,.F.,.F.,(4,1,1,1,1,1,4),(223.053078404875,
223.112488654421,223.612481720935,224.112474787448,224.612467853962,225.112460920476,
225.542622064258),.UNSPECIFIED.);
#1256=B_SPLINE_CURVE_WITH_KNOTS('',3,(#30156,#30157,#30158,#30159,#30160,
#30161),.UNSPECIFIED.,.F.,.F.,(4,1,1,4),(223.053078404875,223.302941468138,
223.802934534652,224.302927601166),.UNSPECIFIED.);
#1257=B_SPLINE_CURVE_WITH_KNOTS('',3,(#30166,#30167,#30168,#30169,#30170,
#30171,#30172,#30173,#30174,#30175,#30176,#30177,#30178,#30179,#30180,#30181),
 .UNSPECIFIED.,.F.,.F.,(4,1,1,1,1,1,1,1,1,1,1,1,1,4),(216.769893097696,
217.112571856256,217.61256492277,218.112557989284,218.612551055797,219.112544122311,
219.612537188825,220.112530255338,220.612523321852,221.112516388366,221.61250945488,
222.112502521393,222.612495587907,223.053078404875),.UNSPECIFIED.);
#1258=B_SPLINE_CURVE_WITH_KNOTS('',3,(#30182,#30183,#30184,#30185,#30186,
#30187,#30188,#30189,#30190,#30191,#30192,#30193,#30194,#30195,#30196,#30197,
#30198),.UNSPECIFIED.,.F.,.F.,(4,1,1,1,1,1,1,1,1,1,1,1,1,1,4),(216.769893097696,
216.80303160346,217.303024669973,217.803017736487,218.303010803001,218.803003869514,
219.302996936028,219.802990002542,220.302983069056,220.802976135569,221.302969202083,
221.802962268597,222.302955335111,222.802948401624,223.053078404875),
 .UNSPECIFIED.);
#1259=B_SPLINE_CURVE_WITH_KNOTS('',3,(#30203,#30204,#30205,#30206,#30207,
#30208,#30209,#30210,#30211,#30212,#30213,#30214,#30215,#30216,#30217,#30218,
#30219),.UNSPECIFIED.,.F.,.F.,(4,1,1,1,1,1,1,1,1,1,1,1,1,1,4),(210.486707790516,
210.612661991577,211.112655058091,211.612648124605,212.112641191119,212.612634257632,
213.112627324146,213.61262039066,214.112613457174,214.612606523687,215.112599590201,
215.612592656715,216.112585723229,216.612578789742,216.769893097696),
 .UNSPECIFIED.);
#1260=B_SPLINE_CURVE_WITH_KNOTS('',3,(#30220,#30221,#30222,#30223,#30224,
#30225,#30226,#30227,#30228,#30229,#30230,#30231,#30232,#30233,#30234,#30235),
 .UNSPECIFIED.,.F.,.F.,(4,1,1,1,1,1,1,1,1,1,1,1,1,4),(210.486707790516,
210.803114805295,211.303107871808,211.803100938322,212.303094004836,212.80308707135,
213.303080137863,213.803073204377,214.303066270891,214.803059337405,215.303052403918,
215.803045470432,216.303038536946,216.769893097696),.UNSPECIFIED.);
#1261=B_SPLINE_CURVE_WITH_KNOTS('',3,(#30240,#30241,#30242,#30243,#30244,
#30245,#30246,#30247,#30248,#30249,#30250,#30251,#30252,#30253,#30254,#30255),
 .UNSPECIFIED.,.F.,.F.,(4,1,1,1,1,1,1,1,1,1,1,1,1,4),(204.203522483337,
204.612745193413,205.112738259926,205.61273132644,206.112724392954,206.612717459468,
207.112710525981,207.612703592495,208.112696659009,208.612689725523,209.112682792036,
209.61267585855,210.112668925064,210.486707790516),.UNSPECIFIED.);
#1262=B_SPLINE_CURVE_WITH_KNOTS('',3,(#30256,#30257,#30258,#30259,#30260,
#30261,#30262,#30263,#30264,#30265,#30266,#30267,#30268,#30269,#30270,#30271,
#30272),.UNSPECIFIED.,.F.,.F.,(4,1,1,1,1,1,1,1,1,1,1,1,1,1,4),(204.203522483337,
204.303204940616,204.80319800713,205.303191073644,205.803184140157,206.303177206671,
206.803170273185,207.303163339699,207.803156406212,208.303149472726,208.80314253924,
209.303135605754,209.803128672267,210.303121738781,210.486707790516),
 .UNSPECIFIED.);
#1263=B_SPLINE_CURVE_WITH_KNOTS('',3,(#30277,#30278,#30279,#30280,#30281,
#30282,#30283,#30284,#30285,#30286,#30287,#30288,#30289,#30290,#30291,#30292,
#30293),.UNSPECIFIED.,.F.,.F.,(4,1,1,1,1,1,1,1,1,1,1,1,1,1,4),(197.920337176157,
198.112835328734,198.612828395248,199.112821461762,199.612814528275,200.112807594789,
200.612800661303,201.112793727816,201.61278679433,202.112779860844,202.612772927358,
203.112765993871,203.612759060385,204.112752126899,204.203522483337),
 .UNSPECIFIED.);
#1264=B_SPLINE_CURVE_WITH_KNOTS('',3,(#30294,#30295,#30296,#30297,#30298,
#30299,#30300,#30301,#30302,#30303,#30304,#30305,#30306,#30307,#30308,#30309),
 .UNSPECIFIED.,.F.,.F.,(4,1,1,1,1,1,1,1,1,1,1,1,1,4),(197.920337176157,
198.303288142451,198.803281208965,199.303274275479,199.803267341993,200.303260408506,
200.80325347502,201.303246541534,201.803239608047,202.303232674561,202.803225741075,
203.303218807589,203.803211874102,204.203522483337),.UNSPECIFIED.);
#1265=B_SPLINE_CURVE_WITH_KNOTS('',3,(#30314,#30315,#30316,#30317,#30318,
#30319,#30320,#30321,#30322,#30323,#30324,#30325,#30326,#30327,#30328,#30329),
 .UNSPECIFIED.,.F.,.F.,(4,1,1,1,1,1,1,1,1,1,1,1,1,4),(191.637151868977,
192.112918530569,192.612911597083,193.112904663597,193.61289773011,194.112890796624,
194.612883863138,195.112876929652,195.612869996165,196.112863062679,196.612856129193,
197.112849195707,197.61284226222,197.920337176157),.UNSPECIFIED.);
#1266=B_SPLINE_CURVE_WITH_KNOTS('',3,(#30330,#30331,#30332,#30333,#30334,
#30335,#30336,#30337,#30338,#30339,#30340,#30341,#30342,#30343,#30344,#30345,
#30346),.UNSPECIFIED.,.F.,.F.,(4,1,1,1,1,1,1,1,1,1,1,1,1,1,4),(191.637151868977,
191.803378277773,192.303371344287,192.8033644108,193.303357477314,193.803350543828,
194.303343610341,194.803336676855,195.303329743369,195.803322809883,196.303315876396,
196.80330894291,197.303302009424,197.803295075938,197.920337176157),
 .UNSPECIFIED.);
#1267=B_SPLINE_CURVE_WITH_KNOTS('',3,(#30351,#30352,#30353,#30354,#30355,
#30356,#30357,#30358,#30359,#30360,#30361,#30362,#30363,#30364,#30365,#30366,
#30367),.UNSPECIFIED.,.F.,.F.,(4,1,1,1,1,1,1,1,1,1,1,1,1,1,4),(185.353966561798,
185.613008665891,186.113001732404,186.612994798918,187.112987865432,187.612980931946,
188.112973998459,188.612967064973,189.112960131487,189.612953198001,190.112946264514,
190.612939331028,191.112932397542,191.612925464056,191.637151868977),
 .UNSPECIFIED.);
#1268=B_SPLINE_CURVE_WITH_KNOTS('',3,(#30368,#30369,#30370,#30371,#30372,
#30373,#30374,#30375,#30376,#30377,#30378,#30379,#30380,#30381,#30382,#30383),
 .UNSPECIFIED.,.F.,.F.,(4,1,1,1,1,1,1,1,1,1,1,1,1,4),(185.353966561798,
185.803461479608,186.303454546122,186.803447612635,187.303440679149,187.803433745663,
188.303426812177,188.80341987869,189.303412945204,189.803406011718,190.303399078232,
190.803392144745,191.303385211259,191.637151868977),.UNSPECIFIED.);
#1269=B_SPLINE_CURVE_WITH_KNOTS('',3,(#30388,#30389,#30390,#30391,#30392,
#30393,#30394,#30395,#30396,#30397,#30398,#30399,#30400,#30401,#30402,#30403,
#30404),.UNSPECIFIED.,.F.,.F.,(4,1,1,1,1,1,1,1,1,1,1,1,1,1,4),(179.070781254618,
179.113098801212,179.613091867726,180.11308493424,180.613078000753,181.113071067267,
181.613064133781,182.113057200295,182.613050266808,183.113043333322,183.613036399836,
184.11302946635,184.613022532863,185.113015599377,185.353966561798),
 .UNSPECIFIED.);
#1270=B_SPLINE_CURVE_WITH_KNOTS('',3,(#30405,#30406,#30407,#30408,#30409,
#30410,#30411,#30412,#30413,#30414,#30415,#30416,#30417,#30418,#30419,#30420,
#30421),.UNSPECIFIED.,.F.,.F.,(4,1,1,1,1,1,1,1,1,1,1,1,1,1,4),(179.070781254618,
179.303551614929,179.803544681443,180.303537747957,180.803530814471,181.303523880984,
181.803516947498,182.303510014012,182.803503080526,183.303496147039,183.803489213553,
184.303482280067,184.803475346581,185.303468413094,185.353966561798),
 .UNSPECIFIED.);
#1271=B_SPLINE_CURVE_WITH_KNOTS('',3,(#30426,#30427,#30428,#30429,#30430,
#30431,#30432,#30433,#30434,#30435,#30436,#30437,#30438,#30439,#30440,#30441),
 .UNSPECIFIED.,.F.,.F.,(4,1,1,1,1,1,1,1,1,1,1,1,1,4),(172.787595947439,
173.113182003047,173.613175069561,174.113168136075,174.613161202589,175.113154269102,
175.613147335616,176.11314040213,176.613133468643,177.113126535157,177.613119601671,
178.113112668185,178.613105734698,179.070781254618),.UNSPECIFIED.);
#1272=B_SPLINE_CURVE_WITH_KNOTS('',3,(#30442,#30443,#30444,#30445,#30446,
#30447,#30448,#30449,#30450,#30451,#30452,#30453,#30454,#30455,#30456,#30457,
#30458),.UNSPECIFIED.,.F.,.F.,(4,1,1,1,1,1,1,1,1,1,1,1,1,1,4),(172.787595947439,
172.803641750251,173.303634816765,173.803627883278,174.303620949792,174.803614016306,
175.30360708282,175.803600149333,176.303593215847,176.803586282361,177.303579348874,
177.803572415388,178.303565481902,178.803558548416,179.070781254618),
 .UNSPECIFIED.);
#1273=B_SPLINE_CURVE_WITH_KNOTS('',3,(#30463,#30464,#30465,#30466,#30467,
#30468,#30469,#30470,#30471,#30472,#30473,#30474,#30475,#30476,#30477,#30478,
#30479),.UNSPECIFIED.,.F.,.F.,(4,1,1,1,1,1,1,1,1,1,1,1,1,1,4),(166.504410640259,
166.613272138369,167.113265204883,167.613258271396,168.11325133791,168.613244404424,
169.113237470937,169.613230537451,170.113223603965,170.613216670479,171.113209736992,
171.613202803506,172.11319587002,172.613188936534,172.787595947439),
 .UNSPECIFIED.);
#1274=B_SPLINE_CURVE_WITH_KNOTS('',3,(#30480,#30481,#30482,#30483,#30484,
#30485,#30486,#30487,#30488,#30489,#30490,#30491,#30492,#30493,#30494,#30495),
 .UNSPECIFIED.,.F.,.F.,(4,1,1,1,1,1,1,1,1,1,1,1,1,4),(166.504410640259,
166.803724952086,167.3037180186,167.803711085113,168.303704151627,168.803697218141,
169.303690284655,169.803683351168,170.303676417682,170.803669484196,171.30366255071,
171.803655617223,172.303648683737,172.787595947439),.UNSPECIFIED.);
#1275=B_SPLINE_CURVE_WITH_KNOTS('',3,(#30500,#30501,#30502,#30503,#30504,
#30505,#30506,#30507,#30508,#30509,#30510,#30511,#30512,#30513,#30514,#30515),
 .UNSPECIFIED.,.F.,.F.,(4,1,1,1,1,1,1,1,1,1,1,1,1,4),(160.22122533308,160.613355340204,
161.113348406718,161.613341473231,162.113334539745,162.613327606259,163.113320672773,
163.613313739286,164.1133068058,164.613299872314,165.113292938828,165.613286005341,
166.113279071855,166.504410640259),.UNSPECIFIED.);
#1276=B_SPLINE_CURVE_WITH_KNOTS('',3,(#30516,#30517,#30518,#30519,#30520,
#30521,#30522,#30523,#30524,#30525,#30526,#30527,#30528,#30529,#30530,#30531,
#30532),.UNSPECIFIED.,.F.,.F.,(4,1,1,1,1,1,1,1,1,1,1,1,1,1,4),(160.22122533308,
160.303815087407,160.803808153921,161.303801220435,161.803794286949,162.303787353462,
162.803780419976,163.30377348649,163.803766553004,164.303759619517,164.803752686031,
165.303745752545,165.803738819059,166.303731885572,166.504410640259),
 .UNSPECIFIED.);
#1277=B_SPLINE_CURVE_WITH_KNOTS('',3,(#30537,#30538,#30539,#30540,#30541,
#30542,#30543,#30544,#30545,#30546,#30547,#30548,#30549,#30550,#30551,#30552,
#30553),.UNSPECIFIED.,.F.,.F.,(4,1,1,1,1,1,1,1,1,1,1,1,1,1,4),(153.9380400259,
154.113445475525,154.613438542039,155.113431608553,155.613424675067,156.11341774158,
156.613410808094,157.113403874608,157.613396941122,158.113390007635,158.613383074149,
159.113376140663,159.613369207177,160.11336227369,160.22122533308),
 .UNSPECIFIED.);
#1278=B_SPLINE_CURVE_WITH_KNOTS('',3,(#30554,#30555,#30556,#30557,#30558,
#30559,#30560,#30561,#30562,#30563,#30564,#30565,#30566,#30567,#30568,#30569),
 .UNSPECIFIED.,.F.,.F.,(4,1,1,1,1,1,1,1,1,1,1,1,1,4),(153.9380400259,154.303898289243,
154.803891355756,155.30388442227,155.803877488784,156.303870555298,156.803863621811,
157.303856688325,157.803849754839,158.303842821353,158.803835887866,159.30382895438,
159.803822020894,160.22122533308),.UNSPECIFIED.);
#1279=B_SPLINE_CURVE_WITH_KNOTS('',3,(#30574,#30575,#30576,#30577,#30578,
#30579,#30580,#30581,#30582,#30583,#30584,#30585,#30586,#30587,#30588,#30589),
 .UNSPECIFIED.,.F.,.F.,(4,1,1,1,1,1,1,1,1,1,1,1,1,4),(147.65485471872,148.113528677361,
148.613521743874,149.113514810388,149.613507876902,150.113500943416,150.613494009929,
151.113487076443,151.613480142957,152.11347320947,152.613466275984,153.113459342498,
153.613452409012,153.9380400259),.UNSPECIFIED.);
#1280=B_SPLINE_CURVE_WITH_KNOTS('',3,(#30590,#30591,#30592,#30593,#30594,
#30595,#30596,#30597,#30598,#30599,#30600,#30601,#30602,#30603,#30604,#30605,
#30606),.UNSPECIFIED.,.F.,.F.,(4,1,1,1,1,1,1,1,1,1,1,1,1,1,4),(147.654854718721,
147.803988424564,148.303981491078,148.803974557592,149.303967624105,149.803960690619,
150.303953757133,150.803946823646,151.30393989016,151.803932956674,152.303926023188,
152.803919089701,153.303912156215,153.803905222729,153.9380400259),
 .UNSPECIFIED.);
#1281=B_SPLINE_CURVE_WITH_KNOTS('',3,(#30611,#30612,#30613,#30614,#30615,
#30616,#30617,#30618,#30619,#30620,#30621,#30622,#30623,#30624,#30625,#30626,
#30627),.UNSPECIFIED.,.F.,.F.,(4,1,1,1,1,1,1,1,1,1,1,1,1,1,4),(141.371669411541,
141.613618812682,142.113611879196,142.61360494571,143.113598012223,143.613591078737,
144.113584145251,144.613577211764,145.113570278278,145.613563344792,146.113556411306,
146.613549477819,147.113542544333,147.613535610847,147.65485471872),
 .UNSPECIFIED.);
#1282=B_SPLINE_CURVE_WITH_KNOTS('',3,(#30628,#30629,#30630,#30631,#30632,
#30633,#30634,#30635,#30636,#30637,#30638,#30639,#30640,#30641,#30642,#30643),
 .UNSPECIFIED.,.F.,.F.,(4,1,1,1,1,1,1,1,1,1,1,1,1,4),(141.371669411541,
141.804071626399,142.304064692913,142.804057759427,143.30405082594,143.804043892454,
144.304036958968,144.804030025482,145.304023091995,145.804016158509,146.304009225023,
146.804002291537,147.30399535805,147.654854718721),.UNSPECIFIED.);
#1283=B_SPLINE_CURVE_WITH_KNOTS('',3,(#30648,#30649,#30650,#30651,#30652,
#30653,#30654,#30655,#30656,#30657,#30658,#30659,#30660,#30661,#30662,#30663,
#30664),.UNSPECIFIED.,.F.,.F.,(4,1,1,1,1,1,1,1,1,1,1,1,1,1,4),(135.088484104361,
135.113708948003,135.613702014517,136.113695081031,136.613688147545,137.113681214058,
137.613674280572,138.113667347086,138.6136604136,139.113653480113,139.613646546627,
140.113639613141,140.613632679655,141.113625746168,141.371669411541),
 .UNSPECIFIED.);
#1284=B_SPLINE_CURVE_WITH_KNOTS('',3,(#30665,#30666,#30667,#30668,#30669,
#30670,#30671,#30672,#30673,#30674,#30675,#30676,#30677,#30678,#30679,#30680,
#30681),.UNSPECIFIED.,.F.,.F.,(4,1,1,1,1,1,1,1,1,1,1,1,1,1,4),(135.088484104361,
135.304161761721,135.804154828234,136.304147894748,136.804140961262,137.304134027776,
137.804127094289,138.304120160803,138.804113227317,139.304106293831,139.804099360344,
140.304092426858,140.804085493372,141.304078559886,141.371669411541),
 .UNSPECIFIED.);
#1285=B_SPLINE_CURVE_WITH_KNOTS('',3,(#30686,#30687,#30688,#30689,#30690,
#30691,#30692,#30693,#30694,#30695,#30696,#30697,#30698,#30699,#30700,#30701),
 .UNSPECIFIED.,.F.,.F.,(4,1,1,1,1,1,1,1,1,1,1,1,1,4),(128.805298797182,
129.113792149839,129.613785216352,130.113778282866,130.61377134938,131.113764415894,
131.613757482407,132.113750548921,132.613743615435,133.113736681949,133.613729748462,
134.113722814976,134.61371588149,135.088484104361),.UNSPECIFIED.);
#1286=B_SPLINE_CURVE_WITH_KNOTS('',3,(#30702,#30703,#30704,#30705,#30706,
#30707,#30708,#30709,#30710,#30711,#30712,#30713,#30714,#30715,#30716,#30717),
 .UNSPECIFIED.,.F.,.F.,(4,1,1,1,1,1,1,1,1,1,1,1,1,4),(128.805298797182,
129.304244963556,129.80423803007,130.304231096583,130.804224163097,131.304217229611,
131.804210296125,132.304203362638,132.804196429152,133.304189495666,133.80418256218,
134.304175628693,134.804168695207,135.088484104361),.UNSPECIFIED.);
#1287=B_SPLINE_CURVE_WITH_KNOTS('',3,(#30722,#30723,#30724,#30725,#30726,
#30727,#30728,#30729,#30730,#30731,#30732,#30733,#30734,#30735,#30736,#30737,
#30738),.UNSPECIFIED.,.F.,.F.,(4,1,1,1,1,1,1,1,1,1,1,1,1,1,4),(122.522113490002,
122.61388228516,123.113875351674,123.613868418188,124.113861484701,124.613854551215,
125.113847617729,125.613840684243,126.113833750756,126.61382681727,127.113819883784,
127.613812950297,128.113806016811,128.613799083325,128.805298797182),
 .UNSPECIFIED.);
#1288=B_SPLINE_CURVE_WITH_KNOTS('',3,(#30739,#30740,#30741,#30742,#30743,
#30744,#30745,#30746,#30747,#30748,#30749,#30750,#30751,#30752,#30753,#30754,
#30755),.UNSPECIFIED.,.F.,.F.,(4,1,1,1,1,1,1,1,1,1,1,1,1,1,4),(122.522113490002,
122.804335098877,123.304328165391,123.804321231905,124.304314298419,124.804307364932,
125.304300431446,125.80429349796,126.304286564473,126.804279630987,127.304272697501,
127.804265764015,128.304258830528,128.804251897042,128.805298797182),
 .UNSPECIFIED.);
#1289=B_SPLINE_CURVE_WITH_KNOTS('',3,(#30760,#30761,#30762,#30763,#30764,
#30765,#30766,#30767,#30768,#30769,#30770,#30771,#30772,#30773,#30774,#30775),
 .UNSPECIFIED.,.F.,.F.,(4,1,1,1,1,1,1,1,1,1,1,1,1,4),(116.238928182823,
116.613965486995,117.113958553509,117.613951620023,118.113944686536,118.61393775305,
119.113930819564,119.613923886078,120.113916952591,120.613910019105,121.113903085619,
121.613896152133,122.113889218646,122.522113490002),.UNSPECIFIED.);
#1290=B_SPLINE_CURVE_WITH_KNOTS('',3,(#30776,#30777,#30778,#30779,#30780,
#30781,#30782,#30783,#30784,#30785,#30786,#30787,#30788,#30789,#30790,#30791,
#30792),.UNSPECIFIED.,.F.,.F.,(4,1,1,1,1,1,1,1,1,1,1,1,1,1,4),(116.238928182823,
116.304425234199,116.804418300713,117.304411367226,117.80440443374,118.304397500254,
118.804390566767,119.304383633281,119.804376699795,120.304369766309,120.804362832822,
121.304355899336,121.80434896585,122.304342032364,122.522113490002),
 .UNSPECIFIED.);
#1291=B_SPLINE_CURVE_WITH_KNOTS('',3,(#30797,#30798,#30799,#30800,#30801,
#30802,#30803,#30804,#30805,#30806,#30807,#30808,#30809,#30810,#30811,#30812,
#30813),.UNSPECIFIED.,.F.,.F.,(4,1,1,1,1,1,1,1,1,1,1,1,1,1,4),(109.955742875643,
110.114055622317,110.61404868883,111.114041755344,111.614034821858,112.114027888372,
112.614020954885,113.114014021399,113.614007087913,114.114000154427,114.61399322094,
115.113986287454,115.613979353968,116.113972420482,116.238928182823),
 .UNSPECIFIED.);
#1292=B_SPLINE_CURVE_WITH_KNOTS('',3,(#30814,#30815,#30816,#30817,#30818,
#30819,#30820,#30821,#30822,#30823,#30824,#30825,#30826,#30827,#30828,#30829),
 .UNSPECIFIED.,.F.,.F.,(4,1,1,1,1,1,1,1,1,1,1,1,1,4),(109.955742875643,
110.304508436034,110.804501502548,111.304494569061,111.804487635575,112.304480702089,
112.804473768603,113.304466835116,113.80445990163,114.304452968144,114.804446034658,
115.304439101171,115.804432167685,116.238928182823),.UNSPECIFIED.);
#1293=B_SPLINE_CURVE_WITH_KNOTS('',3,(#30834,#30835,#30836,#30837,#30838,
#30839,#30840,#30841,#30842,#30843,#30844,#30845,#30846,#30847,#30848,#30849),
 .UNSPECIFIED.,.F.,.F.,(4,1,1,1,1,1,1,1,1,1,1,1,1,4),(103.672557568463,
104.114138824152,104.614131890666,105.114124957179,105.614118023693,106.114111090207,
106.614104156721,107.114097223234,107.614090289748,108.114083356262,108.614076422776,
109.114069489289,109.614062555803,109.955742875643),.UNSPECIFIED.);
#1294=B_SPLINE_CURVE_WITH_KNOTS('',3,(#30850,#30851,#30852,#30853,#30854,
#30855,#30856,#30857,#30858,#30859,#30860,#30861,#30862,#30863,#30864,#30865,
#30866),.UNSPECIFIED.,.F.,.F.,(4,1,1,1,1,1,1,1,1,1,1,1,1,1,4),(103.672557568463,
103.804598571355,104.304591637869,104.804584704383,105.304577770897,105.80457083741,
106.304563903924,106.804556970438,107.304550036952,107.804543103465,108.304536169979,
108.804529236493,109.304522303006,109.80451536952,109.955742875643),
 .UNSPECIFIED.);
#1295=B_SPLINE_CURVE_WITH_KNOTS('',3,(#30871,#30872,#30873,#30874,#30875,
#30876,#30877,#30878,#30879,#30880,#30881,#30882,#30883,#30884,#30885,#30886,
#30887),.UNSPECIFIED.,.F.,.F.,(4,1,1,1,1,1,1,1,1,1,1,1,1,1,4),(97.3893722612838,
97.6142289594734,98.1142220259871,98.6142150925008,99.1142081590146,99.6142012255283,
100.114194292042,100.614187358556,101.11418042507,101.614173491583,102.114166558097,
102.614159624611,103.114152691124,103.614145757638,103.672557568463),
 .UNSPECIFIED.);
#1296=B_SPLINE_CURVE_WITH_KNOTS('',3,(#30888,#30889,#30890,#30891,#30892,
#30893,#30894,#30895,#30896,#30897,#30898,#30899,#30900,#30901,#30902,#30903),
 .UNSPECIFIED.,.F.,.F.,(4,1,1,1,1,1,1,1,1,1,1,1,1,4),(97.3893722612839,
97.8046817731906,98.3046748397043,98.804667906218,99.3046609727318,99.8046540392455,
100.304647105759,100.804640172273,101.304633238787,101.8046263053,102.304619371814,
102.804612438328,103.304605504842,103.672557568463),.UNSPECIFIED.);
#1297=B_SPLINE_CURVE_WITH_KNOTS('',3,(#30908,#30909,#30910,#30911,#30912,
#30913,#30914,#30915,#30916,#30917,#30918,#30919,#30920,#30921,#30922,#30923,
#30924),.UNSPECIFIED.,.F.,.F.,(4,1,1,1,1,1,1,1,1,1,1,1,1,1,4),(91.1061869541042,
91.1143190947948,91.6143121613085,92.1143052278223,92.614298294336,93.1142913608497,
93.6142844273635,94.1142774938772,94.6142705603909,95.1142636269047,95.6142566934184,
96.1142497599322,96.6142428264459,97.1142358929596,97.3893722612838),
 .UNSPECIFIED.);
#1298=B_SPLINE_CURVE_WITH_KNOTS('',3,(#30925,#30926,#30927,#30928,#30929,
#30930,#30931,#30932,#30933,#30934,#30935,#30936,#30937,#30938,#30939,#30940,
#30941),.UNSPECIFIED.,.F.,.F.,(4,1,1,1,1,1,1,1,1,1,1,1,1,1,4),(91.1061869541043,
91.304771908512,91.8047649750257,92.3047580415395,92.8047511080532,93.3047441745669,
93.8047372410807,94.3047303075944,94.8047233741082,95.3047164406219,95.8047095071356,
96.3047025736494,96.8046956401631,97.3046887066768,97.3893722612839),
 .UNSPECIFIED.);
#1299=B_SPLINE_CURVE_WITH_KNOTS('',3,(#30946,#30947,#30948,#30949,#30950,
#30951,#30952,#30953,#30954,#30955,#30956,#30957,#30958,#30959,#30960,#30961),
 .UNSPECIFIED.,.F.,.F.,(4,1,1,1,1,1,1,1,1,1,1,1,1,4),(84.8230016469246,
85.11440229663,85.6143953631437,86.1143884296575,86.6143814961712,87.1143745626849,
87.6143676291987,88.1143606957124,88.6143537622261,89.1143468287399,89.6143398952536,
90.1143329617673,90.6143260282811,91.1061869541042),.UNSPECIFIED.);
#1300=B_SPLINE_CURVE_WITH_KNOTS('',3,(#30962,#30963,#30964,#30965,#30966,
#30967,#30968,#30969,#30970,#30971,#30972,#30973,#30974,#30975,#30976,#30977),
 .UNSPECIFIED.,.F.,.F.,(4,1,1,1,1,1,1,1,1,1,1,1,1,4),(84.8230016469247,
85.3048551103472,85.8048481768609,86.3048412433747,86.8048343098884,87.3048273764021,
87.8048204429159,88.3048135094296,88.8048065759433,89.3047996424571,89.8047927089708,
90.3047857754845,90.8047788419983,91.1061869541043),.UNSPECIFIED.);
#1301=B_SPLINE_CURVE_WITH_KNOTS('',3,(#30982,#30983,#30984,#30985,#30986,
#30987,#30988,#30989,#30990,#30991,#30992,#30993,#30994,#30995,#30996,#30997,
#30998),.UNSPECIFIED.,.F.,.F.,(4,1,1,1,1,1,1,1,1,1,1,1,1,1,4),(78.539816339745,
78.6144924319514,79.1144854984652,79.6144785649789,80.1144716314926,80.6144646980064,
81.1144577645201,81.6144508310338,82.1144438975476,82.6144369640613,83.114430030575,
83.6144230970888,84.1144161636025,84.6144092301162,84.8230016469246),
 .UNSPECIFIED.);
#1302=B_SPLINE_CURVE_WITH_KNOTS('',3,(#30999,#31000,#31001,#31002,#31003,
#31004,#31005,#31006,#31007,#31008,#31009,#31010,#31011,#31012,#31013,#31014,
#31015),.UNSPECIFIED.,.F.,.F.,(4,1,1,1,1,1,1,1,1,1,1,1,1,1,4),(78.5398163397451,
78.8049452456686,79.3049383121824,79.8049313786961,80.3049244452098,80.8049175117236,
81.3049105782373,81.804903644751,82.3048967112648,82.8048897777785,83.3048828442923,
83.804875910806,84.3048689773197,84.8048620438335,84.8230016469247),
 .UNSPECIFIED.);
#1303=B_SPLINE_CURVE_WITH_KNOTS('',3,(#31020,#31021,#31022,#31023,#31024,
#31025,#31026,#31027,#31028,#31029,#31030,#31031,#31032,#31033,#31034,#31035),
 .UNSPECIFIED.,.F.,.F.,(4,1,1,1,1,1,1,1,1,1,1,1,1,4),(72.2566310325655,
72.6145756337866,73.1145687003003,73.6145617668141,74.1145548333278,74.6145478998415,
75.1145409663553,75.614534032869,76.1145270993827,76.6145201658965,77.1145132324102,
77.614506298924,78.1144993654377,78.539816339745),.UNSPECIFIED.);
#1304=B_SPLINE_CURVE_WITH_KNOTS('',3,(#31036,#31037,#31038,#31039,#31040,
#31041,#31042,#31043,#31044,#31045,#31046,#31047,#31048,#31049,#31050,#31051,
#31052),.UNSPECIFIED.,.F.,.F.,(4,1,1,1,1,1,1,1,1,1,1,1,1,1,4),(72.2566310325655,
72.3050353809901,72.8050284475038,73.3050215140175,73.8050145805313,74.305007647045,
74.8050007135587,75.3049937800725,75.8049868465862,76.3049799131,76.8049729796137,
77.3049660461274,77.8049591126412,78.3049521791549,78.5398163397451),
 .UNSPECIFIED.);
#1305=B_SPLINE_CURVE_WITH_KNOTS('',3,(#31057,#31058,#31059,#31060,#31061,
#31062,#31063,#31064,#31065,#31066,#31067,#31068,#31069,#31070,#31071,#31072,
#31073),.UNSPECIFIED.,.F.,.F.,(4,1,1,1,1,1,1,1,1,1,1,1,1,1,4),(65.9734457253858,
66.114665769108,66.6146588356218,67.1146519021355,67.6146449686492,68.114638035163,
68.6146311016767,69.1146241681904,69.6146172347042,70.1146103012179,70.6146033677317,
71.1145964342454,71.6145895007591,72.1145825672729,72.2566310325655),
 .UNSPECIFIED.);
#1306=B_SPLINE_CURVE_WITH_KNOTS('',3,(#31074,#31075,#31076,#31077,#31078,
#31079,#31080,#31081,#31082,#31083,#31084,#31085,#31086,#31087,#31088,#31089),
 .UNSPECIFIED.,.F.,.F.,(4,1,1,1,1,1,1,1,1,1,1,1,1,4),(65.9734457253859,
66.3051185828252,66.805111649339,67.3051047158527,67.8050977823664,68.3050908488802,
68.8050839153939,69.3050769819077,69.8050700484214,70.3050631149351,70.8050561814489,
71.3050492479626,71.8050423144763,72.2566310325655),.UNSPECIFIED.);
#1307=B_SPLINE_CURVE_WITH_KNOTS('',3,(#31094,#31095,#31096,#31097,#31098,
#31099,#31100,#31101,#31102,#31103,#31104,#31105,#31106,#31107,#31108,#31109),
 .UNSPECIFIED.,.F.,.F.,(4,1,1,1,1,1,1,1,1,1,1,1,1,4),(59.6902604182063,
60.1147489709432,60.6147420374569,61.1147351039707,61.6147281704844,62.1147212369982,
62.6147143035119,63.1147073700256,63.6147004365394,64.1146935030531,64.6146865695668,
65.1146796360806,65.6146727025943,65.9734457253858),.UNSPECIFIED.);
#1308=B_SPLINE_CURVE_WITH_KNOTS('',3,(#31110,#31111,#31112,#31113,#31114,
#31115,#31116,#31117,#31118,#31119,#31120,#31121,#31122,#31123,#31124,#31125,
#31126),.UNSPECIFIED.,.F.,.F.,(4,1,1,1,1,1,1,1,1,1,1,1,1,1,4),(59.6902604182063,
59.8052087181467,60.3052017846604,60.8051948511742,61.3051879176879,61.8051809842016,
62.3051740507154,62.8051671172291,63.3051601837428,63.8051532502566,64.3051463167703,
64.805139383284,65.3051324497978,65.8051255163115,65.9734457253859),
 .UNSPECIFIED.);
#1309=B_SPLINE_CURVE_WITH_KNOTS('',3,(#31131,#31132,#31133,#31134,#31135,
#31136,#31137,#31138,#31139,#31140,#31141,#31142,#31143,#31144,#31145,#31146,
#31147),.UNSPECIFIED.,.F.,.F.,(4,1,1,1,1,1,1,1,1,1,1,1,1,1,4),(53.4070751110267,
53.6148391062647,54.1148321727784,54.6148252392921,55.1148183058059,55.6148113723196,
56.1148044388333,56.6147975053471,57.1147905718608,57.6147836383745,58.1147767048883,
58.614769771402,59.1147628379157,59.6147559044295,59.6902604182063),
 .UNSPECIFIED.);
#1310=B_SPLINE_CURVE_WITH_KNOTS('',3,(#31148,#31149,#31150,#31151,#31152,
#31153,#31154,#31155,#31156,#31157,#31158,#31159,#31160,#31161,#31162,#31163),
 .UNSPECIFIED.,.F.,.F.,(4,1,1,1,1,1,1,1,1,1,1,1,1,4),(53.4070751110267,
53.8052919199819,54.3052849864956,54.8052780530093,55.3052711195231,55.8052641860368,
56.3052572525505,56.8052503190643,57.305243385578,57.8052364520917,58.3052295186055,
58.8052225851192,59.3052156516329,59.6902604182063),.UNSPECIFIED.);
#1311=B_SPLINE_CURVE_WITH_KNOTS('',3,(#31168,#31169,#31170,#31171,#31172,
#31173,#31174,#31175,#31176,#31177,#31178,#31179,#31180,#31181,#31182,#31183),
 .UNSPECIFIED.,.F.,.F.,(4,1,1,1,1,1,1,1,1,1,1,1,1,4),(47.1238898038471,
47.6149223080998,48.1149153746136,48.6149084411273,49.114901507641,49.6148945741548,
50.1148876406685,50.6148807071823,51.114873773696,51.6148668402097,52.1148599067235,
52.6148529732372,53.1148460397509,53.4070751110267),.UNSPECIFIED.);
#1312=B_SPLINE_CURVE_WITH_KNOTS('',3,(#31184,#31185,#31186,#31187,#31188,
#31189,#31190,#31191,#31192,#31193,#31194,#31195,#31196,#31197,#31198,#31199,
#31200),.UNSPECIFIED.,.F.,.F.,(4,1,1,1,1,1,1,1,1,1,1,1,1,1,4),(47.1238898038471,
47.3053820553033,47.805375121817,48.3053681883308,48.8053612548445,49.3053543213582,
49.805347387872,50.3053404543857,50.8053335208995,51.3053265874132,51.8053196539269,
52.3053127204407,52.8053057869544,53.3052988534681,53.4070751110267),
 .UNSPECIFIED.);
#1313=B_SPLINE_CURVE_WITH_KNOTS('',3,(#31205,#31206,#31207,#31208,#31209,
#31210,#31211,#31212,#31213,#31214,#31215,#31216,#31217,#31218,#31219,#31220,
#31221),.UNSPECIFIED.,.F.,.F.,(4,1,1,1,1,1,1,1,1,1,1,1,1,1,4),(40.8407044966675,
41.1150124434213,41.615005509935,42.1149985764488,42.6149916429625,43.1149847094762,
43.61497777599,44.1149708425037,44.6149639090174,45.1149569755312,45.6149500420449,
46.1149431085586,46.6149361750724,47.1149292415861,47.1238898038471),
 .UNSPECIFIED.);
#1314=B_SPLINE_CURVE_WITH_KNOTS('',3,(#31222,#31223,#31224,#31225,#31226,
#31227,#31228,#31229,#31230,#31231,#31232,#31233,#31234,#31235,#31236,#31237),
 .UNSPECIFIED.,.F.,.F.,(4,1,1,1,1,1,1,1,1,1,1,1,1,4),(40.8407044966675,
41.3054652571385,41.8054583236522,42.305451390166,42.8054444566797,43.3054375231934,
43.8054305897072,44.3054236562209,44.8054167227346,45.3054097892484,45.8054028557621,
46.3053959222758,46.8053889887896,47.1238898038471),.UNSPECIFIED.);
#1315=B_SPLINE_CURVE_WITH_KNOTS('',3,(#31242,#31243,#31244,#31245,#31246,
#31247,#31248,#31249,#31250,#31251,#31252,#31253,#31254,#31255,#31256,#31257,
#31258),.UNSPECIFIED.,.F.,.F.,(4,1,1,1,1,1,1,1,1,1,1,1,1,1,4),(34.5575191894879,
34.6151025787427,35.1150956452565,35.6150887117702,36.1150817782839,36.6150748447977,
37.1150679113114,37.6150609778251,38.1150540443389,38.6150471108526,39.1150401773663,
39.6150332438801,40.1150263103938,40.6150193769075,40.8407044966675),
 .UNSPECIFIED.);
#1316=B_SPLINE_CURVE_WITH_KNOTS('',3,(#31259,#31260,#31261,#31262,#31263,
#31264,#31265,#31266,#31267,#31268,#31269,#31270,#31271,#31272,#31273,#31274,
#31275),.UNSPECIFIED.,.F.,.F.,(4,1,1,1,1,1,1,1,1,1,1,1,1,1,4),(34.557519189488,
34.8055553924599,35.3055484589737,35.8055415254874,36.3055345920011,36.8055276585149,
37.3055207250286,37.8055137915423,38.3055068580561,38.8054999245698,39.3054929910835,
39.8054860575973,40.305479124111,40.8054721906247,40.8407044966675),
 .UNSPECIFIED.);
#1317=B_SPLINE_CURVE_WITH_KNOTS('',3,(#31280,#31281,#31282,#31283,#31284,
#31285,#31286,#31287,#31288,#31289,#31290,#31291,#31292,#31293,#31294,#31295),
 .UNSPECIFIED.,.F.,.F.,(4,1,1,1,1,1,1,1,1,1,1,1,1,4),(28.2743338823083,
28.6151857805779,29.1151788470916,29.6151719136054,30.1151649801191,30.6151580466328,
31.1151511131466,31.6151441796603,32.115137246174,32.6151303126878,33.1151233792015,
33.6151164457153,34.115109512229,34.5575191894879),.UNSPECIFIED.);
#1318=B_SPLINE_CURVE_WITH_KNOTS('',3,(#31296,#31297,#31298,#31299,#31300,
#31301,#31302,#31303,#31304,#31305,#31306,#31307,#31308,#31309,#31310,#31311,
#31312),.UNSPECIFIED.,.F.,.F.,(4,1,1,1,1,1,1,1,1,1,1,1,1,1,4),(28.2743338823084,
28.3056455277814,28.8056385942951,29.3056316608088,29.8056247273226,30.3056177938363,
30.80561086035,31.3056039268638,31.8055969933775,32.3055900598912,32.805583126405,
33.3055761929187,33.8055692594324,34.3055623259462,34.557519189488),
 .UNSPECIFIED.);
#1319=B_SPLINE_CURVE_WITH_KNOTS('',3,(#31317,#31318,#31319,#31320,#31321,
#31322,#31323,#31324,#31325,#31326,#31327,#31328,#31329,#31330,#31331,#31332,
#31333),.UNSPECIFIED.,.F.,.F.,(4,1,1,1,1,1,1,1,1,1,1,1,1,1,4),(21.9911485751287,
22.1152759158993,22.6152689824131,23.1152620489268,23.6152551154406,24.1152481819543,
24.615241248468,25.1152343149818,25.6152273814955,26.1152204480092,26.615213514523,
27.1152065810367,27.6151996475504,28.1151927140642,28.2743338823083),
 .UNSPECIFIED.);
#1320=B_SPLINE_CURVE_WITH_KNOTS('',3,(#31334,#31335,#31336,#31337,#31338,
#31339,#31340,#31341,#31342,#31343,#31344,#31345,#31346,#31347,#31348,#31349),
 .UNSPECIFIED.,.F.,.F.,(4,1,1,1,1,1,1,1,1,1,1,1,1,4),(21.9911485751288,
22.3057287296165,22.8057217961303,23.305714862644,23.8057079291577,24.3057009956715,
24.8056940621852,25.305687128699,25.8056801952127,26.3056732617264,26.8056663282402,
27.3056593947539,27.8056524612676,28.2743338823084),.UNSPECIFIED.);
#1321=B_SPLINE_CURVE_WITH_KNOTS('',3,(#31354,#31355,#31356,#31357,#31358,
#31359,#31360,#31361,#31362,#31363,#31364,#31365,#31366,#31367,#31368,#31369),
 .UNSPECIFIED.,.F.,.F.,(4,1,1,1,1,1,1,1,1,1,1,1,1,4),(15.7079632679491,
16.1153591177345,16.6153521842483,17.115345250762,17.6153383172757,18.1153313837895,
18.6153244503032,19.1153175168169,19.6153105833307,20.1153036498444,20.6152967163581,
21.1152897828719,21.6152828493856,21.9911485751287),.UNSPECIFIED.);
#1322=B_SPLINE_CURVE_WITH_KNOTS('',3,(#31370,#31371,#31372,#31373,#31374,
#31375,#31376,#31377,#31378,#31379,#31380,#31381,#31382,#31383,#31384,#31385,
#31386),.UNSPECIFIED.,.F.,.F.,(4,1,1,1,1,1,1,1,1,1,1,1,1,1,4),(15.7079632679492,
15.805818864938,16.3058119314517,16.8058049979655,17.3057980644792,17.8057911309929,
18.3057841975067,18.8057772640204,19.3057703305341,19.8057633970479,20.3057564635616,
20.8057495300753,21.3057425965891,21.8057356631028,21.9911485751288),
 .UNSPECIFIED.);
#1323=B_SPLINE_CURVE_WITH_KNOTS('',3,(#33128,#33129,#33130,#33131,#33132,
#33133,#33134,#33135,#33136,#33137,#33138,#33139,#33140,#33141,#33142,#33143,
#33144,#33145,#33146,#33147,#33148,#33149,#33150,#33151,#33152,#33153,#33154,
#33155,#33156,#33157,#33158,#33159,#33160,#33161,#33162,#33163,#33164,#33165,
#33166,#33167,#33168,#33169,#33170,#33171,#33172,#33173,#33174,#33175,#33176,
#33177,#33178,#33179,#33180,#33181,#33182,#33183,#33184,#33185,#33186,#33187,
#33188,#33189,#33190,#33191,#33192,#33193,#33194,#33195,#33196,#33197,#33198,
#33199,#33200,#33201,#33202,#33203,#33204,#33205,#33206,#33207,#33208,#33209,
#33210,#33211,#33212,#33213,#33214,#33215,#33216,#33217,#33218,#33219,#33220,
#33221,#33222,#33223,#33224,#33225,#33226,#33227,#33228,#33229,#33230,#33231,
#33232,#33233,#33234,#33235,#33236),.UNSPECIFIED.,.F.,.F.,(4,3,3,3,3,3,
3,3,3,3,3,3,3,3,3,3,3,3,3,3,3,3,3,3,3,3,3,3,3,3,3,3,3,3,3,3,4),(-1.12653966532766,
-1.08530391285188,-1.03555276854547,-0.985995835508339,-0.97449600456723,
-0.967183168816629,-0.918323363958047,-0.869822311041264,-0.833246511105209,
-0.821905472485523,-0.815371904719748,-0.796670711169154,-0.7489242491,
-0.700999781025762,-0.653716403326253,-0.620120968748125,-0.608348915151015,
-0.601406539983964,-0.554880452923037,-0.519334665013739,-0.47261371763217,
-0.426217608843986,-0.404654224478211,-0.397976651477122,-0.39279021318813,
-0.347324068852467,-0.300517301385129,-0.25371053391779,-0.221996717178066,
-0.205387453912266,-0.194998280364054,-0.18903995937007,-0.144864377715273,
-0.100707092544083,-0.0569734759838599,-0.0141899988762762,0.),
 .UNSPECIFIED.);
#1324=B_SPLINE_CURVE_WITH_KNOTS('',3,(#33237,#33238,#33239,#33240,#33241,
#33242,#33243,#33244,#33245,#33246,#33247,#33248,#33249,#33250,#33251,#33252,
#33253,#33254,#33255,#33256,#33257,#33258,#33259,#33260,#33261,#33262,#33263,
#33264,#33265,#33266,#33267,#33268,#33269,#33270,#33271,#33272,#33273),
 .UNSPECIFIED.,.F.,.F.,(4,3,3,3,3,3,3,3,3,3,3,3,4),(208.463970230464,208.497108736228,
208.997101802741,209.497094869255,209.997087935769,210.497081002283,210.997074068796,
211.49706713531,211.997060201824,212.497053268338,212.997046334851,213.497039401365,
213.927200545147),.UNSPECIFIED.);
#1325=B_SPLINE_CURVE_WITH_KNOTS('',3,(#33275,#33276,#33277,#33278,#33279,
#33280,#33281,#33282,#33283,#33284,#33285,#33286,#33287,#33288,#33289,#33290,
#33291,#33292,#33293,#33294,#33295,#33296,#33297,#33298,#33299,#33300,#33301,
#33302,#33303,#33304,#33305,#33306,#33307,#33308,#33309,#33310,#33311,#33312,
#33313,#33314,#33315,#33316,#33317,#33318,#33319,#33320,#33321,#33322,#33323,
#33324,#33325,#33326,#33327,#33328,#33329,#33330,#33331,#33332,#33333,#33334,
#33335,#33336,#33337,#33338,#33339,#33340,#33341,#33342,#33343,#33344,#33345,
#33346,#33347,#33348,#33349,#33350,#33351,#33352,#33353,#33354,#33355,#33356,
#33357,#33358,#33359,#33360,#33361,#33362,#33363,#33364,#33365,#33366,#33367,
#33368,#33369,#33370,#33371,#33372,#33373,#33374,#33375,#33376,#33377,#33378,
#33379,#33380,#33381,#33382,#33383,#33384,#33385,#33386),.UNSPECIFIED.,
 .F.,.F.,(4,3,3,3,3,3,3,3,3,3,3,3,3,3,3,3,3,3,3,3,3,3,3,3,3,3,3,3,3,3,3,
3,3,3,3,3,3,4),(-1.13094109509778,-1.09616481350051,-1.05252904406664,-1.02447554603566,
-1.00950008969337,-1.00035998114085,-0.993301600393168,-0.94845224485129,
-0.90333045519232,-0.871780285525201,-0.865172051628852,-0.858235225141103,
-0.840230115858081,-0.795263315109601,-0.749591763211198,-0.703490048776212,
-0.670607568572991,-0.660837839774893,-0.654974428744378,-0.607853069321203,
-0.571960127963328,-0.525117783125689,-0.477884601070653,-0.454625076147963,
-0.446675645902694,-0.440719363147554,-0.39273374519351,-0.342271073441322,
-0.291808401689134,-0.255332351477992,-0.239279102906314,-0.22920132207221,
-0.222814956686309,-0.174288185380996,-0.124750052790975,-0.0750207445547947,
-0.0256773244109543,0.),.UNSPECIFIED.);
#1326=B_SPLINE_CURVE_WITH_KNOTS('',3,(#33387,#33388,#33389,#33390,#33391,
#33392,#33393,#33394,#33395,#33396,#33397,#33398,#33399,#33400),
 .UNSPECIFIED.,.F.,.F.,(4,1,1,1,1,1,1,1,1,1,1,4),(10.3757270560181,10.8058881998006,
11.3058812663144,11.8058743328281,12.3058673993418,12.8058604658556,13.3058535323693,
13.805846598883,14.3058396653968,14.8058327319105,15.3058257984242,15.7079632679492),
 .UNSPECIFIED.);
#1327=B_SPLINE_CURVE_WITH_KNOTS('',3,(#33406,#33407,#33408,#33409,#33410,
#33411,#33412,#33413,#33414,#33415,#33416,#33417,#33418,#33419,#33420,#33421,
#33422,#33423,#33424,#33425,#33426,#33427,#33428,#33429,#33430,#33431,#33432,
#33433,#33434,#33435,#33436,#33437,#33438,#33439,#33440,#33441,#33442,#33443,
#33444,#33445,#33446,#33447,#33448,#33449,#33450,#33451,#33452,#33453,#33454,
#33455,#33456,#33457,#33458,#33459,#33460,#33461,#33462,#33463,#33464,#33465,
#33466,#33467,#33468,#33469,#33470,#33471,#33472,#33473,#33474,#33475,#33476,
#33477,#33478,#33479,#33480,#33481,#33482,#33483,#33484,#33485,#33486,#33487,
#33488,#33489,#33490,#33491,#33492,#33493,#33494,#33495,#33496,#33497,#33498,
#33499,#33500,#33501,#33502,#33503,#33504,#33505,#33506,#33507,#33508,#33509,
#33510,#33511,#33512,#33513,#33514),.UNSPECIFIED.,.F.,.F.,(4,3,3,3,3,3,
3,3,3,3,3,3,3,3,3,3,3,3,3,3,3,3,3,3,3,3,3,3,3,3,3,3,3,3,3,3,4),(-1.12653966532775,
-1.08530391285196,-1.03555276855992,-0.985995835290009,-0.974496002923742,
-0.967183166935604,-0.91832336204934,-0.869822308362971,-0.833246509766086,
-0.821905469284664,-0.815371903950458,-0.7966707111692,-0.748924248651515,
-0.700999781941695,-0.653716411224205,-0.620120974671593,-0.608348933883821,
-0.601406545427275,-0.554880462036058,-0.519334665013758,-0.472613715754773,
-0.426217598085471,-0.404654215064511,-0.397976636695719,-0.39279019656135,
-0.347324049934313,-0.300517291926052,-0.253710533917792,-0.221996717178068,
-0.205387451447631,-0.194998278294185,-0.189039958905823,-0.144864372719162,
-0.100707094611733,-0.0569734906965891,-0.014190031158235,0.),
 .UNSPECIFIED.);
#1328=B_SPLINE_CURVE_WITH_KNOTS('',3,(#33517,#33518,#33519,#33520,#33521,
#33522,#33523,#33524,#33525,#33526,#33527,#33528),.UNSPECIFIED.,.F.,.F.,
(4,1,1,1,1,1,1,1,1,4),(11.6154215191109,12.1154145856246,12.6154076521384,
13.1154007186521,13.6153937851658,14.1153868516796,14.6153799181933,15.1153729847071,
15.6153660512208,15.7079632679491),.UNSPECIFIED.);
#1329=B_SPLINE_CURVE_WITH_KNOTS('',3,(#35270,#35271,#35272,#35273,#35274,
#35275,#35276,#35277,#35278,#35279,#35280,#35281,#35282,#35283,#35284,#35285,
#35286,#35287,#35288,#35289,#35290,#35291,#35292,#35293,#35294,#35295,#35296,
#35297,#35298,#35299,#35300,#35301,#35302,#35303,#35304,#35305,#35306,#35307,
#35308,#35309,#35310,#35311,#35312,#35313,#35314,#35315,#35316,#35317,#35318,
#35319,#35320,#35321,#35322,#35323,#35324,#35325,#35326,#35327,#35328,#35329,
#35330,#35331,#35332,#35333,#35334,#35335,#35336,#35337,#35338,#35339,#35340,
#35341,#35342,#35343,#35344,#35345,#35346,#35347,#35348,#35349,#35350,#35351,
#35352,#35353,#35354,#35355,#35356,#35357,#35358,#35359,#35360,#35361,#35362,
#35363,#35364,#35365,#35366,#35367,#35368,#35369,#35370,#35371,#35372,#35373,
#35374,#35375,#35376,#35377,#35378,#35379,#35380,#35381),.UNSPECIFIED.,
 .F.,.F.,(4,3,3,3,3,3,3,3,3,3,3,3,3,3,3,3,3,3,3,3,3,3,3,3,3,3,3,3,3,3,3,
3,3,3,3,3,3,4),(-1.13094109509772,-1.09616481350043,-1.05252904104694,-1.02447554499396,
-1.00950008690807,-1.00036001955662,-0.993301660201014,-0.948452303677702,
-0.903330514169959,-0.871780315013978,-0.865172021997021,-0.858235221378188,
-0.840230115857997,-0.795263319046307,-0.749591768714079,-0.703490054519165,
-0.670607572880205,-0.66083775307683,-0.654974365605059,-0.607853006298655,
-0.571960127963325,-0.52511778596238,-0.477884605450088,-0.454625079979972,
-0.446675651987665,-0.440719364207499,-0.392733749190471,-0.342271075439817,
-0.291808401689163,-0.255332351478017,-0.239279102558647,-0.229201322023436,
-0.222814957347981,-0.174288174494182,-0.124750035428491,-0.0750207266400787,
-0.025677316928006,0.),.UNSPECIFIED.);
#1330=B_SPLINE_CURVE_WITH_KNOTS('',3,(#35382,#35383,#35384,#35385,#35386,
#35387,#35388,#35389,#35390,#35391,#35392,#35393,#35394,#35395,#35396,#35397,
#35398,#35399,#35400,#35401,#35402,#35403,#35404,#35405,#35406,#35407,#35408,
#35409,#35410,#35411,#35412),.UNSPECIFIED.,.F.,.F.,(4,3,3,3,3,3,3,3,3,3,
4),(-215.997004733934,-215.49701166742,-214.997018600906,-214.497025534392,
-213.997032467879,-213.497039401365,-212.997046334851,-212.497053268337,
-211.997060201824,-211.49706713531,-211.437656885764),.UNSPECIFIED.);
#1528=CYLINDRICAL_SURFACE('',#16358,5.91675);
#1529=CYLINDRICAL_SURFACE('',#16360,5.91675);
#1530=CYLINDRICAL_SURFACE('',#16361,5.91675);
#1531=CYLINDRICAL_SURFACE('',#16362,5.91675);
#1532=CYLINDRICAL_SURFACE('',#16363,5.91675);
#1533=CYLINDRICAL_SURFACE('',#16364,5.91675);
#1534=CYLINDRICAL_SURFACE('',#16365,5.91675);
#1535=CYLINDRICAL_SURFACE('',#16366,5.91675);
#1536=CYLINDRICAL_SURFACE('',#16367,5.91675);
#1537=CYLINDRICAL_SURFACE('',#16368,5.91675);
#1538=CYLINDRICAL_SURFACE('',#16369,5.91675);
#1539=CYLINDRICAL_SURFACE('',#16370,5.91675);
#1540=CYLINDRICAL_SURFACE('',#16371,5.91675);
#1541=CYLINDRICAL_SURFACE('',#16372,5.91675);
#1542=CYLINDRICAL_SURFACE('',#16373,5.91675);
#1543=CYLINDRICAL_SURFACE('',#16374,5.91675);
#1544=CYLINDRICAL_SURFACE('',#16375,5.91675);
#1545=CYLINDRICAL_SURFACE('',#16376,5.91675);
#1546=CYLINDRICAL_SURFACE('',#16377,5.91675);
#1547=CYLINDRICAL_SURFACE('',#16378,5.91675);
#1548=CYLINDRICAL_SURFACE('',#16379,5.91675);
#1549=CYLINDRICAL_SURFACE('',#16380,5.91675);
#1550=CYLINDRICAL_SURFACE('',#16381,5.91675);
#1551=CYLINDRICAL_SURFACE('',#16382,5.91675);
#1552=CYLINDRICAL_SURFACE('',#16383,5.91675);
#1553=CYLINDRICAL_SURFACE('',#16384,5.91675);
#1554=CYLINDRICAL_SURFACE('',#16385,5.91675);
#1555=CYLINDRICAL_SURFACE('',#16386,5.91675);
#1556=CYLINDRICAL_SURFACE('',#16387,5.91675);
#1557=CYLINDRICAL_SURFACE('',#16388,5.91675);
#1558=CYLINDRICAL_SURFACE('',#16389,5.91675);
#1559=CYLINDRICAL_SURFACE('',#16390,5.91675);
#1560=CYLINDRICAL_SURFACE('',#16391,5.91675);
#1561=CYLINDRICAL_SURFACE('',#16392,5.91675);
#1562=CYLINDRICAL_SURFACE('',#16393,4.91825);
#1563=CYLINDRICAL_SURFACE('',#16395,4.91825);
#1564=CYLINDRICAL_SURFACE('',#16396,4.91825);
#1565=CYLINDRICAL_SURFACE('',#16397,4.91825);
#1566=CYLINDRICAL_SURFACE('',#16398,4.91825);
#1567=CYLINDRICAL_SURFACE('',#16399,4.91825);
#1568=CYLINDRICAL_SURFACE('',#16400,4.91825);
#1569=CYLINDRICAL_SURFACE('',#16401,4.91825);
#1570=CYLINDRICAL_SURFACE('',#16402,4.91825);
#1571=CYLINDRICAL_SURFACE('',#16403,4.91825);
#1572=CYLINDRICAL_SURFACE('',#16404,4.91825);
#1573=CYLINDRICAL_SURFACE('',#16405,4.91825);
#1574=CYLINDRICAL_SURFACE('',#16406,4.91825);
#1575=CYLINDRICAL_SURFACE('',#16407,4.91825);
#1576=CYLINDRICAL_SURFACE('',#16408,4.91825);
#1577=CYLINDRICAL_SURFACE('',#16409,4.91825);
#1578=CYLINDRICAL_SURFACE('',#16410,4.91825);
#1579=CYLINDRICAL_SURFACE('',#16411,4.91825);
#1580=CYLINDRICAL_SURFACE('',#16412,4.91825);
#1581=CYLINDRICAL_SURFACE('',#16413,4.91825);
#1582=CYLINDRICAL_SURFACE('',#16414,4.91825);
#1583=CYLINDRICAL_SURFACE('',#16415,4.91825);
#1584=CYLINDRICAL_SURFACE('',#16416,4.91825);
#1585=CYLINDRICAL_SURFACE('',#16417,4.91825);
#1586=CYLINDRICAL_SURFACE('',#16418,4.91825);
#1587=CYLINDRICAL_SURFACE('',#16419,4.91825);
#1588=CYLINDRICAL_SURFACE('',#16420,4.91825);
#1589=CYLINDRICAL_SURFACE('',#16421,4.91825);
#1590=CYLINDRICAL_SURFACE('',#16422,4.91825);
#1591=CYLINDRICAL_SURFACE('',#16423,4.91825);
#1592=CYLINDRICAL_SURFACE('',#16424,4.91825);
#1593=CYLINDRICAL_SURFACE('',#16425,4.91825);
#1594=CYLINDRICAL_SURFACE('',#16426,4.91825);
#1595=CYLINDRICAL_SURFACE('',#16427,4.91825);
#1596=CYLINDRICAL_SURFACE('',#16432,4.91825);
#1597=CYLINDRICAL_SURFACE('',#16661,5.91675);
#1598=CYLINDRICAL_SURFACE('',#16665,9.);
#2210=FACE_OUTER_BOUND('',#3197,.T.);
#2211=FACE_OUTER_BOUND('',#3198,.T.);
#2212=FACE_OUTER_BOUND('',#3199,.T.);
#2213=FACE_OUTER_BOUND('',#3200,.T.);
#2214=FACE_OUTER_BOUND('',#3201,.T.);
#2215=FACE_OUTER_BOUND('',#3202,.T.);
#2216=FACE_OUTER_BOUND('',#3203,.T.);
#2217=FACE_OUTER_BOUND('',#3204,.T.);
#2218=FACE_OUTER_BOUND('',#3205,.T.);
#2219=FACE_OUTER_BOUND('',#3206,.T.);
#2220=FACE_OUTER_BOUND('',#3207,.T.);
#2221=FACE_OUTER_BOUND('',#3208,.T.);
#2222=FACE_OUTER_BOUND('',#3209,.T.);
#2223=FACE_OUTER_BOUND('',#3210,.T.);
#2224=FACE_OUTER_BOUND('',#3211,.T.);
#2225=FACE_OUTER_BOUND('',#3212,.T.);
#2226=FACE_OUTER_BOUND('',#3213,.T.);
#2227=FACE_OUTER_BOUND('',#3214,.T.);
#2228=FACE_OUTER_BOUND('',#3215,.T.);
#2229=FACE_OUTER_BOUND('',#3216,.T.);
#2230=FACE_OUTER_BOUND('',#3217,.T.);
#2231=FACE_OUTER_BOUND('',#3218,.T.);
#2232=FACE_OUTER_BOUND('',#3219,.T.);
#2233=FACE_OUTER_BOUND('',#3220,.T.);
#2234=FACE_OUTER_BOUND('',#3221,.T.);
#2235=FACE_OUTER_BOUND('',#3222,.T.);
#2236=FACE_OUTER_BOUND('',#3223,.T.);
#2237=FACE_OUTER_BOUND('',#3224,.T.);
#2238=FACE_OUTER_BOUND('',#3225,.T.);
#2239=FACE_OUTER_BOUND('',#3226,.T.);
#2240=FACE_OUTER_BOUND('',#3227,.T.);
#2241=FACE_OUTER_BOUND('',#3228,.T.);
#2242=FACE_OUTER_BOUND('',#3229,.T.);
#2243=FACE_OUTER_BOUND('',#3230,.T.);
#2244=FACE_OUTER_BOUND('',#3231,.T.);
#2245=FACE_OUTER_BOUND('',#3232,.T.);
#2246=FACE_OUTER_BOUND('',#3233,.T.);
#2247=FACE_OUTER_BOUND('',#3234,.T.);
#2248=FACE_OUTER_BOUND('',#3235,.T.);
#2249=FACE_OUTER_BOUND('',#3236,.T.);
#2250=FACE_OUTER_BOUND('',#3237,.T.);
#2251=FACE_OUTER_BOUND('',#3238,.T.);
#2252=FACE_OUTER_BOUND('',#3239,.T.);
#2253=FACE_OUTER_BOUND('',#3240,.T.);
#2254=FACE_OUTER_BOUND('',#3241,.T.);
#2255=FACE_OUTER_BOUND('',#3242,.T.);
#2256=FACE_OUTER_BOUND('',#3243,.T.);
#2257=FACE_OUTER_BOUND('',#3244,.T.);
#2258=FACE_OUTER_BOUND('',#3245,.T.);
#2259=FACE_OUTER_BOUND('',#3246,.T.);
#2260=FACE_OUTER_BOUND('',#3247,.T.);
#2261=FACE_OUTER_BOUND('',#3248,.T.);
#2262=FACE_OUTER_BOUND('',#3249,.T.);
#2263=FACE_OUTER_BOUND('',#3250,.T.);
#2264=FACE_OUTER_BOUND('',#3251,.T.);
#2265=FACE_OUTER_BOUND('',#3252,.T.);
#2266=FACE_OUTER_BOUND('',#3253,.T.);
#2267=FACE_OUTER_BOUND('',#3254,.T.);
#2268=FACE_OUTER_BOUND('',#3255,.T.);
#2269=FACE_OUTER_BOUND('',#3256,.T.);
#2270=FACE_OUTER_BOUND('',#3257,.T.);
#2271=FACE_OUTER_BOUND('',#3258,.T.);
#2272=FACE_OUTER_BOUND('',#3259,.T.);
#2273=FACE_OUTER_BOUND('',#3260,.T.);
#2274=FACE_OUTER_BOUND('',#3261,.T.);
#2275=FACE_OUTER_BOUND('',#3262,.T.);
#2276=FACE_OUTER_BOUND('',#3263,.T.);
#2277=FACE_OUTER_BOUND('',#3264,.T.);
#2278=FACE_OUTER_BOUND('',#3265,.T.);
#2279=FACE_OUTER_BOUND('',#3266,.T.);
#2280=FACE_OUTER_BOUND('',#3267,.T.);
#2281=FACE_OUTER_BOUND('',#3268,.T.);
#2282=FACE_OUTER_BOUND('',#3269,.T.);
#2283=FACE_OUTER_BOUND('',#3270,.T.);
#2284=FACE_OUTER_BOUND('',#3271,.T.);
#2285=FACE_OUTER_BOUND('',#3272,.T.);
#2286=FACE_OUTER_BOUND('',#3273,.T.);
#2287=FACE_OUTER_BOUND('',#3274,.T.);
#2288=FACE_OUTER_BOUND('',#3275,.T.);
#2289=FACE_OUTER_BOUND('',#3276,.T.);
#2290=FACE_OUTER_BOUND('',#3277,.T.);
#2291=FACE_OUTER_BOUND('',#3278,.T.);
#2292=FACE_OUTER_BOUND('',#3279,.T.);
#2293=FACE_OUTER_BOUND('',#3280,.T.);
#2294=FACE_OUTER_BOUND('',#3281,.T.);
#2295=FACE_OUTER_BOUND('',#3282,.T.);
#2296=FACE_OUTER_BOUND('',#3283,.T.);
#2297=FACE_OUTER_BOUND('',#3284,.T.);
#2298=FACE_OUTER_BOUND('',#3285,.T.);
#2299=FACE_OUTER_BOUND('',#3286,.T.);
#2300=FACE_OUTER_BOUND('',#3287,.T.);
#2301=FACE_OUTER_BOUND('',#3288,.T.);
#2302=FACE_OUTER_BOUND('',#3289,.T.);
#2303=FACE_OUTER_BOUND('',#3290,.T.);
#2304=FACE_OUTER_BOUND('',#3291,.T.);
#2305=FACE_OUTER_BOUND('',#3292,.T.);
#2306=FACE_OUTER_BOUND('',#3293,.T.);
#2307=FACE_OUTER_BOUND('',#3294,.T.);
#2308=FACE_OUTER_BOUND('',#3295,.T.);
#2309=FACE_OUTER_BOUND('',#3296,.T.);
#2310=FACE_OUTER_BOUND('',#3297,.T.);
#2311=FACE_OUTER_BOUND('',#3298,.T.);
#2312=FACE_OUTER_BOUND('',#3299,.T.);
#2313=FACE_OUTER_BOUND('',#3300,.T.);
#2314=FACE_OUTER_BOUND('',#3301,.T.);
#2315=FACE_OUTER_BOUND('',#3302,.T.);
#2316=FACE_OUTER_BOUND('',#3303,.T.);
#2317=FACE_OUTER_BOUND('',#3304,.T.);
#2318=FACE_OUTER_BOUND('',#3305,.T.);
#2319=FACE_OUTER_BOUND('',#3306,.T.);
#2320=FACE_OUTER_BOUND('',#3307,.T.);
#2321=FACE_OUTER_BOUND('',#3308,.T.);
#2322=FACE_OUTER_BOUND('',#3309,.T.);
#2323=FACE_OUTER_BOUND('',#3310,.T.);
#2324=FACE_OUTER_BOUND('',#3311,.T.);
#2325=FACE_OUTER_BOUND('',#3312,.T.);
#2326=FACE_OUTER_BOUND('',#3313,.T.);
#2327=FACE_OUTER_BOUND('',#3314,.T.);
#2328=FACE_OUTER_BOUND('',#3315,.T.);
#2329=FACE_OUTER_BOUND('',#3316,.T.);
#2330=FACE_OUTER_BOUND('',#3317,.T.);
#2331=FACE_OUTER_BOUND('',#3318,.T.);
#2332=FACE_OUTER_BOUND('',#3319,.T.);
#2333=FACE_OUTER_BOUND('',#3320,.T.);
#2334=FACE_OUTER_BOUND('',#3321,.T.);
#2335=FACE_OUTER_BOUND('',#3322,.T.);
#2336=FACE_OUTER_BOUND('',#3323,.T.);
#2337=FACE_OUTER_BOUND('',#3324,.T.);
#2338=FACE_OUTER_BOUND('',#3325,.T.);
#2339=FACE_OUTER_BOUND('',#3326,.T.);
#2340=FACE_OUTER_BOUND('',#3327,.T.);
#2341=FACE_OUTER_BOUND('',#3328,.T.);
#2342=FACE_OUTER_BOUND('',#3329,.T.);
#2343=FACE_OUTER_BOUND('',#3330,.T.);
#2344=FACE_OUTER_BOUND('',#3331,.T.);
#2345=FACE_OUTER_BOUND('',#3332,.T.);
#2346=FACE_OUTER_BOUND('',#3333,.T.);
#2347=FACE_OUTER_BOUND('',#3334,.T.);
#2348=FACE_OUTER_BOUND('',#3335,.T.);
#2349=FACE_OUTER_BOUND('',#3336,.T.);
#2350=FACE_OUTER_BOUND('',#3337,.T.);
#2351=FACE_OUTER_BOUND('',#3338,.T.);
#2352=FACE_OUTER_BOUND('',#3339,.T.);
#2353=FACE_OUTER_BOUND('',#3340,.T.);
#2354=FACE_OUTER_BOUND('',#3341,.T.);
#2355=FACE_OUTER_BOUND('',#3342,.T.);
#2356=FACE_OUTER_BOUND('',#3343,.T.);
#2357=FACE_OUTER_BOUND('',#3344,.T.);
#2358=FACE_OUTER_BOUND('',#3345,.T.);
#2359=FACE_OUTER_BOUND('',#3346,.T.);
#2360=FACE_OUTER_BOUND('',#3347,.T.);
#2361=FACE_OUTER_BOUND('',#3348,.T.);
#2362=FACE_OUTER_BOUND('',#3349,.T.);
#2363=FACE_OUTER_BOUND('',#3350,.T.);
#2364=FACE_OUTER_BOUND('',#3351,.T.);
#2365=FACE_OUTER_BOUND('',#3352,.T.);
#2366=FACE_OUTER_BOUND('',#3353,.T.);
#2367=FACE_OUTER_BOUND('',#3354,.T.);
#2368=FACE_OUTER_BOUND('',#3355,.T.);
#2369=FACE_OUTER_BOUND('',#3356,.T.);
#2370=FACE_OUTER_BOUND('',#3357,.T.);
#2371=FACE_OUTER_BOUND('',#3358,.T.);
#2372=FACE_OUTER_BOUND('',#3359,.T.);
#2373=FACE_OUTER_BOUND('',#3360,.T.);
#2374=FACE_OUTER_BOUND('',#3361,.T.);
#2375=FACE_OUTER_BOUND('',#3362,.T.);
#2376=FACE_OUTER_BOUND('',#3363,.T.);
#2377=FACE_OUTER_BOUND('',#3364,.T.);
#2378=FACE_OUTER_BOUND('',#3365,.T.);
#2379=FACE_OUTER_BOUND('',#3366,.T.);
#2380=FACE_OUTER_BOUND('',#3367,.T.);
#2381=FACE_OUTER_BOUND('',#3368,.T.);
#2382=FACE_OUTER_BOUND('',#3369,.T.);
#2383=FACE_OUTER_BOUND('',#3370,.T.);
#2384=FACE_OUTER_BOUND('',#3371,.T.);
#2385=FACE_OUTER_BOUND('',#3372,.T.);
#2386=FACE_OUTER_BOUND('',#3373,.T.);
#2387=FACE_OUTER_BOUND('',#3374,.T.);
#2388=FACE_OUTER_BOUND('',#3375,.T.);
#2389=FACE_OUTER_BOUND('',#3376,.T.);
#2390=FACE_OUTER_BOUND('',#3377,.T.);
#2391=FACE_OUTER_BOUND('',#3378,.T.);
#2392=FACE_OUTER_BOUND('',#3379,.T.);
#2393=FACE_OUTER_BOUND('',#3380,.T.);
#2394=FACE_OUTER_BOUND('',#3381,.T.);
#2395=FACE_OUTER_BOUND('',#3382,.T.);
#2396=FACE_OUTER_BOUND('',#3383,.T.);
#2397=FACE_OUTER_BOUND('',#3384,.T.);
#2398=FACE_OUTER_BOUND('',#3385,.T.);
#2399=FACE_OUTER_BOUND('',#3386,.T.);
#2400=FACE_OUTER_BOUND('',#3387,.T.);
#2401=FACE_OUTER_BOUND('',#3388,.T.);
#2402=FACE_OUTER_BOUND('',#3389,.T.);
#2403=FACE_OUTER_BOUND('',#3390,.T.);
#2404=FACE_OUTER_BOUND('',#3391,.T.);
#2405=FACE_OUTER_BOUND('',#3392,.T.);
#2406=FACE_OUTER_BOUND('',#3393,.T.);
#2407=FACE_OUTER_BOUND('',#3394,.T.);
#2408=FACE_OUTER_BOUND('',#3395,.T.);
#2409=FACE_OUTER_BOUND('',#3396,.T.);
#2410=FACE_OUTER_BOUND('',#3397,.T.);
#2411=FACE_OUTER_BOUND('',#3398,.T.);
#2412=FACE_OUTER_BOUND('',#3399,.T.);
#2413=FACE_OUTER_BOUND('',#3400,.T.);
#2414=FACE_OUTER_BOUND('',#3401,.T.);
#2415=FACE_OUTER_BOUND('',#3402,.T.);
#2416=FACE_OUTER_BOUND('',#3403,.T.);
#2417=FACE_OUTER_BOUND('',#3404,.T.);
#2418=FACE_OUTER_BOUND('',#3405,.T.);
#2419=FACE_OUTER_BOUND('',#3406,.T.);
#2420=FACE_OUTER_BOUND('',#3407,.T.);
#2421=FACE_OUTER_BOUND('',#3408,.T.);
#2422=FACE_OUTER_BOUND('',#3409,.T.);
#2423=FACE_OUTER_BOUND('',#3410,.T.);
#2424=FACE_OUTER_BOUND('',#3411,.T.);
#2425=FACE_OUTER_BOUND('',#3412,.T.);
#2426=FACE_OUTER_BOUND('',#3413,.T.);
#2427=FACE_OUTER_BOUND('',#3414,.T.);
#2428=FACE_OUTER_BOUND('',#3415,.T.);
#2429=FACE_OUTER_BOUND('',#3416,.T.);
#2430=FACE_OUTER_BOUND('',#3417,.T.);
#2431=FACE_OUTER_BOUND('',#3418,.T.);
#2432=FACE_OUTER_BOUND('',#3419,.T.);
#2433=FACE_OUTER_BOUND('',#3420,.T.);
#2434=FACE_OUTER_BOUND('',#3421,.T.);
#2435=FACE_OUTER_BOUND('',#3422,.T.);
#2436=FACE_OUTER_BOUND('',#3423,.T.);
#2437=FACE_OUTER_BOUND('',#3425,.T.);
#2438=FACE_OUTER_BOUND('',#3461,.T.);
#2439=FACE_OUTER_BOUND('',#3462,.T.);
#3197=EDGE_LOOP('',(#12665,#12666,#12667,#12668));
#3198=EDGE_LOOP('',(#12669,#12670,#12671,#12672));
#3199=EDGE_LOOP('',(#12673,#12674,#12675,#12676));
#3200=EDGE_LOOP('',(#12677,#12678,#12679,#12680));
#3201=EDGE_LOOP('',(#12681,#12682,#12683,#12684));
#3202=EDGE_LOOP('',(#12685,#12686,#12687,#12688));
#3203=EDGE_LOOP('',(#12689,#12690,#12691,#12692));
#3204=EDGE_LOOP('',(#12693,#12694,#12695,#12696));
#3205=EDGE_LOOP('',(#12697,#12698,#12699,#12700));
#3206=EDGE_LOOP('',(#12701,#12702,#12703,#12704));
#3207=EDGE_LOOP('',(#12705,#12706,#12707,#12708));
#3208=EDGE_LOOP('',(#12709,#12710,#12711,#12712));
#3209=EDGE_LOOP('',(#12713,#12714,#12715,#12716));
#3210=EDGE_LOOP('',(#12717,#12718,#12719,#12720));
#3211=EDGE_LOOP('',(#12721,#12722,#12723,#12724));
#3212=EDGE_LOOP('',(#12725,#12726,#12727,#12728));
#3213=EDGE_LOOP('',(#12729,#12730,#12731,#12732));
#3214=EDGE_LOOP('',(#12733,#12734,#12735,#12736));
#3215=EDGE_LOOP('',(#12737,#12738,#12739,#12740));
#3216=EDGE_LOOP('',(#12741,#12742,#12743,#12744));
#3217=EDGE_LOOP('',(#12745,#12746,#12747,#12748));
#3218=EDGE_LOOP('',(#12749,#12750,#12751,#12752));
#3219=EDGE_LOOP('',(#12753,#12754,#12755,#12756));
#3220=EDGE_LOOP('',(#12757,#12758,#12759,#12760));
#3221=EDGE_LOOP('',(#12761,#12762,#12763,#12764));
#3222=EDGE_LOOP('',(#12765,#12766,#12767,#12768));
#3223=EDGE_LOOP('',(#12769,#12770,#12771,#12772));
#3224=EDGE_LOOP('',(#12773,#12774,#12775,#12776));
#3225=EDGE_LOOP('',(#12777,#12778,#12779,#12780));
#3226=EDGE_LOOP('',(#12781,#12782,#12783,#12784));
#3227=EDGE_LOOP('',(#12785,#12786,#12787,#12788));
#3228=EDGE_LOOP('',(#12789,#12790,#12791,#12792));
#3229=EDGE_LOOP('',(#12793,#12794,#12795,#12796));
#3230=EDGE_LOOP('',(#12797,#12798,#12799,#12800));
#3231=EDGE_LOOP('',(#12801,#12802,#12803,#12804));
#3232=EDGE_LOOP('',(#12805,#12806,#12807,#12808));
#3233=EDGE_LOOP('',(#12809,#12810,#12811,#12812));
#3234=EDGE_LOOP('',(#12813,#12814,#12815,#12816));
#3235=EDGE_LOOP('',(#12817,#12818,#12819,#12820));
#3236=EDGE_LOOP('',(#12821,#12822,#12823,#12824));
#3237=EDGE_LOOP('',(#12825,#12826,#12827,#12828));
#3238=EDGE_LOOP('',(#12829,#12830,#12831,#12832));
#3239=EDGE_LOOP('',(#12833,#12834,#12835,#12836));
#3240=EDGE_LOOP('',(#12837,#12838,#12839,#12840));
#3241=EDGE_LOOP('',(#12841,#12842,#12843,#12844));
#3242=EDGE_LOOP('',(#12845,#12846,#12847,#12848));
#3243=EDGE_LOOP('',(#12849,#12850,#12851,#12852));
#3244=EDGE_LOOP('',(#12853,#12854,#12855,#12856));
#3245=EDGE_LOOP('',(#12857,#12858,#12859,#12860));
#3246=EDGE_LOOP('',(#12861,#12862,#12863,#12864));
#3247=EDGE_LOOP('',(#12865,#12866,#12867,#12868));
#3248=EDGE_LOOP('',(#12869,#12870,#12871,#12872));
#3249=EDGE_LOOP('',(#12873,#12874,#12875,#12876));
#3250=EDGE_LOOP('',(#12877,#12878,#12879,#12880));
#3251=EDGE_LOOP('',(#12881,#12882,#12883,#12884));
#3252=EDGE_LOOP('',(#12885,#12886,#12887,#12888));
#3253=EDGE_LOOP('',(#12889,#12890,#12891,#12892));
#3254=EDGE_LOOP('',(#12893,#12894,#12895,#12896));
#3255=EDGE_LOOP('',(#12897,#12898,#12899,#12900));
#3256=EDGE_LOOP('',(#12901,#12902,#12903,#12904));
#3257=EDGE_LOOP('',(#12905,#12906,#12907,#12908));
#3258=EDGE_LOOP('',(#12909,#12910,#12911,#12912));
#3259=EDGE_LOOP('',(#12913,#12914,#12915,#12916));
#3260=EDGE_LOOP('',(#12917,#12918,#12919,#12920));
#3261=EDGE_LOOP('',(#12921,#12922,#12923,#12924));
#3262=EDGE_LOOP('',(#12925,#12926,#12927,#12928));
#3263=EDGE_LOOP('',(#12929,#12930,#12931,#12932));
#3264=EDGE_LOOP('',(#12933,#12934,#12935,#12936));
#3265=EDGE_LOOP('',(#12937,#12938,#12939,#12940,#12941,#12942,#12943,#12944,
#12945,#12946,#12947,#12948,#12949,#12950,#12951,#12952,#12953,#12954,#12955,
#12956,#12957,#12958,#12959,#12960,#12961,#12962,#12963,#12964,#12965,#12966,
#12967,#12968,#12969,#12970,#12971,#12972,#12973,#12974,#12975,#12976,#12977,
#12978,#12979,#12980,#12981,#12982,#12983,#12984,#12985,#12986,#12987,#12988,
#12989,#12990,#12991,#12992,#12993,#12994,#12995,#12996,#12997,#12998,#12999,
#13000,#13001,#13002,#13003,#13004,#13005,#13006,#13007,#13008));
#3266=EDGE_LOOP('',(#13009,#13010,#13011,#13012,#13013));
#3267=EDGE_LOOP('',(#13014,#13015,#13016,#13017));
#3268=EDGE_LOOP('',(#13018,#13019,#13020,#13021,#13022,#13023,#13024,#13025,
#13026,#13027,#13028,#13029,#13030,#13031,#13032,#13033,#13034,#13035,#13036,
#13037,#13038,#13039,#13040,#13041,#13042,#13043,#13044,#13045,#13046,#13047,
#13048,#13049,#13050,#13051,#13052,#13053,#13054,#13055,#13056,#13057,#13058,
#13059,#13060,#13061,#13062,#13063,#13064,#13065,#13066,#13067,#13068,#13069,
#13070,#13071,#13072,#13073,#13074,#13075,#13076,#13077,#13078,#13079,#13080,
#13081,#13082,#13083,#13084,#13085,#13086,#13087,#13088,#13089));
#3269=EDGE_LOOP('',(#13090,#13091,#13092,#13093));
#3270=EDGE_LOOP('',(#13094,#13095,#13096));
#3271=EDGE_LOOP('',(#13097,#13098,#13099,#13100));
#3272=EDGE_LOOP('',(#13101,#13102,#13103));
#3273=EDGE_LOOP('',(#13104,#13105,#13106,#13107));
#3274=EDGE_LOOP('',(#13108,#13109,#13110));
#3275=EDGE_LOOP('',(#13111,#13112,#13113,#13114));
#3276=EDGE_LOOP('',(#13115,#13116,#13117));
#3277=EDGE_LOOP('',(#13118,#13119,#13120,#13121));
#3278=EDGE_LOOP('',(#13122,#13123,#13124));
#3279=EDGE_LOOP('',(#13125,#13126,#13127,#13128));
#3280=EDGE_LOOP('',(#13129,#13130,#13131));
#3281=EDGE_LOOP('',(#13132,#13133,#13134,#13135));
#3282=EDGE_LOOP('',(#13136,#13137,#13138));
#3283=EDGE_LOOP('',(#13139,#13140,#13141,#13142));
#3284=EDGE_LOOP('',(#13143,#13144,#13145));
#3285=EDGE_LOOP('',(#13146,#13147,#13148,#13149));
#3286=EDGE_LOOP('',(#13150,#13151,#13152));
#3287=EDGE_LOOP('',(#13153,#13154,#13155,#13156));
#3288=EDGE_LOOP('',(#13157,#13158,#13159));
#3289=EDGE_LOOP('',(#13160,#13161,#13162,#13163));
#3290=EDGE_LOOP('',(#13164,#13165,#13166));
#3291=EDGE_LOOP('',(#13167,#13168,#13169,#13170));
#3292=EDGE_LOOP('',(#13171,#13172,#13173));
#3293=EDGE_LOOP('',(#13174,#13175,#13176,#13177));
#3294=EDGE_LOOP('',(#13178,#13179,#13180));
#3295=EDGE_LOOP('',(#13181,#13182,#13183,#13184));
#3296=EDGE_LOOP('',(#13185,#13186,#13187));
#3297=EDGE_LOOP('',(#13188,#13189,#13190,#13191));
#3298=EDGE_LOOP('',(#13192,#13193,#13194));
#3299=EDGE_LOOP('',(#13195,#13196,#13197,#13198));
#3300=EDGE_LOOP('',(#13199,#13200,#13201));
#3301=EDGE_LOOP('',(#13202,#13203,#13204,#13205));
#3302=EDGE_LOOP('',(#13206,#13207,#13208));
#3303=EDGE_LOOP('',(#13209,#13210,#13211,#13212));
#3304=EDGE_LOOP('',(#13213,#13214,#13215));
#3305=EDGE_LOOP('',(#13216,#13217,#13218,#13219));
#3306=EDGE_LOOP('',(#13220,#13221,#13222));
#3307=EDGE_LOOP('',(#13223,#13224,#13225,#13226));
#3308=EDGE_LOOP('',(#13227,#13228,#13229));
#3309=EDGE_LOOP('',(#13230,#13231,#13232,#13233));
#3310=EDGE_LOOP('',(#13234,#13235,#13236));
#3311=EDGE_LOOP('',(#13237,#13238,#13239,#13240));
#3312=EDGE_LOOP('',(#13241,#13242,#13243));
#3313=EDGE_LOOP('',(#13244,#13245,#13246,#13247));
#3314=EDGE_LOOP('',(#13248,#13249,#13250));
#3315=EDGE_LOOP('',(#13251,#13252,#13253,#13254));
#3316=EDGE_LOOP('',(#13255,#13256,#13257));
#3317=EDGE_LOOP('',(#13258,#13259,#13260,#13261));
#3318=EDGE_LOOP('',(#13262,#13263,#13264));
#3319=EDGE_LOOP('',(#13265,#13266,#13267,#13268));
#3320=EDGE_LOOP('',(#13269,#13270,#13271));
#3321=EDGE_LOOP('',(#13272,#13273,#13274,#13275));
#3322=EDGE_LOOP('',(#13276,#13277,#13278));
#3323=EDGE_LOOP('',(#13279,#13280,#13281,#13282));
#3324=EDGE_LOOP('',(#13283,#13284,#13285));
#3325=EDGE_LOOP('',(#13286,#13287,#13288,#13289));
#3326=EDGE_LOOP('',(#13290,#13291,#13292));
#3327=EDGE_LOOP('',(#13293,#13294,#13295,#13296));
#3328=EDGE_LOOP('',(#13297,#13298,#13299));
#3329=EDGE_LOOP('',(#13300,#13301,#13302,#13303));
#3330=EDGE_LOOP('',(#13304,#13305,#13306));
#3331=EDGE_LOOP('',(#13307,#13308,#13309,#13310));
#3332=EDGE_LOOP('',(#13311,#13312,#13313));
#3333=EDGE_LOOP('',(#13314,#13315,#13316,#13317));
#3334=EDGE_LOOP('',(#13318,#13319,#13320));
#3335=EDGE_LOOP('',(#13321,#13322,#13323,#13324));
#3336=EDGE_LOOP('',(#13325,#13326,#13327));
#3337=EDGE_LOOP('',(#13328,#13329,#13330,#13331));
#3338=EDGE_LOOP('',(#13332,#13333,#13334,#13335));
#3339=EDGE_LOOP('',(#13336,#13337,#13338,#13339));
#3340=EDGE_LOOP('',(#13340,#13341,#13342,#13343));
#3341=EDGE_LOOP('',(#13344,#13345,#13346,#13347));
#3342=EDGE_LOOP('',(#13348,#13349,#13350));
#3343=EDGE_LOOP('',(#13351,#13352,#13353,#13354));
#3344=EDGE_LOOP('',(#13355,#13356,#13357));
#3345=EDGE_LOOP('',(#13358,#13359,#13360,#13361));
#3346=EDGE_LOOP('',(#13362,#13363,#13364));
#3347=EDGE_LOOP('',(#13365,#13366,#13367,#13368));
#3348=EDGE_LOOP('',(#13369,#13370,#13371));
#3349=EDGE_LOOP('',(#13372,#13373,#13374,#13375));
#3350=EDGE_LOOP('',(#13376,#13377,#13378));
#3351=EDGE_LOOP('',(#13379,#13380,#13381,#13382));
#3352=EDGE_LOOP('',(#13383,#13384,#13385));
#3353=EDGE_LOOP('',(#13386,#13387,#13388,#13389));
#3354=EDGE_LOOP('',(#13390,#13391,#13392));
#3355=EDGE_LOOP('',(#13393,#13394,#13395,#13396));
#3356=EDGE_LOOP('',(#13397,#13398,#13399));
#3357=EDGE_LOOP('',(#13400,#13401,#13402,#13403));
#3358=EDGE_LOOP('',(#13404,#13405,#13406));
#3359=EDGE_LOOP('',(#13407,#13408,#13409,#13410));
#3360=EDGE_LOOP('',(#13411,#13412,#13413));
#3361=EDGE_LOOP('',(#13414,#13415,#13416,#13417));
#3362=EDGE_LOOP('',(#13418,#13419,#13420));
#3363=EDGE_LOOP('',(#13421,#13422,#13423,#13424));
#3364=EDGE_LOOP('',(#13425,#13426,#13427));
#3365=EDGE_LOOP('',(#13428,#13429,#13430,#13431));
#3366=EDGE_LOOP('',(#13432,#13433,#13434));
#3367=EDGE_LOOP('',(#13435,#13436,#13437,#13438));
#3368=EDGE_LOOP('',(#13439,#13440,#13441));
#3369=EDGE_LOOP('',(#13442,#13443,#13444,#13445));
#3370=EDGE_LOOP('',(#13446,#13447,#13448));
#3371=EDGE_LOOP('',(#13449,#13450,#13451,#13452));
#3372=EDGE_LOOP('',(#13453,#13454,#13455));
#3373=EDGE_LOOP('',(#13456,#13457,#13458,#13459));
#3374=EDGE_LOOP('',(#13460,#13461,#13462));
#3375=EDGE_LOOP('',(#13463,#13464,#13465,#13466));
#3376=EDGE_LOOP('',(#13467,#13468,#13469));
#3377=EDGE_LOOP('',(#13470,#13471,#13472,#13473));
#3378=EDGE_LOOP('',(#13474,#13475,#13476));
#3379=EDGE_LOOP('',(#13477,#13478,#13479,#13480));
#3380=EDGE_LOOP('',(#13481,#13482,#13483));
#3381=EDGE_LOOP('',(#13484,#13485,#13486,#13487));
#3382=EDGE_LOOP('',(#13488,#13489,#13490));
#3383=EDGE_LOOP('',(#13491,#13492,#13493,#13494));
#3384=EDGE_LOOP('',(#13495,#13496,#13497));
#3385=EDGE_LOOP('',(#13498,#13499,#13500,#13501));
#3386=EDGE_LOOP('',(#13502,#13503,#13504));
#3387=EDGE_LOOP('',(#13505,#13506,#13507,#13508));
#3388=EDGE_LOOP('',(#13509,#13510,#13511));
#3389=EDGE_LOOP('',(#13512,#13513,#13514,#13515));
#3390=EDGE_LOOP('',(#13516,#13517,#13518));
#3391=EDGE_LOOP('',(#13519,#13520,#13521,#13522));
#3392=EDGE_LOOP('',(#13523,#13524,#13525));
#3393=EDGE_LOOP('',(#13526,#13527,#13528,#13529));
#3394=EDGE_LOOP('',(#13530,#13531,#13532));
#3395=EDGE_LOOP('',(#13533,#13534,#13535,#13536));
#3396=EDGE_LOOP('',(#13537,#13538,#13539));
#3397=EDGE_LOOP('',(#13540,#13541,#13542,#13543));
#3398=EDGE_LOOP('',(#13544,#13545,#13546));
#3399=EDGE_LOOP('',(#13547,#13548,#13549,#13550));
#3400=EDGE_LOOP('',(#13551,#13552,#13553));
#3401=EDGE_LOOP('',(#13554,#13555,#13556,#13557));
#3402=EDGE_LOOP('',(#13558,#13559,#13560));
#3403=EDGE_LOOP('',(#13561,#13562,#13563,#13564));
#3404=EDGE_LOOP('',(#13565,#13566,#13567));
#3405=EDGE_LOOP('',(#13568,#13569,#13570,#13571));
#3406=EDGE_LOOP('',(#13572,#13573,#13574));
#3407=EDGE_LOOP('',(#13575,#13576,#13577,#13578));
#3408=EDGE_LOOP('',(#13579,#13580,#13581));
#3409=EDGE_LOOP('',(#13582,#13583,#13584,#13585));
#3410=EDGE_LOOP('',(#13586,#13587,#13588));
#3411=EDGE_LOOP('',(#13589,#13590,#13591,#13592));
#3412=EDGE_LOOP('',(#13593,#13594,#13595));
#3413=EDGE_LOOP('',(#13596,#13597,#13598,#13599));
#3414=EDGE_LOOP('',(#13600,#13601,#13602,#13603));
#3415=EDGE_LOOP('',(#13604,#13605,#13606,#13607));
#3416=EDGE_LOOP('',(#13608,#13609,#13610,#13611));
#3417=EDGE_LOOP('',(#13612,#13613,#13614,#13615));
#3418=EDGE_LOOP('',(#13616,#13617,#13618,#13619));
#3419=EDGE_LOOP('',(#13620,#13621,#13622,#13623,#13624,#13625));
#3420=EDGE_LOOP('',(#13626));
#3421=EDGE_LOOP('',(#13627,#13628,#13629,#13630,#13631,#13632));
#3422=EDGE_LOOP('',(#13633,#13634,#13635,#13636));
#3423=EDGE_LOOP('',(#13637));
#3424=EDGE_LOOP('',(#13638,#13639,#13640,#13641));
#3425=EDGE_LOOP('',(#13642,#13643,#13644,#13645,#13646,#13647,#13648,#13649,
#13650,#13651,#13652,#13653));
#3426=EDGE_LOOP('',(#13654,#13655,#13656,#13657));
#3427=EDGE_LOOP('',(#13658,#13659,#13660,#13661));
#3428=EDGE_LOOP('',(#13662,#13663,#13664,#13665));
#3429=EDGE_LOOP('',(#13666,#13667,#13668,#13669));
#3430=EDGE_LOOP('',(#13670,#13671,#13672,#13673));
#3431=EDGE_LOOP('',(#13674,#13675,#13676,#13677));
#3432=EDGE_LOOP('',(#13678,#13679,#13680,#13681));
#3433=EDGE_LOOP('',(#13682,#13683,#13684,#13685));
#3434=EDGE_LOOP('',(#13686,#13687,#13688,#13689));
#3435=EDGE_LOOP('',(#13690,#13691,#13692,#13693));
#3436=EDGE_LOOP('',(#13694,#13695,#13696,#13697));
#3437=EDGE_LOOP('',(#13698,#13699,#13700,#13701));
#3438=EDGE_LOOP('',(#13702,#13703,#13704,#13705));
#3439=EDGE_LOOP('',(#13706,#13707,#13708,#13709));
#3440=EDGE_LOOP('',(#13710,#13711,#13712,#13713));
#3441=EDGE_LOOP('',(#13714,#13715,#13716,#13717));
#3442=EDGE_LOOP('',(#13718,#13719,#13720,#13721));
#3443=EDGE_LOOP('',(#13722,#13723,#13724,#13725));
#3444=EDGE_LOOP('',(#13726,#13727,#13728,#13729));
#3445=EDGE_LOOP('',(#13730,#13731,#13732,#13733));
#3446=EDGE_LOOP('',(#13734,#13735,#13736,#13737));
#3447=EDGE_LOOP('',(#13738,#13739,#13740,#13741));
#3448=EDGE_LOOP('',(#13742,#13743,#13744,#13745));
#3449=EDGE_LOOP('',(#13746,#13747,#13748,#13749));
#3450=EDGE_LOOP('',(#13750,#13751,#13752,#13753));
#3451=EDGE_LOOP('',(#13754,#13755,#13756,#13757));
#3452=EDGE_LOOP('',(#13758,#13759,#13760,#13761));
#3453=EDGE_LOOP('',(#13762,#13763,#13764,#13765));
#3454=EDGE_LOOP('',(#13766,#13767,#13768,#13769));
#3455=EDGE_LOOP('',(#13770,#13771,#13772,#13773));
#3456=EDGE_LOOP('',(#13774,#13775,#13776,#13777));
#3457=EDGE_LOOP('',(#13778,#13779,#13780,#13781));
#3458=EDGE_LOOP('',(#13782,#13783,#13784,#13785));
#3459=EDGE_LOOP('',(#13786,#13787,#13788,#13789));
#3460=EDGE_LOOP('',(#13790,#13791,#13792,#13793));
#3461=EDGE_LOOP('',(#13794,#13795,#13796,#13797));
#3462=EDGE_LOOP('',(#13798));
#3463=EDGE_LOOP('',(#13799,#13800,#13801,#13802,#13803,#13804));
#4158=LINE('',#27233,#5227);
#4159=LINE('',#27266,#5228);
#4160=LINE('',#27350,#5229);
#4161=LINE('',#27440,#5230);
#4162=LINE('',#27524,#5231);
#4163=LINE('',#27614,#5232);
#4164=LINE('',#27704,#5233);
#4165=LINE('',#27788,#5234);
#4166=LINE('',#27878,#5235);
#4167=LINE('',#27962,#5236);
#4168=LINE('',#28052,#5237);
#4169=LINE('',#28136,#5238);
#4170=LINE('',#28226,#5239);
#4171=LINE('',#28313,#5240);
#4172=LINE('',#28400,#5241);
#4173=LINE('',#28490,#5242);
#4174=LINE('',#28574,#5243);
#4175=LINE('',#28664,#5244);
#4176=LINE('',#28748,#5245);
#4177=LINE('',#28838,#5246);
#4178=LINE('',#28922,#5247);
#4179=LINE('',#29009,#5248);
#4180=LINE('',#29099,#5249);
#4181=LINE('',#29183,#5250);
#4182=LINE('',#29273,#5251);
#4183=LINE('',#29357,#5252);
#4184=LINE('',#29447,#5253);
#4185=LINE('',#29531,#5254);
#4186=LINE('',#29621,#5255);
#4187=LINE('',#29711,#5256);
#4188=LINE('',#29795,#5257);
#4189=LINE('',#29885,#5258);
#4190=LINE('',#29969,#5259);
#4191=LINE('',#30059,#5260);
#4192=LINE('',#30143,#5261);
#4193=LINE('',#30165,#5262);
#4194=LINE('',#30202,#5263);
#4195=LINE('',#30239,#5264);
#4196=LINE('',#30276,#5265);
#4197=LINE('',#30313,#5266);
#4198=LINE('',#30350,#5267);
#4199=LINE('',#30387,#5268);
#4200=LINE('',#30425,#5269);
#4201=LINE('',#30462,#5270);
#4202=LINE('',#30499,#5271);
#4203=LINE('',#30536,#5272);
#4204=LINE('',#30573,#5273);
#4205=LINE('',#30610,#5274);
#4206=LINE('',#30647,#5275);
#4207=LINE('',#30685,#5276);
#4208=LINE('',#30721,#5277);
#4209=LINE('',#30759,#5278);
#4210=LINE('',#30796,#5279);
#4211=LINE('',#30833,#5280);
#4212=LINE('',#30870,#5281);
#4213=LINE('',#30907,#5282);
#4214=LINE('',#30945,#5283);
#4215=LINE('',#30981,#5284);
#4216=LINE('',#31019,#5285);
#4217=LINE('',#31056,#5286);
#4218=LINE('',#31093,#5287);
#4219=LINE('',#31130,#5288);
#4220=LINE('',#31167,#5289);
#4221=LINE('',#31204,#5290);
#4222=LINE('',#31241,#5291);
#4223=LINE('',#31279,#5292);
#4224=LINE('',#31316,#5293);
#4225=LINE('',#31353,#5294);
#4226=LINE('',#35416,#5295);
#4227=LINE('',#35418,#5296);
#4228=LINE('',#35420,#5297);
#4229=LINE('',#35421,#5298);
#4230=LINE('',#35425,#5299);
#4231=LINE('',#35428,#5300);
#4232=LINE('',#35429,#5301);
#4233=LINE('',#35435,#5302);
#4234=LINE('',#35437,#5303);
#4235=LINE('',#35439,#5304);
#4236=LINE('',#35440,#5305);
#4237=LINE('',#35444,#5306);
#4238=LINE('',#35447,#5307);
#4239=LINE('',#35448,#5308);
#4240=LINE('',#35454,#5309);
#4241=LINE('',#35456,#5310);
#4242=LINE('',#35458,#5311);
#4243=LINE('',#35459,#5312);
#4244=LINE('',#35463,#5313);
#4245=LINE('',#35466,#5314);
#4246=LINE('',#35467,#5315);
#4247=LINE('',#35473,#5316);
#4248=LINE('',#35475,#5317);
#4249=LINE('',#35477,#5318);
#4250=LINE('',#35478,#5319);
#4251=LINE('',#35482,#5320);
#4252=LINE('',#35485,#5321);
#4253=LINE('',#35486,#5322);
#4254=LINE('',#35492,#5323);
#4255=LINE('',#35494,#5324);
#4256=LINE('',#35496,#5325);
#4257=LINE('',#35497,#5326);
#4258=LINE('',#35501,#5327);
#4259=LINE('',#35504,#5328);
#4260=LINE('',#35505,#5329);
#4261=LINE('',#35511,#5330);
#4262=LINE('',#35513,#5331);
#4263=LINE('',#35515,#5332);
#4264=LINE('',#35516,#5333);
#4265=LINE('',#35520,#5334);
#4266=LINE('',#35523,#5335);
#4267=LINE('',#35524,#5336);
#4268=LINE('',#35530,#5337);
#4269=LINE('',#35532,#5338);
#4270=LINE('',#35534,#5339);
#4271=LINE('',#35535,#5340);
#4272=LINE('',#35539,#5341);
#4273=LINE('',#35542,#5342);
#4274=LINE('',#35543,#5343);
#4275=LINE('',#35549,#5344);
#4276=LINE('',#35551,#5345);
#4277=LINE('',#35553,#5346);
#4278=LINE('',#35554,#5347);
#4279=LINE('',#35558,#5348);
#4280=LINE('',#35561,#5349);
#4281=LINE('',#35562,#5350);
#4282=LINE('',#35568,#5351);
#4283=LINE('',#35570,#5352);
#4284=LINE('',#35572,#5353);
#4285=LINE('',#35573,#5354);
#4286=LINE('',#35577,#5355);
#4287=LINE('',#35580,#5356);
#4288=LINE('',#35581,#5357);
#4289=LINE('',#35587,#5358);
#4290=LINE('',#35589,#5359);
#4291=LINE('',#35591,#5360);
#4292=LINE('',#35592,#5361);
#4293=LINE('',#35596,#5362);
#4294=LINE('',#35599,#5363);
#4295=LINE('',#35600,#5364);
#4296=LINE('',#35606,#5365);
#4297=LINE('',#35608,#5366);
#4298=LINE('',#35610,#5367);
#4299=LINE('',#35611,#5368);
#4300=LINE('',#35615,#5369);
#4301=LINE('',#35618,#5370);
#4302=LINE('',#35619,#5371);
#4303=LINE('',#35625,#5372);
#4304=LINE('',#35627,#5373);
#4305=LINE('',#35629,#5374);
#4306=LINE('',#35630,#5375);
#4307=LINE('',#35634,#5376);
#4308=LINE('',#35637,#5377);
#4309=LINE('',#35638,#5378);
#4310=LINE('',#35644,#5379);
#4311=LINE('',#35646,#5380);
#4312=LINE('',#35648,#5381);
#4313=LINE('',#35649,#5382);
#4314=LINE('',#35653,#5383);
#4315=LINE('',#35656,#5384);
#4316=LINE('',#35657,#5385);
#4317=LINE('',#35663,#5386);
#4318=LINE('',#35665,#5387);
#4319=LINE('',#35667,#5388);
#4320=LINE('',#35668,#5389);
#4321=LINE('',#35672,#5390);
#4322=LINE('',#35675,#5391);
#4323=LINE('',#35676,#5392);
#4324=LINE('',#35682,#5393);
#4325=LINE('',#35684,#5394);
#4326=LINE('',#35686,#5395);
#4327=LINE('',#35687,#5396);
#4328=LINE('',#35691,#5397);
#4329=LINE('',#35694,#5398);
#4330=LINE('',#35695,#5399);
#4331=LINE('',#35701,#5400);
#4332=LINE('',#35703,#5401);
#4333=LINE('',#35705,#5402);
#4334=LINE('',#35706,#5403);
#4335=LINE('',#35710,#5404);
#4336=LINE('',#35713,#5405);
#4337=LINE('',#35714,#5406);
#4338=LINE('',#35720,#5407);
#4339=LINE('',#35722,#5408);
#4340=LINE('',#35724,#5409);
#4341=LINE('',#35725,#5410);
#4342=LINE('',#35729,#5411);
#4343=LINE('',#35732,#5412);
#4344=LINE('',#35733,#5413);
#4345=LINE('',#35739,#5414);
#4346=LINE('',#35741,#5415);
#4347=LINE('',#35743,#5416);
#4348=LINE('',#35744,#5417);
#4349=LINE('',#35749,#5418);
#4350=LINE('',#35753,#5419);
#4351=LINE('',#35754,#5420);
#4352=LINE('',#35762,#5421);
#4353=LINE('',#35764,#5422);
#4354=LINE('',#35766,#5423);
#4355=LINE('',#35767,#5424);
#4356=LINE('',#35771,#5425);
#4357=LINE('',#35774,#5426);
#4358=LINE('',#35775,#5427);
#4359=LINE('',#35781,#5428);
#4360=LINE('',#35783,#5429);
#4361=LINE('',#35785,#5430);
#4362=LINE('',#35786,#5431);
#4363=LINE('',#35790,#5432);
#4364=LINE('',#35793,#5433);
#4365=LINE('',#35794,#5434);
#4366=LINE('',#35800,#5435);
#4367=LINE('',#35802,#5436);
#4368=LINE('',#35804,#5437);
#4369=LINE('',#35805,#5438);
#4370=LINE('',#35809,#5439);
#4371=LINE('',#35812,#5440);
#4372=LINE('',#35813,#5441);
#4373=LINE('',#35819,#5442);
#4374=LINE('',#35821,#5443);
#4375=LINE('',#35823,#5444);
#4376=LINE('',#35824,#5445);
#4377=LINE('',#35828,#5446);
#4378=LINE('',#35831,#5447);
#4379=LINE('',#35832,#5448);
#4380=LINE('',#35838,#5449);
#4381=LINE('',#35840,#5450);
#4382=LINE('',#35842,#5451);
#4383=LINE('',#35843,#5452);
#4384=LINE('',#35847,#5453);
#4385=LINE('',#35850,#5454);
#4386=LINE('',#35851,#5455);
#4387=LINE('',#35857,#5456);
#4388=LINE('',#35859,#5457);
#4389=LINE('',#35861,#5458);
#4390=LINE('',#35862,#5459);
#4391=LINE('',#35866,#5460);
#4392=LINE('',#35869,#5461);
#4393=LINE('',#35870,#5462);
#4394=LINE('',#35876,#5463);
#4395=LINE('',#35878,#5464);
#4396=LINE('',#35880,#5465);
#4397=LINE('',#35881,#5466);
#4398=LINE('',#35885,#5467);
#4399=LINE('',#35888,#5468);
#4400=LINE('',#35889,#5469);
#4401=LINE('',#35895,#5470);
#4402=LINE('',#35897,#5471);
#4403=LINE('',#35899,#5472);
#4404=LINE('',#35900,#5473);
#4405=LINE('',#35904,#5474);
#4406=LINE('',#35907,#5475);
#4407=LINE('',#35908,#5476);
#4408=LINE('',#35914,#5477);
#4409=LINE('',#35916,#5478);
#4410=LINE('',#35918,#5479);
#4411=LINE('',#35919,#5480);
#4412=LINE('',#35923,#5481);
#4413=LINE('',#35926,#5482);
#4414=LINE('',#35927,#5483);
#4415=LINE('',#35933,#5484);
#4416=LINE('',#35935,#5485);
#4417=LINE('',#35937,#5486);
#4418=LINE('',#35938,#5487);
#4419=LINE('',#35942,#5488);
#4420=LINE('',#35945,#5489);
#4421=LINE('',#35946,#5490);
#4422=LINE('',#35952,#5491);
#4423=LINE('',#35954,#5492);
#4424=LINE('',#35956,#5493);
#4425=LINE('',#35957,#5494);
#4426=LINE('',#35961,#5495);
#4427=LINE('',#35964,#5496);
#4428=LINE('',#35965,#5497);
#4429=LINE('',#35971,#5498);
#4430=LINE('',#35973,#5499);
#4431=LINE('',#35975,#5500);
#4432=LINE('',#35976,#5501);
#4433=LINE('',#35980,#5502);
#4434=LINE('',#35983,#5503);
#4435=LINE('',#35984,#5504);
#4436=LINE('',#35990,#5505);
#4437=LINE('',#35992,#5506);
#4438=LINE('',#35994,#5507);
#4439=LINE('',#35995,#5508);
#4440=LINE('',#35999,#5509);
#4441=LINE('',#36002,#5510);
#4442=LINE('',#36003,#5511);
#4443=LINE('',#36009,#5512);
#4444=LINE('',#36011,#5513);
#4445=LINE('',#36013,#5514);
#4446=LINE('',#36014,#5515);
#4447=LINE('',#36018,#5516);
#4448=LINE('',#36021,#5517);
#4449=LINE('',#36022,#5518);
#4450=LINE('',#36028,#5519);
#4451=LINE('',#36030,#5520);
#4452=LINE('',#36032,#5521);
#4453=LINE('',#36033,#5522);
#4454=LINE('',#36037,#5523);
#4455=LINE('',#36040,#5524);
#4456=LINE('',#36041,#5525);
#4457=LINE('',#36047,#5526);
#4458=LINE('',#36049,#5527);
#4459=LINE('',#36051,#5528);
#4460=LINE('',#36052,#5529);
#4461=LINE('',#36056,#5530);
#4462=LINE('',#36059,#5531);
#4463=LINE('',#36060,#5532);
#4464=LINE('',#36066,#5533);
#4465=LINE('',#36068,#5534);
#4466=LINE('',#36070,#5535);
#4467=LINE('',#36071,#5536);
#4468=LINE('',#36075,#5537);
#4469=LINE('',#36078,#5538);
#4470=LINE('',#36079,#5539);
#4471=LINE('',#36085,#5540);
#4472=LINE('',#36087,#5541);
#4473=LINE('',#36089,#5542);
#4474=LINE('',#36090,#5543);
#4475=LINE('',#36094,#5544);
#4476=LINE('',#36097,#5545);
#4477=LINE('',#36098,#5546);
#4478=LINE('',#36104,#5547);
#4479=LINE('',#36106,#5548);
#4480=LINE('',#36108,#5549);
#4481=LINE('',#36109,#5550);
#4482=LINE('',#36112,#5551);
#4483=LINE('',#36114,#5552);
#4484=LINE('',#36115,#5553);
#4485=LINE('',#36118,#5554);
#4486=LINE('',#36120,#5555);
#4487=LINE('',#36121,#5556);
#4488=LINE('',#36124,#5557);
#4489=LINE('',#36126,#5558);
#4490=LINE('',#36127,#5559);
#4491=LINE('',#36130,#5560);
#4492=LINE('',#36132,#5561);
#4493=LINE('',#36133,#5562);
#4494=LINE('',#36135,#5563);
#4495=LINE('',#36136,#5564);
#4496=LINE('',#36142,#5565);
#4497=LINE('',#36151,#5566);
#4498=LINE('',#36152,#5567);
#4499=LINE('',#36156,#5568);
#5227=VECTOR('',#19615,6.);
#5228=VECTOR('',#19620,6.);
#5229=VECTOR('',#19623,6.);
#5230=VECTOR('',#19626,6.);
#5231=VECTOR('',#19629,6.);
#5232=VECTOR('',#19632,6.);
#5233=VECTOR('',#19635,6.);
#5234=VECTOR('',#19638,6.);
#5235=VECTOR('',#19641,6.);
#5236=VECTOR('',#19644,6.);
#5237=VECTOR('',#19647,6.);
#5238=VECTOR('',#19650,6.);
#5239=VECTOR('',#19653,6.);
#5240=VECTOR('',#19656,6.);
#5241=VECTOR('',#19659,6.);
#5242=VECTOR('',#19662,6.);
#5243=VECTOR('',#19665,6.);
#5244=VECTOR('',#19668,6.);
#5245=VECTOR('',#19671,6.);
#5246=VECTOR('',#19674,6.);
#5247=VECTOR('',#19677,6.);
#5248=VECTOR('',#19680,6.);
#5249=VECTOR('',#19683,6.);
#5250=VECTOR('',#19686,6.);
#5251=VECTOR('',#19689,6.);
#5252=VECTOR('',#19692,6.);
#5253=VECTOR('',#19695,6.);
#5254=VECTOR('',#19698,6.);
#5255=VECTOR('',#19701,6.);
#5256=VECTOR('',#19704,6.);
#5257=VECTOR('',#19707,6.);
#5258=VECTOR('',#19710,6.);
#5259=VECTOR('',#19713,6.);
#5260=VECTOR('',#19716,6.);
#5261=VECTOR('',#19719,4.91825);
#5262=VECTOR('',#19724,4.91825);
#5263=VECTOR('',#19727,4.91825);
#5264=VECTOR('',#19730,4.91825);
#5265=VECTOR('',#19733,4.91825);
#5266=VECTOR('',#19736,4.91825);
#5267=VECTOR('',#19739,4.91825);
#5268=VECTOR('',#19742,4.91825);
#5269=VECTOR('',#19745,4.91825);
#5270=VECTOR('',#19748,4.91825);
#5271=VECTOR('',#19751,4.91825);
#5272=VECTOR('',#19754,4.91825);
#5273=VECTOR('',#19757,4.91825);
#5274=VECTOR('',#19760,4.91825);
#5275=VECTOR('',#19763,4.91825);
#5276=VECTOR('',#19766,4.91825);
#5277=VECTOR('',#19769,4.91825);
#5278=VECTOR('',#19772,4.91825);
#5279=VECTOR('',#19775,4.91825);
#5280=VECTOR('',#19778,4.91825);
#5281=VECTOR('',#19781,4.91825);
#5282=VECTOR('',#19784,4.91825);
#5283=VECTOR('',#19787,4.91825);
#5284=VECTOR('',#19790,4.91825);
#5285=VECTOR('',#19793,4.91825);
#5286=VECTOR('',#19796,4.91825);
#5287=VECTOR('',#19799,4.91825);
#5288=VECTOR('',#19802,4.91825);
#5289=VECTOR('',#19805,4.91825);
#5290=VECTOR('',#19808,4.91825);
#5291=VECTOR('',#19811,4.91825);
#5292=VECTOR('',#19814,4.91825);
#5293=VECTOR('',#19817,4.91825);
#5294=VECTOR('',#19820,4.91825);
#5295=VECTOR('',#19833,10.);
#5296=VECTOR('',#19834,10.);
#5297=VECTOR('',#19835,10.);
#5298=VECTOR('',#19836,10.);
#5299=VECTOR('',#19841,10.);
#5300=VECTOR('',#19844,10.);
#5301=VECTOR('',#19845,10.);
#5302=VECTOR('',#19852,10.);
#5303=VECTOR('',#19853,10.);
#5304=VECTOR('',#19854,10.);
#5305=VECTOR('',#19855,10.);
#5306=VECTOR('',#19860,10.);
#5307=VECTOR('',#19863,10.);
#5308=VECTOR('',#19864,10.);
#5309=VECTOR('',#19871,10.);
#5310=VECTOR('',#19872,10.);
#5311=VECTOR('',#19873,10.);
#5312=VECTOR('',#19874,10.);
#5313=VECTOR('',#19879,10.);
#5314=VECTOR('',#19882,10.);
#5315=VECTOR('',#19883,10.);
#5316=VECTOR('',#19890,10.);
#5317=VECTOR('',#19891,10.);
#5318=VECTOR('',#19892,10.);
#5319=VECTOR('',#19893,10.);
#5320=VECTOR('',#19898,10.);
#5321=VECTOR('',#19901,10.);
#5322=VECTOR('',#19902,10.);
#5323=VECTOR('',#19909,10.);
#5324=VECTOR('',#19910,10.);
#5325=VECTOR('',#19911,10.);
#5326=VECTOR('',#19912,10.);
#5327=VECTOR('',#19917,10.);
#5328=VECTOR('',#19920,10.);
#5329=VECTOR('',#19921,10.);
#5330=VECTOR('',#19928,10.);
#5331=VECTOR('',#19929,10.);
#5332=VECTOR('',#19930,10.);
#5333=VECTOR('',#19931,10.);
#5334=VECTOR('',#19936,10.);
#5335=VECTOR('',#19939,10.);
#5336=VECTOR('',#19940,10.);
#5337=VECTOR('',#19947,10.);
#5338=VECTOR('',#19948,10.);
#5339=VECTOR('',#19949,10.);
#5340=VECTOR('',#19950,10.);
#5341=VECTOR('',#19955,10.);
#5342=VECTOR('',#19958,10.);
#5343=VECTOR('',#19959,10.);
#5344=VECTOR('',#19966,10.);
#5345=VECTOR('',#19967,10.);
#5346=VECTOR('',#19968,10.);
#5347=VECTOR('',#19969,10.);
#5348=VECTOR('',#19974,10.);
#5349=VECTOR('',#19977,10.);
#5350=VECTOR('',#19978,10.);
#5351=VECTOR('',#19985,10.);
#5352=VECTOR('',#19986,10.);
#5353=VECTOR('',#19987,10.);
#5354=VECTOR('',#19988,10.);
#5355=VECTOR('',#19993,10.);
#5356=VECTOR('',#19996,10.);
#5357=VECTOR('',#19997,10.);
#5358=VECTOR('',#20004,10.);
#5359=VECTOR('',#20005,10.);
#5360=VECTOR('',#20006,10.);
#5361=VECTOR('',#20007,10.);
#5362=VECTOR('',#20012,10.);
#5363=VECTOR('',#20015,10.);
#5364=VECTOR('',#20016,10.);
#5365=VECTOR('',#20023,10.);
#5366=VECTOR('',#20024,10.);
#5367=VECTOR('',#20025,10.);
#5368=VECTOR('',#20026,10.);
#5369=VECTOR('',#20031,10.);
#5370=VECTOR('',#20034,10.);
#5371=VECTOR('',#20035,10.);
#5372=VECTOR('',#20042,10.);
#5373=VECTOR('',#20043,10.);
#5374=VECTOR('',#20044,10.);
#5375=VECTOR('',#20045,10.);
#5376=VECTOR('',#20050,10.);
#5377=VECTOR('',#20053,10.);
#5378=VECTOR('',#20054,10.);
#5379=VECTOR('',#20061,10.);
#5380=VECTOR('',#20062,10.);
#5381=VECTOR('',#20063,10.);
#5382=VECTOR('',#20064,10.);
#5383=VECTOR('',#20069,10.);
#5384=VECTOR('',#20072,10.);
#5385=VECTOR('',#20073,10.);
#5386=VECTOR('',#20080,10.);
#5387=VECTOR('',#20081,10.);
#5388=VECTOR('',#20082,10.);
#5389=VECTOR('',#20083,10.);
#5390=VECTOR('',#20088,10.);
#5391=VECTOR('',#20091,10.);
#5392=VECTOR('',#20092,10.);
#5393=VECTOR('',#20099,10.);
#5394=VECTOR('',#20100,10.);
#5395=VECTOR('',#20101,10.);
#5396=VECTOR('',#20102,10.);
#5397=VECTOR('',#20107,10.);
#5398=VECTOR('',#20110,10.);
#5399=VECTOR('',#20111,10.);
#5400=VECTOR('',#20118,10.);
#5401=VECTOR('',#20119,10.);
#5402=VECTOR('',#20120,10.);
#5403=VECTOR('',#20121,10.);
#5404=VECTOR('',#20126,10.);
#5405=VECTOR('',#20129,10.);
#5406=VECTOR('',#20130,10.);
#5407=VECTOR('',#20137,10.);
#5408=VECTOR('',#20138,10.);
#5409=VECTOR('',#20139,10.);
#5410=VECTOR('',#20140,10.);
#5411=VECTOR('',#20145,10.);
#5412=VECTOR('',#20148,10.);
#5413=VECTOR('',#20149,10.);
#5414=VECTOR('',#20156,10.);
#5415=VECTOR('',#20157,10.);
#5416=VECTOR('',#20158,10.);
#5417=VECTOR('',#20159,10.);
#5418=VECTOR('',#20164,10.);
#5419=VECTOR('',#20169,10.);
#5420=VECTOR('',#20170,10.);
#5421=VECTOR('',#20179,10.);
#5422=VECTOR('',#20180,10.);
#5423=VECTOR('',#20181,10.);
#5424=VECTOR('',#20182,10.);
#5425=VECTOR('',#20187,10.);
#5426=VECTOR('',#20190,10.);
#5427=VECTOR('',#20191,10.);
#5428=VECTOR('',#20198,10.);
#5429=VECTOR('',#20199,10.);
#5430=VECTOR('',#20200,10.);
#5431=VECTOR('',#20201,10.);
#5432=VECTOR('',#20206,10.);
#5433=VECTOR('',#20209,10.);
#5434=VECTOR('',#20210,10.);
#5435=VECTOR('',#20217,10.);
#5436=VECTOR('',#20218,10.);
#5437=VECTOR('',#20219,10.);
#5438=VECTOR('',#20220,10.);
#5439=VECTOR('',#20225,10.);
#5440=VECTOR('',#20228,10.);
#5441=VECTOR('',#20229,10.);
#5442=VECTOR('',#20236,10.);
#5443=VECTOR('',#20237,10.);
#5444=VECTOR('',#20238,10.);
#5445=VECTOR('',#20239,10.);
#5446=VECTOR('',#20244,10.);
#5447=VECTOR('',#20247,10.);
#5448=VECTOR('',#20248,10.);
#5449=VECTOR('',#20255,10.);
#5450=VECTOR('',#20256,10.);
#5451=VECTOR('',#20257,10.);
#5452=VECTOR('',#20258,10.);
#5453=VECTOR('',#20263,10.);
#5454=VECTOR('',#20266,10.);
#5455=VECTOR('',#20267,10.);
#5456=VECTOR('',#20274,10.);
#5457=VECTOR('',#20275,10.);
#5458=VECTOR('',#20276,10.);
#5459=VECTOR('',#20277,10.);
#5460=VECTOR('',#20282,10.);
#5461=VECTOR('',#20285,10.);
#5462=VECTOR('',#20286,10.);
#5463=VECTOR('',#20293,10.);
#5464=VECTOR('',#20294,10.);
#5465=VECTOR('',#20295,10.);
#5466=VECTOR('',#20296,10.);
#5467=VECTOR('',#20301,10.);
#5468=VECTOR('',#20304,10.);
#5469=VECTOR('',#20305,10.);
#5470=VECTOR('',#20312,10.);
#5471=VECTOR('',#20313,10.);
#5472=VECTOR('',#20314,10.);
#5473=VECTOR('',#20315,10.);
#5474=VECTOR('',#20320,10.);
#5475=VECTOR('',#20323,10.);
#5476=VECTOR('',#20324,10.);
#5477=VECTOR('',#20331,10.);
#5478=VECTOR('',#20332,10.);
#5479=VECTOR('',#20333,10.);
#5480=VECTOR('',#20334,10.);
#5481=VECTOR('',#20339,10.);
#5482=VECTOR('',#20342,10.);
#5483=VECTOR('',#20343,10.);
#5484=VECTOR('',#20350,10.);
#5485=VECTOR('',#20351,10.);
#5486=VECTOR('',#20352,10.);
#5487=VECTOR('',#20353,10.);
#5488=VECTOR('',#20358,10.);
#5489=VECTOR('',#20361,10.);
#5490=VECTOR('',#20362,10.);
#5491=VECTOR('',#20369,10.);
#5492=VECTOR('',#20370,10.);
#5493=VECTOR('',#20371,10.);
#5494=VECTOR('',#20372,10.);
#5495=VECTOR('',#20377,10.);
#5496=VECTOR('',#20380,10.);
#5497=VECTOR('',#20381,10.);
#5498=VECTOR('',#20388,10.);
#5499=VECTOR('',#20389,10.);
#5500=VECTOR('',#20390,10.);
#5501=VECTOR('',#20391,10.);
#5502=VECTOR('',#20396,10.);
#5503=VECTOR('',#20399,10.);
#5504=VECTOR('',#20400,10.);
#5505=VECTOR('',#20407,10.);
#5506=VECTOR('',#20408,10.);
#5507=VECTOR('',#20409,10.);
#5508=VECTOR('',#20410,10.);
#5509=VECTOR('',#20415,10.);
#5510=VECTOR('',#20418,10.);
#5511=VECTOR('',#20419,10.);
#5512=VECTOR('',#20426,10.);
#5513=VECTOR('',#20427,10.);
#5514=VECTOR('',#20428,10.);
#5515=VECTOR('',#20429,10.);
#5516=VECTOR('',#20434,10.);
#5517=VECTOR('',#20437,10.);
#5518=VECTOR('',#20438,10.);
#5519=VECTOR('',#20445,10.);
#5520=VECTOR('',#20446,10.);
#5521=VECTOR('',#20447,10.);
#5522=VECTOR('',#20448,10.);
#5523=VECTOR('',#20453,10.);
#5524=VECTOR('',#20456,10.);
#5525=VECTOR('',#20457,10.);
#5526=VECTOR('',#20464,10.);
#5527=VECTOR('',#20465,10.);
#5528=VECTOR('',#20466,10.);
#5529=VECTOR('',#20467,10.);
#5530=VECTOR('',#20472,10.);
#5531=VECTOR('',#20475,10.);
#5532=VECTOR('',#20476,10.);
#5533=VECTOR('',#20483,10.);
#5534=VECTOR('',#20484,10.);
#5535=VECTOR('',#20485,10.);
#5536=VECTOR('',#20486,10.);
#5537=VECTOR('',#20491,10.);
#5538=VECTOR('',#20494,10.);
#5539=VECTOR('',#20495,10.);
#5540=VECTOR('',#20502,10.);
#5541=VECTOR('',#20503,10.);
#5542=VECTOR('',#20504,10.);
#5543=VECTOR('',#20505,10.);
#5544=VECTOR('',#20510,10.);
#5545=VECTOR('',#20513,10.);
#5546=VECTOR('',#20514,10.);
#5547=VECTOR('',#20521,10.);
#5548=VECTOR('',#20522,10.);
#5549=VECTOR('',#20523,10.);
#5550=VECTOR('',#20524,10.);
#5551=VECTOR('',#20527,10.);
#5552=VECTOR('',#20528,10.);
#5553=VECTOR('',#20529,10.);
#5554=VECTOR('',#20532,10.);
#5555=VECTOR('',#20533,10.);
#5556=VECTOR('',#20534,10.);
#5557=VECTOR('',#20537,10.);
#5558=VECTOR('',#20538,10.);
#5559=VECTOR('',#20539,10.);
#5560=VECTOR('',#20542,10.);
#5561=VECTOR('',#20543,10.);
#5562=VECTOR('',#20544,10.);
#5563=VECTOR('',#20547,10.);
#5564=VECTOR('',#20548,10.);
#5565=VECTOR('',#20557,5.75);
#5566=VECTOR('',#20570,9.);
#5567=VECTOR('',#20571,9.);
#5568=VECTOR('',#20576,8.75);
#6175=CIRCLE('',#16359,5.91675);
#6176=CIRCLE('',#16394,4.91825);
#6177=CIRCLE('',#16429,5.91675);
#6178=CIRCLE('',#16430,5.91675);
#6179=CIRCLE('',#16431,4.91825);
#6180=CIRCLE('',#16435,9.);
#6181=CIRCLE('',#16438,9.);
#6182=CIRCLE('',#16441,9.);
#6183=CIRCLE('',#16444,9.);
#6184=CIRCLE('',#16447,9.);
#6185=CIRCLE('',#16450,9.);
#6186=CIRCLE('',#16453,9.);
#6187=CIRCLE('',#16456,9.);
#6188=CIRCLE('',#16459,9.);
#6189=CIRCLE('',#16462,9.);
#6190=CIRCLE('',#16465,9.);
#6191=CIRCLE('',#16468,9.);
#6192=CIRCLE('',#16471,9.);
#6193=CIRCLE('',#16474,9.);
#6194=CIRCLE('',#16477,9.);
#6195=CIRCLE('',#16480,9.);
#6196=CIRCLE('',#16483,9.);
#6197=CIRCLE('',#16486,9.);
#6198=CIRCLE('',#16489,9.);
#6199=CIRCLE('',#16492,9.);
#6200=CIRCLE('',#16495,9.);
#6201=CIRCLE('',#16498,9.);
#6202=CIRCLE('',#16501,9.);
#6203=CIRCLE('',#16504,9.);
#6204=CIRCLE('',#16507,9.);
#6205=CIRCLE('',#16510,9.);
#6206=CIRCLE('',#16513,9.);
#6207=CIRCLE('',#16516,9.);
#6208=CIRCLE('',#16519,9.);
#6209=CIRCLE('',#16522,9.);
#6210=CIRCLE('',#16525,9.);
#6211=CIRCLE('',#16528,9.);
#6212=CIRCLE('',#16531,9.);
#6213=CIRCLE('',#16534,9.);
#6214=CIRCLE('',#16537,9.);
#6215=CIRCLE('',#16538,9.);
#6216=CIRCLE('',#16541,9.);
#6217=CIRCLE('',#16542,9.);
#6218=CIRCLE('',#16545,9.);
#6219=CIRCLE('',#16548,9.);
#6220=CIRCLE('',#16551,9.);
#6221=CIRCLE('',#16554,9.);
#6222=CIRCLE('',#16557,9.);
#6223=CIRCLE('',#16560,9.);
#6224=CIRCLE('',#16563,9.);
#6225=CIRCLE('',#16566,9.);
#6226=CIRCLE('',#16569,9.);
#6227=CIRCLE('',#16572,9.);
#6228=CIRCLE('',#16575,9.);
#6229=CIRCLE('',#16578,9.);
#6230=CIRCLE('',#16581,9.);
#6231=CIRCLE('',#16584,9.);
#6232=CIRCLE('',#16587,9.);
#6233=CIRCLE('',#16590,9.);
#6234=CIRCLE('',#16593,9.);
#6235=CIRCLE('',#16596,9.);
#6236=CIRCLE('',#16599,9.);
#6237=CIRCLE('',#16602,9.);
#6238=CIRCLE('',#16605,9.);
#6239=CIRCLE('',#16608,9.);
#6240=CIRCLE('',#16611,9.);
#6241=CIRCLE('',#16614,9.);
#6242=CIRCLE('',#16617,9.);
#6243=CIRCLE('',#16620,9.);
#6244=CIRCLE('',#16623,9.);
#6245=CIRCLE('',#16626,9.);
#6246=CIRCLE('',#16629,9.);
#6247=CIRCLE('',#16632,9.);
#6248=CIRCLE('',#16635,9.);
#6249=CIRCLE('',#16638,9.);
#6250=CIRCLE('',#16641,9.);
#6251=CIRCLE('',#16644,9.);
#6252=CIRCLE('',#16647,9.);
#6253=CIRCLE('',#16650,9.);
#6254=CIRCLE('',#16659,5.5);
#6255=CIRCLE('',#16662,5.91675);
#6256=CIRCLE('',#16664,9.);
#6257=CIRCLE('',#16666,9.);
#6258=CIRCLE('',#16668,8.5);
#7179=VERTEX_POINT('',#27231);
#7180=VERTEX_POINT('',#27232);
#7181=VERTEX_POINT('',#27234);
#7182=VERTEX_POINT('',#27251);
#7183=VERTEX_POINT('',#27264);
#7184=VERTEX_POINT('',#27265);
#7185=VERTEX_POINT('',#27348);
#7186=VERTEX_POINT('',#27349);
#7187=VERTEX_POINT('',#27438);
#7188=VERTEX_POINT('',#27439);
#7189=VERTEX_POINT('',#27522);
#7190=VERTEX_POINT('',#27523);
#7191=VERTEX_POINT('',#27612);
#7192=VERTEX_POINT('',#27613);
#7193=VERTEX_POINT('',#27702);
#7194=VERTEX_POINT('',#27703);
#7195=VERTEX_POINT('',#27786);
#7196=VERTEX_POINT('',#27787);
#7197=VERTEX_POINT('',#27876);
#7198=VERTEX_POINT('',#27877);
#7199=VERTEX_POINT('',#27960);
#7200=VERTEX_POINT('',#27961);
#7201=VERTEX_POINT('',#28050);
#7202=VERTEX_POINT('',#28051);
#7203=VERTEX_POINT('',#28134);
#7204=VERTEX_POINT('',#28135);
#7205=VERTEX_POINT('',#28224);
#7206=VERTEX_POINT('',#28225);
#7207=VERTEX_POINT('',#28311);
#7208=VERTEX_POINT('',#28312);
#7209=VERTEX_POINT('',#28398);
#7210=VERTEX_POINT('',#28399);
#7211=VERTEX_POINT('',#28488);
#7212=VERTEX_POINT('',#28489);
#7213=VERTEX_POINT('',#28572);
#7214=VERTEX_POINT('',#28573);
#7215=VERTEX_POINT('',#28662);
#7216=VERTEX_POINT('',#28663);
#7217=VERTEX_POINT('',#28746);
#7218=VERTEX_POINT('',#28747);
#7219=VERTEX_POINT('',#28836);
#7220=VERTEX_POINT('',#28837);
#7221=VERTEX_POINT('',#28920);
#7222=VERTEX_POINT('',#28921);
#7223=VERTEX_POINT('',#29007);
#7224=VERTEX_POINT('',#29008);
#7225=VERTEX_POINT('',#29097);
#7226=VERTEX_POINT('',#29098);
#7227=VERTEX_POINT('',#29181);
#7228=VERTEX_POINT('',#29182);
#7229=VERTEX_POINT('',#29271);
#7230=VERTEX_POINT('',#29272);
#7231=VERTEX_POINT('',#29355);
#7232=VERTEX_POINT('',#29356);
#7233=VERTEX_POINT('',#29445);
#7234=VERTEX_POINT('',#29446);
#7235=VERTEX_POINT('',#29529);
#7236=VERTEX_POINT('',#29530);
#7237=VERTEX_POINT('',#29619);
#7238=VERTEX_POINT('',#29620);
#7239=VERTEX_POINT('',#29709);
#7240=VERTEX_POINT('',#29710);
#7241=VERTEX_POINT('',#29793);
#7242=VERTEX_POINT('',#29794);
#7243=VERTEX_POINT('',#29883);
#7244=VERTEX_POINT('',#29884);
#7245=VERTEX_POINT('',#29967);
#7246=VERTEX_POINT('',#29968);
#7247=VERTEX_POINT('',#30057);
#7248=VERTEX_POINT('',#30058);
#7249=VERTEX_POINT('',#30141);
#7250=VERTEX_POINT('',#30142);
#7251=VERTEX_POINT('',#30144);
#7252=VERTEX_POINT('',#30154);
#7253=VERTEX_POINT('',#30163);
#7254=VERTEX_POINT('',#30164);
#7255=VERTEX_POINT('',#30200);
#7256=VERTEX_POINT('',#30201);
#7257=VERTEX_POINT('',#30237);
#7258=VERTEX_POINT('',#30238);
#7259=VERTEX_POINT('',#30274);
#7260=VERTEX_POINT('',#30275);
#7261=VERTEX_POINT('',#30311);
#7262=VERTEX_POINT('',#30312);
#7263=VERTEX_POINT('',#30348);
#7264=VERTEX_POINT('',#30349);
#7265=VERTEX_POINT('',#30385);
#7266=VERTEX_POINT('',#30386);
#7267=VERTEX_POINT('',#30423);
#7268=VERTEX_POINT('',#30424);
#7269=VERTEX_POINT('',#30460);
#7270=VERTEX_POINT('',#30461);
#7271=VERTEX_POINT('',#30497);
#7272=VERTEX_POINT('',#30498);
#7273=VERTEX_POINT('',#30534);
#7274=VERTEX_POINT('',#30535);
#7275=VERTEX_POINT('',#30571);
#7276=VERTEX_POINT('',#30572);
#7277=VERTEX_POINT('',#30608);
#7278=VERTEX_POINT('',#30609);
#7279=VERTEX_POINT('',#30645);
#7280=VERTEX_POINT('',#30646);
#7281=VERTEX_POINT('',#30683);
#7282=VERTEX_POINT('',#30684);
#7283=VERTEX_POINT('',#30719);
#7284=VERTEX_POINT('',#30720);
#7285=VERTEX_POINT('',#30757);
#7286=VERTEX_POINT('',#30758);
#7287=VERTEX_POINT('',#30794);
#7288=VERTEX_POINT('',#30795);
#7289=VERTEX_POINT('',#30831);
#7290=VERTEX_POINT('',#30832);
#7291=VERTEX_POINT('',#30868);
#7292=VERTEX_POINT('',#30869);
#7293=VERTEX_POINT('',#30905);
#7294=VERTEX_POINT('',#30906);
#7295=VERTEX_POINT('',#30943);
#7296=VERTEX_POINT('',#30944);
#7297=VERTEX_POINT('',#30979);
#7298=VERTEX_POINT('',#30980);
#7299=VERTEX_POINT('',#31017);
#7300=VERTEX_POINT('',#31018);
#7301=VERTEX_POINT('',#31054);
#7302=VERTEX_POINT('',#31055);
#7303=VERTEX_POINT('',#31091);
#7304=VERTEX_POINT('',#31092);
#7305=VERTEX_POINT('',#31128);
#7306=VERTEX_POINT('',#31129);
#7307=VERTEX_POINT('',#31165);
#7308=VERTEX_POINT('',#31166);
#7309=VERTEX_POINT('',#31202);
#7310=VERTEX_POINT('',#31203);
#7311=VERTEX_POINT('',#31239);
#7312=VERTEX_POINT('',#31240);
#7313=VERTEX_POINT('',#31277);
#7314=VERTEX_POINT('',#31278);
#7315=VERTEX_POINT('',#31314);
#7316=VERTEX_POINT('',#31315);
#7317=VERTEX_POINT('',#31351);
#7318=VERTEX_POINT('',#31352);
#7319=VERTEX_POINT('',#33127);
#7320=VERTEX_POINT('',#33274);
#7321=VERTEX_POINT('',#33402);
#7322=VERTEX_POINT('',#33405);
#7323=VERTEX_POINT('',#35269);
#7324=VERTEX_POINT('',#35414);
#7325=VERTEX_POINT('',#35415);
#7326=VERTEX_POINT('',#35417);
#7327=VERTEX_POINT('',#35419);
#7328=VERTEX_POINT('',#35423);
#7329=VERTEX_POINT('',#35427);
#7330=VERTEX_POINT('',#35433);
#7331=VERTEX_POINT('',#35434);
#7332=VERTEX_POINT('',#35436);
#7333=VERTEX_POINT('',#35438);
#7334=VERTEX_POINT('',#35442);
#7335=VERTEX_POINT('',#35446);
#7336=VERTEX_POINT('',#35452);
#7337=VERTEX_POINT('',#35453);
#7338=VERTEX_POINT('',#35455);
#7339=VERTEX_POINT('',#35457);
#7340=VERTEX_POINT('',#35461);
#7341=VERTEX_POINT('',#35465);
#7342=VERTEX_POINT('',#35471);
#7343=VERTEX_POINT('',#35472);
#7344=VERTEX_POINT('',#35474);
#7345=VERTEX_POINT('',#35476);
#7346=VERTEX_POINT('',#35480);
#7347=VERTEX_POINT('',#35484);
#7348=VERTEX_POINT('',#35490);
#7349=VERTEX_POINT('',#35491);
#7350=VERTEX_POINT('',#35493);
#7351=VERTEX_POINT('',#35495);
#7352=VERTEX_POINT('',#35499);
#7353=VERTEX_POINT('',#35503);
#7354=VERTEX_POINT('',#35509);
#7355=VERTEX_POINT('',#35510);
#7356=VERTEX_POINT('',#35512);
#7357=VERTEX_POINT('',#35514);
#7358=VERTEX_POINT('',#35518);
#7359=VERTEX_POINT('',#35522);
#7360=VERTEX_POINT('',#35528);
#7361=VERTEX_POINT('',#35529);
#7362=VERTEX_POINT('',#35531);
#7363=VERTEX_POINT('',#35533);
#7364=VERTEX_POINT('',#35537);
#7365=VERTEX_POINT('',#35541);
#7366=VERTEX_POINT('',#35547);
#7367=VERTEX_POINT('',#35548);
#7368=VERTEX_POINT('',#35550);
#7369=VERTEX_POINT('',#35552);
#7370=VERTEX_POINT('',#35556);
#7371=VERTEX_POINT('',#35560);
#7372=VERTEX_POINT('',#35566);
#7373=VERTEX_POINT('',#35567);
#7374=VERTEX_POINT('',#35569);
#7375=VERTEX_POINT('',#35571);
#7376=VERTEX_POINT('',#35575);
#7377=VERTEX_POINT('',#35579);
#7378=VERTEX_POINT('',#35585);
#7379=VERTEX_POINT('',#35586);
#7380=VERTEX_POINT('',#35588);
#7381=VERTEX_POINT('',#35590);
#7382=VERTEX_POINT('',#35594);
#7383=VERTEX_POINT('',#35598);
#7384=VERTEX_POINT('',#35604);
#7385=VERTEX_POINT('',#35605);
#7386=VERTEX_POINT('',#35607);
#7387=VERTEX_POINT('',#35609);
#7388=VERTEX_POINT('',#35613);
#7389=VERTEX_POINT('',#35617);
#7390=VERTEX_POINT('',#35623);
#7391=VERTEX_POINT('',#35624);
#7392=VERTEX_POINT('',#35626);
#7393=VERTEX_POINT('',#35628);
#7394=VERTEX_POINT('',#35632);
#7395=VERTEX_POINT('',#35636);
#7396=VERTEX_POINT('',#35642);
#7397=VERTEX_POINT('',#35643);
#7398=VERTEX_POINT('',#35645);
#7399=VERTEX_POINT('',#35647);
#7400=VERTEX_POINT('',#35651);
#7401=VERTEX_POINT('',#35655);
#7402=VERTEX_POINT('',#35661);
#7403=VERTEX_POINT('',#35662);
#7404=VERTEX_POINT('',#35664);
#7405=VERTEX_POINT('',#35666);
#7406=VERTEX_POINT('',#35670);
#7407=VERTEX_POINT('',#35674);
#7408=VERTEX_POINT('',#35680);
#7409=VERTEX_POINT('',#35681);
#7410=VERTEX_POINT('',#35683);
#7411=VERTEX_POINT('',#35685);
#7412=VERTEX_POINT('',#35689);
#7413=VERTEX_POINT('',#35693);
#7414=VERTEX_POINT('',#35699);
#7415=VERTEX_POINT('',#35700);
#7416=VERTEX_POINT('',#35702);
#7417=VERTEX_POINT('',#35704);
#7418=VERTEX_POINT('',#35708);
#7419=VERTEX_POINT('',#35712);
#7420=VERTEX_POINT('',#35718);
#7421=VERTEX_POINT('',#35719);
#7422=VERTEX_POINT('',#35721);
#7423=VERTEX_POINT('',#35723);
#7424=VERTEX_POINT('',#35727);
#7425=VERTEX_POINT('',#35731);
#7426=VERTEX_POINT('',#35737);
#7427=VERTEX_POINT('',#35738);
#7428=VERTEX_POINT('',#35740);
#7429=VERTEX_POINT('',#35742);
#7430=VERTEX_POINT('',#35746);
#7431=VERTEX_POINT('',#35748);
#7432=VERTEX_POINT('',#35752);
#7433=VERTEX_POINT('',#35756);
#7434=VERTEX_POINT('',#35760);
#7435=VERTEX_POINT('',#35761);
#7436=VERTEX_POINT('',#35763);
#7437=VERTEX_POINT('',#35765);
#7438=VERTEX_POINT('',#35769);
#7439=VERTEX_POINT('',#35773);
#7440=VERTEX_POINT('',#35779);
#7441=VERTEX_POINT('',#35780);
#7442=VERTEX_POINT('',#35782);
#7443=VERTEX_POINT('',#35784);
#7444=VERTEX_POINT('',#35788);
#7445=VERTEX_POINT('',#35792);
#7446=VERTEX_POINT('',#35798);
#7447=VERTEX_POINT('',#35799);
#7448=VERTEX_POINT('',#35801);
#7449=VERTEX_POINT('',#35803);
#7450=VERTEX_POINT('',#35807);
#7451=VERTEX_POINT('',#35811);
#7452=VERTEX_POINT('',#35817);
#7453=VERTEX_POINT('',#35818);
#7454=VERTEX_POINT('',#35820);
#7455=VERTEX_POINT('',#35822);
#7456=VERTEX_POINT('',#35826);
#7457=VERTEX_POINT('',#35830);
#7458=VERTEX_POINT('',#35836);
#7459=VERTEX_POINT('',#35837);
#7460=VERTEX_POINT('',#35839);
#7461=VERTEX_POINT('',#35841);
#7462=VERTEX_POINT('',#35845);
#7463=VERTEX_POINT('',#35849);
#7464=VERTEX_POINT('',#35855);
#7465=VERTEX_POINT('',#35856);
#7466=VERTEX_POINT('',#35858);
#7467=VERTEX_POINT('',#35860);
#7468=VERTEX_POINT('',#35864);
#7469=VERTEX_POINT('',#35868);
#7470=VERTEX_POINT('',#35874);
#7471=VERTEX_POINT('',#35875);
#7472=VERTEX_POINT('',#35877);
#7473=VERTEX_POINT('',#35879);
#7474=VERTEX_POINT('',#35883);
#7475=VERTEX_POINT('',#35887);
#7476=VERTEX_POINT('',#35893);
#7477=VERTEX_POINT('',#35894);
#7478=VERTEX_POINT('',#35896);
#7479=VERTEX_POINT('',#35898);
#7480=VERTEX_POINT('',#35902);
#7481=VERTEX_POINT('',#35906);
#7482=VERTEX_POINT('',#35912);
#7483=VERTEX_POINT('',#35913);
#7484=VERTEX_POINT('',#35915);
#7485=VERTEX_POINT('',#35917);
#7486=VERTEX_POINT('',#35921);
#7487=VERTEX_POINT('',#35925);
#7488=VERTEX_POINT('',#35931);
#7489=VERTEX_POINT('',#35932);
#7490=VERTEX_POINT('',#35934);
#7491=VERTEX_POINT('',#35936);
#7492=VERTEX_POINT('',#35940);
#7493=VERTEX_POINT('',#35944);
#7494=VERTEX_POINT('',#35950);
#7495=VERTEX_POINT('',#35951);
#7496=VERTEX_POINT('',#35953);
#7497=VERTEX_POINT('',#35955);
#7498=VERTEX_POINT('',#35959);
#7499=VERTEX_POINT('',#35963);
#7500=VERTEX_POINT('',#35969);
#7501=VERTEX_POINT('',#35970);
#7502=VERTEX_POINT('',#35972);
#7503=VERTEX_POINT('',#35974);
#7504=VERTEX_POINT('',#35978);
#7505=VERTEX_POINT('',#35982);
#7506=VERTEX_POINT('',#35988);
#7507=VERTEX_POINT('',#35989);
#7508=VERTEX_POINT('',#35991);
#7509=VERTEX_POINT('',#35993);
#7510=VERTEX_POINT('',#35997);
#7511=VERTEX_POINT('',#36001);
#7512=VERTEX_POINT('',#36007);
#7513=VERTEX_POINT('',#36008);
#7514=VERTEX_POINT('',#36010);
#7515=VERTEX_POINT('',#36012);
#7516=VERTEX_POINT('',#36016);
#7517=VERTEX_POINT('',#36020);
#7518=VERTEX_POINT('',#36026);
#7519=VERTEX_POINT('',#36027);
#7520=VERTEX_POINT('',#36029);
#7521=VERTEX_POINT('',#36031);
#7522=VERTEX_POINT('',#36035);
#7523=VERTEX_POINT('',#36039);
#7524=VERTEX_POINT('',#36045);
#7525=VERTEX_POINT('',#36046);
#7526=VERTEX_POINT('',#36048);
#7527=VERTEX_POINT('',#36050);
#7528=VERTEX_POINT('',#36054);
#7529=VERTEX_POINT('',#36058);
#7530=VERTEX_POINT('',#36064);
#7531=VERTEX_POINT('',#36065);
#7532=VERTEX_POINT('',#36067);
#7533=VERTEX_POINT('',#36069);
#7534=VERTEX_POINT('',#36073);
#7535=VERTEX_POINT('',#36077);
#7536=VERTEX_POINT('',#36083);
#7537=VERTEX_POINT('',#36084);
#7538=VERTEX_POINT('',#36086);
#7539=VERTEX_POINT('',#36088);
#7540=VERTEX_POINT('',#36092);
#7541=VERTEX_POINT('',#36096);
#7542=VERTEX_POINT('',#36102);
#7543=VERTEX_POINT('',#36103);
#7544=VERTEX_POINT('',#36105);
#7545=VERTEX_POINT('',#36107);
#7546=VERTEX_POINT('',#36111);
#7547=VERTEX_POINT('',#36113);
#7548=VERTEX_POINT('',#36117);
#7549=VERTEX_POINT('',#36119);
#7550=VERTEX_POINT('',#36123);
#7551=VERTEX_POINT('',#36125);
#7552=VERTEX_POINT('',#36129);
#7553=VERTEX_POINT('',#36131);
#7554=VERTEX_POINT('',#36139);
#7555=VERTEX_POINT('',#36146);
#7556=VERTEX_POINT('',#36149);
#7557=VERTEX_POINT('',#36154);
#9081=EDGE_CURVE('',#7179,#7180,#4158,.T.);
#9082=EDGE_CURVE('',#7179,#7181,#1187,.T.);
#9083=EDGE_CURVE('',#7181,#7182,#6175,.T.);
#9084=EDGE_CURVE('',#7182,#7180,#1188,.T.);
#9085=EDGE_CURVE('',#7183,#7184,#4159,.T.);
#9086=EDGE_CURVE('',#7183,#7179,#1189,.T.);
#9087=EDGE_CURVE('',#7180,#7184,#1190,.T.);
#9088=EDGE_CURVE('',#7185,#7186,#4160,.T.);
#9089=EDGE_CURVE('',#7185,#7183,#1191,.T.);
#9090=EDGE_CURVE('',#7184,#7186,#1192,.T.);
#9091=EDGE_CURVE('',#7187,#7188,#4161,.T.);
#9092=EDGE_CURVE('',#7187,#7185,#1193,.T.);
#9093=EDGE_CURVE('',#7186,#7188,#1194,.T.);
#9094=EDGE_CURVE('',#7189,#7190,#4162,.T.);
#9095=EDGE_CURVE('',#7189,#7187,#1195,.T.);
#9096=EDGE_CURVE('',#7188,#7190,#1196,.T.);
#9097=EDGE_CURVE('',#7191,#7192,#4163,.T.);
#9098=EDGE_CURVE('',#7191,#7189,#1197,.T.);
#9099=EDGE_CURVE('',#7190,#7192,#1198,.T.);
#9100=EDGE_CURVE('',#7193,#7194,#4164,.T.);
#9101=EDGE_CURVE('',#7193,#7191,#1199,.T.);
#9102=EDGE_CURVE('',#7192,#7194,#1200,.T.);
#9103=EDGE_CURVE('',#7195,#7196,#4165,.T.);
#9104=EDGE_CURVE('',#7195,#7193,#1201,.T.);
#9105=EDGE_CURVE('',#7194,#7196,#1202,.T.);
#9106=EDGE_CURVE('',#7197,#7198,#4166,.T.);
#9107=EDGE_CURVE('',#7197,#7195,#1203,.T.);
#9108=EDGE_CURVE('',#7196,#7198,#1204,.T.);
#9109=EDGE_CURVE('',#7199,#7200,#4167,.T.);
#9110=EDGE_CURVE('',#7199,#7197,#1205,.T.);
#9111=EDGE_CURVE('',#7198,#7200,#1206,.T.);
#9112=EDGE_CURVE('',#7201,#7202,#4168,.T.);
#9113=EDGE_CURVE('',#7201,#7199,#1207,.T.);
#9114=EDGE_CURVE('',#7200,#7202,#1208,.T.);
#9115=EDGE_CURVE('',#7203,#7204,#4169,.T.);
#9116=EDGE_CURVE('',#7203,#7201,#1209,.T.);
#9117=EDGE_CURVE('',#7202,#7204,#1210,.T.);
#9118=EDGE_CURVE('',#7205,#7206,#4170,.T.);
#9119=EDGE_CURVE('',#7205,#7203,#1211,.T.);
#9120=EDGE_CURVE('',#7204,#7206,#1212,.T.);
#9121=EDGE_CURVE('',#7207,#7208,#4171,.T.);
#9122=EDGE_CURVE('',#7207,#7205,#1213,.T.);
#9123=EDGE_CURVE('',#7206,#7208,#1214,.T.);
#9124=EDGE_CURVE('',#7209,#7210,#4172,.T.);
#9125=EDGE_CURVE('',#7209,#7207,#1215,.T.);
#9126=EDGE_CURVE('',#7208,#7210,#1216,.T.);
#9127=EDGE_CURVE('',#7211,#7212,#4173,.T.);
#9128=EDGE_CURVE('',#7211,#7209,#1217,.T.);
#9129=EDGE_CURVE('',#7210,#7212,#1218,.T.);
#9130=EDGE_CURVE('',#7213,#7214,#4174,.T.);
#9131=EDGE_CURVE('',#7213,#7211,#1219,.T.);
#9132=EDGE_CURVE('',#7212,#7214,#1220,.T.);
#9133=EDGE_CURVE('',#7215,#7216,#4175,.T.);
#9134=EDGE_CURVE('',#7215,#7213,#1221,.T.);
#9135=EDGE_CURVE('',#7214,#7216,#1222,.T.);
#9136=EDGE_CURVE('',#7217,#7218,#4176,.T.);
#9137=EDGE_CURVE('',#7217,#7215,#1223,.T.);
#9138=EDGE_CURVE('',#7216,#7218,#1224,.T.);
#9139=EDGE_CURVE('',#7219,#7220,#4177,.T.);
#9140=EDGE_CURVE('',#7219,#7217,#1225,.T.);
#9141=EDGE_CURVE('',#7218,#7220,#1226,.T.);
#9142=EDGE_CURVE('',#7221,#7222,#4178,.T.);
#9143=EDGE_CURVE('',#7221,#7219,#1227,.T.);
#9144=EDGE_CURVE('',#7220,#7222,#1228,.T.);
#9145=EDGE_CURVE('',#7223,#7224,#4179,.T.);
#9146=EDGE_CURVE('',#7223,#7221,#1229,.T.);
#9147=EDGE_CURVE('',#7222,#7224,#1230,.T.);
#9148=EDGE_CURVE('',#7225,#7226,#4180,.T.);
#9149=EDGE_CURVE('',#7225,#7223,#1231,.T.);
#9150=EDGE_CURVE('',#7224,#7226,#1232,.T.);
#9151=EDGE_CURVE('',#7227,#7228,#4181,.T.);
#9152=EDGE_CURVE('',#7227,#7225,#1233,.T.);
#9153=EDGE_CURVE('',#7226,#7228,#1234,.T.);
#9154=EDGE_CURVE('',#7229,#7230,#4182,.T.);
#9155=EDGE_CURVE('',#7229,#7227,#1235,.T.);
#9156=EDGE_CURVE('',#7228,#7230,#1236,.T.);
#9157=EDGE_CURVE('',#7231,#7232,#4183,.T.);
#9158=EDGE_CURVE('',#7231,#7229,#1237,.T.);
#9159=EDGE_CURVE('',#7230,#7232,#1238,.T.);
#9160=EDGE_CURVE('',#7233,#7234,#4184,.T.);
#9161=EDGE_CURVE('',#7233,#7231,#1239,.T.);
#9162=EDGE_CURVE('',#7232,#7234,#1240,.T.);
#9163=EDGE_CURVE('',#7235,#7236,#4185,.T.);
#9164=EDGE_CURVE('',#7235,#7233,#1241,.T.);
#9165=EDGE_CURVE('',#7234,#7236,#1242,.T.);
#9166=EDGE_CURVE('',#7237,#7238,#4186,.T.);
#9167=EDGE_CURVE('',#7237,#7235,#1243,.T.);
#9168=EDGE_CURVE('',#7236,#7238,#1244,.T.);
#9169=EDGE_CURVE('',#7239,#7240,#4187,.T.);
#9170=EDGE_CURVE('',#7239,#7237,#1245,.T.);
#9171=EDGE_CURVE('',#7238,#7240,#1246,.T.);
#9172=EDGE_CURVE('',#7241,#7242,#4188,.T.);
#9173=EDGE_CURVE('',#7241,#7239,#1247,.T.);
#9174=EDGE_CURVE('',#7240,#7242,#1248,.T.);
#9175=EDGE_CURVE('',#7243,#7244,#4189,.T.);
#9176=EDGE_CURVE('',#7243,#7241,#1249,.T.);
#9177=EDGE_CURVE('',#7242,#7244,#1250,.T.);
#9178=EDGE_CURVE('',#7245,#7246,#4190,.T.);
#9179=EDGE_CURVE('',#7245,#7243,#1251,.T.);
#9180=EDGE_CURVE('',#7244,#7246,#1252,.T.);
#9181=EDGE_CURVE('',#7247,#7248,#4191,.T.);
#9182=EDGE_CURVE('',#7247,#7245,#1253,.T.);
#9183=EDGE_CURVE('',#7246,#7248,#1254,.T.);
#9184=EDGE_CURVE('',#7249,#7250,#4192,.T.);
#9185=EDGE_CURVE('',#7249,#7251,#1255,.T.);
#9186=EDGE_CURVE('',#7252,#7251,#6176,.T.);
#9187=EDGE_CURVE('',#7250,#7252,#1256,.T.);
#9188=EDGE_CURVE('',#7253,#7254,#4193,.T.);
#9189=EDGE_CURVE('',#7253,#7249,#1257,.T.);
#9190=EDGE_CURVE('',#7254,#7250,#1258,.T.);
#9191=EDGE_CURVE('',#7255,#7256,#4194,.T.);
#9192=EDGE_CURVE('',#7255,#7253,#1259,.T.);
#9193=EDGE_CURVE('',#7256,#7254,#1260,.T.);
#9194=EDGE_CURVE('',#7257,#7258,#4195,.T.);
#9195=EDGE_CURVE('',#7257,#7255,#1261,.T.);
#9196=EDGE_CURVE('',#7258,#7256,#1262,.T.);
#9197=EDGE_CURVE('',#7259,#7260,#4196,.T.);
#9198=EDGE_CURVE('',#7259,#7257,#1263,.T.);
#9199=EDGE_CURVE('',#7260,#7258,#1264,.T.);
#9200=EDGE_CURVE('',#7261,#7262,#4197,.T.);
#9201=EDGE_CURVE('',#7261,#7259,#1265,.T.);
#9202=EDGE_CURVE('',#7262,#7260,#1266,.T.);
#9203=EDGE_CURVE('',#7263,#7264,#4198,.T.);
#9204=EDGE_CURVE('',#7263,#7261,#1267,.T.);
#9205=EDGE_CURVE('',#7264,#7262,#1268,.T.);
#9206=EDGE_CURVE('',#7265,#7266,#4199,.T.);
#9207=EDGE_CURVE('',#7265,#7263,#1269,.T.);
#9208=EDGE_CURVE('',#7266,#7264,#1270,.T.);
#9209=EDGE_CURVE('',#7267,#7268,#4200,.T.);
#9210=EDGE_CURVE('',#7267,#7265,#1271,.T.);
#9211=EDGE_CURVE('',#7268,#7266,#1272,.T.);
#9212=EDGE_CURVE('',#7269,#7270,#4201,.T.);
#9213=EDGE_CURVE('',#7269,#7267,#1273,.T.);
#9214=EDGE_CURVE('',#7270,#7268,#1274,.T.);
#9215=EDGE_CURVE('',#7271,#7272,#4202,.T.);
#9216=EDGE_CURVE('',#7271,#7269,#1275,.T.);
#9217=EDGE_CURVE('',#7272,#7270,#1276,.T.);
#9218=EDGE_CURVE('',#7273,#7274,#4203,.T.);
#9219=EDGE_CURVE('',#7273,#7271,#1277,.T.);
#9220=EDGE_CURVE('',#7274,#7272,#1278,.T.);
#9221=EDGE_CURVE('',#7275,#7276,#4204,.T.);
#9222=EDGE_CURVE('',#7275,#7273,#1279,.T.);
#9223=EDGE_CURVE('',#7276,#7274,#1280,.T.);
#9224=EDGE_CURVE('',#7277,#7278,#4205,.T.);
#9225=EDGE_CURVE('',#7277,#7275,#1281,.T.);
#9226=EDGE_CURVE('',#7278,#7276,#1282,.T.);
#9227=EDGE_CURVE('',#7279,#7280,#4206,.T.);
#9228=EDGE_CURVE('',#7279,#7277,#1283,.T.);
#9229=EDGE_CURVE('',#7280,#7278,#1284,.T.);
#9230=EDGE_CURVE('',#7281,#7282,#4207,.T.);
#9231=EDGE_CURVE('',#7281,#7279,#1285,.T.);
#9232=EDGE_CURVE('',#7282,#7280,#1286,.T.);
#9233=EDGE_CURVE('',#7283,#7284,#4208,.T.);
#9234=EDGE_CURVE('',#7283,#7281,#1287,.T.);
#9235=EDGE_CURVE('',#7284,#7282,#1288,.T.);
#9236=EDGE_CURVE('',#7285,#7286,#4209,.T.);
#9237=EDGE_CURVE('',#7285,#7283,#1289,.T.);
#9238=EDGE_CURVE('',#7286,#7284,#1290,.T.);
#9239=EDGE_CURVE('',#7287,#7288,#4210,.T.);
#9240=EDGE_CURVE('',#7287,#7285,#1291,.T.);
#9241=EDGE_CURVE('',#7288,#7286,#1292,.T.);
#9242=EDGE_CURVE('',#7289,#7290,#4211,.T.);
#9243=EDGE_CURVE('',#7289,#7287,#1293,.T.);
#9244=EDGE_CURVE('',#7290,#7288,#1294,.T.);
#9245=EDGE_CURVE('',#7291,#7292,#4212,.T.);
#9246=EDGE_CURVE('',#7291,#7289,#1295,.T.);
#9247=EDGE_CURVE('',#7292,#7290,#1296,.T.);
#9248=EDGE_CURVE('',#7293,#7294,#4213,.T.);
#9249=EDGE_CURVE('',#7293,#7291,#1297,.T.);
#9250=EDGE_CURVE('',#7294,#7292,#1298,.T.);
#9251=EDGE_CURVE('',#7295,#7296,#4214,.T.);
#9252=EDGE_CURVE('',#7295,#7293,#1299,.T.);
#9253=EDGE_CURVE('',#7296,#7294,#1300,.T.);
#9254=EDGE_CURVE('',#7297,#7298,#4215,.T.);
#9255=EDGE_CURVE('',#7297,#7295,#1301,.T.);
#9256=EDGE_CURVE('',#7298,#7296,#1302,.T.);
#9257=EDGE_CURVE('',#7299,#7300,#4216,.T.);
#9258=EDGE_CURVE('',#7299,#7297,#1303,.T.);
#9259=EDGE_CURVE('',#7300,#7298,#1304,.T.);
#9260=EDGE_CURVE('',#7301,#7302,#4217,.T.);
#9261=EDGE_CURVE('',#7301,#7299,#1305,.T.);
#9262=EDGE_CURVE('',#7302,#7300,#1306,.T.);
#9263=EDGE_CURVE('',#7303,#7304,#4218,.T.);
#9264=EDGE_CURVE('',#7303,#7301,#1307,.T.);
#9265=EDGE_CURVE('',#7304,#7302,#1308,.T.);
#9266=EDGE_CURVE('',#7305,#7306,#4219,.T.);
#9267=EDGE_CURVE('',#7305,#7303,#1309,.T.);
#9268=EDGE_CURVE('',#7306,#7304,#1310,.T.);
#9269=EDGE_CURVE('',#7307,#7308,#4220,.T.);
#9270=EDGE_CURVE('',#7307,#7305,#1311,.T.);
#9271=EDGE_CURVE('',#7308,#7306,#1312,.T.);
#9272=EDGE_CURVE('',#7309,#7310,#4221,.T.);
#9273=EDGE_CURVE('',#7309,#7307,#1313,.T.);
#9274=EDGE_CURVE('',#7310,#7308,#1314,.T.);
#9275=EDGE_CURVE('',#7311,#7312,#4222,.T.);
#9276=EDGE_CURVE('',#7311,#7309,#1315,.T.);
#9277=EDGE_CURVE('',#7312,#7310,#1316,.T.);
#9278=EDGE_CURVE('',#7313,#7314,#4223,.T.);
#9279=EDGE_CURVE('',#7313,#7311,#1317,.T.);
#9280=EDGE_CURVE('',#7314,#7312,#1318,.T.);
#9281=EDGE_CURVE('',#7315,#7316,#4224,.T.);
#9282=EDGE_CURVE('',#7315,#7313,#1319,.T.);
#9283=EDGE_CURVE('',#7316,#7314,#1320,.T.);
#9284=EDGE_CURVE('',#7317,#7318,#4225,.T.);
#9285=EDGE_CURVE('',#7317,#7315,#1321,.T.);
#9286=EDGE_CURVE('',#7318,#7316,#1322,.T.);
#9287=EDGE_CURVE('',#7319,#7252,#1323,.T.);
#9288=EDGE_CURVE('',#7248,#7319,#1324,.T.);
#9289=EDGE_CURVE('',#7320,#7182,#1325,.T.);
#9290=EDGE_CURVE('',#7320,#7318,#1326,.T.);
#9291=EDGE_CURVE('',#7182,#7321,#6177,.T.);
#9292=EDGE_CURVE('',#7321,#7181,#6178,.T.);
#9293=EDGE_CURVE('',#7181,#7322,#1327,.T.);
#9294=EDGE_CURVE('',#7322,#7320,#6179,.T.);
#9295=EDGE_CURVE('',#7322,#7317,#1328,.T.);
#9296=EDGE_CURVE('',#7251,#7323,#1329,.T.);
#9297=EDGE_CURVE('',#7323,#7247,#1330,.T.);
#9298=EDGE_CURVE('',#7324,#7325,#4226,.T.);
#9299=EDGE_CURVE('',#7324,#7326,#4227,.T.);
#9300=EDGE_CURVE('',#7327,#7326,#4228,.T.);
#9301=EDGE_CURVE('',#7325,#7327,#4229,.T.);
#9302=EDGE_CURVE('',#7325,#7328,#6180,.T.);
#9303=EDGE_CURVE('',#7327,#7328,#4230,.T.);
#9304=EDGE_CURVE('',#7328,#7329,#4231,.T.);
#9305=EDGE_CURVE('',#7326,#7329,#4232,.T.);
#9306=EDGE_CURVE('',#7329,#7324,#6181,.T.);
#9307=EDGE_CURVE('',#7330,#7331,#4233,.T.);
#9308=EDGE_CURVE('',#7330,#7332,#4234,.T.);
#9309=EDGE_CURVE('',#7333,#7332,#4235,.T.);
#9310=EDGE_CURVE('',#7331,#7333,#4236,.T.);
#9311=EDGE_CURVE('',#7331,#7334,#6182,.T.);
#9312=EDGE_CURVE('',#7333,#7334,#4237,.T.);
#9313=EDGE_CURVE('',#7334,#7335,#4238,.T.);
#9314=EDGE_CURVE('',#7332,#7335,#4239,.T.);
#9315=EDGE_CURVE('',#7335,#7330,#6183,.T.);
#9316=EDGE_CURVE('',#7336,#7337,#4240,.T.);
#9317=EDGE_CURVE('',#7336,#7338,#4241,.T.);
#9318=EDGE_CURVE('',#7339,#7338,#4242,.T.);
#9319=EDGE_CURVE('',#7337,#7339,#4243,.T.);
#9320=EDGE_CURVE('',#7337,#7340,#6184,.T.);
#9321=EDGE_CURVE('',#7339,#7340,#4244,.T.);
#9322=EDGE_CURVE('',#7340,#7341,#4245,.T.);
#9323=EDGE_CURVE('',#7338,#7341,#4246,.T.);
#9324=EDGE_CURVE('',#7341,#7336,#6185,.T.);
#9325=EDGE_CURVE('',#7342,#7343,#4247,.T.);
#9326=EDGE_CURVE('',#7342,#7344,#4248,.T.);
#9327=EDGE_CURVE('',#7345,#7344,#4249,.T.);
#9328=EDGE_CURVE('',#7343,#7345,#4250,.T.);
#9329=EDGE_CURVE('',#7343,#7346,#6186,.T.);
#9330=EDGE_CURVE('',#7345,#7346,#4251,.T.);
#9331=EDGE_CURVE('',#7346,#7347,#4252,.T.);
#9332=EDGE_CURVE('',#7344,#7347,#4253,.T.);
#9333=EDGE_CURVE('',#7347,#7342,#6187,.T.);
#9334=EDGE_CURVE('',#7348,#7349,#4254,.T.);
#9335=EDGE_CURVE('',#7348,#7350,#4255,.T.);
#9336=EDGE_CURVE('',#7351,#7350,#4256,.T.);
#9337=EDGE_CURVE('',#7349,#7351,#4257,.T.);
#9338=EDGE_CURVE('',#7349,#7352,#6188,.T.);
#9339=EDGE_CURVE('',#7351,#7352,#4258,.T.);
#9340=EDGE_CURVE('',#7352,#7353,#4259,.T.);
#9341=EDGE_CURVE('',#7350,#7353,#4260,.T.);
#9342=EDGE_CURVE('',#7353,#7348,#6189,.T.);
#9343=EDGE_CURVE('',#7354,#7355,#4261,.T.);
#9344=EDGE_CURVE('',#7354,#7356,#4262,.T.);
#9345=EDGE_CURVE('',#7357,#7356,#4263,.T.);
#9346=EDGE_CURVE('',#7355,#7357,#4264,.T.);
#9347=EDGE_CURVE('',#7355,#7358,#6190,.T.);
#9348=EDGE_CURVE('',#7357,#7358,#4265,.T.);
#9349=EDGE_CURVE('',#7358,#7359,#4266,.T.);
#9350=EDGE_CURVE('',#7356,#7359,#4267,.T.);
#9351=EDGE_CURVE('',#7359,#7354,#6191,.T.);
#9352=EDGE_CURVE('',#7360,#7361,#4268,.T.);
#9353=EDGE_CURVE('',#7360,#7362,#4269,.T.);
#9354=EDGE_CURVE('',#7363,#7362,#4270,.T.);
#9355=EDGE_CURVE('',#7361,#7363,#4271,.T.);
#9356=EDGE_CURVE('',#7361,#7364,#6192,.T.);
#9357=EDGE_CURVE('',#7363,#7364,#4272,.T.);
#9358=EDGE_CURVE('',#7364,#7365,#4273,.T.);
#9359=EDGE_CURVE('',#7362,#7365,#4274,.T.);
#9360=EDGE_CURVE('',#7365,#7360,#6193,.T.);
#9361=EDGE_CURVE('',#7366,#7367,#4275,.T.);
#9362=EDGE_CURVE('',#7366,#7368,#4276,.T.);
#9363=EDGE_CURVE('',#7369,#7368,#4277,.T.);
#9364=EDGE_CURVE('',#7367,#7369,#4278,.T.);
#9365=EDGE_CURVE('',#7367,#7370,#6194,.T.);
#9366=EDGE_CURVE('',#7369,#7370,#4279,.T.);
#9367=EDGE_CURVE('',#7370,#7371,#4280,.T.);
#9368=EDGE_CURVE('',#7368,#7371,#4281,.T.);
#9369=EDGE_CURVE('',#7371,#7366,#6195,.T.);
#9370=EDGE_CURVE('',#7372,#7373,#4282,.T.);
#9371=EDGE_CURVE('',#7372,#7374,#4283,.T.);
#9372=EDGE_CURVE('',#7375,#7374,#4284,.T.);
#9373=EDGE_CURVE('',#7373,#7375,#4285,.T.);
#9374=EDGE_CURVE('',#7373,#7376,#6196,.T.);
#9375=EDGE_CURVE('',#7375,#7376,#4286,.T.);
#9376=EDGE_CURVE('',#7376,#7377,#4287,.T.);
#9377=EDGE_CURVE('',#7374,#7377,#4288,.T.);
#9378=EDGE_CURVE('',#7377,#7372,#6197,.T.);
#9379=EDGE_CURVE('',#7378,#7379,#4289,.T.);
#9380=EDGE_CURVE('',#7378,#7380,#4290,.T.);
#9381=EDGE_CURVE('',#7381,#7380,#4291,.T.);
#9382=EDGE_CURVE('',#7379,#7381,#4292,.T.);
#9383=EDGE_CURVE('',#7379,#7382,#6198,.T.);
#9384=EDGE_CURVE('',#7381,#7382,#4293,.T.);
#9385=EDGE_CURVE('',#7382,#7383,#4294,.T.);
#9386=EDGE_CURVE('',#7380,#7383,#4295,.T.);
#9387=EDGE_CURVE('',#7383,#7378,#6199,.T.);
#9388=EDGE_CURVE('',#7384,#7385,#4296,.T.);
#9389=EDGE_CURVE('',#7384,#7386,#4297,.T.);
#9390=EDGE_CURVE('',#7387,#7386,#4298,.T.);
#9391=EDGE_CURVE('',#7385,#7387,#4299,.T.);
#9392=EDGE_CURVE('',#7385,#7388,#6200,.T.);
#9393=EDGE_CURVE('',#7387,#7388,#4300,.T.);
#9394=EDGE_CURVE('',#7388,#7389,#4301,.T.);
#9395=EDGE_CURVE('',#7386,#7389,#4302,.T.);
#9396=EDGE_CURVE('',#7389,#7384,#6201,.T.);
#9397=EDGE_CURVE('',#7390,#7391,#4303,.T.);
#9398=EDGE_CURVE('',#7390,#7392,#4304,.T.);
#9399=EDGE_CURVE('',#7393,#7392,#4305,.T.);
#9400=EDGE_CURVE('',#7391,#7393,#4306,.T.);
#9401=EDGE_CURVE('',#7391,#7394,#6202,.T.);
#9402=EDGE_CURVE('',#7393,#7394,#4307,.T.);
#9403=EDGE_CURVE('',#7394,#7395,#4308,.T.);
#9404=EDGE_CURVE('',#7392,#7395,#4309,.T.);
#9405=EDGE_CURVE('',#7395,#7390,#6203,.T.);
#9406=EDGE_CURVE('',#7396,#7397,#4310,.T.);
#9407=EDGE_CURVE('',#7396,#7398,#4311,.T.);
#9408=EDGE_CURVE('',#7399,#7398,#4312,.T.);
#9409=EDGE_CURVE('',#7397,#7399,#4313,.T.);
#9410=EDGE_CURVE('',#7397,#7400,#6204,.T.);
#9411=EDGE_CURVE('',#7399,#7400,#4314,.T.);
#9412=EDGE_CURVE('',#7400,#7401,#4315,.T.);
#9413=EDGE_CURVE('',#7398,#7401,#4316,.T.);
#9414=EDGE_CURVE('',#7401,#7396,#6205,.T.);
#9415=EDGE_CURVE('',#7402,#7403,#4317,.T.);
#9416=EDGE_CURVE('',#7402,#7404,#4318,.T.);
#9417=EDGE_CURVE('',#7405,#7404,#4319,.T.);
#9418=EDGE_CURVE('',#7403,#7405,#4320,.T.);
#9419=EDGE_CURVE('',#7403,#7406,#6206,.T.);
#9420=EDGE_CURVE('',#7405,#7406,#4321,.T.);
#9421=EDGE_CURVE('',#7406,#7407,#4322,.T.);
#9422=EDGE_CURVE('',#7404,#7407,#4323,.T.);
#9423=EDGE_CURVE('',#7407,#7402,#6207,.T.);
#9424=EDGE_CURVE('',#7408,#7409,#4324,.T.);
#9425=EDGE_CURVE('',#7408,#7410,#4325,.T.);
#9426=EDGE_CURVE('',#7411,#7410,#4326,.T.);
#9427=EDGE_CURVE('',#7409,#7411,#4327,.T.);
#9428=EDGE_CURVE('',#7409,#7412,#6208,.T.);
#9429=EDGE_CURVE('',#7411,#7412,#4328,.T.);
#9430=EDGE_CURVE('',#7412,#7413,#4329,.T.);
#9431=EDGE_CURVE('',#7410,#7413,#4330,.T.);
#9432=EDGE_CURVE('',#7413,#7408,#6209,.T.);
#9433=EDGE_CURVE('',#7414,#7415,#4331,.T.);
#9434=EDGE_CURVE('',#7414,#7416,#4332,.T.);
#9435=EDGE_CURVE('',#7417,#7416,#4333,.T.);
#9436=EDGE_CURVE('',#7415,#7417,#4334,.T.);
#9437=EDGE_CURVE('',#7415,#7418,#6210,.T.);
#9438=EDGE_CURVE('',#7417,#7418,#4335,.T.);
#9439=EDGE_CURVE('',#7418,#7419,#4336,.T.);
#9440=EDGE_CURVE('',#7416,#7419,#4337,.T.);
#9441=EDGE_CURVE('',#7419,#7414,#6211,.T.);
#9442=EDGE_CURVE('',#7420,#7421,#4338,.T.);
#9443=EDGE_CURVE('',#7420,#7422,#4339,.T.);
#9444=EDGE_CURVE('',#7423,#7422,#4340,.T.);
#9445=EDGE_CURVE('',#7421,#7423,#4341,.T.);
#9446=EDGE_CURVE('',#7421,#7424,#6212,.T.);
#9447=EDGE_CURVE('',#7423,#7424,#4342,.T.);
#9448=EDGE_CURVE('',#7424,#7425,#4343,.T.);
#9449=EDGE_CURVE('',#7422,#7425,#4344,.T.);
#9450=EDGE_CURVE('',#7425,#7420,#6213,.T.);
#9451=EDGE_CURVE('',#7426,#7427,#4345,.T.);
#9452=EDGE_CURVE('',#7426,#7428,#4346,.T.);
#9453=EDGE_CURVE('',#7429,#7428,#4347,.T.);
#9454=EDGE_CURVE('',#7427,#7429,#4348,.T.);
#9455=EDGE_CURVE('',#7427,#7430,#6214,.T.);
#9456=EDGE_CURVE('',#7429,#7431,#4349,.T.);
#9457=EDGE_CURVE('',#7430,#7431,#6215,.T.);
#9458=EDGE_CURVE('',#7431,#7432,#4350,.T.);
#9459=EDGE_CURVE('',#7428,#7432,#4351,.T.);
#9460=EDGE_CURVE('',#7432,#7433,#6216,.T.);
#9461=EDGE_CURVE('',#7433,#7426,#6217,.T.);
#9462=EDGE_CURVE('',#7434,#7435,#4352,.T.);
#9463=EDGE_CURVE('',#7434,#7436,#4353,.T.);
#9464=EDGE_CURVE('',#7437,#7436,#4354,.T.);
#9465=EDGE_CURVE('',#7435,#7437,#4355,.T.);
#9466=EDGE_CURVE('',#7435,#7438,#6218,.T.);
#9467=EDGE_CURVE('',#7437,#7438,#4356,.T.);
#9468=EDGE_CURVE('',#7438,#7439,#4357,.T.);
#9469=EDGE_CURVE('',#7436,#7439,#4358,.T.);
#9470=EDGE_CURVE('',#7439,#7434,#6219,.T.);
#9471=EDGE_CURVE('',#7440,#7441,#4359,.T.);
#9472=EDGE_CURVE('',#7440,#7442,#4360,.T.);
#9473=EDGE_CURVE('',#7443,#7442,#4361,.T.);
#9474=EDGE_CURVE('',#7441,#7443,#4362,.T.);
#9475=EDGE_CURVE('',#7441,#7444,#6220,.T.);
#9476=EDGE_CURVE('',#7443,#7444,#4363,.T.);
#9477=EDGE_CURVE('',#7444,#7445,#4364,.T.);
#9478=EDGE_CURVE('',#7442,#7445,#4365,.T.);
#9479=EDGE_CURVE('',#7445,#7440,#6221,.T.);
#9480=EDGE_CURVE('',#7446,#7447,#4366,.T.);
#9481=EDGE_CURVE('',#7446,#7448,#4367,.T.);
#9482=EDGE_CURVE('',#7449,#7448,#4368,.T.);
#9483=EDGE_CURVE('',#7447,#7449,#4369,.T.);
#9484=EDGE_CURVE('',#7447,#7450,#6222,.T.);
#9485=EDGE_CURVE('',#7449,#7450,#4370,.T.);
#9486=EDGE_CURVE('',#7450,#7451,#4371,.T.);
#9487=EDGE_CURVE('',#7448,#7451,#4372,.T.);
#9488=EDGE_CURVE('',#7451,#7446,#6223,.T.);
#9489=EDGE_CURVE('',#7452,#7453,#4373,.T.);
#9490=EDGE_CURVE('',#7452,#7454,#4374,.T.);
#9491=EDGE_CURVE('',#7455,#7454,#4375,.T.);
#9492=EDGE_CURVE('',#7453,#7455,#4376,.T.);
#9493=EDGE_CURVE('',#7453,#7456,#6224,.T.);
#9494=EDGE_CURVE('',#7455,#7456,#4377,.T.);
#9495=EDGE_CURVE('',#7456,#7457,#4378,.T.);
#9496=EDGE_CURVE('',#7454,#7457,#4379,.T.);
#9497=EDGE_CURVE('',#7457,#7452,#6225,.T.);
#9498=EDGE_CURVE('',#7458,#7459,#4380,.T.);
#9499=EDGE_CURVE('',#7458,#7460,#4381,.T.);
#9500=EDGE_CURVE('',#7461,#7460,#4382,.T.);
#9501=EDGE_CURVE('',#7459,#7461,#4383,.T.);
#9502=EDGE_CURVE('',#7459,#7462,#6226,.T.);
#9503=EDGE_CURVE('',#7461,#7462,#4384,.T.);
#9504=EDGE_CURVE('',#7462,#7463,#4385,.T.);
#9505=EDGE_CURVE('',#7460,#7463,#4386,.T.);
#9506=EDGE_CURVE('',#7463,#7458,#6227,.T.);
#9507=EDGE_CURVE('',#7464,#7465,#4387,.T.);
#9508=EDGE_CURVE('',#7464,#7466,#4388,.T.);
#9509=EDGE_CURVE('',#7467,#7466,#4389,.T.);
#9510=EDGE_CURVE('',#7465,#7467,#4390,.T.);
#9511=EDGE_CURVE('',#7465,#7468,#6228,.T.);
#9512=EDGE_CURVE('',#7467,#7468,#4391,.T.);
#9513=EDGE_CURVE('',#7468,#7469,#4392,.T.);
#9514=EDGE_CURVE('',#7466,#7469,#4393,.T.);
#9515=EDGE_CURVE('',#7469,#7464,#6229,.T.);
#9516=EDGE_CURVE('',#7470,#7471,#4394,.T.);
#9517=EDGE_CURVE('',#7470,#7472,#4395,.T.);
#9518=EDGE_CURVE('',#7473,#7472,#4396,.T.);
#9519=EDGE_CURVE('',#7471,#7473,#4397,.T.);
#9520=EDGE_CURVE('',#7471,#7474,#6230,.T.);
#9521=EDGE_CURVE('',#7473,#7474,#4398,.T.);
#9522=EDGE_CURVE('',#7474,#7475,#4399,.T.);
#9523=EDGE_CURVE('',#7472,#7475,#4400,.T.);
#9524=EDGE_CURVE('',#7475,#7470,#6231,.T.);
#9525=EDGE_CURVE('',#7476,#7477,#4401,.T.);
#9526=EDGE_CURVE('',#7476,#7478,#4402,.T.);
#9527=EDGE_CURVE('',#7479,#7478,#4403,.T.);
#9528=EDGE_CURVE('',#7477,#7479,#4404,.T.);
#9529=EDGE_CURVE('',#7477,#7480,#6232,.T.);
#9530=EDGE_CURVE('',#7479,#7480,#4405,.T.);
#9531=EDGE_CURVE('',#7480,#7481,#4406,.T.);
#9532=EDGE_CURVE('',#7478,#7481,#4407,.T.);
#9533=EDGE_CURVE('',#7481,#7476,#6233,.T.);
#9534=EDGE_CURVE('',#7482,#7483,#4408,.T.);
#9535=EDGE_CURVE('',#7482,#7484,#4409,.T.);
#9536=EDGE_CURVE('',#7485,#7484,#4410,.T.);
#9537=EDGE_CURVE('',#7483,#7485,#4411,.T.);
#9538=EDGE_CURVE('',#7483,#7486,#6234,.T.);
#9539=EDGE_CURVE('',#7485,#7486,#4412,.T.);
#9540=EDGE_CURVE('',#7486,#7487,#4413,.T.);
#9541=EDGE_CURVE('',#7484,#7487,#4414,.T.);
#9542=EDGE_CURVE('',#7487,#7482,#6235,.T.);
#9543=EDGE_CURVE('',#7488,#7489,#4415,.T.);
#9544=EDGE_CURVE('',#7488,#7490,#4416,.T.);
#9545=EDGE_CURVE('',#7491,#7490,#4417,.T.);
#9546=EDGE_CURVE('',#7489,#7491,#4418,.T.);
#9547=EDGE_CURVE('',#7489,#7492,#6236,.T.);
#9548=EDGE_CURVE('',#7491,#7492,#4419,.T.);
#9549=EDGE_CURVE('',#7492,#7493,#4420,.T.);
#9550=EDGE_CURVE('',#7490,#7493,#4421,.T.);
#9551=EDGE_CURVE('',#7493,#7488,#6237,.T.);
#9552=EDGE_CURVE('',#7494,#7495,#4422,.T.);
#9553=EDGE_CURVE('',#7494,#7496,#4423,.T.);
#9554=EDGE_CURVE('',#7497,#7496,#4424,.T.);
#9555=EDGE_CURVE('',#7495,#7497,#4425,.T.);
#9556=EDGE_CURVE('',#7495,#7498,#6238,.T.);
#9557=EDGE_CURVE('',#7497,#7498,#4426,.T.);
#9558=EDGE_CURVE('',#7498,#7499,#4427,.T.);
#9559=EDGE_CURVE('',#7496,#7499,#4428,.T.);
#9560=EDGE_CURVE('',#7499,#7494,#6239,.T.);
#9561=EDGE_CURVE('',#7500,#7501,#4429,.T.);
#9562=EDGE_CURVE('',#7500,#7502,#4430,.T.);
#9563=EDGE_CURVE('',#7503,#7502,#4431,.T.);
#9564=EDGE_CURVE('',#7501,#7503,#4432,.T.);
#9565=EDGE_CURVE('',#7501,#7504,#6240,.T.);
#9566=EDGE_CURVE('',#7503,#7504,#4433,.T.);
#9567=EDGE_CURVE('',#7504,#7505,#4434,.T.);
#9568=EDGE_CURVE('',#7502,#7505,#4435,.T.);
#9569=EDGE_CURVE('',#7505,#7500,#6241,.T.);
#9570=EDGE_CURVE('',#7506,#7507,#4436,.T.);
#9571=EDGE_CURVE('',#7506,#7508,#4437,.T.);
#9572=EDGE_CURVE('',#7509,#7508,#4438,.T.);
#9573=EDGE_CURVE('',#7507,#7509,#4439,.T.);
#9574=EDGE_CURVE('',#7507,#7510,#6242,.T.);
#9575=EDGE_CURVE('',#7509,#7510,#4440,.T.);
#9576=EDGE_CURVE('',#7510,#7511,#4441,.T.);
#9577=EDGE_CURVE('',#7508,#7511,#4442,.T.);
#9578=EDGE_CURVE('',#7511,#7506,#6243,.T.);
#9579=EDGE_CURVE('',#7512,#7513,#4443,.T.);
#9580=EDGE_CURVE('',#7512,#7514,#4444,.T.);
#9581=EDGE_CURVE('',#7515,#7514,#4445,.T.);
#9582=EDGE_CURVE('',#7513,#7515,#4446,.T.);
#9583=EDGE_CURVE('',#7513,#7516,#6244,.T.);
#9584=EDGE_CURVE('',#7515,#7516,#4447,.T.);
#9585=EDGE_CURVE('',#7516,#7517,#4448,.T.);
#9586=EDGE_CURVE('',#7514,#7517,#4449,.T.);
#9587=EDGE_CURVE('',#7517,#7512,#6245,.T.);
#9588=EDGE_CURVE('',#7518,#7519,#4450,.T.);
#9589=EDGE_CURVE('',#7518,#7520,#4451,.T.);
#9590=EDGE_CURVE('',#7521,#7520,#4452,.T.);
#9591=EDGE_CURVE('',#7519,#7521,#4453,.T.);
#9592=EDGE_CURVE('',#7519,#7522,#6246,.T.);
#9593=EDGE_CURVE('',#7521,#7522,#4454,.T.);
#9594=EDGE_CURVE('',#7522,#7523,#4455,.T.);
#9595=EDGE_CURVE('',#7520,#7523,#4456,.T.);
#9596=EDGE_CURVE('',#7523,#7518,#6247,.T.);
#9597=EDGE_CURVE('',#7524,#7525,#4457,.T.);
#9598=EDGE_CURVE('',#7524,#7526,#4458,.T.);
#9599=EDGE_CURVE('',#7527,#7526,#4459,.T.);
#9600=EDGE_CURVE('',#7525,#7527,#4460,.T.);
#9601=EDGE_CURVE('',#7525,#7528,#6248,.T.);
#9602=EDGE_CURVE('',#7527,#7528,#4461,.T.);
#9603=EDGE_CURVE('',#7528,#7529,#4462,.T.);
#9604=EDGE_CURVE('',#7526,#7529,#4463,.T.);
#9605=EDGE_CURVE('',#7529,#7524,#6249,.T.);
#9606=EDGE_CURVE('',#7530,#7531,#4464,.T.);
#9607=EDGE_CURVE('',#7530,#7532,#4465,.T.);
#9608=EDGE_CURVE('',#7533,#7532,#4466,.T.);
#9609=EDGE_CURVE('',#7531,#7533,#4467,.T.);
#9610=EDGE_CURVE('',#7531,#7534,#6250,.T.);
#9611=EDGE_CURVE('',#7533,#7534,#4468,.T.);
#9612=EDGE_CURVE('',#7534,#7535,#4469,.T.);
#9613=EDGE_CURVE('',#7532,#7535,#4470,.T.);
#9614=EDGE_CURVE('',#7535,#7530,#6251,.T.);
#9615=EDGE_CURVE('',#7536,#7537,#4471,.T.);
#9616=EDGE_CURVE('',#7536,#7538,#4472,.T.);
#9617=EDGE_CURVE('',#7539,#7538,#4473,.T.);
#9618=EDGE_CURVE('',#7537,#7539,#4474,.T.);
#9619=EDGE_CURVE('',#7537,#7540,#6252,.T.);
#9620=EDGE_CURVE('',#7539,#7540,#4475,.T.);
#9621=EDGE_CURVE('',#7540,#7541,#4476,.T.);
#9622=EDGE_CURVE('',#7538,#7541,#4477,.T.);
#9623=EDGE_CURVE('',#7541,#7536,#6253,.T.);
#9624=EDGE_CURVE('',#7542,#7543,#4478,.T.);
#9625=EDGE_CURVE('',#7542,#7544,#4479,.T.);
#9626=EDGE_CURVE('',#7544,#7545,#4480,.T.);
#9627=EDGE_CURVE('',#7543,#7545,#4481,.T.);
#9628=EDGE_CURVE('',#7546,#7542,#4482,.T.);
#9629=EDGE_CURVE('',#7546,#7547,#4483,.T.);
#9630=EDGE_CURVE('',#7547,#7544,#4484,.T.);
#9631=EDGE_CURVE('',#7548,#7546,#4485,.T.);
#9632=EDGE_CURVE('',#7548,#7549,#4486,.T.);
#9633=EDGE_CURVE('',#7549,#7547,#4487,.T.);
#9634=EDGE_CURVE('',#7550,#7548,#4488,.T.);
#9635=EDGE_CURVE('',#7550,#7551,#4489,.T.);
#9636=EDGE_CURVE('',#7551,#7549,#4490,.T.);
#9637=EDGE_CURVE('',#7552,#7550,#4491,.T.);
#9638=EDGE_CURVE('',#7552,#7553,#4492,.T.);
#9639=EDGE_CURVE('',#7553,#7551,#4493,.T.);
#9640=EDGE_CURVE('',#7543,#7552,#4494,.T.);
#9641=EDGE_CURVE('',#7545,#7553,#4495,.T.);
#9642=EDGE_CURVE('',#7554,#7554,#6254,.T.);
#9643=EDGE_CURVE('',#7321,#7554,#4496,.T.);
#9644=EDGE_CURVE('',#7323,#7319,#6255,.T.);
#9645=EDGE_CURVE('',#7555,#7555,#6256,.T.);
#9646=EDGE_CURVE('',#7556,#7556,#6257,.T.);
#9647=EDGE_CURVE('',#7556,#7433,#4497,.T.);
#9648=EDGE_CURVE('',#7430,#7555,#4498,.T.);
#9649=EDGE_CURVE('',#7557,#7557,#6258,.T.);
#9650=EDGE_CURVE('',#7557,#7556,#4499,.T.);
#12665=ORIENTED_EDGE('',*,*,#9081,.F.);
#12666=ORIENTED_EDGE('',*,*,#9082,.T.);
#12667=ORIENTED_EDGE('',*,*,#9083,.T.);
#12668=ORIENTED_EDGE('',*,*,#9084,.T.);
#12669=ORIENTED_EDGE('',*,*,#9085,.F.);
#12670=ORIENTED_EDGE('',*,*,#9086,.T.);
#12671=ORIENTED_EDGE('',*,*,#9081,.T.);
#12672=ORIENTED_EDGE('',*,*,#9087,.T.);
#12673=ORIENTED_EDGE('',*,*,#9088,.F.);
#12674=ORIENTED_EDGE('',*,*,#9089,.T.);
#12675=ORIENTED_EDGE('',*,*,#9085,.T.);
#12676=ORIENTED_EDGE('',*,*,#9090,.T.);
#12677=ORIENTED_EDGE('',*,*,#9091,.F.);
#12678=ORIENTED_EDGE('',*,*,#9092,.T.);
#12679=ORIENTED_EDGE('',*,*,#9088,.T.);
#12680=ORIENTED_EDGE('',*,*,#9093,.T.);
#12681=ORIENTED_EDGE('',*,*,#9094,.F.);
#12682=ORIENTED_EDGE('',*,*,#9095,.T.);
#12683=ORIENTED_EDGE('',*,*,#9091,.T.);
#12684=ORIENTED_EDGE('',*,*,#9096,.T.);
#12685=ORIENTED_EDGE('',*,*,#9097,.F.);
#12686=ORIENTED_EDGE('',*,*,#9098,.T.);
#12687=ORIENTED_EDGE('',*,*,#9094,.T.);
#12688=ORIENTED_EDGE('',*,*,#9099,.T.);
#12689=ORIENTED_EDGE('',*,*,#9100,.F.);
#12690=ORIENTED_EDGE('',*,*,#9101,.T.);
#12691=ORIENTED_EDGE('',*,*,#9097,.T.);
#12692=ORIENTED_EDGE('',*,*,#9102,.T.);
#12693=ORIENTED_EDGE('',*,*,#9103,.F.);
#12694=ORIENTED_EDGE('',*,*,#9104,.T.);
#12695=ORIENTED_EDGE('',*,*,#9100,.T.);
#12696=ORIENTED_EDGE('',*,*,#9105,.T.);
#12697=ORIENTED_EDGE('',*,*,#9106,.F.);
#12698=ORIENTED_EDGE('',*,*,#9107,.T.);
#12699=ORIENTED_EDGE('',*,*,#9103,.T.);
#12700=ORIENTED_EDGE('',*,*,#9108,.T.);
#12701=ORIENTED_EDGE('',*,*,#9109,.F.);
#12702=ORIENTED_EDGE('',*,*,#9110,.T.);
#12703=ORIENTED_EDGE('',*,*,#9106,.T.);
#12704=ORIENTED_EDGE('',*,*,#9111,.T.);
#12705=ORIENTED_EDGE('',*,*,#9112,.F.);
#12706=ORIENTED_EDGE('',*,*,#9113,.T.);
#12707=ORIENTED_EDGE('',*,*,#9109,.T.);
#12708=ORIENTED_EDGE('',*,*,#9114,.T.);
#12709=ORIENTED_EDGE('',*,*,#9115,.F.);
#12710=ORIENTED_EDGE('',*,*,#9116,.T.);
#12711=ORIENTED_EDGE('',*,*,#9112,.T.);
#12712=ORIENTED_EDGE('',*,*,#9117,.T.);
#12713=ORIENTED_EDGE('',*,*,#9118,.F.);
#12714=ORIENTED_EDGE('',*,*,#9119,.T.);
#12715=ORIENTED_EDGE('',*,*,#9115,.T.);
#12716=ORIENTED_EDGE('',*,*,#9120,.T.);
#12717=ORIENTED_EDGE('',*,*,#9121,.F.);
#12718=ORIENTED_EDGE('',*,*,#9122,.T.);
#12719=ORIENTED_EDGE('',*,*,#9118,.T.);
#12720=ORIENTED_EDGE('',*,*,#9123,.T.);
#12721=ORIENTED_EDGE('',*,*,#9124,.F.);
#12722=ORIENTED_EDGE('',*,*,#9125,.T.);
#12723=ORIENTED_EDGE('',*,*,#9121,.T.);
#12724=ORIENTED_EDGE('',*,*,#9126,.T.);
#12725=ORIENTED_EDGE('',*,*,#9127,.F.);
#12726=ORIENTED_EDGE('',*,*,#9128,.T.);
#12727=ORIENTED_EDGE('',*,*,#9124,.T.);
#12728=ORIENTED_EDGE('',*,*,#9129,.T.);
#12729=ORIENTED_EDGE('',*,*,#9130,.F.);
#12730=ORIENTED_EDGE('',*,*,#9131,.T.);
#12731=ORIENTED_EDGE('',*,*,#9127,.T.);
#12732=ORIENTED_EDGE('',*,*,#9132,.T.);
#12733=ORIENTED_EDGE('',*,*,#9133,.F.);
#12734=ORIENTED_EDGE('',*,*,#9134,.T.);
#12735=ORIENTED_EDGE('',*,*,#9130,.T.);
#12736=ORIENTED_EDGE('',*,*,#9135,.T.);
#12737=ORIENTED_EDGE('',*,*,#9136,.F.);
#12738=ORIENTED_EDGE('',*,*,#9137,.T.);
#12739=ORIENTED_EDGE('',*,*,#9133,.T.);
#12740=ORIENTED_EDGE('',*,*,#9138,.T.);
#12741=ORIENTED_EDGE('',*,*,#9139,.F.);
#12742=ORIENTED_EDGE('',*,*,#9140,.T.);
#12743=ORIENTED_EDGE('',*,*,#9136,.T.);
#12744=ORIENTED_EDGE('',*,*,#9141,.T.);
#12745=ORIENTED_EDGE('',*,*,#9142,.F.);
#12746=ORIENTED_EDGE('',*,*,#9143,.T.);
#12747=ORIENTED_EDGE('',*,*,#9139,.T.);
#12748=ORIENTED_EDGE('',*,*,#9144,.T.);
#12749=ORIENTED_EDGE('',*,*,#9145,.F.);
#12750=ORIENTED_EDGE('',*,*,#9146,.T.);
#12751=ORIENTED_EDGE('',*,*,#9142,.T.);
#12752=ORIENTED_EDGE('',*,*,#9147,.T.);
#12753=ORIENTED_EDGE('',*,*,#9148,.F.);
#12754=ORIENTED_EDGE('',*,*,#9149,.T.);
#12755=ORIENTED_EDGE('',*,*,#9145,.T.);
#12756=ORIENTED_EDGE('',*,*,#9150,.T.);
#12757=ORIENTED_EDGE('',*,*,#9151,.F.);
#12758=ORIENTED_EDGE('',*,*,#9152,.T.);
#12759=ORIENTED_EDGE('',*,*,#9148,.T.);
#12760=ORIENTED_EDGE('',*,*,#9153,.T.);
#12761=ORIENTED_EDGE('',*,*,#9154,.F.);
#12762=ORIENTED_EDGE('',*,*,#9155,.T.);
#12763=ORIENTED_EDGE('',*,*,#9151,.T.);
#12764=ORIENTED_EDGE('',*,*,#9156,.T.);
#12765=ORIENTED_EDGE('',*,*,#9157,.F.);
#12766=ORIENTED_EDGE('',*,*,#9158,.T.);
#12767=ORIENTED_EDGE('',*,*,#9154,.T.);
#12768=ORIENTED_EDGE('',*,*,#9159,.T.);
#12769=ORIENTED_EDGE('',*,*,#9160,.F.);
#12770=ORIENTED_EDGE('',*,*,#9161,.T.);
#12771=ORIENTED_EDGE('',*,*,#9157,.T.);
#12772=ORIENTED_EDGE('',*,*,#9162,.T.);
#12773=ORIENTED_EDGE('',*,*,#9163,.F.);
#12774=ORIENTED_EDGE('',*,*,#9164,.T.);
#12775=ORIENTED_EDGE('',*,*,#9160,.T.);
#12776=ORIENTED_EDGE('',*,*,#9165,.T.);
#12777=ORIENTED_EDGE('',*,*,#9166,.F.);
#12778=ORIENTED_EDGE('',*,*,#9167,.T.);
#12779=ORIENTED_EDGE('',*,*,#9163,.T.);
#12780=ORIENTED_EDGE('',*,*,#9168,.T.);
#12781=ORIENTED_EDGE('',*,*,#9169,.F.);
#12782=ORIENTED_EDGE('',*,*,#9170,.T.);
#12783=ORIENTED_EDGE('',*,*,#9166,.T.);
#12784=ORIENTED_EDGE('',*,*,#9171,.T.);
#12785=ORIENTED_EDGE('',*,*,#9172,.F.);
#12786=ORIENTED_EDGE('',*,*,#9173,.T.);
#12787=ORIENTED_EDGE('',*,*,#9169,.T.);
#12788=ORIENTED_EDGE('',*,*,#9174,.T.);
#12789=ORIENTED_EDGE('',*,*,#9175,.F.);
#12790=ORIENTED_EDGE('',*,*,#9176,.T.);
#12791=ORIENTED_EDGE('',*,*,#9172,.T.);
#12792=ORIENTED_EDGE('',*,*,#9177,.T.);
#12793=ORIENTED_EDGE('',*,*,#9178,.F.);
#12794=ORIENTED_EDGE('',*,*,#9179,.T.);
#12795=ORIENTED_EDGE('',*,*,#9175,.T.);
#12796=ORIENTED_EDGE('',*,*,#9180,.T.);
#12797=ORIENTED_EDGE('',*,*,#9181,.F.);
#12798=ORIENTED_EDGE('',*,*,#9182,.T.);
#12799=ORIENTED_EDGE('',*,*,#9178,.T.);
#12800=ORIENTED_EDGE('',*,*,#9183,.T.);
#12801=ORIENTED_EDGE('',*,*,#9184,.F.);
#12802=ORIENTED_EDGE('',*,*,#9185,.T.);
#12803=ORIENTED_EDGE('',*,*,#9186,.F.);
#12804=ORIENTED_EDGE('',*,*,#9187,.F.);
#12805=ORIENTED_EDGE('',*,*,#9188,.F.);
#12806=ORIENTED_EDGE('',*,*,#9189,.T.);
#12807=ORIENTED_EDGE('',*,*,#9184,.T.);
#12808=ORIENTED_EDGE('',*,*,#9190,.F.);
#12809=ORIENTED_EDGE('',*,*,#9191,.F.);
#12810=ORIENTED_EDGE('',*,*,#9192,.T.);
#12811=ORIENTED_EDGE('',*,*,#9188,.T.);
#12812=ORIENTED_EDGE('',*,*,#9193,.F.);
#12813=ORIENTED_EDGE('',*,*,#9194,.F.);
#12814=ORIENTED_EDGE('',*,*,#9195,.T.);
#12815=ORIENTED_EDGE('',*,*,#9191,.T.);
#12816=ORIENTED_EDGE('',*,*,#9196,.F.);
#12817=ORIENTED_EDGE('',*,*,#9197,.F.);
#12818=ORIENTED_EDGE('',*,*,#9198,.T.);
#12819=ORIENTED_EDGE('',*,*,#9194,.T.);
#12820=ORIENTED_EDGE('',*,*,#9199,.F.);
#12821=ORIENTED_EDGE('',*,*,#9200,.F.);
#12822=ORIENTED_EDGE('',*,*,#9201,.T.);
#12823=ORIENTED_EDGE('',*,*,#9197,.T.);
#12824=ORIENTED_EDGE('',*,*,#9202,.F.);
#12825=ORIENTED_EDGE('',*,*,#9203,.F.);
#12826=ORIENTED_EDGE('',*,*,#9204,.T.);
#12827=ORIENTED_EDGE('',*,*,#9200,.T.);
#12828=ORIENTED_EDGE('',*,*,#9205,.F.);
#12829=ORIENTED_EDGE('',*,*,#9206,.F.);
#12830=ORIENTED_EDGE('',*,*,#9207,.T.);
#12831=ORIENTED_EDGE('',*,*,#9203,.T.);
#12832=ORIENTED_EDGE('',*,*,#9208,.F.);
#12833=ORIENTED_EDGE('',*,*,#9209,.F.);
#12834=ORIENTED_EDGE('',*,*,#9210,.T.);
#12835=ORIENTED_EDGE('',*,*,#9206,.T.);
#12836=ORIENTED_EDGE('',*,*,#9211,.F.);
#12837=ORIENTED_EDGE('',*,*,#9212,.F.);
#12838=ORIENTED_EDGE('',*,*,#9213,.T.);
#12839=ORIENTED_EDGE('',*,*,#9209,.T.);
#12840=ORIENTED_EDGE('',*,*,#9214,.F.);
#12841=ORIENTED_EDGE('',*,*,#9215,.F.);
#12842=ORIENTED_EDGE('',*,*,#9216,.T.);
#12843=ORIENTED_EDGE('',*,*,#9212,.T.);
#12844=ORIENTED_EDGE('',*,*,#9217,.F.);
#12845=ORIENTED_EDGE('',*,*,#9218,.F.);
#12846=ORIENTED_EDGE('',*,*,#9219,.T.);
#12847=ORIENTED_EDGE('',*,*,#9215,.T.);
#12848=ORIENTED_EDGE('',*,*,#9220,.F.);
#12849=ORIENTED_EDGE('',*,*,#9221,.F.);
#12850=ORIENTED_EDGE('',*,*,#9222,.T.);
#12851=ORIENTED_EDGE('',*,*,#9218,.T.);
#12852=ORIENTED_EDGE('',*,*,#9223,.F.);
#12853=ORIENTED_EDGE('',*,*,#9224,.F.);
#12854=ORIENTED_EDGE('',*,*,#9225,.T.);
#12855=ORIENTED_EDGE('',*,*,#9221,.T.);
#12856=ORIENTED_EDGE('',*,*,#9226,.F.);
#12857=ORIENTED_EDGE('',*,*,#9227,.F.);
#12858=ORIENTED_EDGE('',*,*,#9228,.T.);
#12859=ORIENTED_EDGE('',*,*,#9224,.T.);
#12860=ORIENTED_EDGE('',*,*,#9229,.F.);
#12861=ORIENTED_EDGE('',*,*,#9230,.F.);
#12862=ORIENTED_EDGE('',*,*,#9231,.T.);
#12863=ORIENTED_EDGE('',*,*,#9227,.T.);
#12864=ORIENTED_EDGE('',*,*,#9232,.F.);
#12865=ORIENTED_EDGE('',*,*,#9233,.F.);
#12866=ORIENTED_EDGE('',*,*,#9234,.T.);
#12867=ORIENTED_EDGE('',*,*,#9230,.T.);
#12868=ORIENTED_EDGE('',*,*,#9235,.F.);
#12869=ORIENTED_EDGE('',*,*,#9236,.F.);
#12870=ORIENTED_EDGE('',*,*,#9237,.T.);
#12871=ORIENTED_EDGE('',*,*,#9233,.T.);
#12872=ORIENTED_EDGE('',*,*,#9238,.F.);
#12873=ORIENTED_EDGE('',*,*,#9239,.F.);
#12874=ORIENTED_EDGE('',*,*,#9240,.T.);
#12875=ORIENTED_EDGE('',*,*,#9236,.T.);
#12876=ORIENTED_EDGE('',*,*,#9241,.F.);
#12877=ORIENTED_EDGE('',*,*,#9242,.F.);
#12878=ORIENTED_EDGE('',*,*,#9243,.T.);
#12879=ORIENTED_EDGE('',*,*,#9239,.T.);
#12880=ORIENTED_EDGE('',*,*,#9244,.F.);
#12881=ORIENTED_EDGE('',*,*,#9245,.F.);
#12882=ORIENTED_EDGE('',*,*,#9246,.T.);
#12883=ORIENTED_EDGE('',*,*,#9242,.T.);
#12884=ORIENTED_EDGE('',*,*,#9247,.F.);
#12885=ORIENTED_EDGE('',*,*,#9248,.F.);
#12886=ORIENTED_EDGE('',*,*,#9249,.T.);
#12887=ORIENTED_EDGE('',*,*,#9245,.T.);
#12888=ORIENTED_EDGE('',*,*,#9250,.F.);
#12889=ORIENTED_EDGE('',*,*,#9251,.F.);
#12890=ORIENTED_EDGE('',*,*,#9252,.T.);
#12891=ORIENTED_EDGE('',*,*,#9248,.T.);
#12892=ORIENTED_EDGE('',*,*,#9253,.F.);
#12893=ORIENTED_EDGE('',*,*,#9254,.F.);
#12894=ORIENTED_EDGE('',*,*,#9255,.T.);
#12895=ORIENTED_EDGE('',*,*,#9251,.T.);
#12896=ORIENTED_EDGE('',*,*,#9256,.F.);
#12897=ORIENTED_EDGE('',*,*,#9257,.F.);
#12898=ORIENTED_EDGE('',*,*,#9258,.T.);
#12899=ORIENTED_EDGE('',*,*,#9254,.T.);
#12900=ORIENTED_EDGE('',*,*,#9259,.F.);
#12901=ORIENTED_EDGE('',*,*,#9260,.F.);
#12902=ORIENTED_EDGE('',*,*,#9261,.T.);
#12903=ORIENTED_EDGE('',*,*,#9257,.T.);
#12904=ORIENTED_EDGE('',*,*,#9262,.F.);
#12905=ORIENTED_EDGE('',*,*,#9263,.F.);
#12906=ORIENTED_EDGE('',*,*,#9264,.T.);
#12907=ORIENTED_EDGE('',*,*,#9260,.T.);
#12908=ORIENTED_EDGE('',*,*,#9265,.F.);
#12909=ORIENTED_EDGE('',*,*,#9266,.F.);
#12910=ORIENTED_EDGE('',*,*,#9267,.T.);
#12911=ORIENTED_EDGE('',*,*,#9263,.T.);
#12912=ORIENTED_EDGE('',*,*,#9268,.F.);
#12913=ORIENTED_EDGE('',*,*,#9269,.F.);
#12914=ORIENTED_EDGE('',*,*,#9270,.T.);
#12915=ORIENTED_EDGE('',*,*,#9266,.T.);
#12916=ORIENTED_EDGE('',*,*,#9271,.F.);
#12917=ORIENTED_EDGE('',*,*,#9272,.F.);
#12918=ORIENTED_EDGE('',*,*,#9273,.T.);
#12919=ORIENTED_EDGE('',*,*,#9269,.T.);
#12920=ORIENTED_EDGE('',*,*,#9274,.F.);
#12921=ORIENTED_EDGE('',*,*,#9275,.F.);
#12922=ORIENTED_EDGE('',*,*,#9276,.T.);
#12923=ORIENTED_EDGE('',*,*,#9272,.T.);
#12924=ORIENTED_EDGE('',*,*,#9277,.F.);
#12925=ORIENTED_EDGE('',*,*,#9278,.F.);
#12926=ORIENTED_EDGE('',*,*,#9279,.T.);
#12927=ORIENTED_EDGE('',*,*,#9275,.T.);
#12928=ORIENTED_EDGE('',*,*,#9280,.F.);
#12929=ORIENTED_EDGE('',*,*,#9281,.F.);
#12930=ORIENTED_EDGE('',*,*,#9282,.T.);
#12931=ORIENTED_EDGE('',*,*,#9278,.T.);
#12932=ORIENTED_EDGE('',*,*,#9283,.F.);
#12933=ORIENTED_EDGE('',*,*,#9284,.F.);
#12934=ORIENTED_EDGE('',*,*,#9285,.T.);
#12935=ORIENTED_EDGE('',*,*,#9281,.T.);
#12936=ORIENTED_EDGE('',*,*,#9286,.F.);
#12937=ORIENTED_EDGE('',*,*,#9287,.F.);
#12938=ORIENTED_EDGE('',*,*,#9288,.F.);
#12939=ORIENTED_EDGE('',*,*,#9183,.F.);
#12940=ORIENTED_EDGE('',*,*,#9180,.F.);
#12941=ORIENTED_EDGE('',*,*,#9177,.F.);
#12942=ORIENTED_EDGE('',*,*,#9174,.F.);
#12943=ORIENTED_EDGE('',*,*,#9171,.F.);
#12944=ORIENTED_EDGE('',*,*,#9168,.F.);
#12945=ORIENTED_EDGE('',*,*,#9165,.F.);
#12946=ORIENTED_EDGE('',*,*,#9162,.F.);
#12947=ORIENTED_EDGE('',*,*,#9159,.F.);
#12948=ORIENTED_EDGE('',*,*,#9156,.F.);
#12949=ORIENTED_EDGE('',*,*,#9153,.F.);
#12950=ORIENTED_EDGE('',*,*,#9150,.F.);
#12951=ORIENTED_EDGE('',*,*,#9147,.F.);
#12952=ORIENTED_EDGE('',*,*,#9144,.F.);
#12953=ORIENTED_EDGE('',*,*,#9141,.F.);
#12954=ORIENTED_EDGE('',*,*,#9138,.F.);
#12955=ORIENTED_EDGE('',*,*,#9135,.F.);
#12956=ORIENTED_EDGE('',*,*,#9132,.F.);
#12957=ORIENTED_EDGE('',*,*,#9129,.F.);
#12958=ORIENTED_EDGE('',*,*,#9126,.F.);
#12959=ORIENTED_EDGE('',*,*,#9123,.F.);
#12960=ORIENTED_EDGE('',*,*,#9120,.F.);
#12961=ORIENTED_EDGE('',*,*,#9117,.F.);
#12962=ORIENTED_EDGE('',*,*,#9114,.F.);
#12963=ORIENTED_EDGE('',*,*,#9111,.F.);
#12964=ORIENTED_EDGE('',*,*,#9108,.F.);
#12965=ORIENTED_EDGE('',*,*,#9105,.F.);
#12966=ORIENTED_EDGE('',*,*,#9102,.F.);
#12967=ORIENTED_EDGE('',*,*,#9099,.F.);
#12968=ORIENTED_EDGE('',*,*,#9096,.F.);
#12969=ORIENTED_EDGE('',*,*,#9093,.F.);
#12970=ORIENTED_EDGE('',*,*,#9090,.F.);
#12971=ORIENTED_EDGE('',*,*,#9087,.F.);
#12972=ORIENTED_EDGE('',*,*,#9084,.F.);
#12973=ORIENTED_EDGE('',*,*,#9289,.F.);
#12974=ORIENTED_EDGE('',*,*,#9290,.T.);
#12975=ORIENTED_EDGE('',*,*,#9286,.T.);
#12976=ORIENTED_EDGE('',*,*,#9283,.T.);
#12977=ORIENTED_EDGE('',*,*,#9280,.T.);
#12978=ORIENTED_EDGE('',*,*,#9277,.T.);
#12979=ORIENTED_EDGE('',*,*,#9274,.T.);
#12980=ORIENTED_EDGE('',*,*,#9271,.T.);
#12981=ORIENTED_EDGE('',*,*,#9268,.T.);
#12982=ORIENTED_EDGE('',*,*,#9265,.T.);
#12983=ORIENTED_EDGE('',*,*,#9262,.T.);
#12984=ORIENTED_EDGE('',*,*,#9259,.T.);
#12985=ORIENTED_EDGE('',*,*,#9256,.T.);
#12986=ORIENTED_EDGE('',*,*,#9253,.T.);
#12987=ORIENTED_EDGE('',*,*,#9250,.T.);
#12988=ORIENTED_EDGE('',*,*,#9247,.T.);
#12989=ORIENTED_EDGE('',*,*,#9244,.T.);
#12990=ORIENTED_EDGE('',*,*,#9241,.T.);
#12991=ORIENTED_EDGE('',*,*,#9238,.T.);
#12992=ORIENTED_EDGE('',*,*,#9235,.T.);
#12993=ORIENTED_EDGE('',*,*,#9232,.T.);
#12994=ORIENTED_EDGE('',*,*,#9229,.T.);
#12995=ORIENTED_EDGE('',*,*,#9226,.T.);
#12996=ORIENTED_EDGE('',*,*,#9223,.T.);
#12997=ORIENTED_EDGE('',*,*,#9220,.T.);
#12998=ORIENTED_EDGE('',*,*,#9217,.T.);
#12999=ORIENTED_EDGE('',*,*,#9214,.T.);
#13000=ORIENTED_EDGE('',*,*,#9211,.T.);
#13001=ORIENTED_EDGE('',*,*,#9208,.T.);
#13002=ORIENTED_EDGE('',*,*,#9205,.T.);
#13003=ORIENTED_EDGE('',*,*,#9202,.T.);
#13004=ORIENTED_EDGE('',*,*,#9199,.T.);
#13005=ORIENTED_EDGE('',*,*,#9196,.T.);
#13006=ORIENTED_EDGE('',*,*,#9193,.T.);
#13007=ORIENTED_EDGE('',*,*,#9190,.T.);
#13008=ORIENTED_EDGE('',*,*,#9187,.T.);
#13009=ORIENTED_EDGE('',*,*,#9291,.T.);
#13010=ORIENTED_EDGE('',*,*,#9292,.T.);
#13011=ORIENTED_EDGE('',*,*,#9293,.T.);
#13012=ORIENTED_EDGE('',*,*,#9294,.T.);
#13013=ORIENTED_EDGE('',*,*,#9289,.T.);
#13014=ORIENTED_EDGE('',*,*,#9284,.T.);
#13015=ORIENTED_EDGE('',*,*,#9290,.F.);
#13016=ORIENTED_EDGE('',*,*,#9294,.F.);
#13017=ORIENTED_EDGE('',*,*,#9295,.T.);
#13018=ORIENTED_EDGE('',*,*,#9296,.F.);
#13019=ORIENTED_EDGE('',*,*,#9185,.F.);
#13020=ORIENTED_EDGE('',*,*,#9189,.F.);
#13021=ORIENTED_EDGE('',*,*,#9192,.F.);
#13022=ORIENTED_EDGE('',*,*,#9195,.F.);
#13023=ORIENTED_EDGE('',*,*,#9198,.F.);
#13024=ORIENTED_EDGE('',*,*,#9201,.F.);
#13025=ORIENTED_EDGE('',*,*,#9204,.F.);
#13026=ORIENTED_EDGE('',*,*,#9207,.F.);
#13027=ORIENTED_EDGE('',*,*,#9210,.F.);
#13028=ORIENTED_EDGE('',*,*,#9213,.F.);
#13029=ORIENTED_EDGE('',*,*,#9216,.F.);
#13030=ORIENTED_EDGE('',*,*,#9219,.F.);
#13031=ORIENTED_EDGE('',*,*,#9222,.F.);
#13032=ORIENTED_EDGE('',*,*,#9225,.F.);
#13033=ORIENTED_EDGE('',*,*,#9228,.F.);
#13034=ORIENTED_EDGE('',*,*,#9231,.F.);
#13035=ORIENTED_EDGE('',*,*,#9234,.F.);
#13036=ORIENTED_EDGE('',*,*,#9237,.F.);
#13037=ORIENTED_EDGE('',*,*,#9240,.F.);
#13038=ORIENTED_EDGE('',*,*,#9243,.F.);
#13039=ORIENTED_EDGE('',*,*,#9246,.F.);
#13040=ORIENTED_EDGE('',*,*,#9249,.F.);
#13041=ORIENTED_EDGE('',*,*,#9252,.F.);
#13042=ORIENTED_EDGE('',*,*,#9255,.F.);
#13043=ORIENTED_EDGE('',*,*,#9258,.F.);
#13044=ORIENTED_EDGE('',*,*,#9261,.F.);
#13045=ORIENTED_EDGE('',*,*,#9264,.F.);
#13046=ORIENTED_EDGE('',*,*,#9267,.F.);
#13047=ORIENTED_EDGE('',*,*,#9270,.F.);
#13048=ORIENTED_EDGE('',*,*,#9273,.F.);
#13049=ORIENTED_EDGE('',*,*,#9276,.F.);
#13050=ORIENTED_EDGE('',*,*,#9279,.F.);
#13051=ORIENTED_EDGE('',*,*,#9282,.F.);
#13052=ORIENTED_EDGE('',*,*,#9285,.F.);
#13053=ORIENTED_EDGE('',*,*,#9295,.F.);
#13054=ORIENTED_EDGE('',*,*,#9293,.F.);
#13055=ORIENTED_EDGE('',*,*,#9082,.F.);
#13056=ORIENTED_EDGE('',*,*,#9086,.F.);
#13057=ORIENTED_EDGE('',*,*,#9089,.F.);
#13058=ORIENTED_EDGE('',*,*,#9092,.F.);
#13059=ORIENTED_EDGE('',*,*,#9095,.F.);
#13060=ORIENTED_EDGE('',*,*,#9098,.F.);
#13061=ORIENTED_EDGE('',*,*,#9101,.F.);
#13062=ORIENTED_EDGE('',*,*,#9104,.F.);
#13063=ORIENTED_EDGE('',*,*,#9107,.F.);
#13064=ORIENTED_EDGE('',*,*,#9110,.F.);
#13065=ORIENTED_EDGE('',*,*,#9113,.F.);
#13066=ORIENTED_EDGE('',*,*,#9116,.F.);
#13067=ORIENTED_EDGE('',*,*,#9119,.F.);
#13068=ORIENTED_EDGE('',*,*,#9122,.F.);
#13069=ORIENTED_EDGE('',*,*,#9125,.F.);
#13070=ORIENTED_EDGE('',*,*,#9128,.F.);
#13071=ORIENTED_EDGE('',*,*,#9131,.F.);
#13072=ORIENTED_EDGE('',*,*,#9134,.F.);
#13073=ORIENTED_EDGE('',*,*,#9137,.F.);
#13074=ORIENTED_EDGE('',*,*,#9140,.F.);
#13075=ORIENTED_EDGE('',*,*,#9143,.F.);
#13076=ORIENTED_EDGE('',*,*,#9146,.F.);
#13077=ORIENTED_EDGE('',*,*,#9149,.F.);
#13078=ORIENTED_EDGE('',*,*,#9152,.F.);
#13079=ORIENTED_EDGE('',*,*,#9155,.F.);
#13080=ORIENTED_EDGE('',*,*,#9158,.F.);
#13081=ORIENTED_EDGE('',*,*,#9161,.F.);
#13082=ORIENTED_EDGE('',*,*,#9164,.F.);
#13083=ORIENTED_EDGE('',*,*,#9167,.F.);
#13084=ORIENTED_EDGE('',*,*,#9170,.F.);
#13085=ORIENTED_EDGE('',*,*,#9173,.F.);
#13086=ORIENTED_EDGE('',*,*,#9176,.F.);
#13087=ORIENTED_EDGE('',*,*,#9179,.F.);
#13088=ORIENTED_EDGE('',*,*,#9182,.F.);
#13089=ORIENTED_EDGE('',*,*,#9297,.F.);
#13090=ORIENTED_EDGE('',*,*,#9298,.F.);
#13091=ORIENTED_EDGE('',*,*,#9299,.T.);
#13092=ORIENTED_EDGE('',*,*,#9300,.F.);
#13093=ORIENTED_EDGE('',*,*,#9301,.F.);
#13094=ORIENTED_EDGE('',*,*,#9302,.F.);
#13095=ORIENTED_EDGE('',*,*,#9301,.T.);
#13096=ORIENTED_EDGE('',*,*,#9303,.T.);
#13097=ORIENTED_EDGE('',*,*,#9304,.F.);
#13098=ORIENTED_EDGE('',*,*,#9303,.F.);
#13099=ORIENTED_EDGE('',*,*,#9300,.T.);
#13100=ORIENTED_EDGE('',*,*,#9305,.T.);
#13101=ORIENTED_EDGE('',*,*,#9306,.F.);
#13102=ORIENTED_EDGE('',*,*,#9305,.F.);
#13103=ORIENTED_EDGE('',*,*,#9299,.F.);
#13104=ORIENTED_EDGE('',*,*,#9307,.F.);
#13105=ORIENTED_EDGE('',*,*,#9308,.T.);
#13106=ORIENTED_EDGE('',*,*,#9309,.F.);
#13107=ORIENTED_EDGE('',*,*,#9310,.F.);
#13108=ORIENTED_EDGE('',*,*,#9311,.F.);
#13109=ORIENTED_EDGE('',*,*,#9310,.T.);
#13110=ORIENTED_EDGE('',*,*,#9312,.T.);
#13111=ORIENTED_EDGE('',*,*,#9313,.F.);
#13112=ORIENTED_EDGE('',*,*,#9312,.F.);
#13113=ORIENTED_EDGE('',*,*,#9309,.T.);
#13114=ORIENTED_EDGE('',*,*,#9314,.T.);
#13115=ORIENTED_EDGE('',*,*,#9315,.F.);
#13116=ORIENTED_EDGE('',*,*,#9314,.F.);
#13117=ORIENTED_EDGE('',*,*,#9308,.F.);
#13118=ORIENTED_EDGE('',*,*,#9316,.F.);
#13119=ORIENTED_EDGE('',*,*,#9317,.T.);
#13120=ORIENTED_EDGE('',*,*,#9318,.F.);
#13121=ORIENTED_EDGE('',*,*,#9319,.F.);
#13122=ORIENTED_EDGE('',*,*,#9320,.F.);
#13123=ORIENTED_EDGE('',*,*,#9319,.T.);
#13124=ORIENTED_EDGE('',*,*,#9321,.T.);
#13125=ORIENTED_EDGE('',*,*,#9322,.F.);
#13126=ORIENTED_EDGE('',*,*,#9321,.F.);
#13127=ORIENTED_EDGE('',*,*,#9318,.T.);
#13128=ORIENTED_EDGE('',*,*,#9323,.T.);
#13129=ORIENTED_EDGE('',*,*,#9324,.F.);
#13130=ORIENTED_EDGE('',*,*,#9323,.F.);
#13131=ORIENTED_EDGE('',*,*,#9317,.F.);
#13132=ORIENTED_EDGE('',*,*,#9325,.F.);
#13133=ORIENTED_EDGE('',*,*,#9326,.T.);
#13134=ORIENTED_EDGE('',*,*,#9327,.F.);
#13135=ORIENTED_EDGE('',*,*,#9328,.F.);
#13136=ORIENTED_EDGE('',*,*,#9329,.F.);
#13137=ORIENTED_EDGE('',*,*,#9328,.T.);
#13138=ORIENTED_EDGE('',*,*,#9330,.T.);
#13139=ORIENTED_EDGE('',*,*,#9331,.F.);
#13140=ORIENTED_EDGE('',*,*,#9330,.F.);
#13141=ORIENTED_EDGE('',*,*,#9327,.T.);
#13142=ORIENTED_EDGE('',*,*,#9332,.T.);
#13143=ORIENTED_EDGE('',*,*,#9333,.F.);
#13144=ORIENTED_EDGE('',*,*,#9332,.F.);
#13145=ORIENTED_EDGE('',*,*,#9326,.F.);
#13146=ORIENTED_EDGE('',*,*,#9334,.F.);
#13147=ORIENTED_EDGE('',*,*,#9335,.T.);
#13148=ORIENTED_EDGE('',*,*,#9336,.F.);
#13149=ORIENTED_EDGE('',*,*,#9337,.F.);
#13150=ORIENTED_EDGE('',*,*,#9338,.F.);
#13151=ORIENTED_EDGE('',*,*,#9337,.T.);
#13152=ORIENTED_EDGE('',*,*,#9339,.T.);
#13153=ORIENTED_EDGE('',*,*,#9340,.F.);
#13154=ORIENTED_EDGE('',*,*,#9339,.F.);
#13155=ORIENTED_EDGE('',*,*,#9336,.T.);
#13156=ORIENTED_EDGE('',*,*,#9341,.T.);
#13157=ORIENTED_EDGE('',*,*,#9342,.F.);
#13158=ORIENTED_EDGE('',*,*,#9341,.F.);
#13159=ORIENTED_EDGE('',*,*,#9335,.F.);
#13160=ORIENTED_EDGE('',*,*,#9343,.F.);
#13161=ORIENTED_EDGE('',*,*,#9344,.T.);
#13162=ORIENTED_EDGE('',*,*,#9345,.F.);
#13163=ORIENTED_EDGE('',*,*,#9346,.F.);
#13164=ORIENTED_EDGE('',*,*,#9347,.F.);
#13165=ORIENTED_EDGE('',*,*,#9346,.T.);
#13166=ORIENTED_EDGE('',*,*,#9348,.T.);
#13167=ORIENTED_EDGE('',*,*,#9349,.F.);
#13168=ORIENTED_EDGE('',*,*,#9348,.F.);
#13169=ORIENTED_EDGE('',*,*,#9345,.T.);
#13170=ORIENTED_EDGE('',*,*,#9350,.T.);
#13171=ORIENTED_EDGE('',*,*,#9351,.F.);
#13172=ORIENTED_EDGE('',*,*,#9350,.F.);
#13173=ORIENTED_EDGE('',*,*,#9344,.F.);
#13174=ORIENTED_EDGE('',*,*,#9352,.F.);
#13175=ORIENTED_EDGE('',*,*,#9353,.T.);
#13176=ORIENTED_EDGE('',*,*,#9354,.F.);
#13177=ORIENTED_EDGE('',*,*,#9355,.F.);
#13178=ORIENTED_EDGE('',*,*,#9356,.F.);
#13179=ORIENTED_EDGE('',*,*,#9355,.T.);
#13180=ORIENTED_EDGE('',*,*,#9357,.T.);
#13181=ORIENTED_EDGE('',*,*,#9358,.F.);
#13182=ORIENTED_EDGE('',*,*,#9357,.F.);
#13183=ORIENTED_EDGE('',*,*,#9354,.T.);
#13184=ORIENTED_EDGE('',*,*,#9359,.T.);
#13185=ORIENTED_EDGE('',*,*,#9360,.F.);
#13186=ORIENTED_EDGE('',*,*,#9359,.F.);
#13187=ORIENTED_EDGE('',*,*,#9353,.F.);
#13188=ORIENTED_EDGE('',*,*,#9361,.F.);
#13189=ORIENTED_EDGE('',*,*,#9362,.T.);
#13190=ORIENTED_EDGE('',*,*,#9363,.F.);
#13191=ORIENTED_EDGE('',*,*,#9364,.F.);
#13192=ORIENTED_EDGE('',*,*,#9365,.F.);
#13193=ORIENTED_EDGE('',*,*,#9364,.T.);
#13194=ORIENTED_EDGE('',*,*,#9366,.T.);
#13195=ORIENTED_EDGE('',*,*,#9367,.F.);
#13196=ORIENTED_EDGE('',*,*,#9366,.F.);
#13197=ORIENTED_EDGE('',*,*,#9363,.T.);
#13198=ORIENTED_EDGE('',*,*,#9368,.T.);
#13199=ORIENTED_EDGE('',*,*,#9369,.F.);
#13200=ORIENTED_EDGE('',*,*,#9368,.F.);
#13201=ORIENTED_EDGE('',*,*,#9362,.F.);
#13202=ORIENTED_EDGE('',*,*,#9370,.F.);
#13203=ORIENTED_EDGE('',*,*,#9371,.T.);
#13204=ORIENTED_EDGE('',*,*,#9372,.F.);
#13205=ORIENTED_EDGE('',*,*,#9373,.F.);
#13206=ORIENTED_EDGE('',*,*,#9374,.F.);
#13207=ORIENTED_EDGE('',*,*,#9373,.T.);
#13208=ORIENTED_EDGE('',*,*,#9375,.T.);
#13209=ORIENTED_EDGE('',*,*,#9376,.F.);
#13210=ORIENTED_EDGE('',*,*,#9375,.F.);
#13211=ORIENTED_EDGE('',*,*,#9372,.T.);
#13212=ORIENTED_EDGE('',*,*,#9377,.T.);
#13213=ORIENTED_EDGE('',*,*,#9378,.F.);
#13214=ORIENTED_EDGE('',*,*,#9377,.F.);
#13215=ORIENTED_EDGE('',*,*,#9371,.F.);
#13216=ORIENTED_EDGE('',*,*,#9379,.F.);
#13217=ORIENTED_EDGE('',*,*,#9380,.T.);
#13218=ORIENTED_EDGE('',*,*,#9381,.F.);
#13219=ORIENTED_EDGE('',*,*,#9382,.F.);
#13220=ORIENTED_EDGE('',*,*,#9383,.F.);
#13221=ORIENTED_EDGE('',*,*,#9382,.T.);
#13222=ORIENTED_EDGE('',*,*,#9384,.T.);
#13223=ORIENTED_EDGE('',*,*,#9385,.F.);
#13224=ORIENTED_EDGE('',*,*,#9384,.F.);
#13225=ORIENTED_EDGE('',*,*,#9381,.T.);
#13226=ORIENTED_EDGE('',*,*,#9386,.T.);
#13227=ORIENTED_EDGE('',*,*,#9387,.F.);
#13228=ORIENTED_EDGE('',*,*,#9386,.F.);
#13229=ORIENTED_EDGE('',*,*,#9380,.F.);
#13230=ORIENTED_EDGE('',*,*,#9388,.F.);
#13231=ORIENTED_EDGE('',*,*,#9389,.T.);
#13232=ORIENTED_EDGE('',*,*,#9390,.F.);
#13233=ORIENTED_EDGE('',*,*,#9391,.F.);
#13234=ORIENTED_EDGE('',*,*,#9392,.F.);
#13235=ORIENTED_EDGE('',*,*,#9391,.T.);
#13236=ORIENTED_EDGE('',*,*,#9393,.T.);
#13237=ORIENTED_EDGE('',*,*,#9394,.F.);
#13238=ORIENTED_EDGE('',*,*,#9393,.F.);
#13239=ORIENTED_EDGE('',*,*,#9390,.T.);
#13240=ORIENTED_EDGE('',*,*,#9395,.T.);
#13241=ORIENTED_EDGE('',*,*,#9396,.F.);
#13242=ORIENTED_EDGE('',*,*,#9395,.F.);
#13243=ORIENTED_EDGE('',*,*,#9389,.F.);
#13244=ORIENTED_EDGE('',*,*,#9397,.F.);
#13245=ORIENTED_EDGE('',*,*,#9398,.T.);
#13246=ORIENTED_EDGE('',*,*,#9399,.F.);
#13247=ORIENTED_EDGE('',*,*,#9400,.F.);
#13248=ORIENTED_EDGE('',*,*,#9401,.F.);
#13249=ORIENTED_EDGE('',*,*,#9400,.T.);
#13250=ORIENTED_EDGE('',*,*,#9402,.T.);
#13251=ORIENTED_EDGE('',*,*,#9403,.F.);
#13252=ORIENTED_EDGE('',*,*,#9402,.F.);
#13253=ORIENTED_EDGE('',*,*,#9399,.T.);
#13254=ORIENTED_EDGE('',*,*,#9404,.T.);
#13255=ORIENTED_EDGE('',*,*,#9405,.F.);
#13256=ORIENTED_EDGE('',*,*,#9404,.F.);
#13257=ORIENTED_EDGE('',*,*,#9398,.F.);
#13258=ORIENTED_EDGE('',*,*,#9406,.F.);
#13259=ORIENTED_EDGE('',*,*,#9407,.T.);
#13260=ORIENTED_EDGE('',*,*,#9408,.F.);
#13261=ORIENTED_EDGE('',*,*,#9409,.F.);
#13262=ORIENTED_EDGE('',*,*,#9410,.F.);
#13263=ORIENTED_EDGE('',*,*,#9409,.T.);
#13264=ORIENTED_EDGE('',*,*,#9411,.T.);
#13265=ORIENTED_EDGE('',*,*,#9412,.F.);
#13266=ORIENTED_EDGE('',*,*,#9411,.F.);
#13267=ORIENTED_EDGE('',*,*,#9408,.T.);
#13268=ORIENTED_EDGE('',*,*,#9413,.T.);
#13269=ORIENTED_EDGE('',*,*,#9414,.F.);
#13270=ORIENTED_EDGE('',*,*,#9413,.F.);
#13271=ORIENTED_EDGE('',*,*,#9407,.F.);
#13272=ORIENTED_EDGE('',*,*,#9415,.F.);
#13273=ORIENTED_EDGE('',*,*,#9416,.T.);
#13274=ORIENTED_EDGE('',*,*,#9417,.F.);
#13275=ORIENTED_EDGE('',*,*,#9418,.F.);
#13276=ORIENTED_EDGE('',*,*,#9419,.F.);
#13277=ORIENTED_EDGE('',*,*,#9418,.T.);
#13278=ORIENTED_EDGE('',*,*,#9420,.T.);
#13279=ORIENTED_EDGE('',*,*,#9421,.F.);
#13280=ORIENTED_EDGE('',*,*,#9420,.F.);
#13281=ORIENTED_EDGE('',*,*,#9417,.T.);
#13282=ORIENTED_EDGE('',*,*,#9422,.T.);
#13283=ORIENTED_EDGE('',*,*,#9423,.F.);
#13284=ORIENTED_EDGE('',*,*,#9422,.F.);
#13285=ORIENTED_EDGE('',*,*,#9416,.F.);
#13286=ORIENTED_EDGE('',*,*,#9424,.F.);
#13287=ORIENTED_EDGE('',*,*,#9425,.T.);
#13288=ORIENTED_EDGE('',*,*,#9426,.F.);
#13289=ORIENTED_EDGE('',*,*,#9427,.F.);
#13290=ORIENTED_EDGE('',*,*,#9428,.F.);
#13291=ORIENTED_EDGE('',*,*,#9427,.T.);
#13292=ORIENTED_EDGE('',*,*,#9429,.T.);
#13293=ORIENTED_EDGE('',*,*,#9430,.F.);
#13294=ORIENTED_EDGE('',*,*,#9429,.F.);
#13295=ORIENTED_EDGE('',*,*,#9426,.T.);
#13296=ORIENTED_EDGE('',*,*,#9431,.T.);
#13297=ORIENTED_EDGE('',*,*,#9432,.F.);
#13298=ORIENTED_EDGE('',*,*,#9431,.F.);
#13299=ORIENTED_EDGE('',*,*,#9425,.F.);
#13300=ORIENTED_EDGE('',*,*,#9433,.F.);
#13301=ORIENTED_EDGE('',*,*,#9434,.T.);
#13302=ORIENTED_EDGE('',*,*,#9435,.F.);
#13303=ORIENTED_EDGE('',*,*,#9436,.F.);
#13304=ORIENTED_EDGE('',*,*,#9437,.F.);
#13305=ORIENTED_EDGE('',*,*,#9436,.T.);
#13306=ORIENTED_EDGE('',*,*,#9438,.T.);
#13307=ORIENTED_EDGE('',*,*,#9439,.F.);
#13308=ORIENTED_EDGE('',*,*,#9438,.F.);
#13309=ORIENTED_EDGE('',*,*,#9435,.T.);
#13310=ORIENTED_EDGE('',*,*,#9440,.T.);
#13311=ORIENTED_EDGE('',*,*,#9441,.F.);
#13312=ORIENTED_EDGE('',*,*,#9440,.F.);
#13313=ORIENTED_EDGE('',*,*,#9434,.F.);
#13314=ORIENTED_EDGE('',*,*,#9442,.F.);
#13315=ORIENTED_EDGE('',*,*,#9443,.T.);
#13316=ORIENTED_EDGE('',*,*,#9444,.F.);
#13317=ORIENTED_EDGE('',*,*,#9445,.F.);
#13318=ORIENTED_EDGE('',*,*,#9446,.F.);
#13319=ORIENTED_EDGE('',*,*,#9445,.T.);
#13320=ORIENTED_EDGE('',*,*,#9447,.T.);
#13321=ORIENTED_EDGE('',*,*,#9448,.F.);
#13322=ORIENTED_EDGE('',*,*,#9447,.F.);
#13323=ORIENTED_EDGE('',*,*,#9444,.T.);
#13324=ORIENTED_EDGE('',*,*,#9449,.T.);
#13325=ORIENTED_EDGE('',*,*,#9450,.F.);
#13326=ORIENTED_EDGE('',*,*,#9449,.F.);
#13327=ORIENTED_EDGE('',*,*,#9443,.F.);
#13328=ORIENTED_EDGE('',*,*,#9451,.F.);
#13329=ORIENTED_EDGE('',*,*,#9452,.T.);
#13330=ORIENTED_EDGE('',*,*,#9453,.F.);
#13331=ORIENTED_EDGE('',*,*,#9454,.F.);
#13332=ORIENTED_EDGE('',*,*,#9455,.F.);
#13333=ORIENTED_EDGE('',*,*,#9454,.T.);
#13334=ORIENTED_EDGE('',*,*,#9456,.T.);
#13335=ORIENTED_EDGE('',*,*,#9457,.F.);
#13336=ORIENTED_EDGE('',*,*,#9458,.F.);
#13337=ORIENTED_EDGE('',*,*,#9456,.F.);
#13338=ORIENTED_EDGE('',*,*,#9453,.T.);
#13339=ORIENTED_EDGE('',*,*,#9459,.T.);
#13340=ORIENTED_EDGE('',*,*,#9460,.F.);
#13341=ORIENTED_EDGE('',*,*,#9459,.F.);
#13342=ORIENTED_EDGE('',*,*,#9452,.F.);
#13343=ORIENTED_EDGE('',*,*,#9461,.F.);
#13344=ORIENTED_EDGE('',*,*,#9462,.F.);
#13345=ORIENTED_EDGE('',*,*,#9463,.T.);
#13346=ORIENTED_EDGE('',*,*,#9464,.F.);
#13347=ORIENTED_EDGE('',*,*,#9465,.F.);
#13348=ORIENTED_EDGE('',*,*,#9466,.F.);
#13349=ORIENTED_EDGE('',*,*,#9465,.T.);
#13350=ORIENTED_EDGE('',*,*,#9467,.T.);
#13351=ORIENTED_EDGE('',*,*,#9468,.F.);
#13352=ORIENTED_EDGE('',*,*,#9467,.F.);
#13353=ORIENTED_EDGE('',*,*,#9464,.T.);
#13354=ORIENTED_EDGE('',*,*,#9469,.T.);
#13355=ORIENTED_EDGE('',*,*,#9470,.F.);
#13356=ORIENTED_EDGE('',*,*,#9469,.F.);
#13357=ORIENTED_EDGE('',*,*,#9463,.F.);
#13358=ORIENTED_EDGE('',*,*,#9471,.F.);
#13359=ORIENTED_EDGE('',*,*,#9472,.T.);
#13360=ORIENTED_EDGE('',*,*,#9473,.F.);
#13361=ORIENTED_EDGE('',*,*,#9474,.F.);
#13362=ORIENTED_EDGE('',*,*,#9475,.F.);
#13363=ORIENTED_EDGE('',*,*,#9474,.T.);
#13364=ORIENTED_EDGE('',*,*,#9476,.T.);
#13365=ORIENTED_EDGE('',*,*,#9477,.F.);
#13366=ORIENTED_EDGE('',*,*,#9476,.F.);
#13367=ORIENTED_EDGE('',*,*,#9473,.T.);
#13368=ORIENTED_EDGE('',*,*,#9478,.T.);
#13369=ORIENTED_EDGE('',*,*,#9479,.F.);
#13370=ORIENTED_EDGE('',*,*,#9478,.F.);
#13371=ORIENTED_EDGE('',*,*,#9472,.F.);
#13372=ORIENTED_EDGE('',*,*,#9480,.F.);
#13373=ORIENTED_EDGE('',*,*,#9481,.T.);
#13374=ORIENTED_EDGE('',*,*,#9482,.F.);
#13375=ORIENTED_EDGE('',*,*,#9483,.F.);
#13376=ORIENTED_EDGE('',*,*,#9484,.F.);
#13377=ORIENTED_EDGE('',*,*,#9483,.T.);
#13378=ORIENTED_EDGE('',*,*,#9485,.T.);
#13379=ORIENTED_EDGE('',*,*,#9486,.F.);
#13380=ORIENTED_EDGE('',*,*,#9485,.F.);
#13381=ORIENTED_EDGE('',*,*,#9482,.T.);
#13382=ORIENTED_EDGE('',*,*,#9487,.T.);
#13383=ORIENTED_EDGE('',*,*,#9488,.F.);
#13384=ORIENTED_EDGE('',*,*,#9487,.F.);
#13385=ORIENTED_EDGE('',*,*,#9481,.F.);
#13386=ORIENTED_EDGE('',*,*,#9489,.F.);
#13387=ORIENTED_EDGE('',*,*,#9490,.T.);
#13388=ORIENTED_EDGE('',*,*,#9491,.F.);
#13389=ORIENTED_EDGE('',*,*,#9492,.F.);
#13390=ORIENTED_EDGE('',*,*,#9493,.F.);
#13391=ORIENTED_EDGE('',*,*,#9492,.T.);
#13392=ORIENTED_EDGE('',*,*,#9494,.T.);
#13393=ORIENTED_EDGE('',*,*,#9495,.F.);
#13394=ORIENTED_EDGE('',*,*,#9494,.F.);
#13395=ORIENTED_EDGE('',*,*,#9491,.T.);
#13396=ORIENTED_EDGE('',*,*,#9496,.T.);
#13397=ORIENTED_EDGE('',*,*,#9497,.F.);
#13398=ORIENTED_EDGE('',*,*,#9496,.F.);
#13399=ORIENTED_EDGE('',*,*,#9490,.F.);
#13400=ORIENTED_EDGE('',*,*,#9498,.F.);
#13401=ORIENTED_EDGE('',*,*,#9499,.T.);
#13402=ORIENTED_EDGE('',*,*,#9500,.F.);
#13403=ORIENTED_EDGE('',*,*,#9501,.F.);
#13404=ORIENTED_EDGE('',*,*,#9502,.F.);
#13405=ORIENTED_EDGE('',*,*,#9501,.T.);
#13406=ORIENTED_EDGE('',*,*,#9503,.T.);
#13407=ORIENTED_EDGE('',*,*,#9504,.F.);
#13408=ORIENTED_EDGE('',*,*,#9503,.F.);
#13409=ORIENTED_EDGE('',*,*,#9500,.T.);
#13410=ORIENTED_EDGE('',*,*,#9505,.T.);
#13411=ORIENTED_EDGE('',*,*,#9506,.F.);
#13412=ORIENTED_EDGE('',*,*,#9505,.F.);
#13413=ORIENTED_EDGE('',*,*,#9499,.F.);
#13414=ORIENTED_EDGE('',*,*,#9507,.F.);
#13415=ORIENTED_EDGE('',*,*,#9508,.T.);
#13416=ORIENTED_EDGE('',*,*,#9509,.F.);
#13417=ORIENTED_EDGE('',*,*,#9510,.F.);
#13418=ORIENTED_EDGE('',*,*,#9511,.F.);
#13419=ORIENTED_EDGE('',*,*,#9510,.T.);
#13420=ORIENTED_EDGE('',*,*,#9512,.T.);
#13421=ORIENTED_EDGE('',*,*,#9513,.F.);
#13422=ORIENTED_EDGE('',*,*,#9512,.F.);
#13423=ORIENTED_EDGE('',*,*,#9509,.T.);
#13424=ORIENTED_EDGE('',*,*,#9514,.T.);
#13425=ORIENTED_EDGE('',*,*,#9515,.F.);
#13426=ORIENTED_EDGE('',*,*,#9514,.F.);
#13427=ORIENTED_EDGE('',*,*,#9508,.F.);
#13428=ORIENTED_EDGE('',*,*,#9516,.F.);
#13429=ORIENTED_EDGE('',*,*,#9517,.T.);
#13430=ORIENTED_EDGE('',*,*,#9518,.F.);
#13431=ORIENTED_EDGE('',*,*,#9519,.F.);
#13432=ORIENTED_EDGE('',*,*,#9520,.F.);
#13433=ORIENTED_EDGE('',*,*,#9519,.T.);
#13434=ORIENTED_EDGE('',*,*,#9521,.T.);
#13435=ORIENTED_EDGE('',*,*,#9522,.F.);
#13436=ORIENTED_EDGE('',*,*,#9521,.F.);
#13437=ORIENTED_EDGE('',*,*,#9518,.T.);
#13438=ORIENTED_EDGE('',*,*,#9523,.T.);
#13439=ORIENTED_EDGE('',*,*,#9524,.F.);
#13440=ORIENTED_EDGE('',*,*,#9523,.F.);
#13441=ORIENTED_EDGE('',*,*,#9517,.F.);
#13442=ORIENTED_EDGE('',*,*,#9525,.F.);
#13443=ORIENTED_EDGE('',*,*,#9526,.T.);
#13444=ORIENTED_EDGE('',*,*,#9527,.F.);
#13445=ORIENTED_EDGE('',*,*,#9528,.F.);
#13446=ORIENTED_EDGE('',*,*,#9529,.F.);
#13447=ORIENTED_EDGE('',*,*,#9528,.T.);
#13448=ORIENTED_EDGE('',*,*,#9530,.T.);
#13449=ORIENTED_EDGE('',*,*,#9531,.F.);
#13450=ORIENTED_EDGE('',*,*,#9530,.F.);
#13451=ORIENTED_EDGE('',*,*,#9527,.T.);
#13452=ORIENTED_EDGE('',*,*,#9532,.T.);
#13453=ORIENTED_EDGE('',*,*,#9533,.F.);
#13454=ORIENTED_EDGE('',*,*,#9532,.F.);
#13455=ORIENTED_EDGE('',*,*,#9526,.F.);
#13456=ORIENTED_EDGE('',*,*,#9534,.F.);
#13457=ORIENTED_EDGE('',*,*,#9535,.T.);
#13458=ORIENTED_EDGE('',*,*,#9536,.F.);
#13459=ORIENTED_EDGE('',*,*,#9537,.F.);
#13460=ORIENTED_EDGE('',*,*,#9538,.F.);
#13461=ORIENTED_EDGE('',*,*,#9537,.T.);
#13462=ORIENTED_EDGE('',*,*,#9539,.T.);
#13463=ORIENTED_EDGE('',*,*,#9540,.F.);
#13464=ORIENTED_EDGE('',*,*,#9539,.F.);
#13465=ORIENTED_EDGE('',*,*,#9536,.T.);
#13466=ORIENTED_EDGE('',*,*,#9541,.T.);
#13467=ORIENTED_EDGE('',*,*,#9542,.F.);
#13468=ORIENTED_EDGE('',*,*,#9541,.F.);
#13469=ORIENTED_EDGE('',*,*,#9535,.F.);
#13470=ORIENTED_EDGE('',*,*,#9543,.F.);
#13471=ORIENTED_EDGE('',*,*,#9544,.T.);
#13472=ORIENTED_EDGE('',*,*,#9545,.F.);
#13473=ORIENTED_EDGE('',*,*,#9546,.F.);
#13474=ORIENTED_EDGE('',*,*,#9547,.F.);
#13475=ORIENTED_EDGE('',*,*,#9546,.T.);
#13476=ORIENTED_EDGE('',*,*,#9548,.T.);
#13477=ORIENTED_EDGE('',*,*,#9549,.F.);
#13478=ORIENTED_EDGE('',*,*,#9548,.F.);
#13479=ORIENTED_EDGE('',*,*,#9545,.T.);
#13480=ORIENTED_EDGE('',*,*,#9550,.T.);
#13481=ORIENTED_EDGE('',*,*,#9551,.F.);
#13482=ORIENTED_EDGE('',*,*,#9550,.F.);
#13483=ORIENTED_EDGE('',*,*,#9544,.F.);
#13484=ORIENTED_EDGE('',*,*,#9552,.F.);
#13485=ORIENTED_EDGE('',*,*,#9553,.T.);
#13486=ORIENTED_EDGE('',*,*,#9554,.F.);
#13487=ORIENTED_EDGE('',*,*,#9555,.F.);
#13488=ORIENTED_EDGE('',*,*,#9556,.F.);
#13489=ORIENTED_EDGE('',*,*,#9555,.T.);
#13490=ORIENTED_EDGE('',*,*,#9557,.T.);
#13491=ORIENTED_EDGE('',*,*,#9558,.F.);
#13492=ORIENTED_EDGE('',*,*,#9557,.F.);
#13493=ORIENTED_EDGE('',*,*,#9554,.T.);
#13494=ORIENTED_EDGE('',*,*,#9559,.T.);
#13495=ORIENTED_EDGE('',*,*,#9560,.F.);
#13496=ORIENTED_EDGE('',*,*,#9559,.F.);
#13497=ORIENTED_EDGE('',*,*,#9553,.F.);
#13498=ORIENTED_EDGE('',*,*,#9561,.F.);
#13499=ORIENTED_EDGE('',*,*,#9562,.T.);
#13500=ORIENTED_EDGE('',*,*,#9563,.F.);
#13501=ORIENTED_EDGE('',*,*,#9564,.F.);
#13502=ORIENTED_EDGE('',*,*,#9565,.F.);
#13503=ORIENTED_EDGE('',*,*,#9564,.T.);
#13504=ORIENTED_EDGE('',*,*,#9566,.T.);
#13505=ORIENTED_EDGE('',*,*,#9567,.F.);
#13506=ORIENTED_EDGE('',*,*,#9566,.F.);
#13507=ORIENTED_EDGE('',*,*,#9563,.T.);
#13508=ORIENTED_EDGE('',*,*,#9568,.T.);
#13509=ORIENTED_EDGE('',*,*,#9569,.F.);
#13510=ORIENTED_EDGE('',*,*,#9568,.F.);
#13511=ORIENTED_EDGE('',*,*,#9562,.F.);
#13512=ORIENTED_EDGE('',*,*,#9570,.F.);
#13513=ORIENTED_EDGE('',*,*,#9571,.T.);
#13514=ORIENTED_EDGE('',*,*,#9572,.F.);
#13515=ORIENTED_EDGE('',*,*,#9573,.F.);
#13516=ORIENTED_EDGE('',*,*,#9574,.F.);
#13517=ORIENTED_EDGE('',*,*,#9573,.T.);
#13518=ORIENTED_EDGE('',*,*,#9575,.T.);
#13519=ORIENTED_EDGE('',*,*,#9576,.F.);
#13520=ORIENTED_EDGE('',*,*,#9575,.F.);
#13521=ORIENTED_EDGE('',*,*,#9572,.T.);
#13522=ORIENTED_EDGE('',*,*,#9577,.T.);
#13523=ORIENTED_EDGE('',*,*,#9578,.F.);
#13524=ORIENTED_EDGE('',*,*,#9577,.F.);
#13525=ORIENTED_EDGE('',*,*,#9571,.F.);
#13526=ORIENTED_EDGE('',*,*,#9579,.F.);
#13527=ORIENTED_EDGE('',*,*,#9580,.T.);
#13528=ORIENTED_EDGE('',*,*,#9581,.F.);
#13529=ORIENTED_EDGE('',*,*,#9582,.F.);
#13530=ORIENTED_EDGE('',*,*,#9583,.F.);
#13531=ORIENTED_EDGE('',*,*,#9582,.T.);
#13532=ORIENTED_EDGE('',*,*,#9584,.T.);
#13533=ORIENTED_EDGE('',*,*,#9585,.F.);
#13534=ORIENTED_EDGE('',*,*,#9584,.F.);
#13535=ORIENTED_EDGE('',*,*,#9581,.T.);
#13536=ORIENTED_EDGE('',*,*,#9586,.T.);
#13537=ORIENTED_EDGE('',*,*,#9587,.F.);
#13538=ORIENTED_EDGE('',*,*,#9586,.F.);
#13539=ORIENTED_EDGE('',*,*,#9580,.F.);
#13540=ORIENTED_EDGE('',*,*,#9588,.F.);
#13541=ORIENTED_EDGE('',*,*,#9589,.T.);
#13542=ORIENTED_EDGE('',*,*,#9590,.F.);
#13543=ORIENTED_EDGE('',*,*,#9591,.F.);
#13544=ORIENTED_EDGE('',*,*,#9592,.F.);
#13545=ORIENTED_EDGE('',*,*,#9591,.T.);
#13546=ORIENTED_EDGE('',*,*,#9593,.T.);
#13547=ORIENTED_EDGE('',*,*,#9594,.F.);
#13548=ORIENTED_EDGE('',*,*,#9593,.F.);
#13549=ORIENTED_EDGE('',*,*,#9590,.T.);
#13550=ORIENTED_EDGE('',*,*,#9595,.T.);
#13551=ORIENTED_EDGE('',*,*,#9596,.F.);
#13552=ORIENTED_EDGE('',*,*,#9595,.F.);
#13553=ORIENTED_EDGE('',*,*,#9589,.F.);
#13554=ORIENTED_EDGE('',*,*,#9597,.F.);
#13555=ORIENTED_EDGE('',*,*,#9598,.T.);
#13556=ORIENTED_EDGE('',*,*,#9599,.F.);
#13557=ORIENTED_EDGE('',*,*,#9600,.F.);
#13558=ORIENTED_EDGE('',*,*,#9601,.F.);
#13559=ORIENTED_EDGE('',*,*,#9600,.T.);
#13560=ORIENTED_EDGE('',*,*,#9602,.T.);
#13561=ORIENTED_EDGE('',*,*,#9603,.F.);
#13562=ORIENTED_EDGE('',*,*,#9602,.F.);
#13563=ORIENTED_EDGE('',*,*,#9599,.T.);
#13564=ORIENTED_EDGE('',*,*,#9604,.T.);
#13565=ORIENTED_EDGE('',*,*,#9605,.F.);
#13566=ORIENTED_EDGE('',*,*,#9604,.F.);
#13567=ORIENTED_EDGE('',*,*,#9598,.F.);
#13568=ORIENTED_EDGE('',*,*,#9606,.F.);
#13569=ORIENTED_EDGE('',*,*,#9607,.T.);
#13570=ORIENTED_EDGE('',*,*,#9608,.F.);
#13571=ORIENTED_EDGE('',*,*,#9609,.F.);
#13572=ORIENTED_EDGE('',*,*,#9610,.F.);
#13573=ORIENTED_EDGE('',*,*,#9609,.T.);
#13574=ORIENTED_EDGE('',*,*,#9611,.T.);
#13575=ORIENTED_EDGE('',*,*,#9612,.F.);
#13576=ORIENTED_EDGE('',*,*,#9611,.F.);
#13577=ORIENTED_EDGE('',*,*,#9608,.T.);
#13578=ORIENTED_EDGE('',*,*,#9613,.T.);
#13579=ORIENTED_EDGE('',*,*,#9614,.F.);
#13580=ORIENTED_EDGE('',*,*,#9613,.F.);
#13581=ORIENTED_EDGE('',*,*,#9607,.F.);
#13582=ORIENTED_EDGE('',*,*,#9615,.F.);
#13583=ORIENTED_EDGE('',*,*,#9616,.T.);
#13584=ORIENTED_EDGE('',*,*,#9617,.F.);
#13585=ORIENTED_EDGE('',*,*,#9618,.F.);
#13586=ORIENTED_EDGE('',*,*,#9619,.F.);
#13587=ORIENTED_EDGE('',*,*,#9618,.T.);
#13588=ORIENTED_EDGE('',*,*,#9620,.T.);
#13589=ORIENTED_EDGE('',*,*,#9621,.F.);
#13590=ORIENTED_EDGE('',*,*,#9620,.F.);
#13591=ORIENTED_EDGE('',*,*,#9617,.T.);
#13592=ORIENTED_EDGE('',*,*,#9622,.T.);
#13593=ORIENTED_EDGE('',*,*,#9623,.F.);
#13594=ORIENTED_EDGE('',*,*,#9622,.F.);
#13595=ORIENTED_EDGE('',*,*,#9616,.F.);
#13596=ORIENTED_EDGE('',*,*,#9624,.F.);
#13597=ORIENTED_EDGE('',*,*,#9625,.T.);
#13598=ORIENTED_EDGE('',*,*,#9626,.T.);
#13599=ORIENTED_EDGE('',*,*,#9627,.F.);
#13600=ORIENTED_EDGE('',*,*,#9628,.F.);
#13601=ORIENTED_EDGE('',*,*,#9629,.T.);
#13602=ORIENTED_EDGE('',*,*,#9630,.T.);
#13603=ORIENTED_EDGE('',*,*,#9625,.F.);
#13604=ORIENTED_EDGE('',*,*,#9631,.F.);
#13605=ORIENTED_EDGE('',*,*,#9632,.T.);
#13606=ORIENTED_EDGE('',*,*,#9633,.T.);
#13607=ORIENTED_EDGE('',*,*,#9629,.F.);
#13608=ORIENTED_EDGE('',*,*,#9634,.F.);
#13609=ORIENTED_EDGE('',*,*,#9635,.T.);
#13610=ORIENTED_EDGE('',*,*,#9636,.T.);
#13611=ORIENTED_EDGE('',*,*,#9632,.F.);
#13612=ORIENTED_EDGE('',*,*,#9637,.F.);
#13613=ORIENTED_EDGE('',*,*,#9638,.T.);
#13614=ORIENTED_EDGE('',*,*,#9639,.T.);
#13615=ORIENTED_EDGE('',*,*,#9635,.F.);
#13616=ORIENTED_EDGE('',*,*,#9640,.F.);
#13617=ORIENTED_EDGE('',*,*,#9627,.T.);
#13618=ORIENTED_EDGE('',*,*,#9641,.T.);
#13619=ORIENTED_EDGE('',*,*,#9638,.F.);
#13620=ORIENTED_EDGE('',*,*,#9641,.F.);
#13621=ORIENTED_EDGE('',*,*,#9626,.F.);
#13622=ORIENTED_EDGE('',*,*,#9630,.F.);
#13623=ORIENTED_EDGE('',*,*,#9633,.F.);
#13624=ORIENTED_EDGE('',*,*,#9636,.F.);
#13625=ORIENTED_EDGE('',*,*,#9639,.F.);
#13626=ORIENTED_EDGE('',*,*,#9642,.F.);
#13627=ORIENTED_EDGE('',*,*,#9291,.F.);
#13628=ORIENTED_EDGE('',*,*,#9083,.F.);
#13629=ORIENTED_EDGE('',*,*,#9292,.F.);
#13630=ORIENTED_EDGE('',*,*,#9643,.T.);
#13631=ORIENTED_EDGE('',*,*,#9642,.T.);
#13632=ORIENTED_EDGE('',*,*,#9643,.F.);
#13633=ORIENTED_EDGE('',*,*,#9181,.T.);
#13634=ORIENTED_EDGE('',*,*,#9288,.T.);
#13635=ORIENTED_EDGE('',*,*,#9644,.F.);
#13636=ORIENTED_EDGE('',*,*,#9297,.T.);
#13637=ORIENTED_EDGE('',*,*,#9645,.F.);
#13638=ORIENTED_EDGE('',*,*,#9644,.T.);
#13639=ORIENTED_EDGE('',*,*,#9287,.T.);
#13640=ORIENTED_EDGE('',*,*,#9186,.T.);
#13641=ORIENTED_EDGE('',*,*,#9296,.T.);
#13642=ORIENTED_EDGE('',*,*,#9646,.F.);
#13643=ORIENTED_EDGE('',*,*,#9647,.T.);
#13644=ORIENTED_EDGE('',*,*,#9461,.T.);
#13645=ORIENTED_EDGE('',*,*,#9451,.T.);
#13646=ORIENTED_EDGE('',*,*,#9455,.T.);
#13647=ORIENTED_EDGE('',*,*,#9648,.T.);
#13648=ORIENTED_EDGE('',*,*,#9645,.T.);
#13649=ORIENTED_EDGE('',*,*,#9648,.F.);
#13650=ORIENTED_EDGE('',*,*,#9457,.T.);
#13651=ORIENTED_EDGE('',*,*,#9458,.T.);
#13652=ORIENTED_EDGE('',*,*,#9460,.T.);
#13653=ORIENTED_EDGE('',*,*,#9647,.F.);
#13654=ORIENTED_EDGE('',*,*,#9304,.T.);
#13655=ORIENTED_EDGE('',*,*,#9306,.T.);
#13656=ORIENTED_EDGE('',*,*,#9298,.T.);
#13657=ORIENTED_EDGE('',*,*,#9302,.T.);
#13658=ORIENTED_EDGE('',*,*,#9313,.T.);
#13659=ORIENTED_EDGE('',*,*,#9315,.T.);
#13660=ORIENTED_EDGE('',*,*,#9307,.T.);
#13661=ORIENTED_EDGE('',*,*,#9311,.T.);
#13662=ORIENTED_EDGE('',*,*,#9322,.T.);
#13663=ORIENTED_EDGE('',*,*,#9324,.T.);
#13664=ORIENTED_EDGE('',*,*,#9316,.T.);
#13665=ORIENTED_EDGE('',*,*,#9320,.T.);
#13666=ORIENTED_EDGE('',*,*,#9331,.T.);
#13667=ORIENTED_EDGE('',*,*,#9333,.T.);
#13668=ORIENTED_EDGE('',*,*,#9325,.T.);
#13669=ORIENTED_EDGE('',*,*,#9329,.T.);
#13670=ORIENTED_EDGE('',*,*,#9340,.T.);
#13671=ORIENTED_EDGE('',*,*,#9342,.T.);
#13672=ORIENTED_EDGE('',*,*,#9334,.T.);
#13673=ORIENTED_EDGE('',*,*,#9338,.T.);
#13674=ORIENTED_EDGE('',*,*,#9349,.T.);
#13675=ORIENTED_EDGE('',*,*,#9351,.T.);
#13676=ORIENTED_EDGE('',*,*,#9343,.T.);
#13677=ORIENTED_EDGE('',*,*,#9347,.T.);
#13678=ORIENTED_EDGE('',*,*,#9358,.T.);
#13679=ORIENTED_EDGE('',*,*,#9360,.T.);
#13680=ORIENTED_EDGE('',*,*,#9352,.T.);
#13681=ORIENTED_EDGE('',*,*,#9356,.T.);
#13682=ORIENTED_EDGE('',*,*,#9367,.T.);
#13683=ORIENTED_EDGE('',*,*,#9369,.T.);
#13684=ORIENTED_EDGE('',*,*,#9361,.T.);
#13685=ORIENTED_EDGE('',*,*,#9365,.T.);
#13686=ORIENTED_EDGE('',*,*,#9376,.T.);
#13687=ORIENTED_EDGE('',*,*,#9378,.T.);
#13688=ORIENTED_EDGE('',*,*,#9370,.T.);
#13689=ORIENTED_EDGE('',*,*,#9374,.T.);
#13690=ORIENTED_EDGE('',*,*,#9385,.T.);
#13691=ORIENTED_EDGE('',*,*,#9387,.T.);
#13692=ORIENTED_EDGE('',*,*,#9379,.T.);
#13693=ORIENTED_EDGE('',*,*,#9383,.T.);
#13694=ORIENTED_EDGE('',*,*,#9394,.T.);
#13695=ORIENTED_EDGE('',*,*,#9396,.T.);
#13696=ORIENTED_EDGE('',*,*,#9388,.T.);
#13697=ORIENTED_EDGE('',*,*,#9392,.T.);
#13698=ORIENTED_EDGE('',*,*,#9403,.T.);
#13699=ORIENTED_EDGE('',*,*,#9405,.T.);
#13700=ORIENTED_EDGE('',*,*,#9397,.T.);
#13701=ORIENTED_EDGE('',*,*,#9401,.T.);
#13702=ORIENTED_EDGE('',*,*,#9412,.T.);
#13703=ORIENTED_EDGE('',*,*,#9414,.T.);
#13704=ORIENTED_EDGE('',*,*,#9406,.T.);
#13705=ORIENTED_EDGE('',*,*,#9410,.T.);
#13706=ORIENTED_EDGE('',*,*,#9421,.T.);
#13707=ORIENTED_EDGE('',*,*,#9423,.T.);
#13708=ORIENTED_EDGE('',*,*,#9415,.T.);
#13709=ORIENTED_EDGE('',*,*,#9419,.T.);
#13710=ORIENTED_EDGE('',*,*,#9430,.T.);
#13711=ORIENTED_EDGE('',*,*,#9432,.T.);
#13712=ORIENTED_EDGE('',*,*,#9424,.T.);
#13713=ORIENTED_EDGE('',*,*,#9428,.T.);
#13714=ORIENTED_EDGE('',*,*,#9439,.T.);
#13715=ORIENTED_EDGE('',*,*,#9441,.T.);
#13716=ORIENTED_EDGE('',*,*,#9433,.T.);
#13717=ORIENTED_EDGE('',*,*,#9437,.T.);
#13718=ORIENTED_EDGE('',*,*,#9448,.T.);
#13719=ORIENTED_EDGE('',*,*,#9450,.T.);
#13720=ORIENTED_EDGE('',*,*,#9442,.T.);
#13721=ORIENTED_EDGE('',*,*,#9446,.T.);
#13722=ORIENTED_EDGE('',*,*,#9468,.T.);
#13723=ORIENTED_EDGE('',*,*,#9470,.T.);
#13724=ORIENTED_EDGE('',*,*,#9462,.T.);
#13725=ORIENTED_EDGE('',*,*,#9466,.T.);
#13726=ORIENTED_EDGE('',*,*,#9477,.T.);
#13727=ORIENTED_EDGE('',*,*,#9479,.T.);
#13728=ORIENTED_EDGE('',*,*,#9471,.T.);
#13729=ORIENTED_EDGE('',*,*,#9475,.T.);
#13730=ORIENTED_EDGE('',*,*,#9486,.T.);
#13731=ORIENTED_EDGE('',*,*,#9488,.T.);
#13732=ORIENTED_EDGE('',*,*,#9480,.T.);
#13733=ORIENTED_EDGE('',*,*,#9484,.T.);
#13734=ORIENTED_EDGE('',*,*,#9495,.T.);
#13735=ORIENTED_EDGE('',*,*,#9497,.T.);
#13736=ORIENTED_EDGE('',*,*,#9489,.T.);
#13737=ORIENTED_EDGE('',*,*,#9493,.T.);
#13738=ORIENTED_EDGE('',*,*,#9504,.T.);
#13739=ORIENTED_EDGE('',*,*,#9506,.T.);
#13740=ORIENTED_EDGE('',*,*,#9498,.T.);
#13741=ORIENTED_EDGE('',*,*,#9502,.T.);
#13742=ORIENTED_EDGE('',*,*,#9513,.T.);
#13743=ORIENTED_EDGE('',*,*,#9515,.T.);
#13744=ORIENTED_EDGE('',*,*,#9507,.T.);
#13745=ORIENTED_EDGE('',*,*,#9511,.T.);
#13746=ORIENTED_EDGE('',*,*,#9522,.T.);
#13747=ORIENTED_EDGE('',*,*,#9524,.T.);
#13748=ORIENTED_EDGE('',*,*,#9516,.T.);
#13749=ORIENTED_EDGE('',*,*,#9520,.T.);
#13750=ORIENTED_EDGE('',*,*,#9531,.T.);
#13751=ORIENTED_EDGE('',*,*,#9533,.T.);
#13752=ORIENTED_EDGE('',*,*,#9525,.T.);
#13753=ORIENTED_EDGE('',*,*,#9529,.T.);
#13754=ORIENTED_EDGE('',*,*,#9540,.T.);
#13755=ORIENTED_EDGE('',*,*,#9542,.T.);
#13756=ORIENTED_EDGE('',*,*,#9534,.T.);
#13757=ORIENTED_EDGE('',*,*,#9538,.T.);
#13758=ORIENTED_EDGE('',*,*,#9549,.T.);
#13759=ORIENTED_EDGE('',*,*,#9551,.T.);
#13760=ORIENTED_EDGE('',*,*,#9543,.T.);
#13761=ORIENTED_EDGE('',*,*,#9547,.T.);
#13762=ORIENTED_EDGE('',*,*,#9558,.T.);
#13763=ORIENTED_EDGE('',*,*,#9560,.T.);
#13764=ORIENTED_EDGE('',*,*,#9552,.T.);
#13765=ORIENTED_EDGE('',*,*,#9556,.T.);
#13766=ORIENTED_EDGE('',*,*,#9567,.T.);
#13767=ORIENTED_EDGE('',*,*,#9569,.T.);
#13768=ORIENTED_EDGE('',*,*,#9561,.T.);
#13769=ORIENTED_EDGE('',*,*,#9565,.T.);
#13770=ORIENTED_EDGE('',*,*,#9576,.T.);
#13771=ORIENTED_EDGE('',*,*,#9578,.T.);
#13772=ORIENTED_EDGE('',*,*,#9570,.T.);
#13773=ORIENTED_EDGE('',*,*,#9574,.T.);
#13774=ORIENTED_EDGE('',*,*,#9585,.T.);
#13775=ORIENTED_EDGE('',*,*,#9587,.T.);
#13776=ORIENTED_EDGE('',*,*,#9579,.T.);
#13777=ORIENTED_EDGE('',*,*,#9583,.T.);
#13778=ORIENTED_EDGE('',*,*,#9594,.T.);
#13779=ORIENTED_EDGE('',*,*,#9596,.T.);
#13780=ORIENTED_EDGE('',*,*,#9588,.T.);
#13781=ORIENTED_EDGE('',*,*,#9592,.T.);
#13782=ORIENTED_EDGE('',*,*,#9603,.T.);
#13783=ORIENTED_EDGE('',*,*,#9605,.T.);
#13784=ORIENTED_EDGE('',*,*,#9597,.T.);
#13785=ORIENTED_EDGE('',*,*,#9601,.T.);
#13786=ORIENTED_EDGE('',*,*,#9612,.T.);
#13787=ORIENTED_EDGE('',*,*,#9614,.T.);
#13788=ORIENTED_EDGE('',*,*,#9606,.T.);
#13789=ORIENTED_EDGE('',*,*,#9610,.T.);
#13790=ORIENTED_EDGE('',*,*,#9621,.T.);
#13791=ORIENTED_EDGE('',*,*,#9623,.T.);
#13792=ORIENTED_EDGE('',*,*,#9615,.T.);
#13793=ORIENTED_EDGE('',*,*,#9619,.T.);
#13794=ORIENTED_EDGE('',*,*,#9649,.F.);
#13795=ORIENTED_EDGE('',*,*,#9650,.T.);
#13796=ORIENTED_EDGE('',*,*,#9646,.T.);
#13797=ORIENTED_EDGE('',*,*,#9650,.F.);
#13798=ORIENTED_EDGE('',*,*,#9649,.T.);
#13799=ORIENTED_EDGE('',*,*,#9624,.T.);
#13800=ORIENTED_EDGE('',*,*,#9640,.T.);
#13801=ORIENTED_EDGE('',*,*,#9637,.T.);
#13802=ORIENTED_EDGE('',*,*,#9634,.T.);
#13803=ORIENTED_EDGE('',*,*,#9631,.T.);
#13804=ORIENTED_EDGE('',*,*,#9628,.T.);
#14181=CONICAL_SURFACE('',#16660,5.75,0.78539816339745);
#14182=CONICAL_SURFACE('',#16667,8.75,0.785398163397448);
#14777=ADVANCED_FACE('',(#2210),#1528,.T.);
#14778=ADVANCED_FACE('',(#2211),#1529,.T.);
#14779=ADVANCED_FACE('',(#2212),#1530,.T.);
#14780=ADVANCED_FACE('',(#2213),#1531,.T.);
#14781=ADVANCED_FACE('',(#2214),#1532,.T.);
#14782=ADVANCED_FACE('',(#2215),#1533,.T.);
#14783=ADVANCED_FACE('',(#2216),#1534,.T.);
#14784=ADVANCED_FACE('',(#2217),#1535,.T.);
#14785=ADVANCED_FACE('',(#2218),#1536,.T.);
#14786=ADVANCED_FACE('',(#2219),#1537,.T.);
#14787=ADVANCED_FACE('',(#2220),#1538,.T.);
#14788=ADVANCED_FACE('',(#2221),#1539,.T.);
#14789=ADVANCED_FACE('',(#2222),#1540,.T.);
#14790=ADVANCED_FACE('',(#2223),#1541,.T.);
#14791=ADVANCED_FACE('',(#2224),#1542,.T.);
#14792=ADVANCED_FACE('',(#2225),#1543,.T.);
#14793=ADVANCED_FACE('',(#2226),#1544,.T.);
#14794=ADVANCED_FACE('',(#2227),#1545,.T.);
#14795=ADVANCED_FACE('',(#2228),#1546,.T.);
#14796=ADVANCED_FACE('',(#2229),#1547,.T.);
#14797=ADVANCED_FACE('',(#2230),#1548,.T.);
#14798=ADVANCED_FACE('',(#2231),#1549,.T.);
#14799=ADVANCED_FACE('',(#2232),#1550,.T.);
#14800=ADVANCED_FACE('',(#2233),#1551,.T.);
#14801=ADVANCED_FACE('',(#2234),#1552,.T.);
#14802=ADVANCED_FACE('',(#2235),#1553,.T.);
#14803=ADVANCED_FACE('',(#2236),#1554,.T.);
#14804=ADVANCED_FACE('',(#2237),#1555,.T.);
#14805=ADVANCED_FACE('',(#2238),#1556,.T.);
#14806=ADVANCED_FACE('',(#2239),#1557,.T.);
#14807=ADVANCED_FACE('',(#2240),#1558,.T.);
#14808=ADVANCED_FACE('',(#2241),#1559,.T.);
#14809=ADVANCED_FACE('',(#2242),#1560,.T.);
#14810=ADVANCED_FACE('',(#2243),#1561,.T.);
#14811=ADVANCED_FACE('',(#2244),#1562,.T.);
#14812=ADVANCED_FACE('',(#2245),#1563,.T.);
#14813=ADVANCED_FACE('',(#2246),#1564,.T.);
#14814=ADVANCED_FACE('',(#2247),#1565,.T.);
#14815=ADVANCED_FACE('',(#2248),#1566,.T.);
#14816=ADVANCED_FACE('',(#2249),#1567,.T.);
#14817=ADVANCED_FACE('',(#2250),#1568,.T.);
#14818=ADVANCED_FACE('',(#2251),#1569,.T.);
#14819=ADVANCED_FACE('',(#2252),#1570,.T.);
#14820=ADVANCED_FACE('',(#2253),#1571,.T.);
#14821=ADVANCED_FACE('',(#2254),#1572,.T.);
#14822=ADVANCED_FACE('',(#2255),#1573,.T.);
#14823=ADVANCED_FACE('',(#2256),#1574,.T.);
#14824=ADVANCED_FACE('',(#2257),#1575,.T.);
#14825=ADVANCED_FACE('',(#2258),#1576,.T.);
#14826=ADVANCED_FACE('',(#2259),#1577,.T.);
#14827=ADVANCED_FACE('',(#2260),#1578,.T.);
#14828=ADVANCED_FACE('',(#2261),#1579,.T.);
#14829=ADVANCED_FACE('',(#2262),#1580,.T.);
#14830=ADVANCED_FACE('',(#2263),#1581,.T.);
#14831=ADVANCED_FACE('',(#2264),#1582,.T.);
#14832=ADVANCED_FACE('',(#2265),#1583,.T.);
#14833=ADVANCED_FACE('',(#2266),#1584,.T.);
#14834=ADVANCED_FACE('',(#2267),#1585,.T.);
#14835=ADVANCED_FACE('',(#2268),#1586,.T.);
#14836=ADVANCED_FACE('',(#2269),#1587,.T.);
#14837=ADVANCED_FACE('',(#2270),#1588,.T.);
#14838=ADVANCED_FACE('',(#2271),#1589,.T.);
#14839=ADVANCED_FACE('',(#2272),#1590,.T.);
#14840=ADVANCED_FACE('',(#2273),#1591,.T.);
#14841=ADVANCED_FACE('',(#2274),#1592,.T.);
#14842=ADVANCED_FACE('',(#2275),#1593,.T.);
#14843=ADVANCED_FACE('',(#2276),#1594,.T.);
#14844=ADVANCED_FACE('',(#2277),#1595,.T.);
#14845=ADVANCED_FACE('',(#2278),#252,.F.);
#14846=ADVANCED_FACE('',(#2279),#811,.T.);
#14847=ADVANCED_FACE('',(#2280),#1596,.T.);
#14848=ADVANCED_FACE('',(#2281),#253,.F.);
#14849=ADVANCED_FACE('',(#2282),#812,.F.);
#14850=ADVANCED_FACE('',(#2283),#813,.T.);
#14851=ADVANCED_FACE('',(#2284),#814,.F.);
#14852=ADVANCED_FACE('',(#2285),#815,.F.);
#14853=ADVANCED_FACE('',(#2286),#816,.F.);
#14854=ADVANCED_FACE('',(#2287),#817,.T.);
#14855=ADVANCED_FACE('',(#2288),#818,.F.);
#14856=ADVANCED_FACE('',(#2289),#819,.F.);
#14857=ADVANCED_FACE('',(#2290),#820,.F.);
#14858=ADVANCED_FACE('',(#2291),#821,.T.);
#14859=ADVANCED_FACE('',(#2292),#822,.F.);
#14860=ADVANCED_FACE('',(#2293),#823,.F.);
#14861=ADVANCED_FACE('',(#2294),#824,.F.);
#14862=ADVANCED_FACE('',(#2295),#825,.T.);
#14863=ADVANCED_FACE('',(#2296),#826,.F.);
#14864=ADVANCED_FACE('',(#2297),#827,.F.);
#14865=ADVANCED_FACE('',(#2298),#828,.F.);
#14866=ADVANCED_FACE('',(#2299),#829,.T.);
#14867=ADVANCED_FACE('',(#2300),#830,.F.);
#14868=ADVANCED_FACE('',(#2301),#831,.F.);
#14869=ADVANCED_FACE('',(#2302),#832,.F.);
#14870=ADVANCED_FACE('',(#2303),#833,.T.);
#14871=ADVANCED_FACE('',(#2304),#834,.F.);
#14872=ADVANCED_FACE('',(#2305),#835,.F.);
#14873=ADVANCED_FACE('',(#2306),#836,.F.);
#14874=ADVANCED_FACE('',(#2307),#837,.T.);
#14875=ADVANCED_FACE('',(#2308),#838,.F.);
#14876=ADVANCED_FACE('',(#2309),#839,.F.);
#14877=ADVANCED_FACE('',(#2310),#840,.F.);
#14878=ADVANCED_FACE('',(#2311),#841,.T.);
#14879=ADVANCED_FACE('',(#2312),#842,.F.);
#14880=ADVANCED_FACE('',(#2313),#843,.F.);
#14881=ADVANCED_FACE('',(#2314),#844,.F.);
#14882=ADVANCED_FACE('',(#2315),#845,.T.);
#14883=ADVANCED_FACE('',(#2316),#846,.F.);
#14884=ADVANCED_FACE('',(#2317),#847,.F.);
#14885=ADVANCED_FACE('',(#2318),#848,.F.);
#14886=ADVANCED_FACE('',(#2319),#849,.T.);
#14887=ADVANCED_FACE('',(#2320),#850,.F.);
#14888=ADVANCED_FACE('',(#2321),#851,.F.);
#14889=ADVANCED_FACE('',(#2322),#852,.F.);
#14890=ADVANCED_FACE('',(#2323),#853,.T.);
#14891=ADVANCED_FACE('',(#2324),#854,.F.);
#14892=ADVANCED_FACE('',(#2325),#855,.F.);
#14893=ADVANCED_FACE('',(#2326),#856,.F.);
#14894=ADVANCED_FACE('',(#2327),#857,.T.);
#14895=ADVANCED_FACE('',(#2328),#858,.F.);
#14896=ADVANCED_FACE('',(#2329),#859,.F.);
#14897=ADVANCED_FACE('',(#2330),#860,.F.);
#14898=ADVANCED_FACE('',(#2331),#861,.T.);
#14899=ADVANCED_FACE('',(#2332),#862,.F.);
#14900=ADVANCED_FACE('',(#2333),#863,.F.);
#14901=ADVANCED_FACE('',(#2334),#864,.F.);
#14902=ADVANCED_FACE('',(#2335),#865,.T.);
#14903=ADVANCED_FACE('',(#2336),#866,.F.);
#14904=ADVANCED_FACE('',(#2337),#867,.F.);
#14905=ADVANCED_FACE('',(#2338),#868,.F.);
#14906=ADVANCED_FACE('',(#2339),#869,.T.);
#14907=ADVANCED_FACE('',(#2340),#870,.F.);
#14908=ADVANCED_FACE('',(#2341),#871,.F.);
#14909=ADVANCED_FACE('',(#2342),#872,.F.);
#14910=ADVANCED_FACE('',(#2343),#873,.T.);
#14911=ADVANCED_FACE('',(#2344),#874,.F.);
#14912=ADVANCED_FACE('',(#2345),#875,.F.);
#14913=ADVANCED_FACE('',(#2346),#876,.F.);
#14914=ADVANCED_FACE('',(#2347),#877,.T.);
#14915=ADVANCED_FACE('',(#2348),#878,.F.);
#14916=ADVANCED_FACE('',(#2349),#879,.F.);
#14917=ADVANCED_FACE('',(#2350),#880,.F.);
#14918=ADVANCED_FACE('',(#2351),#881,.T.);
#14919=ADVANCED_FACE('',(#2352),#882,.F.);
#14920=ADVANCED_FACE('',(#2353),#883,.F.);
#14921=ADVANCED_FACE('',(#2354),#884,.F.);
#14922=ADVANCED_FACE('',(#2355),#885,.T.);
#14923=ADVANCED_FACE('',(#2356),#886,.F.);
#14924=ADVANCED_FACE('',(#2357),#887,.F.);
#14925=ADVANCED_FACE('',(#2358),#888,.F.);
#14926=ADVANCED_FACE('',(#2359),#889,.T.);
#14927=ADVANCED_FACE('',(#2360),#890,.F.);
#14928=ADVANCED_FACE('',(#2361),#891,.F.);
#14929=ADVANCED_FACE('',(#2362),#892,.F.);
#14930=ADVANCED_FACE('',(#2363),#893,.T.);
#14931=ADVANCED_FACE('',(#2364),#894,.F.);
#14932=ADVANCED_FACE('',(#2365),#895,.F.);
#14933=ADVANCED_FACE('',(#2366),#896,.F.);
#14934=ADVANCED_FACE('',(#2367),#897,.T.);
#14935=ADVANCED_FACE('',(#2368),#898,.F.);
#14936=ADVANCED_FACE('',(#2369),#899,.F.);
#14937=ADVANCED_FACE('',(#2370),#900,.F.);
#14938=ADVANCED_FACE('',(#2371),#901,.T.);
#14939=ADVANCED_FACE('',(#2372),#902,.F.);
#14940=ADVANCED_FACE('',(#2373),#903,.F.);
#14941=ADVANCED_FACE('',(#2374),#904,.F.);
#14942=ADVANCED_FACE('',(#2375),#905,.T.);
#14943=ADVANCED_FACE('',(#2376),#906,.F.);
#14944=ADVANCED_FACE('',(#2377),#907,.F.);
#14945=ADVANCED_FACE('',(#2378),#908,.F.);
#14946=ADVANCED_FACE('',(#2379),#909,.T.);
#14947=ADVANCED_FACE('',(#2380),#910,.F.);
#14948=ADVANCED_FACE('',(#2381),#911,.F.);
#14949=ADVANCED_FACE('',(#2382),#912,.F.);
#14950=ADVANCED_FACE('',(#2383),#913,.T.);
#14951=ADVANCED_FACE('',(#2384),#914,.F.);
#14952=ADVANCED_FACE('',(#2385),#915,.F.);
#14953=ADVANCED_FACE('',(#2386),#916,.F.);
#14954=ADVANCED_FACE('',(#2387),#917,.T.);
#14955=ADVANCED_FACE('',(#2388),#918,.F.);
#14956=ADVANCED_FACE('',(#2389),#919,.F.);
#14957=ADVANCED_FACE('',(#2390),#920,.F.);
#14958=ADVANCED_FACE('',(#2391),#921,.T.);
#14959=ADVANCED_FACE('',(#2392),#922,.F.);
#14960=ADVANCED_FACE('',(#2393),#923,.F.);
#14961=ADVANCED_FACE('',(#2394),#924,.F.);
#14962=ADVANCED_FACE('',(#2395),#925,.T.);
#14963=ADVANCED_FACE('',(#2396),#926,.F.);
#14964=ADVANCED_FACE('',(#2397),#927,.F.);
#14965=ADVANCED_FACE('',(#2398),#928,.F.);
#14966=ADVANCED_FACE('',(#2399),#929,.T.);
#14967=ADVANCED_FACE('',(#2400),#930,.F.);
#14968=ADVANCED_FACE('',(#2401),#931,.F.);
#14969=ADVANCED_FACE('',(#2402),#932,.F.);
#14970=ADVANCED_FACE('',(#2403),#933,.T.);
#14971=ADVANCED_FACE('',(#2404),#934,.F.);
#14972=ADVANCED_FACE('',(#2405),#935,.F.);
#14973=ADVANCED_FACE('',(#2406),#936,.F.);
#14974=ADVANCED_FACE('',(#2407),#937,.T.);
#14975=ADVANCED_FACE('',(#2408),#938,.F.);
#14976=ADVANCED_FACE('',(#2409),#939,.F.);
#14977=ADVANCED_FACE('',(#2410),#940,.F.);
#14978=ADVANCED_FACE('',(#2411),#941,.T.);
#14979=ADVANCED_FACE('',(#2412),#942,.F.);
#14980=ADVANCED_FACE('',(#2413),#943,.F.);
#14981=ADVANCED_FACE('',(#2414),#944,.F.);
#14982=ADVANCED_FACE('',(#2415),#945,.T.);
#14983=ADVANCED_FACE('',(#2416),#946,.F.);
#14984=ADVANCED_FACE('',(#2417),#947,.F.);
#14985=ADVANCED_FACE('',(#2418),#948,.F.);
#14986=ADVANCED_FACE('',(#2419),#949,.T.);
#14987=ADVANCED_FACE('',(#2420),#950,.F.);
#14988=ADVANCED_FACE('',(#2421),#951,.F.);
#14989=ADVANCED_FACE('',(#2422),#952,.F.);
#14990=ADVANCED_FACE('',(#2423),#953,.T.);
#14991=ADVANCED_FACE('',(#2424),#954,.F.);
#14992=ADVANCED_FACE('',(#2425),#955,.F.);
#14993=ADVANCED_FACE('',(#2426),#956,.F.);
#14994=ADVANCED_FACE('',(#2427),#957,.F.);
#14995=ADVANCED_FACE('',(#2428),#958,.F.);
#14996=ADVANCED_FACE('',(#2429),#959,.F.);
#14997=ADVANCED_FACE('',(#2430),#960,.F.);
#14998=ADVANCED_FACE('',(#2431),#961,.F.);
#14999=ADVANCED_FACE('',(#2432),#962,.F.);
#15000=ADVANCED_FACE('',(#2433),#963,.T.);
#15001=ADVANCED_FACE('',(#2434),#14181,.T.);
#15002=ADVANCED_FACE('',(#2435),#1597,.T.);
#15003=ADVANCED_FACE('',(#2436,#517),#964,.T.);
#15004=ADVANCED_FACE('',(#2437,#518,#519,#520,#521,#522,#523,#524,#525,
#526,#527,#528,#529,#530,#531,#532,#533,#534,#535,#536,#537,#538,#539,#540,
#541,#542,#543,#544,#545,#546,#547,#548,#549,#550,#551,#552),#1598,.T.);
#15005=ADVANCED_FACE('',(#2438),#14182,.T.);
#15006=ADVANCED_FACE('',(#2439,#553),#965,.T.);
#15084=CLOSED_SHELL('',(#14777,#14778,#14779,#14780,#14781,#14782,#14783,
#14784,#14785,#14786,#14787,#14788,#14789,#14790,#14791,#14792,#14793,#14794,
#14795,#14796,#14797,#14798,#14799,#14800,#14801,#14802,#14803,#14804,#14805,
#14806,#14807,#14808,#14809,#14810,#14811,#14812,#14813,#14814,#14815,#14816,
#14817,#14818,#14819,#14820,#14821,#14822,#14823,#14824,#14825,#14826,#14827,
#14828,#14829,#14830,#14831,#14832,#14833,#14834,#14835,#14836,#14837,#14838,
#14839,#14840,#14841,#14842,#14843,#14844,#14845,#14846,#14847,#14848,#14849,
#14850,#14851,#14852,#14853,#14854,#14855,#14856,#14857,#14858,#14859,#14860,
#14861,#14862,#14863,#14864,#14865,#14866,#14867,#14868,#14869,#14870,#14871,
#14872,#14873,#14874,#14875,#14876,#14877,#14878,#14879,#14880,#14881,#14882,
#14883,#14884,#14885,#14886,#14887,#14888,#14889,#14890,#14891,#14892,#14893,
#14894,#14895,#14896,#14897,#14898,#14899,#14900,#14901,#14902,#14903,#14904,
#14905,#14906,#14907,#14908,#14909,#14910,#14911,#14912,#14913,#14914,#14915,
#14916,#14917,#14918,#14919,#14920,#14921,#14922,#14923,#14924,#14925,#14926,
#14927,#14928,#14929,#14930,#14931,#14932,#14933,#14934,#14935,#14936,#14937,
#14938,#14939,#14940,#14941,#14942,#14943,#14944,#14945,#14946,#14947,#14948,
#14949,#14950,#14951,#14952,#14953,#14954,#14955,#14956,#14957,#14958,#14959,
#14960,#14961,#14962,#14963,#14964,#14965,#14966,#14967,#14968,#14969,#14970,
#14971,#14972,#14973,#14974,#14975,#14976,#14977,#14978,#14979,#14980,#14981,
#14982,#14983,#14984,#14985,#14986,#14987,#14988,#14989,#14990,#14991,#14992,
#14993,#14994,#14995,#14996,#14997,#14998,#14999,#15000,#15001,#15002,#15003,
#15004,#15005,#15006));
#16357=AXIS2_PLACEMENT_3D('',#27229,#19611,#19612);
#16358=AXIS2_PLACEMENT_3D('',#27230,#19613,#19614);
#16359=AXIS2_PLACEMENT_3D('',#27252,#19616,#19617);
#16360=AXIS2_PLACEMENT_3D('',#27263,#19618,#19619);
#16361=AXIS2_PLACEMENT_3D('',#27347,#19621,#19622);
#16362=AXIS2_PLACEMENT_3D('',#27437,#19624,#19625);
#16363=AXIS2_PLACEMENT_3D('',#27521,#19627,#19628);
#16364=AXIS2_PLACEMENT_3D('',#27611,#19630,#19631);
#16365=AXIS2_PLACEMENT_3D('',#27701,#19633,#19634);
#16366=AXIS2_PLACEMENT_3D('',#27785,#19636,#19637);
#16367=AXIS2_PLACEMENT_3D('',#27875,#19639,#19640);
#16368=AXIS2_PLACEMENT_3D('',#27959,#19642,#19643);
#16369=AXIS2_PLACEMENT_3D('',#28049,#19645,#19646);
#16370=AXIS2_PLACEMENT_3D('',#28133,#19648,#19649);
#16371=AXIS2_PLACEMENT_3D('',#28223,#19651,#19652);
#16372=AXIS2_PLACEMENT_3D('',#28310,#19654,#19655);
#16373=AXIS2_PLACEMENT_3D('',#28397,#19657,#19658);
#16374=AXIS2_PLACEMENT_3D('',#28487,#19660,#19661);
#16375=AXIS2_PLACEMENT_3D('',#28571,#19663,#19664);
#16376=AXIS2_PLACEMENT_3D('',#28661,#19666,#19667);
#16377=AXIS2_PLACEMENT_3D('',#28745,#19669,#19670);
#16378=AXIS2_PLACEMENT_3D('',#28835,#19672,#19673);
#16379=AXIS2_PLACEMENT_3D('',#28919,#19675,#19676);
#16380=AXIS2_PLACEMENT_3D('',#29006,#19678,#19679);
#16381=AXIS2_PLACEMENT_3D('',#29096,#19681,#19682);
#16382=AXIS2_PLACEMENT_3D('',#29180,#19684,#19685);
#16383=AXIS2_PLACEMENT_3D('',#29270,#19687,#19688);
#16384=AXIS2_PLACEMENT_3D('',#29354,#19690,#19691);
#16385=AXIS2_PLACEMENT_3D('',#29444,#19693,#19694);
#16386=AXIS2_PLACEMENT_3D('',#29528,#19696,#19697);
#16387=AXIS2_PLACEMENT_3D('',#29618,#19699,#19700);
#16388=AXIS2_PLACEMENT_3D('',#29708,#19702,#19703);
#16389=AXIS2_PLACEMENT_3D('',#29792,#19705,#19706);
#16390=AXIS2_PLACEMENT_3D('',#29882,#19708,#19709);
#16391=AXIS2_PLACEMENT_3D('',#29966,#19711,#19712);
#16392=AXIS2_PLACEMENT_3D('',#30056,#19714,#19715);
#16393=AXIS2_PLACEMENT_3D('',#30140,#19717,#19718);
#16394=AXIS2_PLACEMENT_3D('',#30155,#19720,#19721);
#16395=AXIS2_PLACEMENT_3D('',#30162,#19722,#19723);
#16396=AXIS2_PLACEMENT_3D('',#30199,#19725,#19726);
#16397=AXIS2_PLACEMENT_3D('',#30236,#19728,#19729);
#16398=AXIS2_PLACEMENT_3D('',#30273,#19731,#19732);
#16399=AXIS2_PLACEMENT_3D('',#30310,#19734,#19735);
#16400=AXIS2_PLACEMENT_3D('',#30347,#19737,#19738);
#16401=AXIS2_PLACEMENT_3D('',#30384,#19740,#19741);
#16402=AXIS2_PLACEMENT_3D('',#30422,#19743,#19744);
#16403=AXIS2_PLACEMENT_3D('',#30459,#19746,#19747);
#16404=AXIS2_PLACEMENT_3D('',#30496,#19749,#19750);
#16405=AXIS2_PLACEMENT_3D('',#30533,#19752,#19753);
#16406=AXIS2_PLACEMENT_3D('',#30570,#19755,#19756);
#16407=AXIS2_PLACEMENT_3D('',#30607,#19758,#19759);
#16408=AXIS2_PLACEMENT_3D('',#30644,#19761,#19762);
#16409=AXIS2_PLACEMENT_3D('',#30682,#19764,#19765);
#16410=AXIS2_PLACEMENT_3D('',#30718,#19767,#19768);
#16411=AXIS2_PLACEMENT_3D('',#30756,#19770,#19771);
#16412=AXIS2_PLACEMENT_3D('',#30793,#19773,#19774);
#16413=AXIS2_PLACEMENT_3D('',#30830,#19776,#19777);
#16414=AXIS2_PLACEMENT_3D('',#30867,#19779,#19780);
#16415=AXIS2_PLACEMENT_3D('',#30904,#19782,#19783);
#16416=AXIS2_PLACEMENT_3D('',#30942,#19785,#19786);
#16417=AXIS2_PLACEMENT_3D('',#30978,#19788,#19789);
#16418=AXIS2_PLACEMENT_3D('',#31016,#19791,#19792);
#16419=AXIS2_PLACEMENT_3D('',#31053,#19794,#19795);
#16420=AXIS2_PLACEMENT_3D('',#31090,#19797,#19798);
#16421=AXIS2_PLACEMENT_3D('',#31127,#19800,#19801);
#16422=AXIS2_PLACEMENT_3D('',#31164,#19803,#19804);
#16423=AXIS2_PLACEMENT_3D('',#31201,#19806,#19807);
#16424=AXIS2_PLACEMENT_3D('',#31238,#19809,#19810);
#16425=AXIS2_PLACEMENT_3D('',#31276,#19812,#19813);
#16426=AXIS2_PLACEMENT_3D('',#31313,#19815,#19816);
#16427=AXIS2_PLACEMENT_3D('',#31350,#19818,#19819);
#16428=AXIS2_PLACEMENT_3D('',#33401,#19821,#19822);
#16429=AXIS2_PLACEMENT_3D('',#33403,#19823,#19824);
#16430=AXIS2_PLACEMENT_3D('',#33404,#19825,#19826);
#16431=AXIS2_PLACEMENT_3D('',#33515,#19827,#19828);
#16432=AXIS2_PLACEMENT_3D('',#33516,#19829,#19830);
#16433=AXIS2_PLACEMENT_3D('',#35413,#19831,#19832);
#16434=AXIS2_PLACEMENT_3D('',#35422,#19837,#19838);
#16435=AXIS2_PLACEMENT_3D('',#35424,#19839,#19840);
#16436=AXIS2_PLACEMENT_3D('',#35426,#19842,#19843);
#16437=AXIS2_PLACEMENT_3D('',#35430,#19846,#19847);
#16438=AXIS2_PLACEMENT_3D('',#35431,#19848,#19849);
#16439=AXIS2_PLACEMENT_3D('',#35432,#19850,#19851);
#16440=AXIS2_PLACEMENT_3D('',#35441,#19856,#19857);
#16441=AXIS2_PLACEMENT_3D('',#35443,#19858,#19859);
#16442=AXIS2_PLACEMENT_3D('',#35445,#19861,#19862);
#16443=AXIS2_PLACEMENT_3D('',#35449,#19865,#19866);
#16444=AXIS2_PLACEMENT_3D('',#35450,#19867,#19868);
#16445=AXIS2_PLACEMENT_3D('',#35451,#19869,#19870);
#16446=AXIS2_PLACEMENT_3D('',#35460,#19875,#19876);
#16447=AXIS2_PLACEMENT_3D('',#35462,#19877,#19878);
#16448=AXIS2_PLACEMENT_3D('',#35464,#19880,#19881);
#16449=AXIS2_PLACEMENT_3D('',#35468,#19884,#19885);
#16450=AXIS2_PLACEMENT_3D('',#35469,#19886,#19887);
#16451=AXIS2_PLACEMENT_3D('',#35470,#19888,#19889);
#16452=AXIS2_PLACEMENT_3D('',#35479,#19894,#19895);
#16453=AXIS2_PLACEMENT_3D('',#35481,#19896,#19897);
#16454=AXIS2_PLACEMENT_3D('',#35483,#19899,#19900);
#16455=AXIS2_PLACEMENT_3D('',#35487,#19903,#19904);
#16456=AXIS2_PLACEMENT_3D('',#35488,#19905,#19906);
#16457=AXIS2_PLACEMENT_3D('',#35489,#19907,#19908);
#16458=AXIS2_PLACEMENT_3D('',#35498,#19913,#19914);
#16459=AXIS2_PLACEMENT_3D('',#35500,#19915,#19916);
#16460=AXIS2_PLACEMENT_3D('',#35502,#19918,#19919);
#16461=AXIS2_PLACEMENT_3D('',#35506,#19922,#19923);
#16462=AXIS2_PLACEMENT_3D('',#35507,#19924,#19925);
#16463=AXIS2_PLACEMENT_3D('',#35508,#19926,#19927);
#16464=AXIS2_PLACEMENT_3D('',#35517,#19932,#19933);
#16465=AXIS2_PLACEMENT_3D('',#35519,#19934,#19935);
#16466=AXIS2_PLACEMENT_3D('',#35521,#19937,#19938);
#16467=AXIS2_PLACEMENT_3D('',#35525,#19941,#19942);
#16468=AXIS2_PLACEMENT_3D('',#35526,#19943,#19944);
#16469=AXIS2_PLACEMENT_3D('',#35527,#19945,#19946);
#16470=AXIS2_PLACEMENT_3D('',#35536,#19951,#19952);
#16471=AXIS2_PLACEMENT_3D('',#35538,#19953,#19954);
#16472=AXIS2_PLACEMENT_3D('',#35540,#19956,#19957);
#16473=AXIS2_PLACEMENT_3D('',#35544,#19960,#19961);
#16474=AXIS2_PLACEMENT_3D('',#35545,#19962,#19963);
#16475=AXIS2_PLACEMENT_3D('',#35546,#19964,#19965);
#16476=AXIS2_PLACEMENT_3D('',#35555,#19970,#19971);
#16477=AXIS2_PLACEMENT_3D('',#35557,#19972,#19973);
#16478=AXIS2_PLACEMENT_3D('',#35559,#19975,#19976);
#16479=AXIS2_PLACEMENT_3D('',#35563,#19979,#19980);
#16480=AXIS2_PLACEMENT_3D('',#35564,#19981,#19982);
#16481=AXIS2_PLACEMENT_3D('',#35565,#19983,#19984);
#16482=AXIS2_PLACEMENT_3D('',#35574,#19989,#19990);
#16483=AXIS2_PLACEMENT_3D('',#35576,#19991,#19992);
#16484=AXIS2_PLACEMENT_3D('',#35578,#19994,#19995);
#16485=AXIS2_PLACEMENT_3D('',#35582,#19998,#19999);
#16486=AXIS2_PLACEMENT_3D('',#35583,#20000,#20001);
#16487=AXIS2_PLACEMENT_3D('',#35584,#20002,#20003);
#16488=AXIS2_PLACEMENT_3D('',#35593,#20008,#20009);
#16489=AXIS2_PLACEMENT_3D('',#35595,#20010,#20011);
#16490=AXIS2_PLACEMENT_3D('',#35597,#20013,#20014);
#16491=AXIS2_PLACEMENT_3D('',#35601,#20017,#20018);
#16492=AXIS2_PLACEMENT_3D('',#35602,#20019,#20020);
#16493=AXIS2_PLACEMENT_3D('',#35603,#20021,#20022);
#16494=AXIS2_PLACEMENT_3D('',#35612,#20027,#20028);
#16495=AXIS2_PLACEMENT_3D('',#35614,#20029,#20030);
#16496=AXIS2_PLACEMENT_3D('',#35616,#20032,#20033);
#16497=AXIS2_PLACEMENT_3D('',#35620,#20036,#20037);
#16498=AXIS2_PLACEMENT_3D('',#35621,#20038,#20039);
#16499=AXIS2_PLACEMENT_3D('',#35622,#20040,#20041);
#16500=AXIS2_PLACEMENT_3D('',#35631,#20046,#20047);
#16501=AXIS2_PLACEMENT_3D('',#35633,#20048,#20049);
#16502=AXIS2_PLACEMENT_3D('',#35635,#20051,#20052);
#16503=AXIS2_PLACEMENT_3D('',#35639,#20055,#20056);
#16504=AXIS2_PLACEMENT_3D('',#35640,#20057,#20058);
#16505=AXIS2_PLACEMENT_3D('',#35641,#20059,#20060);
#16506=AXIS2_PLACEMENT_3D('',#35650,#20065,#20066);
#16507=AXIS2_PLACEMENT_3D('',#35652,#20067,#20068);
#16508=AXIS2_PLACEMENT_3D('',#35654,#20070,#20071);
#16509=AXIS2_PLACEMENT_3D('',#35658,#20074,#20075);
#16510=AXIS2_PLACEMENT_3D('',#35659,#20076,#20077);
#16511=AXIS2_PLACEMENT_3D('',#35660,#20078,#20079);
#16512=AXIS2_PLACEMENT_3D('',#35669,#20084,#20085);
#16513=AXIS2_PLACEMENT_3D('',#35671,#20086,#20087);
#16514=AXIS2_PLACEMENT_3D('',#35673,#20089,#20090);
#16515=AXIS2_PLACEMENT_3D('',#35677,#20093,#20094);
#16516=AXIS2_PLACEMENT_3D('',#35678,#20095,#20096);
#16517=AXIS2_PLACEMENT_3D('',#35679,#20097,#20098);
#16518=AXIS2_PLACEMENT_3D('',#35688,#20103,#20104);
#16519=AXIS2_PLACEMENT_3D('',#35690,#20105,#20106);
#16520=AXIS2_PLACEMENT_3D('',#35692,#20108,#20109);
#16521=AXIS2_PLACEMENT_3D('',#35696,#20112,#20113);
#16522=AXIS2_PLACEMENT_3D('',#35697,#20114,#20115);
#16523=AXIS2_PLACEMENT_3D('',#35698,#20116,#20117);
#16524=AXIS2_PLACEMENT_3D('',#35707,#20122,#20123);
#16525=AXIS2_PLACEMENT_3D('',#35709,#20124,#20125);
#16526=AXIS2_PLACEMENT_3D('',#35711,#20127,#20128);
#16527=AXIS2_PLACEMENT_3D('',#35715,#20131,#20132);
#16528=AXIS2_PLACEMENT_3D('',#35716,#20133,#20134);
#16529=AXIS2_PLACEMENT_3D('',#35717,#20135,#20136);
#16530=AXIS2_PLACEMENT_3D('',#35726,#20141,#20142);
#16531=AXIS2_PLACEMENT_3D('',#35728,#20143,#20144);
#16532=AXIS2_PLACEMENT_3D('',#35730,#20146,#20147);
#16533=AXIS2_PLACEMENT_3D('',#35734,#20150,#20151);
#16534=AXIS2_PLACEMENT_3D('',#35735,#20152,#20153);
#16535=AXIS2_PLACEMENT_3D('',#35736,#20154,#20155);
#16536=AXIS2_PLACEMENT_3D('',#35745,#20160,#20161);
#16537=AXIS2_PLACEMENT_3D('',#35747,#20162,#20163);
#16538=AXIS2_PLACEMENT_3D('',#35750,#20165,#20166);
#16539=AXIS2_PLACEMENT_3D('',#35751,#20167,#20168);
#16540=AXIS2_PLACEMENT_3D('',#35755,#20171,#20172);
#16541=AXIS2_PLACEMENT_3D('',#35757,#20173,#20174);
#16542=AXIS2_PLACEMENT_3D('',#35758,#20175,#20176);
#16543=AXIS2_PLACEMENT_3D('',#35759,#20177,#20178);
#16544=AXIS2_PLACEMENT_3D('',#35768,#20183,#20184);
#16545=AXIS2_PLACEMENT_3D('',#35770,#20185,#20186);
#16546=AXIS2_PLACEMENT_3D('',#35772,#20188,#20189);
#16547=AXIS2_PLACEMENT_3D('',#35776,#20192,#20193);
#16548=AXIS2_PLACEMENT_3D('',#35777,#20194,#20195);
#16549=AXIS2_PLACEMENT_3D('',#35778,#20196,#20197);
#16550=AXIS2_PLACEMENT_3D('',#35787,#20202,#20203);
#16551=AXIS2_PLACEMENT_3D('',#35789,#20204,#20205);
#16552=AXIS2_PLACEMENT_3D('',#35791,#20207,#20208);
#16553=AXIS2_PLACEMENT_3D('',#35795,#20211,#20212);
#16554=AXIS2_PLACEMENT_3D('',#35796,#20213,#20214);
#16555=AXIS2_PLACEMENT_3D('',#35797,#20215,#20216);
#16556=AXIS2_PLACEMENT_3D('',#35806,#20221,#20222);
#16557=AXIS2_PLACEMENT_3D('',#35808,#20223,#20224);
#16558=AXIS2_PLACEMENT_3D('',#35810,#20226,#20227);
#16559=AXIS2_PLACEMENT_3D('',#35814,#20230,#20231);
#16560=AXIS2_PLACEMENT_3D('',#35815,#20232,#20233);
#16561=AXIS2_PLACEMENT_3D('',#35816,#20234,#20235);
#16562=AXIS2_PLACEMENT_3D('',#35825,#20240,#20241);
#16563=AXIS2_PLACEMENT_3D('',#35827,#20242,#20243);
#16564=AXIS2_PLACEMENT_3D('',#35829,#20245,#20246);
#16565=AXIS2_PLACEMENT_3D('',#35833,#20249,#20250);
#16566=AXIS2_PLACEMENT_3D('',#35834,#20251,#20252);
#16567=AXIS2_PLACEMENT_3D('',#35835,#20253,#20254);
#16568=AXIS2_PLACEMENT_3D('',#35844,#20259,#20260);
#16569=AXIS2_PLACEMENT_3D('',#35846,#20261,#20262);
#16570=AXIS2_PLACEMENT_3D('',#35848,#20264,#20265);
#16571=AXIS2_PLACEMENT_3D('',#35852,#20268,#20269);
#16572=AXIS2_PLACEMENT_3D('',#35853,#20270,#20271);
#16573=AXIS2_PLACEMENT_3D('',#35854,#20272,#20273);
#16574=AXIS2_PLACEMENT_3D('',#35863,#20278,#20279);
#16575=AXIS2_PLACEMENT_3D('',#35865,#20280,#20281);
#16576=AXIS2_PLACEMENT_3D('',#35867,#20283,#20284);
#16577=AXIS2_PLACEMENT_3D('',#35871,#20287,#20288);
#16578=AXIS2_PLACEMENT_3D('',#35872,#20289,#20290);
#16579=AXIS2_PLACEMENT_3D('',#35873,#20291,#20292);
#16580=AXIS2_PLACEMENT_3D('',#35882,#20297,#20298);
#16581=AXIS2_PLACEMENT_3D('',#35884,#20299,#20300);
#16582=AXIS2_PLACEMENT_3D('',#35886,#20302,#20303);
#16583=AXIS2_PLACEMENT_3D('',#35890,#20306,#20307);
#16584=AXIS2_PLACEMENT_3D('',#35891,#20308,#20309);
#16585=AXIS2_PLACEMENT_3D('',#35892,#20310,#20311);
#16586=AXIS2_PLACEMENT_3D('',#35901,#20316,#20317);
#16587=AXIS2_PLACEMENT_3D('',#35903,#20318,#20319);
#16588=AXIS2_PLACEMENT_3D('',#35905,#20321,#20322);
#16589=AXIS2_PLACEMENT_3D('',#35909,#20325,#20326);
#16590=AXIS2_PLACEMENT_3D('',#35910,#20327,#20328);
#16591=AXIS2_PLACEMENT_3D('',#35911,#20329,#20330);
#16592=AXIS2_PLACEMENT_3D('',#35920,#20335,#20336);
#16593=AXIS2_PLACEMENT_3D('',#35922,#20337,#20338);
#16594=AXIS2_PLACEMENT_3D('',#35924,#20340,#20341);
#16595=AXIS2_PLACEMENT_3D('',#35928,#20344,#20345);
#16596=AXIS2_PLACEMENT_3D('',#35929,#20346,#20347);
#16597=AXIS2_PLACEMENT_3D('',#35930,#20348,#20349);
#16598=AXIS2_PLACEMENT_3D('',#35939,#20354,#20355);
#16599=AXIS2_PLACEMENT_3D('',#35941,#20356,#20357);
#16600=AXIS2_PLACEMENT_3D('',#35943,#20359,#20360);
#16601=AXIS2_PLACEMENT_3D('',#35947,#20363,#20364);
#16602=AXIS2_PLACEMENT_3D('',#35948,#20365,#20366);
#16603=AXIS2_PLACEMENT_3D('',#35949,#20367,#20368);
#16604=AXIS2_PLACEMENT_3D('',#35958,#20373,#20374);
#16605=AXIS2_PLACEMENT_3D('',#35960,#20375,#20376);
#16606=AXIS2_PLACEMENT_3D('',#35962,#20378,#20379);
#16607=AXIS2_PLACEMENT_3D('',#35966,#20382,#20383);
#16608=AXIS2_PLACEMENT_3D('',#35967,#20384,#20385);
#16609=AXIS2_PLACEMENT_3D('',#35968,#20386,#20387);
#16610=AXIS2_PLACEMENT_3D('',#35977,#20392,#20393);
#16611=AXIS2_PLACEMENT_3D('',#35979,#20394,#20395);
#16612=AXIS2_PLACEMENT_3D('',#35981,#20397,#20398);
#16613=AXIS2_PLACEMENT_3D('',#35985,#20401,#20402);
#16614=AXIS2_PLACEMENT_3D('',#35986,#20403,#20404);
#16615=AXIS2_PLACEMENT_3D('',#35987,#20405,#20406);
#16616=AXIS2_PLACEMENT_3D('',#35996,#20411,#20412);
#16617=AXIS2_PLACEMENT_3D('',#35998,#20413,#20414);
#16618=AXIS2_PLACEMENT_3D('',#36000,#20416,#20417);
#16619=AXIS2_PLACEMENT_3D('',#36004,#20420,#20421);
#16620=AXIS2_PLACEMENT_3D('',#36005,#20422,#20423);
#16621=AXIS2_PLACEMENT_3D('',#36006,#20424,#20425);
#16622=AXIS2_PLACEMENT_3D('',#36015,#20430,#20431);
#16623=AXIS2_PLACEMENT_3D('',#36017,#20432,#20433);
#16624=AXIS2_PLACEMENT_3D('',#36019,#20435,#20436);
#16625=AXIS2_PLACEMENT_3D('',#36023,#20439,#20440);
#16626=AXIS2_PLACEMENT_3D('',#36024,#20441,#20442);
#16627=AXIS2_PLACEMENT_3D('',#36025,#20443,#20444);
#16628=AXIS2_PLACEMENT_3D('',#36034,#20449,#20450);
#16629=AXIS2_PLACEMENT_3D('',#36036,#20451,#20452);
#16630=AXIS2_PLACEMENT_3D('',#36038,#20454,#20455);
#16631=AXIS2_PLACEMENT_3D('',#36042,#20458,#20459);
#16632=AXIS2_PLACEMENT_3D('',#36043,#20460,#20461);
#16633=AXIS2_PLACEMENT_3D('',#36044,#20462,#20463);
#16634=AXIS2_PLACEMENT_3D('',#36053,#20468,#20469);
#16635=AXIS2_PLACEMENT_3D('',#36055,#20470,#20471);
#16636=AXIS2_PLACEMENT_3D('',#36057,#20473,#20474);
#16637=AXIS2_PLACEMENT_3D('',#36061,#20477,#20478);
#16638=AXIS2_PLACEMENT_3D('',#36062,#20479,#20480);
#16639=AXIS2_PLACEMENT_3D('',#36063,#20481,#20482);
#16640=AXIS2_PLACEMENT_3D('',#36072,#20487,#20488);
#16641=AXIS2_PLACEMENT_3D('',#36074,#20489,#20490);
#16642=AXIS2_PLACEMENT_3D('',#36076,#20492,#20493);
#16643=AXIS2_PLACEMENT_3D('',#36080,#20496,#20497);
#16644=AXIS2_PLACEMENT_3D('',#36081,#20498,#20499);
#16645=AXIS2_PLACEMENT_3D('',#36082,#20500,#20501);
#16646=AXIS2_PLACEMENT_3D('',#36091,#20506,#20507);
#16647=AXIS2_PLACEMENT_3D('',#36093,#20508,#20509);
#16648=AXIS2_PLACEMENT_3D('',#36095,#20511,#20512);
#16649=AXIS2_PLACEMENT_3D('',#36099,#20515,#20516);
#16650=AXIS2_PLACEMENT_3D('',#36100,#20517,#20518);
#16651=AXIS2_PLACEMENT_3D('',#36101,#20519,#20520);
#16652=AXIS2_PLACEMENT_3D('',#36110,#20525,#20526);
#16653=AXIS2_PLACEMENT_3D('',#36116,#20530,#20531);
#16654=AXIS2_PLACEMENT_3D('',#36122,#20535,#20536);
#16655=AXIS2_PLACEMENT_3D('',#36128,#20540,#20541);
#16656=AXIS2_PLACEMENT_3D('',#36134,#20545,#20546);
#16657=AXIS2_PLACEMENT_3D('',#36137,#20549,#20550);
#16658=AXIS2_PLACEMENT_3D('',#36138,#20551,#20552);
#16659=AXIS2_PLACEMENT_3D('',#36140,#20553,#20554);
#16660=AXIS2_PLACEMENT_3D('',#36141,#20555,#20556);
#16661=AXIS2_PLACEMENT_3D('',#36143,#20558,#20559);
#16662=AXIS2_PLACEMENT_3D('',#36144,#20560,#20561);
#16663=AXIS2_PLACEMENT_3D('',#36145,#20562,#20563);
#16664=AXIS2_PLACEMENT_3D('',#36147,#20564,#20565);
#16665=AXIS2_PLACEMENT_3D('',#36148,#20566,#20567);
#16666=AXIS2_PLACEMENT_3D('',#36150,#20568,#20569);
#16667=AXIS2_PLACEMENT_3D('',#36153,#20572,#20573);
#16668=AXIS2_PLACEMENT_3D('',#36155,#20574,#20575);
#16669=AXIS2_PLACEMENT_3D('',#36157,#20577,#20578);
#19611=DIRECTION('axis',(0.,0.,1.));
#19612=DIRECTION('refdir',(1.,0.,0.));
#19613=DIRECTION('center_axis',(1.,0.,0.));
#19614=DIRECTION('ref_axis',(0.,1.,0.));
#19615=DIRECTION('',(-1.,0.,0.));
#19616=DIRECTION('center_axis',(1.,0.,0.));
#19617=DIRECTION('ref_axis',(0.,1.,0.));
#19618=DIRECTION('center_axis',(1.,0.,0.));
#19619=DIRECTION('ref_axis',(0.,1.,0.));
#19620=DIRECTION('',(-1.,0.,0.));
#19621=DIRECTION('center_axis',(1.,0.,0.));
#19622=DIRECTION('ref_axis',(0.,1.,0.));
#19623=DIRECTION('',(-1.,0.,0.));
#19624=DIRECTION('center_axis',(1.,0.,0.));
#19625=DIRECTION('ref_axis',(0.,1.,0.));
#19626=DIRECTION('',(-1.,0.,0.));
#19627=DIRECTION('center_axis',(1.,0.,0.));
#19628=DIRECTION('ref_axis',(0.,1.,0.));
#19629=DIRECTION('',(-1.,0.,0.));
#19630=DIRECTION('center_axis',(1.,0.,0.));
#19631=DIRECTION('ref_axis',(0.,1.,0.));
#19632=DIRECTION('',(-1.,0.,0.));
#19633=DIRECTION('center_axis',(1.,0.,0.));
#19634=DIRECTION('ref_axis',(0.,1.,0.));
#19635=DIRECTION('',(-1.,0.,0.));
#19636=DIRECTION('center_axis',(1.,0.,0.));
#19637=DIRECTION('ref_axis',(0.,1.,0.));
#19638=DIRECTION('',(-1.,0.,0.));
#19639=DIRECTION('center_axis',(1.,0.,0.));
#19640=DIRECTION('ref_axis',(0.,1.,0.));
#19641=DIRECTION('',(-1.,0.,0.));
#19642=DIRECTION('center_axis',(1.,0.,0.));
#19643=DIRECTION('ref_axis',(0.,1.,0.));
#19644=DIRECTION('',(-1.,0.,0.));
#19645=DIRECTION('center_axis',(1.,0.,0.));
#19646=DIRECTION('ref_axis',(0.,1.,0.));
#19647=DIRECTION('',(-1.,0.,0.));
#19648=DIRECTION('center_axis',(1.,0.,0.));
#19649=DIRECTION('ref_axis',(0.,1.,0.));
#19650=DIRECTION('',(-1.,0.,0.));
#19651=DIRECTION('center_axis',(1.,0.,0.));
#19652=DIRECTION('ref_axis',(0.,1.,0.));
#19653=DIRECTION('',(-1.,0.,0.));
#19654=DIRECTION('center_axis',(1.,0.,0.));
#19655=DIRECTION('ref_axis',(0.,1.,0.));
#19656=DIRECTION('',(-1.,0.,0.));
#19657=DIRECTION('center_axis',(1.,0.,0.));
#19658=DIRECTION('ref_axis',(0.,1.,0.));
#19659=DIRECTION('',(-1.,0.,0.));
#19660=DIRECTION('center_axis',(1.,0.,0.));
#19661=DIRECTION('ref_axis',(0.,1.,0.));
#19662=DIRECTION('',(-1.,0.,0.));
#19663=DIRECTION('center_axis',(1.,0.,0.));
#19664=DIRECTION('ref_axis',(0.,1.,0.));
#19665=DIRECTION('',(-1.,0.,0.));
#19666=DIRECTION('center_axis',(1.,0.,0.));
#19667=DIRECTION('ref_axis',(0.,1.,0.));
#19668=DIRECTION('',(-1.,0.,0.));
#19669=DIRECTION('center_axis',(1.,0.,0.));
#19670=DIRECTION('ref_axis',(0.,1.,0.));
#19671=DIRECTION('',(-1.,0.,0.));
#19672=DIRECTION('center_axis',(1.,0.,0.));
#19673=DIRECTION('ref_axis',(0.,1.,0.));
#19674=DIRECTION('',(-1.,0.,0.));
#19675=DIRECTION('center_axis',(1.,0.,0.));
#19676=DIRECTION('ref_axis',(0.,1.,0.));
#19677=DIRECTION('',(-1.,0.,0.));
#19678=DIRECTION('center_axis',(1.,0.,0.));
#19679=DIRECTION('ref_axis',(0.,1.,0.));
#19680=DIRECTION('',(-1.,0.,0.));
#19681=DIRECTION('center_axis',(1.,0.,0.));
#19682=DIRECTION('ref_axis',(0.,1.,0.));
#19683=DIRECTION('',(-1.,0.,0.));
#19684=DIRECTION('center_axis',(1.,0.,0.));
#19685=DIRECTION('ref_axis',(0.,1.,0.));
#19686=DIRECTION('',(-1.,0.,0.));
#19687=DIRECTION('center_axis',(1.,0.,0.));
#19688=DIRECTION('ref_axis',(0.,1.,0.));
#19689=DIRECTION('',(-1.,0.,0.));
#19690=DIRECTION('center_axis',(1.,0.,0.));
#19691=DIRECTION('ref_axis',(0.,1.,0.));
#19692=DIRECTION('',(-1.,0.,0.));
#19693=DIRECTION('center_axis',(1.,0.,0.));
#19694=DIRECTION('ref_axis',(0.,1.,0.));
#19695=DIRECTION('',(-1.,0.,0.));
#19696=DIRECTION('center_axis',(1.,0.,0.));
#19697=DIRECTION('ref_axis',(0.,1.,0.));
#19698=DIRECTION('',(-1.,0.,0.));
#19699=DIRECTION('center_axis',(1.,0.,0.));
#19700=DIRECTION('ref_axis',(0.,1.,0.));
#19701=DIRECTION('',(-1.,0.,0.));
#19702=DIRECTION('center_axis',(1.,0.,0.));
#19703=DIRECTION('ref_axis',(0.,1.,0.));
#19704=DIRECTION('',(-1.,0.,0.));
#19705=DIRECTION('center_axis',(1.,0.,0.));
#19706=DIRECTION('ref_axis',(0.,1.,0.));
#19707=DIRECTION('',(-1.,0.,0.));
#19708=DIRECTION('center_axis',(1.,0.,0.));
#19709=DIRECTION('ref_axis',(0.,1.,0.));
#19710=DIRECTION('',(-1.,0.,0.));
#19711=DIRECTION('center_axis',(1.,0.,0.));
#19712=DIRECTION('ref_axis',(0.,1.,0.));
#19713=DIRECTION('',(-1.,0.,0.));
#19714=DIRECTION('center_axis',(1.,0.,0.));
#19715=DIRECTION('ref_axis',(0.,1.,0.));
#19716=DIRECTION('',(-1.,0.,0.));
#19717=DIRECTION('center_axis',(1.,0.,0.));
#19718=DIRECTION('ref_axis',(0.,-0.320272933918672,-0.947325312550618));
#19719=DIRECTION('',(1.,0.,0.));
#19720=DIRECTION('center_axis',(1.,0.,0.));
#19721=DIRECTION('ref_axis',(0.,1.,-2.86062230339267E-13));
#19722=DIRECTION('center_axis',(1.,0.,0.));
#19723=DIRECTION('ref_axis',(0.,1.,-2.86062230339267E-13));
#19724=DIRECTION('',(1.,0.,0.));
#19725=DIRECTION('center_axis',(1.,0.,0.));
#19726=DIRECTION('ref_axis',(0.,1.,-2.86062230339267E-13));
#19727=DIRECTION('',(1.,0.,0.));
#19728=DIRECTION('center_axis',(1.,0.,0.));
#19729=DIRECTION('ref_axis',(0.,1.,-2.86062230339267E-13));
#19730=DIRECTION('',(1.,0.,0.));
#19731=DIRECTION('center_axis',(1.,0.,0.));
#19732=DIRECTION('ref_axis',(0.,1.,-2.86062230339267E-13));
#19733=DIRECTION('',(1.,0.,0.));
#19734=DIRECTION('center_axis',(1.,0.,0.));
#19735=DIRECTION('ref_axis',(0.,1.,-2.86062230339267E-13));
#19736=DIRECTION('',(1.,0.,0.));
#19737=DIRECTION('center_axis',(1.,0.,0.));
#19738=DIRECTION('ref_axis',(0.,1.,-2.86062230339267E-13));
#19739=DIRECTION('',(1.,0.,0.));
#19740=DIRECTION('center_axis',(1.,0.,0.));
#19741=DIRECTION('ref_axis',(0.,1.,-2.86062230339267E-13));
#19742=DIRECTION('',(1.,0.,0.));
#19743=DIRECTION('center_axis',(1.,0.,0.));
#19744=DIRECTION('ref_axis',(0.,1.,-2.86062230339267E-13));
#19745=DIRECTION('',(1.,0.,0.));
#19746=DIRECTION('center_axis',(1.,0.,0.));
#19747=DIRECTION('ref_axis',(0.,1.,-2.86062230339267E-13));
#19748=DIRECTION('',(1.,0.,0.));
#19749=DIRECTION('center_axis',(1.,0.,0.));
#19750=DIRECTION('ref_axis',(0.,1.,-2.86062230339267E-13));
#19751=DIRECTION('',(1.,0.,0.));
#19752=DIRECTION('center_axis',(1.,0.,0.));
#19753=DIRECTION('ref_axis',(0.,1.,-2.86062230339267E-13));
#19754=DIRECTION('',(1.,0.,0.));
#19755=DIRECTION('center_axis',(1.,0.,0.));
#19756=DIRECTION('ref_axis',(0.,1.,-2.86062230339267E-13));
#19757=DIRECTION('',(1.,0.,0.));
#19758=DIRECTION('center_axis',(1.,0.,0.));
#19759=DIRECTION('ref_axis',(0.,1.,-2.86062230339267E-13));
#19760=DIRECTION('',(1.,0.,0.));
#19761=DIRECTION('center_axis',(1.,0.,0.));
#19762=DIRECTION('ref_axis',(0.,1.,-2.86062230339267E-13));
#19763=DIRECTION('',(1.,0.,0.));
#19764=DIRECTION('center_axis',(1.,0.,0.));
#19765=DIRECTION('ref_axis',(0.,1.,-2.86062230339267E-13));
#19766=DIRECTION('',(1.,0.,0.));
#19767=DIRECTION('center_axis',(1.,0.,0.));
#19768=DIRECTION('ref_axis',(0.,1.,-2.86062230339267E-13));
#19769=DIRECTION('',(1.,0.,0.));
#19770=DIRECTION('center_axis',(1.,0.,0.));
#19771=DIRECTION('ref_axis',(0.,1.,-2.86062230339267E-13));
#19772=DIRECTION('',(1.,0.,0.));
#19773=DIRECTION('center_axis',(1.,0.,0.));
#19774=DIRECTION('ref_axis',(0.,1.,-2.86062230339267E-13));
#19775=DIRECTION('',(1.,0.,0.));
#19776=DIRECTION('center_axis',(1.,0.,0.));
#19777=DIRECTION('ref_axis',(0.,1.,-2.86062230339267E-13));
#19778=DIRECTION('',(1.,0.,0.));
#19779=DIRECTION('center_axis',(1.,0.,0.));
#19780=DIRECTION('ref_axis',(0.,1.,-2.86062230339267E-13));
#19781=DIRECTION('',(1.,0.,0.));
#19782=DIRECTION('center_axis',(1.,0.,0.));
#19783=DIRECTION('ref_axis',(0.,1.,-2.86062230339267E-13));
#19784=DIRECTION('',(1.,0.,0.));
#19785=DIRECTION('center_axis',(1.,0.,0.));
#19786=DIRECTION('ref_axis',(0.,1.,-2.86062230339267E-13));
#19787=DIRECTION('',(1.,0.,0.));
#19788=DIRECTION('center_axis',(1.,0.,0.));
#19789=DIRECTION('ref_axis',(0.,1.,-2.86062230339267E-13));
#19790=DIRECTION('',(1.,0.,0.));
#19791=DIRECTION('center_axis',(1.,0.,0.));
#19792=DIRECTION('ref_axis',(0.,1.,-2.86062230339267E-13));
#19793=DIRECTION('',(1.,0.,0.));
#19794=DIRECTION('center_axis',(1.,0.,0.));
#19795=DIRECTION('ref_axis',(0.,1.,-2.86062230339267E-13));
#19796=DIRECTION('',(1.,0.,0.));
#19797=DIRECTION('center_axis',(1.,0.,0.));
#19798=DIRECTION('ref_axis',(0.,1.,-2.86062230339267E-13));
#19799=DIRECTION('',(1.,0.,0.));
#19800=DIRECTION('center_axis',(1.,0.,0.));
#19801=DIRECTION('ref_axis',(0.,1.,-2.86062230339267E-13));
#19802=DIRECTION('',(1.,0.,0.));
#19803=DIRECTION('center_axis',(1.,0.,0.));
#19804=DIRECTION('ref_axis',(0.,1.,-2.86062230339267E-13));
#19805=DIRECTION('',(1.,0.,0.));
#19806=DIRECTION('center_axis',(1.,0.,0.));
#19807=DIRECTION('ref_axis',(0.,1.,-2.86062230339267E-13));
#19808=DIRECTION('',(1.,0.,0.));
#19809=DIRECTION('center_axis',(1.,0.,0.));
#19810=DIRECTION('ref_axis',(0.,1.,-2.86062230339267E-13));
#19811=DIRECTION('',(1.,0.,0.));
#19812=DIRECTION('center_axis',(1.,0.,0.));
#19813=DIRECTION('ref_axis',(0.,1.,-2.86062230339267E-13));
#19814=DIRECTION('',(1.,0.,0.));
#19815=DIRECTION('center_axis',(1.,0.,0.));
#19816=DIRECTION('ref_axis',(0.,1.,-2.86062230339267E-13));
#19817=DIRECTION('',(1.,0.,0.));
#19818=DIRECTION('center_axis',(1.,0.,0.));
#19819=DIRECTION('ref_axis',(0.,1.,-2.86062230339267E-13));
#19820=DIRECTION('',(1.,0.,0.));
#19821=DIRECTION('center_axis',(1.,0.,0.));
#19822=DIRECTION('ref_axis',(0.,0.,-1.));
#19823=DIRECTION('center_axis',(1.,0.,0.));
#19824=DIRECTION('ref_axis',(0.,1.,0.));
#19825=DIRECTION('center_axis',(1.,0.,0.));
#19826=DIRECTION('ref_axis',(0.,1.,0.));
#19827=DIRECTION('center_axis',(-1.,0.,0.));
#19828=DIRECTION('ref_axis',(0.,1.,-2.86062230339267E-13));
#19829=DIRECTION('center_axis',(1.,0.,0.));
#19830=DIRECTION('ref_axis',(0.,0.889074354998743,0.457762811162691));
#19831=DIRECTION('center_axis',(0.,-0.45196610967378,0.892035109009925));
#19832=DIRECTION('ref_axis',(0.,-0.892035109009925,-0.45196610967378));
#19833=DIRECTION('',(-1.,0.,0.));
#19834=DIRECTION('',(0.,-0.892035109009925,-0.45196610967378));
#19835=DIRECTION('',(1.,0.,0.));
#19836=DIRECTION('',(0.,-0.892035109009925,-0.45196610967378));
#19837=DIRECTION('center_axis',(1.,0.,0.));
#19838=DIRECTION('ref_axis',(0.,-0.17364817766693,-0.984807753012208));
#19839=DIRECTION('center_axis',(-1.,0.,0.));
#19840=DIRECTION('ref_axis',(0.,1.,0.));
#19841=DIRECTION('',(0.,0.683657295809609,-0.729803193940869));
#19842=DIRECTION('center_axis',(0.,-0.729803193940869,-0.683657295809609));
#19843=DIRECTION('ref_axis',(0.,0.683657295809609,-0.729803193940869));
#19844=DIRECTION('',(1.,0.,0.));
#19845=DIRECTION('',(0.,0.683657295809609,-0.729803193940869));
#19846=DIRECTION('center_axis',(1.,0.,0.));
#19847=DIRECTION('ref_axis',(0.,-0.17364817766693,-0.984807753012208));
#19848=DIRECTION('center_axis',(1.,0.,0.));
#19849=DIRECTION('ref_axis',(0.,1.,0.));
#19850=DIRECTION('center_axis',(0.,-0.290199457811009,0.956966182624128));
#19851=DIRECTION('ref_axis',(0.,-0.956966182624128,-0.290199457811009));
#19852=DIRECTION('',(-1.,0.,0.));
#19853=DIRECTION('',(0.,-0.956966182624128,-0.290199457811009));
#19854=DIRECTION('',(1.,0.,0.));
#19855=DIRECTION('',(0.,-0.956966182624128,-0.290199457811009));
#19856=DIRECTION('center_axis',(1.,0.,0.));
#19857=DIRECTION('ref_axis',(0.,-0.342020143325669,-0.939692620785908));
#19858=DIRECTION('center_axis',(-1.,0.,0.));
#19859=DIRECTION('ref_axis',(0.,1.,0.));
#19860=DIRECTION('',(0.,0.546542010633325,-0.83743168713208));
#19861=DIRECTION('center_axis',(0.,-0.83743168713208,-0.546542010633325));
#19862=DIRECTION('ref_axis',(0.,0.546542010633325,-0.83743168713208));
#19863=DIRECTION('',(1.,0.,0.));
#19864=DIRECTION('',(0.,0.546542010633325,-0.83743168713208));
#19865=DIRECTION('center_axis',(1.,0.,0.));
#19866=DIRECTION('ref_axis',(0.,-0.342020143325669,-0.939692620785908));
#19867=DIRECTION('center_axis',(1.,0.,0.));
#19868=DIRECTION('ref_axis',(0.,1.,0.));
#19869=DIRECTION('center_axis',(0.,-0.119615242270662,0.992820323027551));
#19870=DIRECTION('ref_axis',(0.,-0.992820323027551,-0.119615242270662));
#19871=DIRECTION('',(-1.,0.,0.));
#19872=DIRECTION('',(0.,-0.992820323027551,-0.119615242270662));
#19873=DIRECTION('',(1.,0.,0.));
#19874=DIRECTION('',(0.,-0.992820323027551,-0.119615242270662));
#19875=DIRECTION('center_axis',(1.,0.,0.));
#19876=DIRECTION('ref_axis',(0.,-0.5,-0.866025403784438));
#19877=DIRECTION('center_axis',(-1.,0.,0.));
#19878=DIRECTION('ref_axis',(0.,1.,0.));
#19879=DIRECTION('',(0.,0.392820323027551,-0.919615242270663));
#19880=DIRECTION('center_axis',(0.,-0.919615242270663,-0.392820323027551));
#19881=DIRECTION('ref_axis',(0.,0.392820323027551,-0.919615242270663));
#19882=DIRECTION('',(1.,0.,0.));
#19883=DIRECTION('',(0.,0.392820323027551,-0.919615242270663));
#19884=DIRECTION('center_axis',(1.,0.,0.));
#19885=DIRECTION('ref_axis',(0.,-0.5,-0.866025403784438));
#19886=DIRECTION('center_axis',(1.,0.,0.));
#19887=DIRECTION('ref_axis',(0.,1.,0.));
#19888=DIRECTION('center_axis',(0.,0.0546034218778454,0.998508120307106));
#19889=DIRECTION('ref_axis',(0.,-0.998508120307106,0.0546034218778454));
#19890=DIRECTION('',(-1.,0.,0.));
#19891=DIRECTION('',(0.,-0.998508120307106,0.0546034218778454));
#19892=DIRECTION('',(1.,0.,0.));
#19893=DIRECTION('',(0.,-0.998508120307106,0.0546034218778454));
#19894=DIRECTION('center_axis',(1.,0.,0.));
#19895=DIRECTION('ref_axis',(0.,-0.64278760968654,-0.766044443118978));
#19896=DIRECTION('center_axis',(-1.,0.,0.));
#19897=DIRECTION('ref_axis',(0.,1.,0.));
#19898=DIRECTION('',(0.,0.227162988683259,-0.973856753620618));
#19899=DIRECTION('center_axis',(0.,-0.973856753620618,-0.227162988683259));
#19900=DIRECTION('ref_axis',(0.,0.227162988683259,-0.973856753620618));
#19901=DIRECTION('',(1.,0.,0.));
#19902=DIRECTION('',(0.,0.227162988683259,-0.973856753620618));
#19903=DIRECTION('center_axis',(1.,0.,0.));
#19904=DIRECTION('ref_axis',(0.,-0.64278760968654,-0.766044443118978));
#19905=DIRECTION('center_axis',(1.,0.,0.));
#19906=DIRECTION('ref_axis',(0.,1.,0.));
#19907=DIRECTION('center_axis',(0.,0.227162988683259,0.973856753620618));
#19908=DIRECTION('ref_axis',(0.,-0.973856753620618,0.227162988683259));
#19909=DIRECTION('',(-1.,0.,0.));
#19910=DIRECTION('',(0.,-0.973856753620618,0.227162988683259));
#19911=DIRECTION('',(1.,0.,0.));
#19912=DIRECTION('',(0.,-0.973856753620618,0.227162988683259));
#19913=DIRECTION('center_axis',(1.,0.,0.));
#19914=DIRECTION('ref_axis',(0.,-0.766044443118978,-0.642787609686539));
#19915=DIRECTION('center_axis',(-1.,0.,0.));
#19916=DIRECTION('ref_axis',(0.,1.,0.));
#19917=DIRECTION('',(0.,0.054603421877845,-0.998508120307106));
#19918=DIRECTION('center_axis',(0.,-0.998508120307106,-0.054603421877845));
#19919=DIRECTION('ref_axis',(0.,0.054603421877845,-0.998508120307106));
#19920=DIRECTION('',(1.,0.,0.));
#19921=DIRECTION('',(0.,0.054603421877845,-0.998508120307106));
#19922=DIRECTION('center_axis',(1.,0.,0.));
#19923=DIRECTION('ref_axis',(0.,-0.766044443118978,-0.642787609686539));
#19924=DIRECTION('center_axis',(1.,0.,0.));
#19925=DIRECTION('ref_axis',(0.,1.,0.));
#19926=DIRECTION('center_axis',(0.,0.392820323027551,0.919615242270663));
#19927=DIRECTION('ref_axis',(0.,-0.919615242270663,0.392820323027551));
#19928=DIRECTION('',(-1.,0.,0.));
#19929=DIRECTION('',(0.,-0.919615242270663,0.392820323027551));
#19930=DIRECTION('',(1.,0.,0.));
#19931=DIRECTION('',(0.,-0.919615242270663,0.392820323027551));
#19932=DIRECTION('center_axis',(1.,0.,0.));
#19933=DIRECTION('ref_axis',(0.,-0.866025403784439,-0.5));
#19934=DIRECTION('center_axis',(-1.,0.,0.));
#19935=DIRECTION('ref_axis',(0.,1.,0.));
#19936=DIRECTION('',(0.,-0.119615242270663,-0.992820323027551));
#19937=DIRECTION('center_axis',(0.,-0.992820323027551,0.119615242270663));
#19938=DIRECTION('ref_axis',(0.,-0.119615242270663,-0.992820323027551));
#19939=DIRECTION('',(1.,0.,0.));
#19940=DIRECTION('',(0.,-0.119615242270663,-0.992820323027551));
#19941=DIRECTION('center_axis',(1.,0.,0.));
#19942=DIRECTION('ref_axis',(0.,-0.866025403784439,-0.5));
#19943=DIRECTION('center_axis',(1.,0.,0.));
#19944=DIRECTION('ref_axis',(0.,1.,0.));
#19945=DIRECTION('center_axis',(0.,0.546542010633326,0.837431687132079));
#19946=DIRECTION('ref_axis',(0.,-0.837431687132079,0.546542010633326));
#19947=DIRECTION('',(-1.,0.,0.));
#19948=DIRECTION('',(0.,-0.837431687132079,0.546542010633326));
#19949=DIRECTION('',(1.,0.,0.));
#19950=DIRECTION('',(0.,-0.837431687132079,0.546542010633326));
#19951=DIRECTION('center_axis',(1.,0.,0.));
#19952=DIRECTION('ref_axis',(0.,-0.939692620785909,-0.342020143325668));
#19953=DIRECTION('center_axis',(-1.,0.,0.));
#19954=DIRECTION('ref_axis',(0.,1.,0.));
#19955=DIRECTION('',(0.,-0.29019945781101,-0.956966182624128));
#19956=DIRECTION('center_axis',(0.,-0.956966182624128,0.29019945781101));
#19957=DIRECTION('ref_axis',(0.,-0.29019945781101,-0.956966182624128));
#19958=DIRECTION('',(1.,0.,0.));
#19959=DIRECTION('',(0.,-0.29019945781101,-0.956966182624128));
#19960=DIRECTION('center_axis',(1.,0.,0.));
#19961=DIRECTION('ref_axis',(0.,-0.939692620785909,-0.342020143325668));
#19962=DIRECTION('center_axis',(1.,0.,0.));
#19963=DIRECTION('ref_axis',(0.,1.,0.));
#19964=DIRECTION('center_axis',(0.,0.683657295809609,0.729803193940869));
#19965=DIRECTION('ref_axis',(0.,-0.729803193940869,0.683657295809609));
#19966=DIRECTION('',(-1.,0.,0.));
#19967=DIRECTION('',(0.,-0.729803193940869,0.683657295809609));
#19968=DIRECTION('',(1.,0.,0.));
#19969=DIRECTION('',(0.,-0.729803193940869,0.683657295809609));
#19970=DIRECTION('center_axis',(1.,0.,0.));
#19971=DIRECTION('ref_axis',(0.,-0.984807753012208,-0.17364817766693));
#19972=DIRECTION('center_axis',(-1.,0.,0.));
#19973=DIRECTION('ref_axis',(0.,1.,0.));
#19974=DIRECTION('',(0.,-0.45196610967378,-0.892035109009925));
#19975=DIRECTION('center_axis',(0.,-0.892035109009925,0.451966109673781));
#19976=DIRECTION('ref_axis',(0.,-0.45196610967378,-0.892035109009925));
#19977=DIRECTION('',(1.,0.,0.));
#19978=DIRECTION('',(0.,-0.45196610967378,-0.892035109009925));
#19979=DIRECTION('center_axis',(1.,0.,0.));
#19980=DIRECTION('ref_axis',(0.,-0.984807753012208,-0.17364817766693));
#19981=DIRECTION('center_axis',(1.,0.,0.));
#19982=DIRECTION('ref_axis',(0.,1.,0.));
#19983=DIRECTION('center_axis',(0.,0.8,0.6));
#19984=DIRECTION('ref_axis',(0.,-0.6,0.8));
#19985=DIRECTION('',(-1.,0.,0.));
#19986=DIRECTION('',(0.,-0.6,0.8));
#19987=DIRECTION('',(1.,0.,0.));
#19988=DIRECTION('',(0.,-0.6,0.8));
#19989=DIRECTION('center_axis',(1.,0.,0.));
#19990=DIRECTION('ref_axis',(0.,-1.,1.83697019872103E-16));
#19991=DIRECTION('center_axis',(-1.,0.,0.));
#19992=DIRECTION('ref_axis',(0.,1.,0.));
#19993=DIRECTION('',(0.,-0.6,-0.8));
#19994=DIRECTION('center_axis',(0.,-0.8,0.6));
#19995=DIRECTION('ref_axis',(0.,-0.6,-0.8));
#19996=DIRECTION('',(1.,0.,0.));
#19997=DIRECTION('',(0.,-0.6,-0.8));
#19998=DIRECTION('center_axis',(1.,0.,0.));
#19999=DIRECTION('ref_axis',(0.,-1.,1.83697019872103E-16));
#20000=DIRECTION('center_axis',(1.,0.,0.));
#20001=DIRECTION('ref_axis',(0.,1.,0.));
#20002=DIRECTION('center_axis',(0.,0.892035109009925,0.45196610967378));
#20003=DIRECTION('ref_axis',(0.,-0.45196610967378,0.892035109009925));
#20004=DIRECTION('',(-1.,0.,0.));
#20005=DIRECTION('',(0.,-0.45196610967378,0.892035109009925));
#20006=DIRECTION('',(1.,0.,0.));
#20007=DIRECTION('',(0.,-0.45196610967378,0.892035109009925));
#20008=DIRECTION('center_axis',(1.,0.,0.));
#20009=DIRECTION('ref_axis',(0.,-0.984807753012208,0.17364817766693));
#20010=DIRECTION('center_axis',(-1.,0.,0.));
#20011=DIRECTION('ref_axis',(0.,1.,0.));
#20012=DIRECTION('',(0.,-0.729803193940869,-0.683657295809609));
#20013=DIRECTION('center_axis',(0.,-0.683657295809609,0.729803193940869));
#20014=DIRECTION('ref_axis',(0.,-0.729803193940869,-0.683657295809609));
#20015=DIRECTION('',(1.,0.,0.));
#20016=DIRECTION('',(0.,-0.729803193940869,-0.683657295809609));
#20017=DIRECTION('center_axis',(1.,0.,0.));
#20018=DIRECTION('ref_axis',(0.,-0.984807753012208,0.17364817766693));
#20019=DIRECTION('center_axis',(1.,0.,0.));
#20020=DIRECTION('ref_axis',(0.,1.,0.));
#20021=DIRECTION('center_axis',(0.,0.956966182624128,0.290199457811009));
#20022=DIRECTION('ref_axis',(0.,-0.290199457811009,0.956966182624128));
#20023=DIRECTION('',(-1.,0.,0.));
#20024=DIRECTION('',(0.,-0.290199457811009,0.956966182624128));
#20025=DIRECTION('',(1.,0.,0.));
#20026=DIRECTION('',(0.,-0.290199457811009,0.956966182624128));
#20027=DIRECTION('center_axis',(1.,0.,0.));
#20028=DIRECTION('ref_axis',(0.,-0.939692620785908,0.342020143325669));
#20029=DIRECTION('center_axis',(-1.,0.,0.));
#20030=DIRECTION('ref_axis',(0.,1.,0.));
#20031=DIRECTION('',(0.,-0.83743168713208,-0.546542010633325));
#20032=DIRECTION('center_axis',(0.,-0.546542010633325,0.83743168713208));
#20033=DIRECTION('ref_axis',(0.,-0.83743168713208,-0.546542010633325));
#20034=DIRECTION('',(1.,0.,0.));
#20035=DIRECTION('',(0.,-0.83743168713208,-0.546542010633325));
#20036=DIRECTION('center_axis',(1.,0.,0.));
#20037=DIRECTION('ref_axis',(0.,-0.939692620785908,0.342020143325669));
#20038=DIRECTION('center_axis',(1.,0.,0.));
#20039=DIRECTION('ref_axis',(0.,1.,0.));
#20040=DIRECTION('center_axis',(0.,0.992820323027551,0.119615242270662));
#20041=DIRECTION('ref_axis',(0.,-0.119615242270662,0.992820323027551));
#20042=DIRECTION('',(-1.,0.,0.));
#20043=DIRECTION('',(0.,-0.119615242270662,0.992820323027551));
#20044=DIRECTION('',(1.,0.,0.));
#20045=DIRECTION('',(0.,-0.119615242270662,0.992820323027551));
#20046=DIRECTION('center_axis',(1.,0.,0.));
#20047=DIRECTION('ref_axis',(0.,-0.866025403784438,0.5));
#20048=DIRECTION('center_axis',(-1.,0.,0.));
#20049=DIRECTION('ref_axis',(0.,1.,0.));
#20050=DIRECTION('',(0.,-0.919615242270663,-0.392820323027551));
#20051=DIRECTION('center_axis',(0.,-0.392820323027551,0.919615242270663));
#20052=DIRECTION('ref_axis',(0.,-0.919615242270663,-0.392820323027551));
#20053=DIRECTION('',(1.,0.,0.));
#20054=DIRECTION('',(0.,-0.919615242270663,-0.392820323027551));
#20055=DIRECTION('center_axis',(1.,0.,0.));
#20056=DIRECTION('ref_axis',(0.,-0.866025403784438,0.5));
#20057=DIRECTION('center_axis',(1.,0.,0.));
#20058=DIRECTION('ref_axis',(0.,1.,0.));
#20059=DIRECTION('center_axis',(0.,0.998508120307106,-0.0546034218778453));
#20060=DIRECTION('ref_axis',(0.,0.0546034218778453,0.998508120307106));
#20061=DIRECTION('',(-1.,0.,0.));
#20062=DIRECTION('',(0.,0.0546034218778453,0.998508120307106));
#20063=DIRECTION('',(1.,0.,0.));
#20064=DIRECTION('',(0.,0.0546034218778453,0.998508120307106));
#20065=DIRECTION('center_axis',(1.,0.,0.));
#20066=DIRECTION('ref_axis',(0.,-0.766044443118978,0.642787609686539));
#20067=DIRECTION('center_axis',(-1.,0.,0.));
#20068=DIRECTION('ref_axis',(0.,1.,0.));
#20069=DIRECTION('',(0.,-0.973856753620618,-0.227162988683259));
#20070=DIRECTION('center_axis',(0.,-0.227162988683259,0.973856753620618));
#20071=DIRECTION('ref_axis',(0.,-0.973856753620618,-0.227162988683259));
#20072=DIRECTION('',(1.,0.,0.));
#20073=DIRECTION('',(0.,-0.973856753620618,-0.227162988683259));
#20074=DIRECTION('center_axis',(1.,0.,0.));
#20075=DIRECTION('ref_axis',(0.,-0.766044443118978,0.642787609686539));
#20076=DIRECTION('center_axis',(1.,0.,0.));
#20077=DIRECTION('ref_axis',(0.,1.,0.));
#20078=DIRECTION('center_axis',(0.,0.973856753620618,-0.227162988683259));
#20079=DIRECTION('ref_axis',(0.,0.227162988683259,0.973856753620618));
#20080=DIRECTION('',(-1.,0.,0.));
#20081=DIRECTION('',(0.,0.227162988683259,0.973856753620618));
#20082=DIRECTION('',(1.,0.,0.));
#20083=DIRECTION('',(0.,0.227162988683259,0.973856753620618));
#20084=DIRECTION('center_axis',(1.,0.,0.));
#20085=DIRECTION('ref_axis',(0.,-0.642787609686539,0.766044443118978));
#20086=DIRECTION('center_axis',(-1.,0.,0.));
#20087=DIRECTION('ref_axis',(0.,1.,0.));
#20088=DIRECTION('',(0.,-0.998508120307106,-0.054603421877845));
#20089=DIRECTION('center_axis',(0.,-0.054603421877845,0.998508120307106));
#20090=DIRECTION('ref_axis',(0.,-0.998508120307106,-0.054603421877845));
#20091=DIRECTION('',(1.,0.,0.));
#20092=DIRECTION('',(0.,-0.998508120307106,-0.054603421877845));
#20093=DIRECTION('center_axis',(1.,0.,0.));
#20094=DIRECTION('ref_axis',(0.,-0.642787609686539,0.766044443118978));
#20095=DIRECTION('center_axis',(1.,0.,0.));
#20096=DIRECTION('ref_axis',(0.,1.,0.));
#20097=DIRECTION('center_axis',(0.,0.919615242270663,-0.392820323027552));
#20098=DIRECTION('ref_axis',(0.,0.392820323027552,0.919615242270663));
#20099=DIRECTION('',(-1.,0.,0.));
#20100=DIRECTION('',(0.,0.392820323027552,0.919615242270663));
#20101=DIRECTION('',(1.,0.,0.));
#20102=DIRECTION('',(0.,0.392820323027552,0.919615242270663));
#20103=DIRECTION('center_axis',(1.,0.,0.));
#20104=DIRECTION('ref_axis',(0.,-0.5,0.866025403784439));
#20105=DIRECTION('center_axis',(-1.,0.,0.));
#20106=DIRECTION('ref_axis',(0.,1.,0.));
#20107=DIRECTION('',(0.,-0.992820323027551,0.119615242270663));
#20108=DIRECTION('center_axis',(0.,0.119615242270663,0.992820323027551));
#20109=DIRECTION('ref_axis',(0.,-0.992820323027551,0.119615242270663));
#20110=DIRECTION('',(1.,0.,0.));
#20111=DIRECTION('',(0.,-0.992820323027551,0.119615242270663));
#20112=DIRECTION('center_axis',(1.,0.,0.));
#20113=DIRECTION('ref_axis',(0.,-0.5,0.866025403784439));
#20114=DIRECTION('center_axis',(1.,0.,0.));
#20115=DIRECTION('ref_axis',(0.,1.,0.));
#20116=DIRECTION('center_axis',(0.,0.83743168713208,-0.546542010633326));
#20117=DIRECTION('ref_axis',(0.,0.546542010633326,0.83743168713208));
#20118=DIRECTION('',(-1.,0.,0.));
#20119=DIRECTION('',(0.,0.546542010633326,0.83743168713208));
#20120=DIRECTION('',(1.,0.,0.));
#20121=DIRECTION('',(0.,0.546542010633326,0.83743168713208));
#20122=DIRECTION('center_axis',(1.,0.,0.));
#20123=DIRECTION('ref_axis',(0.,-0.342020143325669,0.939692620785909));
#20124=DIRECTION('center_axis',(-1.,0.,0.));
#20125=DIRECTION('ref_axis',(0.,1.,0.));
#20126=DIRECTION('',(0.,-0.956966182624128,0.29019945781101));
#20127=DIRECTION('center_axis',(0.,0.29019945781101,0.956966182624128));
#20128=DIRECTION('ref_axis',(0.,-0.956966182624128,0.29019945781101));
#20129=DIRECTION('',(1.,0.,0.));
#20130=DIRECTION('',(0.,-0.956966182624128,0.29019945781101));
#20131=DIRECTION('center_axis',(1.,0.,0.));
#20132=DIRECTION('ref_axis',(0.,-0.342020143325669,0.939692620785909));
#20133=DIRECTION('center_axis',(1.,0.,0.));
#20134=DIRECTION('ref_axis',(0.,1.,0.));
#20135=DIRECTION('center_axis',(0.,0.729803193940869,-0.683657295809609));
#20136=DIRECTION('ref_axis',(0.,0.683657295809609,0.729803193940869));
#20137=DIRECTION('',(-1.,0.,0.));
#20138=DIRECTION('',(0.,0.683657295809609,0.729803193940869));
#20139=DIRECTION('',(1.,0.,0.));
#20140=DIRECTION('',(0.,0.683657295809609,0.729803193940869));
#20141=DIRECTION('center_axis',(1.,0.,0.));
#20142=DIRECTION('ref_axis',(0.,-0.17364817766693,0.984807753012208));
#20143=DIRECTION('center_axis',(-1.,0.,0.));
#20144=DIRECTION('ref_axis',(0.,1.,0.));
#20145=DIRECTION('',(0.,-0.892035109009925,0.45196610967378));
#20146=DIRECTION('center_axis',(0.,0.45196610967378,0.892035109009925));
#20147=DIRECTION('ref_axis',(0.,-0.892035109009925,0.45196610967378));
#20148=DIRECTION('',(1.,0.,0.));
#20149=DIRECTION('',(0.,-0.892035109009925,0.45196610967378));
#20150=DIRECTION('center_axis',(1.,0.,0.));
#20151=DIRECTION('ref_axis',(0.,-0.17364817766693,0.984807753012208));
#20152=DIRECTION('center_axis',(1.,0.,0.));
#20153=DIRECTION('ref_axis',(0.,1.,0.));
#20154=DIRECTION('center_axis',(0.,0.6,-0.8));
#20155=DIRECTION('ref_axis',(0.,0.8,0.6));
#20156=DIRECTION('',(-1.,0.,0.));
#20157=DIRECTION('',(0.,0.8,0.6));
#20158=DIRECTION('',(1.,0.,0.));
#20159=DIRECTION('',(0.,0.8,0.6));
#20160=DIRECTION('center_axis',(1.,0.,0.));
#20161=DIRECTION('ref_axis',(0.,1.22464679914735E-16,1.));
#20162=DIRECTION('center_axis',(-1.,0.,0.));
#20163=DIRECTION('ref_axis',(0.,1.,0.));
#20164=DIRECTION('',(0.,-0.8,0.6));
#20165=DIRECTION('center_axis',(-1.,0.,0.));
#20166=DIRECTION('ref_axis',(0.,1.,0.));
#20167=DIRECTION('center_axis',(0.,0.6,0.8));
#20168=DIRECTION('ref_axis',(0.,-0.8,0.6));
#20169=DIRECTION('',(1.,0.,0.));
#20170=DIRECTION('',(0.,-0.8,0.6));
#20171=DIRECTION('center_axis',(1.,0.,0.));
#20172=DIRECTION('ref_axis',(0.,1.22464679914735E-16,1.));
#20173=DIRECTION('center_axis',(1.,0.,0.));
#20174=DIRECTION('ref_axis',(0.,1.,0.));
#20175=DIRECTION('center_axis',(1.,0.,0.));
#20176=DIRECTION('ref_axis',(0.,1.,0.));
#20177=DIRECTION('center_axis',(0.,0.45196610967378,-0.892035109009925));
#20178=DIRECTION('ref_axis',(0.,0.892035109009925,0.45196610967378));
#20179=DIRECTION('',(-1.,0.,0.));
#20180=DIRECTION('',(0.,0.892035109009925,0.45196610967378));
#20181=DIRECTION('',(1.,0.,0.));
#20182=DIRECTION('',(0.,0.892035109009925,0.45196610967378));
#20183=DIRECTION('center_axis',(1.,0.,0.));
#20184=DIRECTION('ref_axis',(0.,0.173648177666931,0.984807753012208));
#20185=DIRECTION('center_axis',(-1.,0.,0.));
#20186=DIRECTION('ref_axis',(0.,1.,0.));
#20187=DIRECTION('',(0.,-0.683657295809608,0.729803193940869));
#20188=DIRECTION('center_axis',(0.,0.729803193940869,0.683657295809608));
#20189=DIRECTION('ref_axis',(0.,-0.683657295809608,0.729803193940869));
#20190=DIRECTION('',(1.,0.,0.));
#20191=DIRECTION('',(0.,-0.683657295809608,0.729803193940869));
#20192=DIRECTION('center_axis',(1.,0.,0.));
#20193=DIRECTION('ref_axis',(0.,0.173648177666931,0.984807753012208));
#20194=DIRECTION('center_axis',(1.,0.,0.));
#20195=DIRECTION('ref_axis',(0.,1.,0.));
#20196=DIRECTION('center_axis',(0.,0.290199457811009,-0.956966182624128));
#20197=DIRECTION('ref_axis',(0.,0.956966182624128,0.290199457811009));
#20198=DIRECTION('',(-1.,0.,0.));
#20199=DIRECTION('',(0.,0.956966182624128,0.290199457811009));
#20200=DIRECTION('',(1.,0.,0.));
#20201=DIRECTION('',(0.,0.956966182624128,0.290199457811009));
#20202=DIRECTION('center_axis',(1.,0.,0.));
#20203=DIRECTION('ref_axis',(0.,0.342020143325669,0.939692620785908));
#20204=DIRECTION('center_axis',(-1.,0.,0.));
#20205=DIRECTION('ref_axis',(0.,1.,0.));
#20206=DIRECTION('',(0.,-0.546542010633326,0.83743168713208));
#20207=DIRECTION('center_axis',(0.,0.83743168713208,0.546542010633326));
#20208=DIRECTION('ref_axis',(0.,-0.546542010633326,0.83743168713208));
#20209=DIRECTION('',(1.,0.,0.));
#20210=DIRECTION('',(0.,-0.546542010633326,0.83743168713208));
#20211=DIRECTION('center_axis',(1.,0.,0.));
#20212=DIRECTION('ref_axis',(0.,0.342020143325669,0.939692620785908));
#20213=DIRECTION('center_axis',(1.,0.,0.));
#20214=DIRECTION('ref_axis',(0.,1.,0.));
#20215=DIRECTION('center_axis',(0.,0.119615242270663,-0.992820323027551));
#20216=DIRECTION('ref_axis',(0.,0.992820323027551,0.119615242270663));
#20217=DIRECTION('',(-1.,0.,0.));
#20218=DIRECTION('',(0.,0.992820323027551,0.119615242270663));
#20219=DIRECTION('',(1.,0.,0.));
#20220=DIRECTION('',(0.,0.992820323027551,0.119615242270663));
#20221=DIRECTION('center_axis',(1.,0.,0.));
#20222=DIRECTION('ref_axis',(0.,0.5,0.866025403784439));
#20223=DIRECTION('center_axis',(-1.,0.,0.));
#20224=DIRECTION('ref_axis',(0.,1.,0.));
#20225=DIRECTION('',(0.,-0.392820323027551,0.919615242270663));
#20226=DIRECTION('center_axis',(0.,0.919615242270663,0.392820323027551));
#20227=DIRECTION('ref_axis',(0.,-0.392820323027551,0.919615242270663));
#20228=DIRECTION('',(1.,0.,0.));
#20229=DIRECTION('',(0.,-0.392820323027551,0.919615242270663));
#20230=DIRECTION('center_axis',(1.,0.,0.));
#20231=DIRECTION('ref_axis',(0.,0.5,0.866025403784439));
#20232=DIRECTION('center_axis',(1.,0.,0.));
#20233=DIRECTION('ref_axis',(0.,1.,0.));
#20234=DIRECTION('center_axis',(0.,-0.0546034218778453,-0.998508120307106));
#20235=DIRECTION('ref_axis',(0.,0.998508120307106,-0.0546034218778453));
#20236=DIRECTION('',(-1.,0.,0.));
#20237=DIRECTION('',(0.,0.998508120307106,-0.0546034218778453));
#20238=DIRECTION('',(1.,0.,0.));
#20239=DIRECTION('',(0.,0.998508120307106,-0.0546034218778453));
#20240=DIRECTION('center_axis',(1.,0.,0.));
#20241=DIRECTION('ref_axis',(0.,0.642787609686539,0.766044443118978));
#20242=DIRECTION('center_axis',(-1.,0.,0.));
#20243=DIRECTION('ref_axis',(0.,1.,0.));
#20244=DIRECTION('',(0.,-0.227162988683259,0.973856753620618));
#20245=DIRECTION('center_axis',(0.,0.973856753620618,0.227162988683259));
#20246=DIRECTION('ref_axis',(0.,-0.227162988683259,0.973856753620618));
#20247=DIRECTION('',(1.,0.,0.));
#20248=DIRECTION('',(0.,-0.227162988683259,0.973856753620618));
#20249=DIRECTION('center_axis',(1.,0.,0.));
#20250=DIRECTION('ref_axis',(0.,0.642787609686539,0.766044443118978));
#20251=DIRECTION('center_axis',(1.,0.,0.));
#20252=DIRECTION('ref_axis',(0.,1.,0.));
#20253=DIRECTION('center_axis',(0.,-0.227162988683259,-0.973856753620618));
#20254=DIRECTION('ref_axis',(0.,0.973856753620618,-0.227162988683259));
#20255=DIRECTION('',(-1.,0.,0.));
#20256=DIRECTION('',(0.,0.973856753620618,-0.227162988683259));
#20257=DIRECTION('',(1.,0.,0.));
#20258=DIRECTION('',(0.,0.973856753620618,-0.227162988683259));
#20259=DIRECTION('center_axis',(1.,0.,0.));
#20260=DIRECTION('ref_axis',(0.,0.766044443118978,0.642787609686539));
#20261=DIRECTION('center_axis',(-1.,0.,0.));
#20262=DIRECTION('ref_axis',(0.,1.,0.));
#20263=DIRECTION('',(0.,-0.0546034218778451,0.998508120307106));
#20264=DIRECTION('center_axis',(0.,0.998508120307106,0.0546034218778451));
#20265=DIRECTION('ref_axis',(0.,-0.0546034218778451,0.998508120307106));
#20266=DIRECTION('',(1.,0.,0.));
#20267=DIRECTION('',(0.,-0.0546034218778451,0.998508120307106));
#20268=DIRECTION('center_axis',(1.,0.,0.));
#20269=DIRECTION('ref_axis',(0.,0.766044443118978,0.642787609686539));
#20270=DIRECTION('center_axis',(1.,0.,0.));
#20271=DIRECTION('ref_axis',(0.,1.,0.));
#20272=DIRECTION('center_axis',(0.,-0.392820323027552,-0.919615242270663));
#20273=DIRECTION('ref_axis',(0.,0.919615242270663,-0.392820323027551));
#20274=DIRECTION('',(-1.,0.,0.));
#20275=DIRECTION('',(0.,0.919615242270663,-0.392820323027551));
#20276=DIRECTION('',(1.,0.,0.));
#20277=DIRECTION('',(0.,0.919615242270663,-0.392820323027551));
#20278=DIRECTION('center_axis',(1.,0.,0.));
#20279=DIRECTION('ref_axis',(0.,0.866025403784439,0.5));
#20280=DIRECTION('center_axis',(-1.,0.,0.));
#20281=DIRECTION('ref_axis',(0.,1.,0.));
#20282=DIRECTION('',(0.,0.119615242270663,0.992820323027551));
#20283=DIRECTION('center_axis',(0.,0.992820323027551,-0.119615242270663));
#20284=DIRECTION('ref_axis',(0.,0.119615242270663,0.992820323027551));
#20285=DIRECTION('',(1.,0.,0.));
#20286=DIRECTION('',(0.,0.119615242270663,0.992820323027551));
#20287=DIRECTION('center_axis',(1.,0.,0.));
#20288=DIRECTION('ref_axis',(0.,0.866025403784439,0.5));
#20289=DIRECTION('center_axis',(1.,0.,0.));
#20290=DIRECTION('ref_axis',(0.,1.,0.));
#20291=DIRECTION('center_axis',(0.,-0.546542010633326,-0.83743168713208));
#20292=DIRECTION('ref_axis',(0.,0.83743168713208,-0.546542010633326));
#20293=DIRECTION('',(-1.,0.,0.));
#20294=DIRECTION('',(0.,0.83743168713208,-0.546542010633326));
#20295=DIRECTION('',(1.,0.,0.));
#20296=DIRECTION('',(0.,0.83743168713208,-0.546542010633326));
#20297=DIRECTION('center_axis',(1.,0.,0.));
#20298=DIRECTION('ref_axis',(0.,0.939692620785908,0.342020143325669));
#20299=DIRECTION('center_axis',(-1.,0.,0.));
#20300=DIRECTION('ref_axis',(0.,1.,0.));
#20301=DIRECTION('',(0.,0.29019945781101,0.956966182624128));
#20302=DIRECTION('center_axis',(0.,0.956966182624128,-0.29019945781101));
#20303=DIRECTION('ref_axis',(0.,0.29019945781101,0.956966182624128));
#20304=DIRECTION('',(1.,0.,0.));
#20305=DIRECTION('',(0.,0.29019945781101,0.956966182624128));
#20306=DIRECTION('center_axis',(1.,0.,0.));
#20307=DIRECTION('ref_axis',(0.,0.939692620785908,0.342020143325669));
#20308=DIRECTION('center_axis',(1.,0.,0.));
#20309=DIRECTION('ref_axis',(0.,1.,0.));
#20310=DIRECTION('center_axis',(0.,-0.683657295809609,-0.729803193940869));
#20311=DIRECTION('ref_axis',(0.,0.729803193940869,-0.683657295809609));
#20312=DIRECTION('',(-1.,0.,0.));
#20313=DIRECTION('',(0.,0.729803193940869,-0.683657295809609));
#20314=DIRECTION('',(1.,0.,0.));
#20315=DIRECTION('',(0.,0.729803193940869,-0.683657295809609));
#20316=DIRECTION('center_axis',(1.,0.,0.));
#20317=DIRECTION('ref_axis',(0.,0.984807753012208,0.17364817766693));
#20318=DIRECTION('center_axis',(-1.,0.,0.));
#20319=DIRECTION('ref_axis',(0.,1.,0.));
#20320=DIRECTION('',(0.,0.45196610967378,0.892035109009925));
#20321=DIRECTION('center_axis',(0.,0.892035109009925,-0.45196610967378));
#20322=DIRECTION('ref_axis',(0.,0.45196610967378,0.892035109009925));
#20323=DIRECTION('',(1.,0.,0.));
#20324=DIRECTION('',(0.,0.45196610967378,0.892035109009925));
#20325=DIRECTION('center_axis',(1.,0.,0.));
#20326=DIRECTION('ref_axis',(0.,0.984807753012208,0.17364817766693));
#20327=DIRECTION('center_axis',(1.,0.,0.));
#20328=DIRECTION('ref_axis',(0.,1.,0.));
#20329=DIRECTION('center_axis',(0.,-0.8,-0.6));
#20330=DIRECTION('ref_axis',(0.,0.6,-0.8));
#20331=DIRECTION('',(-1.,0.,0.));
#20332=DIRECTION('',(0.,0.6,-0.8));
#20333=DIRECTION('',(1.,0.,0.));
#20334=DIRECTION('',(0.,0.6,-0.8));
#20335=DIRECTION('center_axis',(1.,0.,0.));
#20336=DIRECTION('ref_axis',(0.,1.,-6.12323399573677E-17));
#20337=DIRECTION('center_axis',(-1.,0.,0.));
#20338=DIRECTION('ref_axis',(0.,1.,0.));
#20339=DIRECTION('',(0.,0.6,0.8));
#20340=DIRECTION('center_axis',(0.,0.8,-0.6));
#20341=DIRECTION('ref_axis',(0.,0.6,0.8));
#20342=DIRECTION('',(1.,0.,0.));
#20343=DIRECTION('',(0.,0.6,0.8));
#20344=DIRECTION('center_axis',(1.,0.,0.));
#20345=DIRECTION('ref_axis',(0.,1.,-6.12323399573677E-17));
#20346=DIRECTION('center_axis',(1.,0.,0.));
#20347=DIRECTION('ref_axis',(0.,1.,0.));
#20348=DIRECTION('center_axis',(0.,-0.892035109009925,-0.45196610967378));
#20349=DIRECTION('ref_axis',(0.,0.45196610967378,-0.892035109009925));
#20350=DIRECTION('',(-1.,0.,0.));
#20351=DIRECTION('',(0.,0.45196610967378,-0.892035109009925));
#20352=DIRECTION('',(1.,0.,0.));
#20353=DIRECTION('',(0.,0.45196610967378,-0.892035109009925));
#20354=DIRECTION('center_axis',(1.,0.,0.));
#20355=DIRECTION('ref_axis',(0.,0.984807753012208,-0.17364817766693));
#20356=DIRECTION('center_axis',(-1.,0.,0.));
#20357=DIRECTION('ref_axis',(0.,1.,0.));
#20358=DIRECTION('',(0.,0.729803193940869,0.683657295809609));
#20359=DIRECTION('center_axis',(0.,0.683657295809609,-0.729803193940869));
#20360=DIRECTION('ref_axis',(0.,0.729803193940869,0.683657295809609));
#20361=DIRECTION('',(1.,0.,0.));
#20362=DIRECTION('',(0.,0.729803193940869,0.683657295809609));
#20363=DIRECTION('center_axis',(1.,0.,0.));
#20364=DIRECTION('ref_axis',(0.,0.984807753012208,-0.17364817766693));
#20365=DIRECTION('center_axis',(1.,0.,0.));
#20366=DIRECTION('ref_axis',(0.,1.,0.));
#20367=DIRECTION('center_axis',(0.,-0.956966182624128,-0.290199457811009));
#20368=DIRECTION('ref_axis',(0.,0.290199457811009,-0.956966182624128));
#20369=DIRECTION('',(-1.,0.,0.));
#20370=DIRECTION('',(0.,0.290199457811009,-0.956966182624128));
#20371=DIRECTION('',(1.,0.,0.));
#20372=DIRECTION('',(0.,0.290199457811009,-0.956966182624128));
#20373=DIRECTION('center_axis',(1.,0.,0.));
#20374=DIRECTION('ref_axis',(0.,0.939692620785908,-0.342020143325669));
#20375=DIRECTION('center_axis',(-1.,0.,0.));
#20376=DIRECTION('ref_axis',(0.,1.,0.));
#20377=DIRECTION('',(0.,0.83743168713208,0.546542010633326));
#20378=DIRECTION('center_axis',(0.,0.546542010633326,-0.83743168713208));
#20379=DIRECTION('ref_axis',(0.,0.83743168713208,0.546542010633326));
#20380=DIRECTION('',(1.,0.,0.));
#20381=DIRECTION('',(0.,0.83743168713208,0.546542010633326));
#20382=DIRECTION('center_axis',(1.,0.,0.));
#20383=DIRECTION('ref_axis',(0.,0.939692620785908,-0.342020143325669));
#20384=DIRECTION('center_axis',(1.,0.,0.));
#20385=DIRECTION('ref_axis',(0.,1.,0.));
#20386=DIRECTION('center_axis',(0.,-0.992820323027551,-0.119615242270663));
#20387=DIRECTION('ref_axis',(0.,0.119615242270663,-0.992820323027551));
#20388=DIRECTION('',(-1.,0.,0.));
#20389=DIRECTION('',(0.,0.119615242270663,-0.992820323027551));
#20390=DIRECTION('',(1.,0.,0.));
#20391=DIRECTION('',(0.,0.119615242270663,-0.992820323027551));
#20392=DIRECTION('center_axis',(1.,0.,0.));
#20393=DIRECTION('ref_axis',(0.,0.866025403784439,-0.5));
#20394=DIRECTION('center_axis',(-1.,0.,0.));
#20395=DIRECTION('ref_axis',(0.,1.,0.));
#20396=DIRECTION('',(0.,0.919615242270663,0.392820323027551));
#20397=DIRECTION('center_axis',(0.,0.392820323027551,-0.919615242270663));
#20398=DIRECTION('ref_axis',(0.,0.919615242270663,0.392820323027551));
#20399=DIRECTION('',(1.,0.,0.));
#20400=DIRECTION('',(0.,0.919615242270663,0.392820323027551));
#20401=DIRECTION('center_axis',(1.,0.,0.));
#20402=DIRECTION('ref_axis',(0.,0.866025403784439,-0.5));
#20403=DIRECTION('center_axis',(1.,0.,0.));
#20404=DIRECTION('ref_axis',(0.,1.,0.));
#20405=DIRECTION('center_axis',(0.,-0.998508120307106,0.0546034218778451));
#20406=DIRECTION('ref_axis',(0.,-0.0546034218778451,-0.998508120307106));
#20407=DIRECTION('',(-1.,0.,0.));
#20408=DIRECTION('',(0.,-0.0546034218778451,-0.998508120307106));
#20409=DIRECTION('',(1.,0.,0.));
#20410=DIRECTION('',(0.,-0.0546034218778451,-0.998508120307106));
#20411=DIRECTION('center_axis',(1.,0.,0.));
#20412=DIRECTION('ref_axis',(0.,0.766044443118978,-0.642787609686539));
#20413=DIRECTION('center_axis',(-1.,0.,0.));
#20414=DIRECTION('ref_axis',(0.,1.,0.));
#20415=DIRECTION('',(0.,0.973856753620618,0.227162988683259));
#20416=DIRECTION('center_axis',(0.,0.227162988683259,-0.973856753620618));
#20417=DIRECTION('ref_axis',(0.,0.973856753620618,0.227162988683259));
#20418=DIRECTION('',(1.,0.,0.));
#20419=DIRECTION('',(0.,0.973856753620618,0.227162988683259));
#20420=DIRECTION('center_axis',(1.,0.,0.));
#20421=DIRECTION('ref_axis',(0.,0.766044443118978,-0.642787609686539));
#20422=DIRECTION('center_axis',(1.,0.,0.));
#20423=DIRECTION('ref_axis',(0.,1.,0.));
#20424=DIRECTION('center_axis',(0.,-0.973856753620618,0.227162988683259));
#20425=DIRECTION('ref_axis',(0.,-0.227162988683259,-0.973856753620618));
#20426=DIRECTION('',(-1.,0.,0.));
#20427=DIRECTION('',(0.,-0.227162988683259,-0.973856753620618));
#20428=DIRECTION('',(1.,0.,0.));
#20429=DIRECTION('',(0.,-0.227162988683259,-0.973856753620618));
#20430=DIRECTION('center_axis',(1.,0.,0.));
#20431=DIRECTION('ref_axis',(0.,0.642787609686539,-0.766044443118978));
#20432=DIRECTION('center_axis',(-1.,0.,0.));
#20433=DIRECTION('ref_axis',(0.,1.,0.));
#20434=DIRECTION('',(0.,0.998508120307106,0.054603421877845));
#20435=DIRECTION('center_axis',(0.,0.054603421877845,-0.998508120307106));
#20436=DIRECTION('ref_axis',(0.,0.998508120307106,0.054603421877845));
#20437=DIRECTION('',(1.,0.,0.));
#20438=DIRECTION('',(0.,0.998508120307106,0.054603421877845));
#20439=DIRECTION('center_axis',(1.,0.,0.));
#20440=DIRECTION('ref_axis',(0.,0.642787609686539,-0.766044443118978));
#20441=DIRECTION('center_axis',(1.,0.,0.));
#20442=DIRECTION('ref_axis',(0.,1.,0.));
#20443=DIRECTION('center_axis',(0.,-0.919615242270663,0.392820323027551));
#20444=DIRECTION('ref_axis',(0.,-0.392820323027551,-0.919615242270663));
#20445=DIRECTION('',(-1.,0.,0.));
#20446=DIRECTION('',(0.,-0.392820323027551,-0.919615242270663));
#20447=DIRECTION('',(1.,0.,0.));
#20448=DIRECTION('',(0.,-0.392820323027551,-0.919615242270663));
#20449=DIRECTION('center_axis',(1.,0.,0.));
#20450=DIRECTION('ref_axis',(0.,0.5,-0.866025403784439));
#20451=DIRECTION('center_axis',(-1.,0.,0.));
#20452=DIRECTION('ref_axis',(0.,1.,0.));
#20453=DIRECTION('',(0.,0.992820323027551,-0.119615242270663));
#20454=DIRECTION('center_axis',(0.,-0.119615242270663,-0.992820323027551));
#20455=DIRECTION('ref_axis',(0.,0.992820323027551,-0.119615242270663));
#20456=DIRECTION('',(1.,0.,0.));
#20457=DIRECTION('',(0.,0.992820323027551,-0.119615242270663));
#20458=DIRECTION('center_axis',(1.,0.,0.));
#20459=DIRECTION('ref_axis',(0.,0.5,-0.866025403784439));
#20460=DIRECTION('center_axis',(1.,0.,0.));
#20461=DIRECTION('ref_axis',(0.,1.,0.));
#20462=DIRECTION('center_axis',(0.,-0.83743168713208,0.546542010633326));
#20463=DIRECTION('ref_axis',(0.,-0.546542010633326,-0.83743168713208));
#20464=DIRECTION('',(-1.,0.,0.));
#20465=DIRECTION('',(0.,-0.546542010633326,-0.83743168713208));
#20466=DIRECTION('',(1.,0.,0.));
#20467=DIRECTION('',(0.,-0.546542010633326,-0.83743168713208));
#20468=DIRECTION('center_axis',(1.,0.,0.));
#20469=DIRECTION('ref_axis',(0.,0.342020143325669,-0.939692620785908));
#20470=DIRECTION('center_axis',(-1.,0.,0.));
#20471=DIRECTION('ref_axis',(0.,1.,0.));
#20472=DIRECTION('',(0.,0.956966182624128,-0.29019945781101));
#20473=DIRECTION('center_axis',(0.,-0.29019945781101,-0.956966182624128));
#20474=DIRECTION('ref_axis',(0.,0.956966182624128,-0.29019945781101));
#20475=DIRECTION('',(1.,0.,0.));
#20476=DIRECTION('',(0.,0.956966182624128,-0.29019945781101));
#20477=DIRECTION('center_axis',(1.,0.,0.));
#20478=DIRECTION('ref_axis',(0.,0.342020143325669,-0.939692620785908));
#20479=DIRECTION('center_axis',(1.,0.,0.));
#20480=DIRECTION('ref_axis',(0.,1.,0.));
#20481=DIRECTION('center_axis',(0.,-0.729803193940869,0.683657295809609));
#20482=DIRECTION('ref_axis',(0.,-0.683657295809609,-0.729803193940869));
#20483=DIRECTION('',(-1.,0.,0.));
#20484=DIRECTION('',(0.,-0.683657295809609,-0.729803193940869));
#20485=DIRECTION('',(1.,0.,0.));
#20486=DIRECTION('',(0.,-0.683657295809609,-0.729803193940869));
#20487=DIRECTION('center_axis',(1.,0.,0.));
#20488=DIRECTION('ref_axis',(0.,0.17364817766693,-0.984807753012208));
#20489=DIRECTION('center_axis',(-1.,0.,0.));
#20490=DIRECTION('ref_axis',(0.,1.,0.));
#20491=DIRECTION('',(0.,0.892035109009925,-0.45196610967378));
#20492=DIRECTION('center_axis',(0.,-0.45196610967378,-0.892035109009925));
#20493=DIRECTION('ref_axis',(0.,0.892035109009925,-0.45196610967378));
#20494=DIRECTION('',(1.,0.,0.));
#20495=DIRECTION('',(0.,0.892035109009925,-0.45196610967378));
#20496=DIRECTION('center_axis',(1.,0.,0.));
#20497=DIRECTION('ref_axis',(0.,0.17364817766693,-0.984807753012208));
#20498=DIRECTION('center_axis',(1.,0.,0.));
#20499=DIRECTION('ref_axis',(0.,1.,0.));
#20500=DIRECTION('center_axis',(0.,-0.6,0.8));
#20501=DIRECTION('ref_axis',(0.,-0.8,-0.6));
#20502=DIRECTION('',(-1.,0.,0.));
#20503=DIRECTION('',(0.,-0.8,-0.6));
#20504=DIRECTION('',(1.,0.,0.));
#20505=DIRECTION('',(0.,-0.8,-0.6));
#20506=DIRECTION('center_axis',(1.,0.,0.));
#20507=DIRECTION('ref_axis',(0.,0.,-1.));
#20508=DIRECTION('center_axis',(-1.,0.,0.));
#20509=DIRECTION('ref_axis',(0.,1.,0.));
#20510=DIRECTION('',(0.,0.8,-0.6));
#20511=DIRECTION('center_axis',(0.,-0.6,-0.8));
#20512=DIRECTION('ref_axis',(0.,0.8,-0.6));
#20513=DIRECTION('',(1.,0.,0.));
#20514=DIRECTION('',(0.,0.8,-0.6));
#20515=DIRECTION('center_axis',(1.,0.,0.));
#20516=DIRECTION('ref_axis',(0.,0.,-1.));
#20517=DIRECTION('center_axis',(1.,0.,0.));
#20518=DIRECTION('ref_axis',(0.,1.,0.));
#20519=DIRECTION('center_axis',(0.,0.5,0.866025403784439));
#20520=DIRECTION('ref_axis',(0.,0.866025403784439,-0.5));
#20521=DIRECTION('',(0.,0.866025403784439,-0.5));
#20522=DIRECTION('',(-1.,0.,0.));
#20523=DIRECTION('',(0.,0.866025403784439,-0.5));
#20524=DIRECTION('',(-1.,0.,0.));
#20525=DIRECTION('center_axis',(0.,-0.5,0.866025403784439));
#20526=DIRECTION('ref_axis',(0.,0.866025403784439,0.5));
#20527=DIRECTION('',(0.,0.866025403784439,0.5));
#20528=DIRECTION('',(-1.,0.,0.));
#20529=DIRECTION('',(0.,0.866025403784439,0.5));
#20530=DIRECTION('center_axis',(0.,-1.,-1.92296268638356E-16));
#20531=DIRECTION('ref_axis',(0.,-1.92296268638356E-16,1.));
#20532=DIRECTION('',(0.,-1.92296268638356E-16,1.));
#20533=DIRECTION('',(-1.,0.,0.));
#20534=DIRECTION('',(0.,-1.92296268638356E-16,1.));
#20535=DIRECTION('center_axis',(0.,-0.5,-0.866025403784439));
#20536=DIRECTION('ref_axis',(0.,-0.866025403784439,0.5));
#20537=DIRECTION('',(0.,-0.866025403784439,0.5));
#20538=DIRECTION('',(-1.,0.,0.));
#20539=DIRECTION('',(0.,-0.866025403784439,0.5));
#20540=DIRECTION('center_axis',(0.,0.5,-0.866025403784439));
#20541=DIRECTION('ref_axis',(0.,-0.866025403784439,-0.5));
#20542=DIRECTION('',(0.,-0.866025403784439,-0.5));
#20543=DIRECTION('',(-1.,0.,0.));
#20544=DIRECTION('',(0.,-0.866025403784439,-0.5));
#20545=DIRECTION('center_axis',(0.,1.,-3.84592537276713E-16));
#20546=DIRECTION('ref_axis',(0.,-3.84592537276713E-16,-1.));
#20547=DIRECTION('',(0.,-3.84592537276713E-16,-1.));
#20548=DIRECTION('',(0.,-3.84592537276713E-16,-1.));
#20549=DIRECTION('center_axis',(-1.,0.,0.));
#20550=DIRECTION('ref_axis',(0.,0.,1.));
#20551=DIRECTION('center_axis',(-1.,0.,0.));
#20552=DIRECTION('ref_axis',(0.,0.,1.));
#20553=DIRECTION('center_axis',(1.,0.,0.));
#20554=DIRECTION('ref_axis',(0.,0.,-1.));
#20555=DIRECTION('center_axis',(1.,0.,0.));
#20556=DIRECTION('ref_axis',(0.,1.,0.));
#20557=DIRECTION('',(-0.707106781186547,0.707106781186548,8.65956056235494E-17));
#20558=DIRECTION('center_axis',(1.,0.,0.));
#20559=DIRECTION('ref_axis',(0.,1.,0.));
#20560=DIRECTION('center_axis',(1.,0.,0.));
#20561=DIRECTION('ref_axis',(0.,1.,0.));
#20562=DIRECTION('center_axis',(-1.,0.,0.));
#20563=DIRECTION('ref_axis',(0.,0.,1.));
#20564=DIRECTION('center_axis',(1.,0.,0.));
#20565=DIRECTION('ref_axis',(0.,0.,-1.));
#20566=DIRECTION('center_axis',(1.,0.,0.));
#20567=DIRECTION('ref_axis',(0.,1.,0.));
#20568=DIRECTION('center_axis',(1.,0.,0.));
#20569=DIRECTION('ref_axis',(0.,0.,-1.));
#20570=DIRECTION('',(-1.,0.,0.));
#20571=DIRECTION('',(-1.,0.,0.));
#20572=DIRECTION('center_axis',(-1.,0.,0.));
#20573=DIRECTION('ref_axis',(0.,1.,0.));
#20574=DIRECTION('center_axis',(1.,0.,0.));
#20575=DIRECTION('ref_axis',(0.,0.,-1.));
#20576=DIRECTION('',(-0.707106781186547,-0.707106781186548,-8.65956056235494E-17));
#20577=DIRECTION('center_axis',(1.,0.,0.));
#20578=DIRECTION('ref_axis',(0.,0.,-1.));
#27229=CARTESIAN_POINT('',(0.,0.,0.));
#27230=CARTESIAN_POINT('Origin',(-29.75,0.,0.));
#27231=CARTESIAN_POINT('',(-59.0198748077951,-5.9168929925076,0.000147316400840244));
#27232=CARTESIAN_POINT('',(-59.2716251922048,-5.91673468093559,9.87673099418387E-5));
#27233=CARTESIAN_POINT('',(-29.75,-5.91675,-7.2459289488551E-16));
#27234=CARTESIAN_POINT('',(-59.58325,2.58403649360107,5.32282025590616));
#27235=CARTESIAN_POINT('Ctrl Pts',(-59.0198748077951,-5.9168929925076,0.000147316400840244));
#27236=CARTESIAN_POINT('Ctrl Pts',(-59.0284715689044,-5.91708038654053,
0.182755768972575));
#27237=CARTESIAN_POINT('Ctrl Pts',(-59.0370683300138,-5.90879517539952,
0.365347221437024));
#27238=CARTESIAN_POINT('Ctrl Pts',(-59.0456650911231,-5.89191334558682,
0.547140283985201));
#27239=CARTESIAN_POINT('Ctrl Pts',(-59.0920846391508,-5.80075728113219,
1.52876018602797));
#27240=CARTESIAN_POINT('Ctrl Pts',(-59.1385041871784,-5.45895580385933,
2.48710200888682));
#27241=CARTESIAN_POINT('Ctrl Pts',(-59.184923735206,-4.90835058319102,3.3048580525707));
#27242=CARTESIAN_POINT('Ctrl Pts',(-59.2313432832336,-4.35774536252271,
4.12261409625457));
#27243=CARTESIAN_POINT('Ctrl Pts',(-59.2777628312612,-3.59833639845895,
4.79978436076348));
#27244=CARTESIAN_POINT('Ctrl Pts',(-59.3241823792888,-2.72308539444232,
5.25346025315473));
#27245=CARTESIAN_POINT('Ctrl Pts',(-59.3706019273164,-1.84783439042568,
5.70713614554599));
#27246=CARTESIAN_POINT('Ctrl Pts',(-59.4170214753441,-0.856741346456157,
5.93731766581958));
#27247=CARTESIAN_POINT('Ctrl Pts',(-59.4634410233717,0.128868647897307,
5.91585348664495));
#27248=CARTESIAN_POINT('Ctrl Pts',(-59.5033773489145,0.976822651441423,
5.8973871188441));
#27249=CARTESIAN_POINT('Ctrl Pts',(-59.5433136744572,1.8207182389207,5.69265890393189));
#27250=CARTESIAN_POINT('Ctrl Pts',(-59.58325,2.58415317085807,5.32292607787877));
#27251=CARTESIAN_POINT('',(-59.58325,-2.58391981634379,5.32271443393368));
#27252=CARTESIAN_POINT('Origin',(-59.58325,0.,0.));
#27253=CARTESIAN_POINT('Ctrl Pts',(-59.58325,-2.58391981634379,5.32271443393368));
#27254=CARTESIAN_POINT('Ctrl Pts',(-59.5368304519724,-3.47102658701026,
4.89206710306723));
#27255=CARTESIAN_POINT('Ctrl Pts',(-59.4904109039448,-4.24793472784974,
4.23556933641632));
#27256=CARTESIAN_POINT('Ctrl Pts',(-59.4439913559172,-4.81982763361711,
3.43270692109267));
#27257=CARTESIAN_POINT('Ctrl Pts',(-59.3975718078896,-5.39172053938448,
2.62984450576901));
#27258=CARTESIAN_POINT('Ctrl Pts',(-59.3511522598619,-5.75859821007974,
1.68061744177261));
#27259=CARTESIAN_POINT('Ctrl Pts',(-59.3047327118343,-5.87551327073906,
0.701680759602287));
#27260=CARTESIAN_POINT('Ctrl Pts',(-59.2936968719578,-5.90330879963607,
0.468947160661655));
#27261=CARTESIAN_POINT('Ctrl Pts',(-59.2826610320813,-5.9169762201901,0.234534347760465));
#27262=CARTESIAN_POINT('Ctrl Pts',(-59.2716251922048,-5.91673468093559,
9.87673099418387E-5));
#27263=CARTESIAN_POINT('Origin',(-29.75,0.,0.));
#27264=CARTESIAN_POINT('',(-57.2698748077951,-5.91669521102349,-0.000155415116674662));
#27265=CARTESIAN_POINT('',(-57.5216251922048,-5.91686007623345,-0.000149468482956774));
#27266=CARTESIAN_POINT('',(-29.75,-5.91675,-7.2459289488551E-16));
#27267=CARTESIAN_POINT('Ctrl Pts',(-57.2698748077951,-5.91669521102349,
-0.000155415116674662));
#27268=CARTESIAN_POINT('Ctrl Pts',(-57.3047703259064,-5.91594092446023,
0.741150481904227));
#27269=CARTESIAN_POINT('Ctrl Pts',(-57.3396658440178,-5.77622172722126,
1.48273266306714));
#27270=CARTESIAN_POINT('Ctrl Pts',(-57.3745613621291,-5.50418014344905,
2.17209688647092));
#27271=CARTESIAN_POINT('Ctrl Pts',(-57.4209809101567,-5.1422985022843,3.08911939849433));
#27272=CARTESIAN_POINT('Ctrl Pts',(-57.4674004581843,-4.5462659573424,3.91373969254815));
#27273=CARTESIAN_POINT('Ctrl Pts',(-57.5138200062119,-3.78904530466483,
4.54501260817227));
#27274=CARTESIAN_POINT('Ctrl Pts',(-57.5602395542395,-3.03182465198727,
5.17628552379639));
#27275=CARTESIAN_POINT('Ctrl Pts',(-57.6066591022671,-2.11341589157402,
5.61421106099084));
#27276=CARTESIAN_POINT('Ctrl Pts',(-57.6530786502948,-1.14624521793713,
5.80518094870228));
#27277=CARTESIAN_POINT('Ctrl Pts',(-57.6994981983224,-0.179074544300242,
5.99615083641373));
#27278=CARTESIAN_POINT('Ctrl Pts',(-57.74591774635,0.836858042560288,5.94016507464217));
#27279=CARTESIAN_POINT('Ctrl Pts',(-57.7923372943776,1.77718805466837,5.64407711940241));
#27280=CARTESIAN_POINT('Ctrl Pts',(-57.8387568424052,2.71751806677645,5.34798916416265));
#27281=CARTESIAN_POINT('Ctrl Pts',(-57.8851763904328,3.58224550413209,4.8117990154547));
#27282=CARTESIAN_POINT('Ctrl Pts',(-57.9315959384604,4.26551552444564,4.10114389853271));
#27283=CARTESIAN_POINT('Ctrl Pts',(-57.9780154864881,4.94878554475919,3.39048878161072));
#27284=CARTESIAN_POINT('Ctrl Pts',(-58.0244350345156,5.45059814803065,2.5053686964747));
#27285=CARTESIAN_POINT('Ctrl Pts',(-58.0708545825433,5.70952438737617,1.55413486686007));
#27286=CARTESIAN_POINT('Ctrl Pts',(-58.1172741305709,5.9684506267217,0.602901037245434));
#27287=CARTESIAN_POINT('Ctrl Pts',(-58.1636936785985,5.98449050214128,-0.414446536847809));
#27288=CARTESIAN_POINT('Ctrl Pts',(-58.2101132266261,5.75568050969606,-1.37337021725454));
#27289=CARTESIAN_POINT('Ctrl Pts',(-58.2565327746537,5.52687051725085,-2.33229389766127));
#27290=CARTESIAN_POINT('Ctrl Pts',(-58.3029523226813,5.05321065694084,-3.23279368438148));
#27291=CARTESIAN_POINT('Ctrl Pts',(-58.3493718707089,4.39268357467904,-3.96463556937447));
#27292=CARTESIAN_POINT('Ctrl Pts',(-58.3957914187365,3.73215649241724,-4.69647745436745));
#27293=CARTESIAN_POINT('Ctrl Pts',(-58.4422109667642,2.88476218820364,-5.2596614376332));
#27294=CARTESIAN_POINT('Ctrl Pts',(-58.4886305147918,1.95423369721252,-5.58524609364036));
#27295=CARTESIAN_POINT('Ctrl Pts',(-58.5350500628194,1.0237052062214,-5.91083074964752));
#27296=CARTESIAN_POINT('Ctrl Pts',(-58.581469610847,0.0100425284527469,
-5.99881607839609));
#27297=CARTESIAN_POINT('Ctrl Pts',(-58.6278891588746,-0.962667741224851,
-5.83843096005687));
#27298=CARTESIAN_POINT('Ctrl Pts',(-58.6743087069022,-1.93537801090245,
-5.67804584171765));
#27299=CARTESIAN_POINT('Ctrl Pts',(-58.7207282549299,-2.867135872489,-5.26929027629065));
#27300=CARTESIAN_POINT('Ctrl Pts',(-58.7671478029575,-3.64388096648873,
-4.66220263851837));
#27301=CARTESIAN_POINT('Ctrl Pts',(-58.8135673509851,-4.42062606048846,
-4.05511500074609));
#27302=CARTESIAN_POINT('Ctrl Pts',(-58.8599868990127,-5.04235838690136,
-3.24969529062854));
#27303=CARTESIAN_POINT('Ctrl Pts',(-58.9064064470403,-5.43296922428961,
-2.34453644495641));
#27304=CARTESIAN_POINT('Ctrl Pts',(-58.9442292339585,-5.75124010580946,
-1.60701030345509));
#27305=CARTESIAN_POINT('Ctrl Pts',(-58.9820520208768,-5.91606852332821,
-0.803266958259637));
#27306=CARTESIAN_POINT('Ctrl Pts',(-59.0198748077951,-5.9168929925076,0.000147316400840244));
#27307=CARTESIAN_POINT('Ctrl Pts',(-59.2716251922048,-5.91673468093559,
9.87673099418387E-5));
#27308=CARTESIAN_POINT('Ctrl Pts',(-59.2362414840537,-5.91596024468205,
-0.751561301314473));
#27309=CARTESIAN_POINT('Ctrl Pts',(-59.2008577759026,-5.77220078208614,
-1.50345542185119));
#27310=CARTESIAN_POINT('Ctrl Pts',(-59.1654740677515,-5.49267953958377,
-2.20098628354733));
#27311=CARTESIAN_POINT('Ctrl Pts',(-59.1190545197239,-5.12597829714577,
-3.1160703441824));
#27312=CARTESIAN_POINT('Ctrl Pts',(-59.0726349716963,-4.52562336164638,
-3.93759216510828));
#27313=CARTESIAN_POINT('Ctrl Pts',(-59.0262154236687,-3.76509506266973,
-4.56488611193625));
#27314=CARTESIAN_POINT('Ctrl Pts',(-58.979795875641,-3.00456676369308,-5.19218005876421));
#27315=CARTESIAN_POINT('Ctrl Pts',(-58.9333763276134,-2.08386510123916,
-5.62524613149425));
#27316=CARTESIAN_POINT('Ctrl Pts',(-58.8869567795858,-1.11570292286205,
-5.81112178033337));
#27317=CARTESIAN_POINT('Ctrl Pts',(-58.8405372315582,-0.147540744484937,
-5.99699742917248));
#27318=CARTESIAN_POINT('Ctrl Pts',(-58.7941176835306,0.868081949815372,
-5.93568265412068));
#27319=CARTESIAN_POINT('Ctrl Pts',(-58.747698135503,1.8068416706146,-5.63465720893411));
#27320=CARTESIAN_POINT('Ctrl Pts',(-58.7012785874754,2.74560139141385,-5.33363176374754));
#27321=CARTESIAN_POINT('Ctrl Pts',(-58.6548590394477,3.60749813871201,-4.79289564842621));
#27322=CARTESIAN_POINT('Ctrl Pts',(-58.6084394914201,4.28702201532277,-4.07865594235945));
#27323=CARTESIAN_POINT('Ctrl Pts',(-58.5620199433925,4.96654589193352,-3.36441623629269));
#27324=CARTESIAN_POINT('Ctrl Pts',(-58.5156003953649,5.46369689785686,-2.47667293948052));
#27325=CARTESIAN_POINT('Ctrl Pts',(-58.4691808473373,5.7176175382941,-1.52409151899249));
#27326=CARTESIAN_POINT('Ctrl Pts',(-58.4227612993097,5.97153817873133,-0.571510098504466));
#27327=CARTESIAN_POINT('Ctrl Pts',(-58.3763417512821,5.98222845368246,0.445909445659409));
#27328=CARTESIAN_POINT('Ctrl Pts',(-58.3299222032545,5.74837930985091,1.40361709377507));
#27329=CARTESIAN_POINT('Ctrl Pts',(-58.2835026552269,5.51453016601937,2.36132474189074));
#27330=CARTESIAN_POINT('Ctrl Pts',(-58.2370831071992,5.03614160340517,3.25932049395819));
#27331=CARTESIAN_POINT('Ctrl Pts',(-58.1906635591716,4.37177534567143,3.98767879377327));
#27332=CARTESIAN_POINT('Ctrl Pts',(-58.144244011144,3.70740908793767,4.71603709358836));
#27333=CARTESIAN_POINT('Ctrl Pts',(-58.0978244631164,2.85706513508438,5.27475794115106));
#27334=CARTESIAN_POINT('Ctrl Pts',(-58.0514049150888,1.92483748024982,5.59544509705575));
#27335=CARTESIAN_POINT('Ctrl Pts',(-58.0049853670612,0.992609825415271,
5.91613225296045));
#27336=CARTESIAN_POINT('Ctrl Pts',(-57.9585658190336,-0.0215015314005408,
5.99878571720714));
#27337=CARTESIAN_POINT('Ctrl Pts',(-57.912146271006,-0.993354991301984,
5.83328801179188));
#27338=CARTESIAN_POINT('Ctrl Pts',(-57.8657267229784,-1.96520845120343,
5.66779030637661));
#27339=CARTESIAN_POINT('Ctrl Pts',(-57.8193071749508,-2.89480401419051,
5.2541414312994));
#27340=CARTESIAN_POINT('Ctrl Pts',(-57.7728876269231,-3.66834609151454,
4.6429776048486));
#27341=CARTESIAN_POINT('Ctrl Pts',(-57.7264680788955,-4.44188816883857,
4.0318137783978));
#27342=CARTESIAN_POINT('Ctrl Pts',(-57.6800485308679,-5.05937676049954,
3.22313500057342));
#27343=CARTESIAN_POINT('Ctrl Pts',(-57.6336289828403,-5.44522253300335,
2.31593509171118));
#27344=CARTESIAN_POINT('Ctrl Pts',(-57.5962943859618,-5.75555292150966,
1.586286822292));
#27345=CARTESIAN_POINT('Ctrl Pts',(-57.5589597890833,-5.91603910242325,
0.79290758609723));
#27346=CARTESIAN_POINT('Ctrl Pts',(-57.5216251922048,-5.91686007623345,
-0.000149468482956774));
#27347=CARTESIAN_POINT('Origin',(-29.75,0.,0.));
#27348=CARTESIAN_POINT('',(-55.5198748077951,-5.91649353122104,0.000138118266801851));
#27349=CARTESIAN_POINT('',(-55.7716251922049,-5.91637209757686,0.000108738722670239));
#27350=CARTESIAN_POINT('',(-29.75,-5.91675,-7.2459289488551E-16));
#27351=CARTESIAN_POINT('Ctrl Pts',(-55.5198748077951,-5.91649353122104,
0.000138118266801851));
#27352=CARTESIAN_POINT('Ctrl Pts',(-55.5346495348808,-5.91676214941988,
0.314037003843105));
#27353=CARTESIAN_POINT('Ctrl Pts',(-55.5494242619665,-5.8922161605167,0.627894292230318));
#27354=CARTESIAN_POINT('Ctrl Pts',(-55.5641989890522,-5.84249117704565,
0.937710392677676));
#27355=CARTESIAN_POINT('Ctrl Pts',(-55.6106185370798,-5.68626417907686,
1.91109712740557));
#27356=CARTESIAN_POINT('Ctrl Pts',(-55.6570380851074,-5.28149433666472,
2.844593137236));
#27357=CARTESIAN_POINT('Ctrl Pts',(-55.703457633135,-4.67773119145832,3.62392533516499));
#27358=CARTESIAN_POINT('Ctrl Pts',(-55.7498771811627,-4.07396804625193,
4.40325753309398));
#27359=CARTESIAN_POINT('Ctrl Pts',(-55.7962967291902,-3.27121159825127,
5.02842591912155));
#27360=CARTESIAN_POINT('Ctrl Pts',(-55.8427162772178,-2.36773056682856,
5.42290105914683));
#27361=CARTESIAN_POINT('Ctrl Pts',(-55.8891358252455,-1.46424953540586,
5.81737619917211));
#27362=CARTESIAN_POINT('Ctrl Pts',(-55.9355553732731,-0.460043920561111,
5.98115809319512));
#27363=CARTESIAN_POINT('Ctrl Pts',(-55.9819749213007,0.521957337050214,
5.89419752576172));
#27364=CARTESIAN_POINT('Ctrl Pts',(-56.0283944693283,1.50395859466155,5.80723695832833));
#27365=CARTESIAN_POINT('Ctrl Pts',(-56.0748140173559,2.46375549503949,5.46953392943853));
#27366=CARTESIAN_POINT('Ctrl Pts',(-56.1212335653835,3.28385535096541,4.92242805618543));
#27367=CARTESIAN_POINT('Ctrl Pts',(-56.1676531134111,4.10395520689133,4.37532218293233));
#27368=CARTESIAN_POINT('Ctrl Pts',(-56.2140726614388,4.78435801836524,3.61881346531596));
#27369=CARTESIAN_POINT('Ctrl Pts',(-56.2604922094664,5.24177287803033,2.74550924776157));
#27370=CARTESIAN_POINT('Ctrl Pts',(-56.306911757494,5.69918773769542,1.87220503020718));
#27371=CARTESIAN_POINT('Ctrl Pts',(-56.3533313055216,5.93361464555165,0.882105312714779));
#27372=CARTESIAN_POINT('Ctrl Pts',(-56.3997508535492,5.91635643936607,-0.103587724976462));
#27373=CARTESIAN_POINT('Ctrl Pts',(-56.4461704015768,5.89909823318048,-1.08928076266769));
#27374=CARTESIAN_POINT('Ctrl Pts',(-56.4925899496044,5.63015491295308,-2.07056712055777));
#27375=CARTESIAN_POINT('Ctrl Pts',(-56.5390094976321,5.14244893695761,-2.92732349854667));
#27376=CARTESIAN_POINT('Ctrl Pts',(-56.5854290456597,4.65474296096214,-3.78407987653557));
#27377=CARTESIAN_POINT('Ctrl Pts',(-56.6318485936873,3.9482743291986,-4.5163062746233));
#27378=CARTESIAN_POINT('Ctrl Pts',(-56.6782681417149,3.10952477331956,-5.03436784697009));
#27379=CARTESIAN_POINT('Ctrl Pts',(-56.7246876897425,2.27077521744052,-5.55242941931689));
#27380=CARTESIAN_POINT('Ctrl Pts',(-56.7711072377701,1.29974473744598,-5.85632616592275));
#27381=CARTESIAN_POINT('Ctrl Pts',(-56.8175267857977,0.315301169254638,
-5.90885683587198));
#27382=CARTESIAN_POINT('Ctrl Pts',(-56.8639463338253,-0.669142398936689,
-5.96138750582122));
#27383=CARTESIAN_POINT('Ctrl Pts',(-56.910365881853,-1.66699905532482,-5.76255209911383));
#27384=CARTESIAN_POINT('Ctrl Pts',(-56.9567854298806,-2.55611706138655,
-5.33669087574605));
#27385=CARTESIAN_POINT('Ctrl Pts',(-57.0032049779082,-3.44523506744831,
-4.91082965237827));
#27386=CARTESIAN_POINT('Ctrl Pts',(-57.0496245259358,-4.22561442318367,
-4.25794261235009));
#27387=CARTESIAN_POINT('Ctrl Pts',(-57.0960440739634,-4.80172568112968,
-3.45795234453877));
#27388=CARTESIAN_POINT('Ctrl Pts',(-57.142463621991,-5.37783693907569,-2.65796207672745));
#27389=CARTESIAN_POINT('Ctrl Pts',(-57.1888831700186,-5.74968009923236,
-1.71086858113299));
#27390=CARTESIAN_POINT('Ctrl Pts',(-57.2353027180462,-5.87173631061688,
-0.732609468339251));
#27391=CARTESIAN_POINT('Ctrl Pts',(-57.2468267479625,-5.90203775669358,
-0.48974869608429));
#27392=CARTESIAN_POINT('Ctrl Pts',(-57.2583507778788,-5.91694430951495,
-0.244967121512084));
#27393=CARTESIAN_POINT('Ctrl Pts',(-57.2698748077951,-5.91669521102349,
-0.000155415116674662));
#27394=CARTESIAN_POINT('Ctrl Pts',(-57.5216251922048,-5.91686007623345,
-0.000149468482956774));
#27395=CARTESIAN_POINT('Ctrl Pts',(-57.5125402410557,-5.91705985090853,
-0.193130917372952));
#27396=CARTESIAN_POINT('Ctrl Pts',(-57.5034552899066,-5.90780525658231,
-0.3860932886948));
#27397=CARTESIAN_POINT('Ctrl Pts',(-57.4943703387574,-5.8889547826199,-0.578113641592445));
#27398=CARTESIAN_POINT('Ctrl Pts',(-57.4479507907298,-5.79263830638598,
-1.55924142613374));
#27399=CARTESIAN_POINT('Ctrl Pts',(-57.4015312427023,-5.4458024005715,-2.51577595531623));
#27400=CARTESIAN_POINT('Ctrl Pts',(-57.3551116946746,-4.89090467146282,
-3.33062386955801));
#27401=CARTESIAN_POINT('Ctrl Pts',(-57.308692146647,-4.33600694235414,-4.14547178379979));
#27402=CARTESIAN_POINT('Ctrl Pts',(-57.2622725986194,-3.57304738995126,
-4.81863308310086));
#27403=CARTESIAN_POINT('Ctrl Pts',(-57.2158530505918,-2.69542303387945,
-5.26770334013568));
#27404=CARTESIAN_POINT('Ctrl Pts',(-57.1694335025641,-1.81779867780764,
-5.71677359717049));
#27405=CARTESIAN_POINT('Ctrl Pts',(-57.1230139545365,-0.825509518066903,
-5.94175281193905));
#27406=CARTESIAN_POINT('Ctrl Pts',(-57.0765944065089,0.159974247990831,
-5.91510034460887));
#27407=CARTESIAN_POINT('Ctrl Pts',(-57.0301748584813,1.14545801404857,-5.88844787727869));
#27408=CARTESIAN_POINT('Ctrl Pts',(-56.9837553104537,2.12413638642329,-5.61016372784978));
#27409=CARTESIAN_POINT('Ctrl Pts',(-56.9373357624261,2.97620531871277,-5.11431380832405));
#27410=CARTESIAN_POINT('Ctrl Pts',(-56.8909162143985,3.82827425100224,-4.61846388879832));
#27411=CARTESIAN_POINT('Ctrl Pts',(-56.8444966663709,4.55373374320647,-3.90504819917577));
#27412=CARTESIAN_POINT('Ctrl Pts',(-56.7980771183432,5.06377731458045,-3.06139888678933));
#27413=CARTESIAN_POINT('Ctrl Pts',(-56.7516575703156,5.57382088595442,-2.21774957440287));
#27414=CARTESIAN_POINT('Ctrl Pts',(-56.7052380222881,5.86844853649814,-1.24386663925252));
#27415=CARTESIAN_POINT('Ctrl Pts',(-56.6588184742604,5.91159368326249,-0.25896709917957));
#27416=CARTESIAN_POINT('Ctrl Pts',(-56.6123989262328,5.95473883002684,0.725932440893382));
#27417=CARTESIAN_POINT('Ctrl Pts',(-56.5659793782052,5.74640147301182,1.72184858588893));
#27418=CARTESIAN_POINT('Ctrl Pts',(-56.5195598301776,5.31208504526766,2.60686714385153));
#27419=CARTESIAN_POINT('Ctrl Pts',(-56.47314028215,4.8777686175235,3.49188570181413));
#27420=CARTESIAN_POINT('Ctrl Pts',(-56.4267207341224,4.2174731190502,4.2660066727438));
#27421=CARTESIAN_POINT('Ctrl Pts',(-56.3803011860948,3.41202803826244,4.83446672352035));
#27422=CARTESIAN_POINT('Ctrl Pts',(-56.3338816380672,2.60658295747469,5.40292677429689));
#27423=CARTESIAN_POINT('Ctrl Pts',(-56.2874620900395,1.65598829437247,5.76572590492033));
#27424=CARTESIAN_POINT('Ctrl Pts',(-56.2410425420119,0.676610252469253,
5.8784523813965));
#27425=CARTESIAN_POINT('Ctrl Pts',(-56.1946229939843,-0.302767789433966,
5.99117885787268));
#27426=CARTESIAN_POINT('Ctrl Pts',(-56.1482034459567,-1.31092921013819,
5.85383268020161));
#27427=CARTESIAN_POINT('Ctrl Pts',(-56.1017838979291,-2.22446082252765,
5.48322695895988));
#27428=CARTESIAN_POINT('Ctrl Pts',(-56.0553643499015,-3.13799243491712,
5.11262123771814));
#27429=CARTESIAN_POINT('Ctrl Pts',(-56.0089448018738,-3.95689423899183,
4.50875597290575));
#27430=CARTESIAN_POINT('Ctrl Pts',(-55.9625252538462,-4.58092109591514,
3.74555279595537));
#27431=CARTESIAN_POINT('Ctrl Pts',(-55.9161057058186,-5.20494795283845,
2.98234961900499));
#27432=CARTESIAN_POINT('Ctrl Pts',(-55.8696861577911,-5.63409986261035,
2.05980852991662));
#27433=CARTESIAN_POINT('Ctrl Pts',(-55.8232666097634,-5.81584257440986,
1.09086157875583));
#27434=CARTESIAN_POINT('Ctrl Pts',(-55.8060528039106,-5.88323839985449,
0.73154604450996));
#27435=CARTESIAN_POINT('Ctrl Pts',(-55.7888389980577,-5.91661159960697,
0.365848980037442));
#27436=CARTESIAN_POINT('Ctrl Pts',(-55.7716251922049,-5.91637209757686,
0.000108738722670239));
#27437=CARTESIAN_POINT('Origin',(-29.75,0.,0.));
#27438=CARTESIAN_POINT('',(-53.7698748077951,-5.91709501868191,-0.000108451466299675));
#27439=CARTESIAN_POINT('',(-54.0216251922049,-5.91720758741406,-6.39274240385461E-5));
#27440=CARTESIAN_POINT('',(-29.75,-5.91675,-7.2459289488551E-16));
#27441=CARTESIAN_POINT('Ctrl Pts',(-53.7698748077951,-5.91709501868191,
-0.000108451466299675));
#27442=CARTESIAN_POINT('Ctrl Pts',(-53.8109482918828,-5.91635855568918,
0.872269577364956));
#27443=CARTESIAN_POINT('Ctrl Pts',(-53.8520217759704,-5.72101511215826,
1.74496643472829));
#27444=CARTESIAN_POINT('Ctrl Pts',(-53.8930952600581,-5.34756485588097,
2.53328917546711));
#27445=CARTESIAN_POINT('Ctrl Pts',(-53.9395148080857,-4.92550686659082,
3.42421883818736));
#27446=CARTESIAN_POINT('Ctrl Pts',(-53.9859343561134,-4.275960475547,4.20738096161857));
#27447=CARTESIAN_POINT('Ctrl Pts',(-54.032353904141,-3.47843932873723,4.78690544827096));
#27448=CARTESIAN_POINT('Ctrl Pts',(-54.0787734521686,-2.68091818192746,
5.36642993492334));
#27449=CARTESIAN_POINT('Ctrl Pts',(-54.1251930001962,-1.73542227935175,
5.74231678479689));
#27450=CARTESIAN_POINT('Ctrl Pts',(-54.1716125482238,-0.75769366425266,
5.86855214218494));
#27451=CARTESIAN_POINT('Ctrl Pts',(-54.2180320962514,0.220034950846445,
5.99478749957299));
#27452=CARTESIAN_POINT('Ctrl Pts',(-54.264451644279,1.22999627846893,5.87137136447552));
#27453=CARTESIAN_POINT('Ctrl Pts',(-54.3108711923066,2.14855679747888,5.51341161372878));
#27454=CARTESIAN_POINT('Ctrl Pts',(-54.3572907403343,3.06711731648883,5.15545186298203));
#27455=CARTESIAN_POINT('Ctrl Pts',(-54.4037102883619,3.89427702688625,4.56294849658601));
#27456=CARTESIAN_POINT('Ctrl Pts',(-54.4501298363895,4.52877990555298,3.808432289204));
#27457=CARTESIAN_POINT('Ctrl Pts',(-54.4965493844171,5.1632827842197,3.053916081822));
#27458=CARTESIAN_POINT('Ctrl Pts',(-54.5429689324447,5.60512883115574,2.13738703345401));
#27459=CARTESIAN_POINT('Ctrl Pts',(-54.5893884804723,5.80022985398318,1.17104123554823));
#27460=CARTESIAN_POINT('Ctrl Pts',(-54.6358080284999,5.99533087681063,0.20469543764244));
#27461=CARTESIAN_POINT('Ctrl Pts',(-54.6822275765276,5.94368687552949,-0.811467109801146));
#27462=CARTESIAN_POINT('Ctrl Pts',(-54.7286471245552,5.65161980480209,-1.75305376881625));
#27463=CARTESIAN_POINT('Ctrl Pts',(-54.7750666725828,5.35955273407469,-2.69464042783133));
#27464=CARTESIAN_POINT('Ctrl Pts',(-54.8214862206104,4.82706259390104,-3.56165119841793));
#27465=CARTESIAN_POINT('Ctrl Pts',(-54.867905768638,4.11933369302571,-4.24795172523127));
#27466=CARTESIAN_POINT('Ctrl Pts',(-54.9143253166656,3.41160479215037,-4.9342522520446));
#27467=CARTESIAN_POINT('Ctrl Pts',(-54.9607448646932,2.52863713057334,-5.43984253508467));
#27468=CARTESIAN_POINT('Ctrl Pts',(-55.0071644127209,1.57851841231285,-5.70283118778572));
#27469=CARTESIAN_POINT('Ctrl Pts',(-55.0535839607485,0.628399694052342,
-5.96581984048676));
#27470=CARTESIAN_POINT('Ctrl Pts',(-55.1000035087761,-0.388870080891639,
-5.98620686284878));
#27471=CARTESIAN_POINT('Ctrl Pts',(-55.1464230568037,-1.34876273427931,
-5.76149659559141));
#27472=CARTESIAN_POINT('Ctrl Pts',(-55.1928426048313,-2.30865538766697,
-5.53678632833405));
#27473=CARTESIAN_POINT('Ctrl Pts',(-55.2392621528589,-3.21117091949832,
-5.06697877145731));
#27474=CARTESIAN_POINT('Ctrl Pts',(-55.2856817008865,-3.9458286905366,-4.40958500080568));
#27475=CARTESIAN_POINT('Ctrl Pts',(-55.3321012489141,-4.68048646157487,
-3.75219123015404));
#27476=CARTESIAN_POINT('Ctrl Pts',(-55.3785207969418,-5.24728647182007,
-2.9072112457275));
#27477=CARTESIAN_POINT('Ctrl Pts',(-55.4249403449694,-5.57684440017996,
-1.97808252370154));
#27478=CARTESIAN_POINT('Ctrl Pts',(-55.4565851659113,-5.80150840653206,
-1.34468316309142));
#27479=CARTESIAN_POINT('Ctrl Pts',(-55.4882299868532,-5.91591819911813,
-0.672177110996802));
#27480=CARTESIAN_POINT('Ctrl Pts',(-55.5198748077951,-5.91649353122104,
0.000138118266801851));
#27481=CARTESIAN_POINT('Ctrl Pts',(-55.7716251922049,-5.91637209757686,
0.000108738722670239));
#27482=CARTESIAN_POINT('Ctrl Pts',(-55.7424194500301,-5.9159657473135,-0.620423134477549));
#27483=CARTESIAN_POINT('Ctrl Pts',(-55.7132137078553,-5.8188015680181,-1.24107929692855));
#27484=CARTESIAN_POINT('Ctrl Pts',(-55.6840079656806,-5.62688162061698,
-1.83090334586271));
#27485=CARTESIAN_POINT('Ctrl Pts',(-55.6375884176529,-5.32184444119746,
-2.76836850608727));
#27486=CARTESIAN_POINT('Ctrl Pts',(-55.5911688696254,-4.77743656853128,
-3.62794601330318));
#27487=CARTESIAN_POINT('Ctrl Pts',(-55.5447493215977,-4.0603012100281,-4.30441144852113));
#27488=CARTESIAN_POINT('Ctrl Pts',(-55.4983297735701,-3.34316585152493,
-4.98087688373906));
#27489=CARTESIAN_POINT('Ctrl Pts',(-55.4519102255425,-2.45330300718477,
-5.47423024695903));
#27490=CARTESIAN_POINT('Ctrl Pts',(-55.4054906775148,-1.4996444487146,-5.72407812331081));
#27491=CARTESIAN_POINT('Ctrl Pts',(-55.3590711294872,-0.545985890244415,
-5.97392599966261));
#27492=CARTESIAN_POINT('Ctrl Pts',(-55.3126515814597,0.471468382355783,
-5.98026838914621));
#27493=CARTESIAN_POINT('Ctrl Pts',(-55.2662320334321,1.42816760572891,-5.74232889377354));
#27494=CARTESIAN_POINT('Ctrl Pts',(-55.2198124854045,2.38486682910203,-5.50438939840087));
#27495=CARTESIAN_POINT('Ctrl Pts',(-55.1733929373768,3.28081100324809,-5.02216801817193));
#27496=CARTESIAN_POINT('Ctrl Pts',(-55.1269733893492,4.00632391585948,-4.35469545611802));
#27497=CARTESIAN_POINT('Ctrl Pts',(-55.0805538413215,4.73183682847088,-3.6872228940641));
#27498=CARTESIAN_POINT('Ctrl Pts',(-55.034134293294,5.28691847954762,-2.83449915018519));
#27499=CARTESIAN_POINT('Ctrl Pts',(-54.9877147452664,5.60361904055304,-1.90090964610978));
#27500=CARTESIAN_POINT('Ctrl Pts',(-54.9412951972388,5.92031960155846,-0.96732014203436));
#27501=CARTESIAN_POINT('Ctrl Pts',(-54.8948756492112,5.99863907249256,0.047135122237555));
#27502=CARTESIAN_POINT('Ctrl Pts',(-54.8484561011835,5.82899004470886,1.01827250429678));
#27503=CARTESIAN_POINT('Ctrl Pts',(-54.8020365531559,5.65934101692516,1.98940988635599));
#27504=CARTESIAN_POINT('Ctrl Pts',(-54.7556170051283,5.24172349042367,2.9172293862025));
#27505=CARTESIAN_POINT('Ctrl Pts',(-54.7091974571007,4.62725974471876,3.68815280177316));
#27506=CARTESIAN_POINT('Ctrl Pts',(-54.6627779090731,4.01279599901386,4.45907621734382));
#27507=CARTESIAN_POINT('Ctrl Pts',(-54.6163583610455,3.20148603410555,5.07310354863862));
#27508=CARTESIAN_POINT('Ctrl Pts',(-54.5699388130179,2.29264564056018,5.45506918390062));
#27509=CARTESIAN_POINT('Ctrl Pts',(-54.5235192649903,1.3838052470148,5.83703481916262));
#27510=CARTESIAN_POINT('Ctrl Pts',(-54.4770997169626,0.377434424832348,
5.98693875839182));
#27511=CARTESIAN_POINT('Ctrl Pts',(-54.430680168935,-0.603272833393652,
5.88643064367627));
#27512=CARTESIAN_POINT('Ctrl Pts',(-54.3842606209074,-1.58398009161965,
5.78592252896073));
#27513=CARTESIAN_POINT('Ctrl Pts',(-54.3378410728798,-2.53902378588921,
5.43500236030046));
#27514=CARTESIAN_POINT('Ctrl Pts',(-54.2914215248522,-3.3514930884985,4.87662771924089));
#27515=CARTESIAN_POINT('Ctrl Pts',(-54.2450019768246,-4.16396239110779,
4.31825307818133));
#27516=CARTESIAN_POINT('Ctrl Pts',(-54.198582428797,-4.83385730205682,3.55242396472248));
#27517=CARTESIAN_POINT('Ctrl Pts',(-54.1521628807693,-5.27917322932164,
2.6728886712947));
#27518=CARTESIAN_POINT('Ctrl Pts',(-54.1086503179145,-5.69660162099499,
1.84843353623915));
#27519=CARTESIAN_POINT('Ctrl Pts',(-54.0651377550597,-5.9166984185426,0.924067797853219));
#27520=CARTESIAN_POINT('Ctrl Pts',(-54.0216251922049,-5.91720758741406,
-6.39274240385461E-5));
#27521=CARTESIAN_POINT('Origin',(-29.75,0.,0.));
#27522=CARTESIAN_POINT('',(-52.0198748077951,-5.91625820056289,4.45556367170696E-5));
#27523=CARTESIAN_POINT('',(-52.2716251922048,-5.91623884227222,-3.64161732908164E-6));
#27524=CARTESIAN_POINT('',(-29.75,-5.91675,-7.2459289488551E-16));
#27525=CARTESIAN_POINT('Ctrl Pts',(-52.0198748077951,-5.91625820056289,
4.45556367170696E-5));
#27526=CARTESIAN_POINT('Ctrl Pts',(-52.0408275008571,-5.91637479742008,
0.445249139576727));
#27527=CARTESIAN_POINT('Ctrl Pts',(-52.0617801939192,-5.86678403741804,
0.890428155919709));
#27528=CARTESIAN_POINT('Ctrl Pts',(-52.0827328869812,-5.7672074757706,1.32413060753377));
#27529=CARTESIAN_POINT('Ctrl Pts',(-52.1291524350089,-5.54660103763264,
2.28497472063982));
#27530=CARTESIAN_POINT('Ctrl Pts',(-52.1755719830365,-5.08065436583636,
3.18948957664679));
#27531=CARTESIAN_POINT('Ctrl Pts',(-52.2219915310641,-4.42640590939973,
3.92694979082025));
#27532=CARTESIAN_POINT('Ctrl Pts',(-52.2684110790917,-3.7721574529631,4.66441000499372));
#27533=CARTESIAN_POINT('Ctrl Pts',(-52.3148306271193,-2.92960721188612,
5.23481557733369));
#27534=CARTESIAN_POINT('Ctrl Pts',(-52.3612501751469,-2.0018952274647,5.56834081505848));
#27535=CARTESIAN_POINT('Ctrl Pts',(-52.4076697231746,-1.07418324304329,
5.90186605278327));
#27536=CARTESIAN_POINT('Ctrl Pts',(-52.4540892712022,-0.0613095152774347,
5.99851095589289));
#27537=CARTESIAN_POINT('Ctrl Pts',(-52.5005088192298,0.912735915813663,
5.84644482419666));
#27538=CARTESIAN_POINT('Ctrl Pts',(-52.5469283672574,1.88678134690476,5.69437869250042));
#27539=CARTESIAN_POINT('Ctrl Pts',(-52.593347915285,2.82199848132111,5.29360152599834));
#27540=CARTESIAN_POINT('Ctrl Pts',(-52.6397674633126,3.60390354211778,4.69317410645535));
#27541=CARTESIAN_POINT('Ctrl Pts',(-52.6861870113402,4.38580860291444,4.09274668691237));
#27542=CARTESIAN_POINT('Ctrl Pts',(-52.7326065593678,5.01440159009144,3.29266901432849));
#27543=CARTESIAN_POINT('Ctrl Pts',(-52.7790261073954,5.41273385003153,2.39088188815653));
#27544=CARTESIAN_POINT('Ctrl Pts',(-52.825445655423,5.81106610997162,1.48909476198456));
#27545=CARTESIAN_POINT('Ctrl Pts',(-52.8718652034507,5.9791376426748,0.485598182224505));
#27546=CARTESIAN_POINT('Ctrl Pts',(-52.9182847514783,5.89637412036982,-0.496765706369812));
#27547=CARTESIAN_POINT('Ctrl Pts',(-52.9647042995059,5.81361059806484,-1.47912959496415));
#27548=CARTESIAN_POINT('Ctrl Pts',(-53.0111238475335,5.48001202075168,-2.44036079239273));
#27549=CARTESIAN_POINT('Ctrl Pts',(-53.0575433955611,4.93641556271725,-3.26279103323443));
#27550=CARTESIAN_POINT('Ctrl Pts',(-53.1039629435887,4.39281910468283,-4.08522127407612));
#27551=CARTESIAN_POINT('Ctrl Pts',(-53.1503824916163,3.63922476592713,-4.76885055833092));
#27552=CARTESIAN_POINT('Ctrl Pts',(-53.196802039644,2.76788312977477,-5.22999301283475));
#27553=CARTESIAN_POINT('Ctrl Pts',(-53.2432215876716,1.89654149362241,-5.69113546733857));
#27554=CARTESIAN_POINT('Ctrl Pts',(-53.2896411356992,0.90745256007338,-5.92979109209143));
#27555=CARTESIAN_POINT('Ctrl Pts',(-53.3360606837268,-0.0783052253648198,
-5.91674507022845));
#27556=CARTESIAN_POINT('Ctrl Pts',(-53.3824802317544,-1.06406301080302,
-5.90369904836547));
#27557=CARTESIAN_POINT('Ctrl Pts',(-53.428899779782,-2.04648964813039,-5.63895137988666));
#27558=CARTESIAN_POINT('Ctrl Pts',(-53.4753193278097,-2.90532225092888,
-5.1549109160731));
#27559=CARTESIAN_POINT('Ctrl Pts',(-53.5217388758373,-3.76415485372738,
-4.67087045225953));
#27560=CARTESIAN_POINT('Ctrl Pts',(-53.5681584238649,-4.49939342199699,
-3.96753719311121));
#27561=CARTESIAN_POINT('Ctrl Pts',(-53.6145779718925,-5.02103437779471,
-3.13100905642186));
#27562=CARTESIAN_POINT('Ctrl Pts',(-53.6609975199201,-5.54267533359243,
-2.29448091973252));
#27563=CARTESIAN_POINT('Ctrl Pts',(-53.7074170679477,-5.85071867691826,
-1.32475790550216));
#27564=CARTESIAN_POINT('Ctrl Pts',(-53.7538366159753,-5.90745555481293,
-0.340547797382322));
#27565=CARTESIAN_POINT('Ctrl Pts',(-53.7591826799153,-5.91398984887363,
-0.227197918033964));
#27566=CARTESIAN_POINT('Ctrl Pts',(-53.7645287438552,-5.91719087561579,
-0.113655885425565));
#27567=CARTESIAN_POINT('Ctrl Pts',(-53.7698748077951,-5.91709501868191,
-0.000108451466299675));
#27568=CARTESIAN_POINT('Ctrl Pts',(-54.0216251922049,-5.91720758741406,
-6.39274240385461E-5));
#27569=CARTESIAN_POINT('Ctrl Pts',(-54.0187182070321,-5.91724160394314,
-0.061803274564678));
#27570=CARTESIAN_POINT('Ctrl Pts',(-54.0158112218593,-5.91629553449657,
-0.123541577234064));
#27571=CARTESIAN_POINT('Ctrl Pts',(-54.0129042366865,-5.91436274267908,
-0.185248973901452));
#27572=CARTESIAN_POINT('Ctrl Pts',(-53.9664846886589,-5.88349938519108,
-1.17060985227313));
#27573=CARTESIAN_POINT('Ctrl Pts',(-53.9200651406313,-5.60103572663448,
-2.14809013561975));
#27574=CARTESIAN_POINT('Ctrl Pts',(-53.8736455926037,-5.10154930552007,
-2.99803244106357));
#27575=CARTESIAN_POINT('Ctrl Pts',(-53.8272260445761,-4.60206288440565,
-3.84797474650739));
#27576=CARTESIAN_POINT('Ctrl Pts',(-53.7808064965484,-3.88555370073343,
-4.5703790740484));
#27577=CARTESIAN_POINT('Ctrl Pts',(-53.7343869485208,-3.03973259142438,
-5.07681293795175));
#27578=CARTESIAN_POINT('Ctrl Pts',(-53.6879674004932,-2.19391148211535,
-5.58324680185509));
#27579=CARTESIAN_POINT('Ctrl Pts',(-53.6415478524656,-1.2187784471695,-5.87371020212078));
#27580=CARTESIAN_POINT('Ctrl Pts',(-53.595128304438,-0.233703533131209,
-5.91264631894415));
#27581=CARTESIAN_POINT('Ctrl Pts',(-53.5487087564104,0.751371380907081,
-5.95158243576752));
#27582=CARTESIAN_POINT('Ctrl Pts',(-53.5022892083828,1.74638817403782,-5.73899126914857));
#27583=CARTESIAN_POINT('Ctrl Pts',(-53.4558696603552,2.62954274707465,-5.30089697840176));
#27584=CARTESIAN_POINT('Ctrl Pts',(-53.4094501123276,3.51269732011148,-4.86280268765496));
#27585=CARTESIAN_POINT('Ctrl Pts',(-53.3630305642999,4.2839896730544,-4.19920527278031));
#27586=CARTESIAN_POINT('Ctrl Pts',(-53.3166110162723,4.84900273585183,-3.39133842339913));
#27587=CARTESIAN_POINT('Ctrl Pts',(-53.2701914682447,5.41401579864927,-2.58347157401794));
#27588=CARTESIAN_POINT('Ctrl Pts',(-53.2237719202171,5.77274957130122,-1.63133529013022));
#27589=CARTESIAN_POINT('Ctrl Pts',(-53.1773523721895,5.88128997685213,-0.651484491373765));
#27590=CARTESIAN_POINT('Ctrl Pts',(-53.1309328241619,5.98983038240304,0.328366307382695));
#27591=CARTESIAN_POINT('Ctrl Pts',(-53.0845132761342,5.84817742085291,1.33593162100792));
#27592=CARTESIAN_POINT('Ctrl Pts',(-53.0380937281066,5.4736714139911,2.24787123429668));
#27593=CARTESIAN_POINT('Ctrl Pts',(-52.991674180079,5.09916540712929,3.15981084758544));
#27594=CARTESIAN_POINT('Ctrl Pts',(-52.9452546320514,4.49180635495582,3.97612476053773));
#27595=CARTESIAN_POINT('Ctrl Pts',(-52.8988350840238,3.72594357774684,4.59688462872073));
#27596=CARTESIAN_POINT('Ctrl Pts',(-52.8524155359962,2.96008080053786,5.21764449690374));
#27597=CARTESIAN_POINT('Ctrl Pts',(-52.8059959879686,2.03571429829339,5.64285032031743));
#27598=CARTESIAN_POINT('Ctrl Pts',(-52.759576439941,1.06599957743425,5.82045090480384));
#27599=CARTESIAN_POINT('Ctrl Pts',(-52.7131568919134,0.0962848565751215,
5.99805148929024));
#27600=CARTESIAN_POINT('Ctrl Pts',(-52.6667373438857,-0.918778082898684,
5.92804683484937));
#27601=CARTESIAN_POINT('Ctrl Pts',(-52.6203177958581,-1.85493121055628,
5.6190064992333));
#27602=CARTESIAN_POINT('Ctrl Pts',(-52.5738982478305,-2.79108433821389,
5.30996616361722));
#27603=CARTESIAN_POINT('Ctrl Pts',(-52.5274786998029,-3.6483276540553,4.76189014682594));
#27604=CARTESIAN_POINT('Ctrl Pts',(-52.4810591517753,-4.3217224770548,4.04187068888172));
#27605=CARTESIAN_POINT('Ctrl Pts',(-52.4346396037477,-4.9951173000543,3.32185123093749));
#27606=CARTESIAN_POINT('Ctrl Pts',(-52.38822005572,-5.48466363021188,2.42988833184032));
#27607=CARTESIAN_POINT('Ctrl Pts',(-52.3418005076924,-5.7304340872396,1.47517083964002));
#27608=CARTESIAN_POINT('Ctrl Pts',(-52.3184087358632,-5.85428291165581,
0.994068918406044));
#27609=CARTESIAN_POINT('Ctrl Pts',(-52.295016964034,-5.91622824475799,0.497031341361674));
#27610=CARTESIAN_POINT('Ctrl Pts',(-52.2716251922048,-5.91623884227222,
-3.64161732908164E-6));
#27611=CARTESIAN_POINT('Origin',(-29.75,0.,0.));
#27612=CARTESIAN_POINT('',(-50.2698748077951,-5.91725823033598,1.89064590639526E-5));
#27613=CARTESIAN_POINT('',(-50.5216251922048,-5.91719392214832,7.12702798121252E-5));
#27614=CARTESIAN_POINT('',(-29.75,-5.91675,-7.2459289488551E-16));
#27615=CARTESIAN_POINT('Ctrl Pts',(-50.2698748077951,-5.91725823033598,
1.89064590639526E-5));
#27616=CARTESIAN_POINT('Ctrl Pts',(-50.2707067098315,-5.91726143750099,
0.0176866299085558));
#27617=CARTESIAN_POINT('Ctrl Pts',(-50.271538611868,-5.9171839715363,0.0353543251200561));
#27618=CARTESIAN_POINT('Ctrl Pts',(-50.2723705139044,-5.91702566130763,
0.0530212959021068));
#27619=CARTESIAN_POINT('Ctrl Pts',(-50.318790061932,-5.90819206198753,1.03882582914462));
#27620=CARTESIAN_POINT('Ctrl Pts',(-50.3652096099596,-5.64764487955008,
2.0223748067859));
#27621=CARTESIAN_POINT('Ctrl Pts',(-50.4116291579872,-5.16727876649904,
2.88326795211271));
#27622=CARTESIAN_POINT('Ctrl Pts',(-50.4580487060148,-4.68691265344798,
3.74416109743955));
#27623=CARTESIAN_POINT('Ctrl Pts',(-50.5044682540424,-3.98672760978333,
4.48239841045192));
#27624=CARTESIAN_POINT('Ctrl Pts',(-50.55088780207,-3.15243616728958,5.00760922452588));
#27625=CARTESIAN_POINT('Ctrl Pts',(-50.5973073500976,-2.31814472479584,
5.53282003859983));
#27626=CARTESIAN_POINT('Ctrl Pts',(-50.6437268981253,-1.34974688347302,
5.84500435373537));
#27627=CARTESIAN_POINT('Ctrl Pts',(-50.6901464461529,-0.365788207105206,
5.90594640357791));
#27628=CARTESIAN_POINT('Ctrl Pts',(-50.7365659941805,0.618170469262604,
5.96688845342044));
#27629=CARTESIAN_POINT('Ctrl Pts',(-50.7829855422081,1.6176899806754,5.77658823796997));
#27630=CARTESIAN_POINT('Ctrl Pts',(-50.8294050902357,2.51041503167754,5.35834118950254));
#27631=CARTESIAN_POINT('Ctrl Pts',(-50.8758246382633,3.40314008267966,4.94009414103513));
#27632=CARTESIAN_POINT('Ctrl Pts',(-50.9222441862909,4.18907067327115,4.29390025955077));
#27633=CARTESIAN_POINT('Ctrl Pts',(-50.9686637343185,4.77199780650754,3.49886279654966));
#27634=CARTESIAN_POINT('Ctrl Pts',(-51.0150832823462,5.35492493974395,2.70382533354852));
#27635=CARTESIAN_POINT('Ctrl Pts',(-51.0615028303738,5.73484861562527,1.75994428903063));
#27636=CARTESIAN_POINT('Ctrl Pts',(-51.1079223784014,5.86526081396552,0.782764024820095));
#27637=CARTESIAN_POINT('Ctrl Pts',(-51.154341926429,5.99567301230578,-0.194416239390436));
#27638=CARTESIAN_POINT('Ctrl Pts',(-51.2007614744566,5.87657373310498,-1.2048957232936));
#27639=CARTESIAN_POINT('Ctrl Pts',(-51.2471810224842,5.52254240910932,-2.12497747611146));
#27640=CARTESIAN_POINT('Ctrl Pts',(-51.2936005705118,5.16851108511367,-3.04505922892933));
#27641=CARTESIAN_POINT('Ctrl Pts',(-51.3400201185395,4.57954771632317,-3.87474325066188));
#27642=CARTESIAN_POINT('Ctrl Pts',(-51.3864396665671,3.82774973173052,-4.51246450685531));
#27643=CARTESIAN_POINT('Ctrl Pts',(-51.4328592145947,3.07595174713789,-5.15018576304874));
#27644=CARTESIAN_POINT('Ctrl Pts',(-51.4792787626223,2.1613191467431,-5.59594425370305));
#27645=CARTESIAN_POINT('Ctrl Pts',(-51.5256983106499,1.19581586999591,-5.79517284810884));
#27646=CARTESIAN_POINT('Ctrl Pts',(-51.5721178586775,0.230312593248732,
-5.99440144251464));
#27647=CARTESIAN_POINT('Ctrl Pts',(-51.6185374067051,-0.786061359850855,
-5.94710014067192));
#27648=CARTESIAN_POINT('Ctrl Pts',(-51.6649569547327,-1.7288874723005,-5.65905928953872));
#27649=CARTESIAN_POINT('Ctrl Pts',(-51.7113765027604,-2.67171358475018,
-5.37101843840551));
#27650=CARTESIAN_POINT('Ctrl Pts',(-51.757796050788,-3.54099185654992,-4.84223803798179));
#27651=CARTESIAN_POINT('Ctrl Pts',(-51.8042155988156,-4.23031035820282,
-4.13744827250734));
#27652=CARTESIAN_POINT('Ctrl Pts',(-51.8506351468432,-4.91962885985571,
-3.4326585070329));
#27653=CARTESIAN_POINT('Ctrl Pts',(-51.8970546948708,-5.42898759136177,
-2.55185937650774));
#27654=CARTESIAN_POINT('Ctrl Pts',(-51.9434742428984,-5.69603385487499,
-1.60287312614258));
#27655=CARTESIAN_POINT('Ctrl Pts',(-51.968941097864,-5.84254171096053,-1.08223696682489));
#27656=CARTESIAN_POINT('Ctrl Pts',(-51.9944079528295,-5.91611648344602,
-0.541077319991566));
#27657=CARTESIAN_POINT('Ctrl Pts',(-52.0198748077951,-5.91625820056289,
4.45556367170696E-5));
#27658=CARTESIAN_POINT('Ctrl Pts',(-52.2716251922048,-5.91623884227222,
-3.64161732908164E-6));
#27659=CARTESIAN_POINT('Ctrl Pts',(-52.2485974160064,-5.91624927488023,
-0.489304342495949));
#27660=CARTESIAN_POINT('Ctrl Pts',(-52.225569639808,-5.85623748812403,-0.97860252941275));
#27661=CARTESIAN_POINT('Ctrl Pts',(-52.2025418636096,-5.73617367371246,
-1.45269247238703));
#27662=CARTESIAN_POINT('Ctrl Pts',(-52.156122315582,-5.49414821925973,-2.40836620691037));
#27663=CARTESIAN_POINT('Ctrl Pts',(-52.1097027675544,-5.0081027264564,-3.30224159065363));
#27664=CARTESIAN_POINT('Ctrl Pts',(-52.0632832195268,-4.33753602368729,
-4.02489566045343));
#27665=CARTESIAN_POINT('Ctrl Pts',(-52.0168636714992,-3.6669693209182,-4.74754973025321));
#27666=CARTESIAN_POINT('Ctrl Pts',(-51.9704441234715,-2.81188140818333,
-5.29898248610953));
#27667=CARTESIAN_POINT('Ctrl Pts',(-51.9240245754439,-1.87694711474672,
-5.61169077576142));
#27668=CARTESIAN_POINT('Ctrl Pts',(-51.8776050274163,-0.94201282131012,
-5.9243990654133));
#27669=CARTESIAN_POINT('Ctrl Pts',(-51.8311854793887,0.0727678528282248,
-5.99838288886075));
#27670=CARTESIAN_POINT('Ctrl Pts',(-51.7847659313611,1.0431714304984,-5.82458558190312));
#27671=CARTESIAN_POINT('Ctrl Pts',(-51.7383463833335,2.0135750081686,-5.6507882749455));
#27672=CARTESIAN_POINT('Ctrl Pts',(-51.6919268353059,2.93960148937063,-5.22920983758279));
#27673=CARTESIAN_POINT('Ctrl Pts',(-51.6455072872783,3.70789216283027,-4.61145742072327));
#27674=CARTESIAN_POINT('Ctrl Pts',(-51.5990877392506,4.47618283628991,-3.99370500386375));
#27675=CARTESIAN_POINT('Ctrl Pts',(-51.552668191223,5.08673770200714,-3.17977860750742));
#27676=CARTESIAN_POINT('Ctrl Pts',(-51.5062486431954,5.46481622702219,-2.26931431035827));
#27677=CARTESIAN_POINT('Ctrl Pts',(-51.4598290951678,5.84289475203723,-1.35885001320913));
#27678=CARTESIAN_POINT('Ctrl Pts',(-51.4134095471402,5.98849693635009,-0.351847815267173));
#27679=CARTESIAN_POINT('Ctrl Pts',(-51.3669899991126,5.88379901756576,0.628421001569855));
#27680=CARTESIAN_POINT('Ctrl Pts',(-51.320570451085,5.77910109878143,1.60868981840687));
#27681=CARTESIAN_POINT('Ctrl Pts',(-51.2741509030574,5.42410307689992,2.56222525413896));
#27682=CARTESIAN_POINT('Ctrl Pts',(-51.2277313550298,4.86226172025593,3.37230111319492));
#27683=CARTESIAN_POINT('Ctrl Pts',(-51.1813118070021,4.30042036361194,4.18237697225088));
#27684=CARTESIAN_POINT('Ctrl Pts',(-51.1348922589745,3.53173567220546,4.8489932546307));
#27685=CARTESIAN_POINT('Ctrl Pts',(-51.0884727109469,2.65030550151139,5.29054671872201));
#27686=CARTESIAN_POINT('Ctrl Pts',(-51.0420531629193,1.76887533081731,5.73210018281333));
#27687=CARTESIAN_POINT('Ctrl Pts',(-50.9956336148917,0.774699680835636,
5.94859082861613));
#27688=CARTESIAN_POINT('Ctrl Pts',(-50.9492140668641,-0.210520317040655,
5.91351714552642));
#27689=CARTESIAN_POINT('Ctrl Pts',(-50.9027945188365,-1.19574031491695,
5.87844346243672));
#27690=CARTESIAN_POINT('Ctrl Pts',(-50.8563749708089,-2.17200466068785,
5.59180545045453));
#27691=CARTESIAN_POINT('Ctrl Pts',(-50.8099554227812,-3.01980481939666,
5.08869164786692));
#27692=CARTESIAN_POINT('Ctrl Pts',(-50.7635358747536,-3.86760497810546,
4.58557784527932));
#27693=CARTESIAN_POINT('Ctrl Pts',(-50.717116326726,-4.58694094975216,3.86598825208632));
#27694=CARTESIAN_POINT('Ctrl Pts',(-50.6706967786984,-5.08975585867029,
3.01801079081128));
#27695=CARTESIAN_POINT('Ctrl Pts',(-50.6242772306708,-5.59257076758842,
2.17003332953624));
#27696=CARTESIAN_POINT('Ctrl Pts',(-50.5778576826432,-5.87886461377798,
1.19366800017916));
#27697=CARTESIAN_POINT('Ctrl Pts',(-50.5314381346156,-5.91359098970248,
0.208435699512988));
#27698=CARTESIAN_POINT('Ctrl Pts',(-50.528167153812,-5.91603800424384,0.139010724917649));
#27699=CARTESIAN_POINT('Ctrl Pts',(-50.5248961730084,-5.9172358858531,0.0695417222694849));
#27700=CARTESIAN_POINT('Ctrl Pts',(-50.5216251922048,-5.91719392214832,
7.12702798121252E-5));
#27701=CARTESIAN_POINT('Origin',(-29.75,0.,0.));
#27702=CARTESIAN_POINT('',(-48.5198748077951,-5.91629691922315,-7.52784257820883E-5));
#27703=CARTESIAN_POINT('',(-48.7716251922048,-5.91638811723421,-0.000113882446527966));
#27704=CARTESIAN_POINT('',(-29.75,-5.91675,-7.2459289488551E-16));
#27705=CARTESIAN_POINT('Ctrl Pts',(-48.5198748077951,-5.91629691922315,
-7.52784257820882E-5));
#27706=CARTESIAN_POINT('Ctrl Pts',(-48.5470054668335,-5.91603979408007,
0.576388453514846));
#27707=CARTESIAN_POINT('Ctrl Pts',(-48.5741361258719,-5.8323893316429,1.15292520994488));
#27708=CARTESIAN_POINT('Ctrl Pts',(-48.6012667849103,-5.66639543983512,
1.70468960629431));
#27709=CARTESIAN_POINT('Ctrl Pts',(-48.6476863329379,-5.38238606792292,
2.64873795617079));
#27710=CARTESIAN_POINT('Ctrl Pts',(-48.6941058809656,-4.85732506278092,
3.52026785615966));
#27711=CARTESIAN_POINT('Ctrl Pts',(-48.7405254289932,-4.1554873021707,4.21259174569411));
#27712=CARTESIAN_POINT('Ctrl Pts',(-48.7869449770208,-3.45364954156048,
4.90491563522857));
#27713=CARTESIAN_POINT('Ctrl Pts',(-48.8333645250484,-2.57503502548203,
5.41803351430862));
#27714=CARTESIAN_POINT('Ctrl Pts',(-48.879784073076,-1.62719857150409,5.6891325123684));
#27715=CARTESIAN_POINT('Ctrl Pts',(-48.9262036211036,-0.679362117526128,
5.96023151042818));
#27716=CARTESIAN_POINT('Ctrl Pts',(-48.9726231691312,0.337696274351328,
5.9893116274677));
#27717=CARTESIAN_POINT('Ctrl Pts',(-49.0190427171588,1.29947430215932,5.77281304672337));
#27718=CARTESIAN_POINT('Ctrl Pts',(-49.0654622651865,2.26125232996726,5.55631446597905));
#27719=CARTESIAN_POINT('Ctrl Pts',(-49.1118818132141,3.1677499937057,5.09423718745094));
#27720=CARTESIAN_POINT('Ctrl Pts',(-49.1583013612417,3.90799918498855,4.44314599180816));
#27721=CARTESIAN_POINT('Ctrl Pts',(-49.2047209092693,4.64824837627141,3.79205479616537));
#27722=CARTESIAN_POINT('Ctrl Pts',(-49.2511404572969,5.22224909509864,2.95194968340791));
#27723=CARTESIAN_POINT('Ctrl Pts',(-49.2975600053245,5.55973555201645,2.02567137661478));
#27724=CARTESIAN_POINT('Ctrl Pts',(-49.3439795533521,5.89722200893427,1.09939306982164));
#27725=CARTESIAN_POINT('Ctrl Pts',(-49.3903991013797,5.99819420394269,0.0869415689928164));
#27726=CARTESIAN_POINT('Ctrl Pts',(-49.4368186494074,5.85029171524704,-0.887744772388931));
#27727=CARTESIAN_POINT('Ctrl Pts',(-49.483238197435,5.7023892265514,-1.86243111377068));
#27728=CARTESIAN_POINT('Ctrl Pts',(-49.5296577454626,5.3056120541517,-2.79935229570535));
#27729=CARTESIAN_POINT('Ctrl Pts',(-49.5760772934902,4.70853132407867,-3.58381594178078));
#27730=CARTESIAN_POINT('Ctrl Pts',(-49.6224968415178,4.11145059400564,-4.36827958785621));
#27731=CARTESIAN_POINT('Ctrl Pts',(-49.6689163895454,3.31406630625929,-5.00028569807241));
#27732=CARTESIAN_POINT('Ctrl Pts',(-49.715335937573,2.41398955197377,-5.40246780437918));
#27733=CARTESIAN_POINT('Ctrl Pts',(-49.7617554856006,1.51391279768828,-5.80464991068593));
#27734=CARTESIAN_POINT('Ctrl Pts',(-49.8081750336282,0.511143576863623,
-5.97700801308327));
#27735=CARTESIAN_POINT('Ctrl Pts',(-49.8545945816558,-0.471565004746035,
-5.89844304716854));
#27736=CARTESIAN_POINT('Ctrl Pts',(-49.9010141296834,-1.45427358635572,
-5.81987808125382));
#27737=CARTESIAN_POINT('Ctrl Pts',(-49.9474336777111,-2.41692152875041,
-5.49039004702702));
#27738=CARTESIAN_POINT('Ctrl Pts',(-49.9938532257387,-3.24166713692909,
-4.95031293028491));
#27739=CARTESIAN_POINT('Ctrl Pts',(-50.0402727737663,-4.06641274510778,
-4.41023581354281));
#27740=CARTESIAN_POINT('Ctrl Pts',(-50.0866923217939,-4.75325601907047,
-3.65956961428539));
#27741=CARTESIAN_POINT('Ctrl Pts',(-50.1331118698215,-5.21811764795045,
-2.79020647023479));
#27742=CARTESIAN_POINT('Ctrl Pts',(-50.1786995158127,-5.67464831816857,
-1.93642350739356));
#27743=CARTESIAN_POINT('Ctrl Pts',(-50.2242871618039,-5.91708247995128,
-0.968159901647365));
#27744=CARTESIAN_POINT('Ctrl Pts',(-50.2698748077951,-5.91725823033598,
1.89064590639526E-5));
#27745=CARTESIAN_POINT('Ctrl Pts',(-50.5216251922048,-5.91719392214832,
7.12702798121252E-5));
#27746=CARTESIAN_POINT('Ctrl Pts',(-50.4784766249808,-5.91664036532686,
-0.916335962829449));
#27747=CARTESIAN_POINT('Ctrl Pts',(-50.4353280577568,-5.7003400533041,-1.83299539734153));
#27748=CARTESIAN_POINT('Ctrl Pts',(-50.3921794905327,-5.28961211713201,
-2.65217033476586));
#27749=CARTESIAN_POINT('Ctrl Pts',(-50.3457599425051,-4.84774796297761,
-3.53344479640325));
#27750=CARTESIAN_POINT('Ctrl Pts',(-50.2993403944775,-4.18086074900938,
-4.30189444770271));
#27751=CARTESIAN_POINT('Ctrl Pts',(-50.2529208464499,-3.37058688269006,
-4.86345020541586));
#27752=CARTESIAN_POINT('Ctrl Pts',(-50.2065012984223,-2.56031301637074,
-5.425005963129));
#27753=CARTESIAN_POINT('Ctrl Pts',(-50.1600817503947,-1.60665249770033,
-5.77966782725582));
#27754=CARTESIAN_POINT('Ctrl Pts',(-50.113662202367,-0.626346834167139,
-5.88402017991531));
#27755=CARTESIAN_POINT('Ctrl Pts',(-50.0672426543394,0.35395882936604,-5.98837253257481));
#27756=CARTESIAN_POINT('Ctrl Pts',(-50.0208231063118,1.36090963776204,-5.842415373767));
#27757=CARTESIAN_POINT('Ctrl Pts',(-49.9744035582842,2.27124059992882,-5.4640159197752));
#27758=CARTESIAN_POINT('Ctrl Pts',(-49.9279840102566,3.18157156209561,-5.08561646578339));
#27759=CARTESIAN_POINT('Ctrl Pts',(-49.881564462229,3.9952826780332,-4.47477471660759));
#27760=CARTESIAN_POINT('Ctrl Pts',(-49.8351449142014,4.61276422239933,-3.70626632379198));
#27761=CARTESIAN_POINT('Ctrl Pts',(-49.7887253661737,5.23024576676547,-2.93775793097636));
#27762=CARTESIAN_POINT('Ctrl Pts',(-49.7423058181462,5.65149773956015,-2.01158289452093));
#27763=CARTESIAN_POINT('Ctrl Pts',(-49.6958862701186,5.82495295374594,-1.04111811095968));
#27764=CARTESIAN_POINT('Ctrl Pts',(-49.6494667220909,5.99840816793174,-0.0706533273984164));
#27765=CARTESIAN_POINT('Ctrl Pts',(-49.6030471740633,5.92406662350867,0.944101203268662));
#27766=CARTESIAN_POINT('Ctrl Pts',(-49.5566276260357,5.61102877477366,1.87892520420157));
#27767=CARTESIAN_POINT('Ctrl Pts',(-49.5102080780081,5.29799092603865,2.81374920513445));
#27768=CARTESIAN_POINT('Ctrl Pts',(-49.4637885299805,4.74625677299171,3.66864267633316));
#27769=CARTESIAN_POINT('Ctrl Pts',(-49.4173689819529,4.0233663631639,4.33895459092201));
#27770=CARTESIAN_POINT('Ctrl Pts',(-49.3709494339252,3.30047595333607,5.00926650551086));
#27771=CARTESIAN_POINT('Ctrl Pts',(-49.3245298858977,2.40642928672737,5.49499686348987));
#27772=CARTESIAN_POINT('Ctrl Pts',(-49.27811033787,1.45067029394137,5.73668541342454));
#27773=CARTESIAN_POINT('Ctrl Pts',(-49.2316907898424,0.494911301155378,
5.97837396335922));
#27774=CARTESIAN_POINT('Ctrl Pts',(-49.1852712418148,-0.522560017807911,
5.97602070524955));
#27775=CARTESIAN_POINT('Ctrl Pts',(-49.1388516937872,-1.47719081287612,
5.72991371110214));
#27776=CARTESIAN_POINT('Ctrl Pts',(-49.0924321457596,-2.43182160794432,
5.48380671695473));
#27777=CARTESIAN_POINT('Ctrl Pts',(-49.046012597732,-3.32361187911748,4.99394598676957));
#27778=CARTESIAN_POINT('Ctrl Pts',(-48.9995930497044,-4.0433939104401,4.32029738783544));
#27779=CARTESIAN_POINT('Ctrl Pts',(-48.9531735016768,-4.76317594176271,
3.64664878890133));
#27780=CARTESIAN_POINT('Ctrl Pts',(-48.9067539536491,-5.3109497332348,2.78921232121828));
#27781=CARTESIAN_POINT('Ctrl Pts',(-48.8603344056215,-5.61966004147882,
1.85295031032353));
#27782=CARTESIAN_POINT('Ctrl Pts',(-48.8307646678159,-5.81631173802741,
1.2565416127853));
#27783=CARTESIAN_POINT('Ctrl Pts',(-48.8011949300104,-5.91595569718159,
0.628146902608916));
#27784=CARTESIAN_POINT('Ctrl Pts',(-48.7716251922048,-5.91638811723421,
-0.000113882446527966));
#27785=CARTESIAN_POINT('Origin',(-29.75,0.,0.));
#27786=CARTESIAN_POINT('',(-46.7698748077951,-5.91699642112564,0.00013125821292051));
#27787=CARTESIAN_POINT('',(-47.0216251922048,-5.91683542453774,0.000151426803681578));
#27788=CARTESIAN_POINT('',(-29.75,-5.91675,-7.2459289488551E-16));
#27789=CARTESIAN_POINT('Ctrl Pts',(-46.7698748077951,-5.91699642112564,
0.00013125821292051));
#27790=CARTESIAN_POINT('Ctrl Pts',(-46.7768846758079,-5.91714010263027,
0.149024142477122));
#27791=CARTESIAN_POINT('Ctrl Pts',(-46.7838945438206,-5.91163420665211,
0.297906424512786));
#27792=CARTESIAN_POINT('Ctrl Pts',(-46.7909044118334,-5.90040426837894,
0.446355692343765));
#27793=CARTESIAN_POINT('Ctrl Pts',(-46.837323959861,-5.826039293451,1.42939102270706));
#27794=CARTESIAN_POINT('Ctrl Pts',(-46.8837435078887,-5.5006678187631,2.39343813211343));
#27795=CARTESIAN_POINT('Ctrl Pts',(-46.9301630559163,-4.96411990512314,
3.22048404777175));
#27796=CARTESIAN_POINT('Ctrl Pts',(-46.9765826039439,-4.42757199148317,
4.04752996343008));
#27797=CARTESIAN_POINT('Ctrl Pts',(-47.0230021519715,-3.67984763889115,
4.73757468534036));
#27798=CARTESIAN_POINT('Ctrl Pts',(-47.0694216999991,-2.81247886151601,
5.20614700022172));
#27799=CARTESIAN_POINT('Ctrl Pts',(-47.1158412480267,-1.9451100841409,5.67471931510307));
#27800=CARTESIAN_POINT('Ctrl Pts',(-47.1622607960543,-0.958096881982646,
5.92181922295553));
#27801=CARTESIAN_POINT('Ctrl Pts',(-47.2086803440819,0.0277363982703663,
5.91719820747988));
#27802=CARTESIAN_POINT('Ctrl Pts',(-47.2550998921095,1.01356967852341,5.91257719200423));
#27803=CARTESIAN_POINT('Ctrl Pts',(-47.3015194401372,1.99822303687121,5.65623525320047));
#27804=CARTESIAN_POINT('Ctrl Pts',(-47.3479389881648,2.86116100481487,5.17955226239864));
#27805=CARTESIAN_POINT('Ctrl Pts',(-47.3943585361924,3.72409897275852,4.70286927159681));
#27806=CARTESIAN_POINT('Ctrl Pts',(-47.44077808422,4.46532155029799,4.00584522879691));
#27807=CARTESIAN_POINT('Ctrl Pts',(-47.4871976322476,4.99409263229707,3.17380571466311));
#27808=CARTESIAN_POINT('Ctrl Pts',(-47.5336171802752,5.52286371429616,2.3417662005293));
#27809=CARTESIAN_POINT('Ctrl Pts',(-47.5800367283028,5.83918330075486,1.37471121506159));
#27810=CARTESIAN_POINT('Ctrl Pts',(-47.6264562763305,5.90432940974324,0.391021937534293));
#27811=CARTESIAN_POINT('Ctrl Pts',(-47.6728758243581,5.96947551873162,-0.592667339993006));
#27812=CARTESIAN_POINT('Ctrl Pts',(-47.7192953723857,5.78344815024968,-1.59299090957989));
#27813=CARTESIAN_POINT('Ctrl Pts',(-47.7657149204133,5.36901967979738,-2.48749504770171));
#27814=CARTESIAN_POINT('Ctrl Pts',(-47.8121344684409,4.95459120934508,-3.38199918582354));
#27815=CARTESIAN_POINT('Ctrl Pts',(-47.8585540164685,4.31176163692242,-4.1706838924803));
#27816=CARTESIAN_POINT('Ctrl Pts',(-47.9049735644961,3.51922237511646,-4.75700302804946));
#27817=CARTESIAN_POINT('Ctrl Pts',(-47.9513931125237,2.7266831133105,-5.34332216361862));
#27818=CARTESIAN_POINT('Ctrl Pts',(-47.9978126605514,1.78443416212123,-5.72727572810017));
#27819=CARTESIAN_POINT('Ctrl Pts',(-48.044232208579,0.807820092113927,-5.86186238606547));
#27820=CARTESIAN_POINT('Ctrl Pts',(-48.0906517566066,-0.168793977893349,
-5.99644904403077));
#27821=CARTESIAN_POINT('Ctrl Pts',(-48.1370713046342,-1.17977316671866,
-5.88166879547983));
#27822=CARTESIAN_POINT('Ctrl Pts',(-48.1834908526618,-2.10135935264875,
-5.53157236284835));
#27823=CARTESIAN_POINT('Ctrl Pts',(-48.2299104006894,-3.02294553857886,
-5.18147593021687));
#27824=CARTESIAN_POINT('Ctrl Pts',(-48.2763299487171,-3.85513872161374,
-4.59606331350482));
#27825=CARTESIAN_POINT('Ctrl Pts',(-48.3227494967447,-4.49606671054176,
-3.84699727953507));
#27826=CARTESIAN_POINT('Ctrl Pts',(-48.3691690447723,-5.13699469946979,
-3.09793124556532));
#27827=CARTESIAN_POINT('Ctrl Pts',(-48.4155885927998,-5.58665749429096,
-2.18521179433785));
#27828=CARTESIAN_POINT('Ctrl Pts',(-48.4620081408275,-5.79001002236034,
-1.22056866884206));
#27829=CARTESIAN_POINT('Ctrl Pts',(-48.4812970298167,-5.87450986146415,
-0.819726890916495));
#27830=CARTESIAN_POINT('Ctrl Pts',(-48.5005859188059,-5.91647972563172,
-0.40991954044558));
#27831=CARTESIAN_POINT('Ctrl Pts',(-48.5198748077951,-5.91629691922315,
-7.52784257820882E-5));
#27832=CARTESIAN_POINT('Ctrl Pts',(-48.7716251922048,-5.91638811723421,
-0.000113882446527966));
#27833=CARTESIAN_POINT('Ctrl Pts',(-48.7547753819828,-5.91663452441816,
-0.358117564040023));
#27834=CARTESIAN_POINT('Ctrl Pts',(-48.7379255717607,-5.88466599601319,
-0.716077758865912));
#27835=CARTESIAN_POINT('Ctrl Pts',(-48.7210757615387,-5.82007476214659,
-1.06805130838649));
#27836=CARTESIAN_POINT('Ctrl Pts',(-48.6746562135111,-5.64213234955439,
-2.0377033620953));
#27837=CARTESIAN_POINT('Ctrl Pts',(-48.6282366654835,-5.21660069935406,
-2.96191991540646));
#27838=CARTESIAN_POINT('Ctrl Pts',(-48.5818171174559,-4.59557089150098,
-3.727563817765));
#27839=CARTESIAN_POINT('Ctrl Pts',(-48.5353975694282,-3.9745410836479,-4.49320772012353));
#27840=CARTESIAN_POINT('Ctrl Pts',(-48.4889780214006,-3.15801311814206,
-5.10027897152943));
#27841=CARTESIAN_POINT('Ctrl Pts',(-48.442558473373,-2.24594154247006,-5.47446348258247));
#27842=CARTESIAN_POINT('Ctrl Pts',(-48.3961389253454,-1.33386996679804,
-5.84864799363553));
#27843=CARTESIAN_POINT('Ctrl Pts',(-48.3497193773178,-0.326254780959847,
-5.98994576433573));
#27844=CARTESIAN_POINT('Ctrl Pts',(-48.3032998292902,0.653557694776576,
-5.88105995326694));
#27845=CARTESIAN_POINT('Ctrl Pts',(-48.2568802812626,1.63337017051296,-5.77217414219816));
#27846=CARTESIAN_POINT('Ctrl Pts',(-48.2104607332349,2.58537993614758,-5.4131047493604));
#27847=CARTESIAN_POINT('Ctrl Pts',(-48.1640411852073,3.3930475596625,-4.84780693635691));
#27848=CARTESIAN_POINT('Ctrl Pts',(-48.1176216371797,4.20071518317745,-4.28250912335339));
#27849=CARTESIAN_POINT('Ctrl Pts',(-48.0712020891521,4.86404066457271,-3.51098289018414));
#27850=CARTESIAN_POINT('Ctrl Pts',(-48.0247825411245,5.3018236027229,-2.62767393714141));
#27851=CARTESIAN_POINT('Ctrl Pts',(-47.9783629930969,5.73960654087308,-1.74436498409869));
#27852=CARTESIAN_POINT('Ctrl Pts',(-47.9319434450693,5.95184693577819,-0.749273311182518));
#27853=CARTESIAN_POINT('Ctrl Pts',(-47.8855238970416,5.91256356753235,0.235787816078176));
#27854=CARTESIAN_POINT('Ctrl Pts',(-47.839104349014,5.87328019928651,1.22084894333886));
#27855=CARTESIAN_POINT('Ctrl Pts',(-47.7926848009865,5.58247306788974,2.19587952494403));
#27856=CARTESIAN_POINT('Ctrl Pts',(-47.7462652529588,5.07574107068855,3.0415220560843));
#27857=CARTESIAN_POINT('Ctrl Pts',(-47.6998457049312,4.56900907348736,3.88716458722458));
#27858=CARTESIAN_POINT('Ctrl Pts',(-47.6534261569035,3.84635221048174,4.60341906789995));
#27859=CARTESIAN_POINT('Ctrl Pts',(-47.6070066088759,2.99623388131174,5.10260584043109));
#27860=CARTESIAN_POINT('Ctrl Pts',(-47.5605870608483,2.14611555214175,5.60179261296221));
#27861=CARTESIAN_POINT('Ctrl Pts',(-47.5141675128208,1.16853575680737,5.88391167734911));
#27862=CARTESIAN_POINT('Ctrl Pts',(-47.4677479647932,0.183164059858164,
5.914427678271));
#27863=CARTESIAN_POINT('Ctrl Pts',(-47.4213284167656,-0.802207637091027,
5.94494367919289));
#27864=CARTESIAN_POINT('Ctrl Pts',(-47.3749088687379,-1.79537123565506,
5.72385661664975));
#27865=CARTESIAN_POINT('Ctrl Pts',(-47.3284893207102,-2.67474949381855,
5.27823066752859));
#27866=CARTESIAN_POINT('Ctrl Pts',(-47.2820697726826,-3.55412775198207,
4.83260471840741));
#27867=CARTESIAN_POINT('Ctrl Pts',(-47.2356502246551,-4.31972066974506,
4.16243988270822));
#27868=CARTESIAN_POINT('Ctrl Pts',(-47.1892306766275,-4.87780886836403,
3.34977379505408));
#27869=CARTESIAN_POINT('Ctrl Pts',(-47.1428111285999,-5.43589706698301,
2.53710770739995));
#27870=CARTESIAN_POINT('Ctrl Pts',(-47.0963915805722,-5.78648054645795,
1.5819403677909));
#27871=CARTESIAN_POINT('Ctrl Pts',(-47.0499720325446,-5.88664294075176,
0.601197739865422));
#27872=CARTESIAN_POINT('Ctrl Pts',(-47.0405230857647,-5.90703153075849,
0.401562342929505));
#27873=CARTESIAN_POINT('Ctrl Pts',(-47.0310741389847,-5.91704397930712,
0.200867239662508));
#27874=CARTESIAN_POINT('Ctrl Pts',(-47.0216251922048,-5.91683542453774,
0.000151426803681578));
#27875=CARTESIAN_POINT('Origin',(-29.75,0.,0.));
#27876=CARTESIAN_POINT('',(-45.0198748077951,-5.91659248732073,-0.000150399349319874));
#27877=CARTESIAN_POINT('',(-45.2716251922049,-5.91675241673656,-0.000155248934938149));
#27878=CARTESIAN_POINT('',(-29.75,-5.91675,-7.2459289488551E-16));
#27879=CARTESIAN_POINT('Ctrl Pts',(-45.0198748077951,-5.91659248732073,
-0.000150399349319874));
#27880=CARTESIAN_POINT('Ctrl Pts',(-45.0531834328098,-5.91591598728341,
0.707479493305166));
#27881=CARTESIAN_POINT('Ctrl Pts',(-45.0864920578246,-5.78888701238488,
1.41534572504519));
#27882=CARTESIAN_POINT('Ctrl Pts',(-45.1198006828394,-5.54050131005888,
2.07770285835773));
#27883=CARTESIAN_POINT('Ctrl Pts',(-45.166220230867,-5.1943461615535,3.00077664923348));
#27884=CARTESIAN_POINT('Ctrl Pts',(-45.2126397788946,-4.61249498655612,
3.83546379772058));
#27885=CARTESIAN_POINT('Ctrl Pts',(-45.2590593269222,-3.86617458115737,
4.47958681603613));
#27886=CARTESIAN_POINT('Ctrl Pts',(-45.3054788749499,-3.11985417575861,
5.12370983435168));
#27887=CARTESIAN_POINT('Ctrl Pts',(-45.3518984229774,-2.20906453995847,
5.57726872249568));
#27888=CARTESIAN_POINT('Ctrl Pts',(-45.398317971005,-1.24529918010056,5.78474147101086));
#27889=CARTESIAN_POINT('Ctrl Pts',(-45.4447375190326,-0.281533820242672,
5.99221421952604));
#27890=CARTESIAN_POINT('Ctrl Pts',(-45.4911570670603,0.735207263672997,
5.95360082841241));
#27891=CARTESIAN_POINT('Ctrl Pts',(-45.5375766150879,1.6804606126505,5.67362812173325));
#27892=CARTESIAN_POINT('Ctrl Pts',(-45.5839961631155,2.62571396162803,5.39365541505408));
#27893=CARTESIAN_POINT('Ctrl Pts',(-45.6304157111431,3.4994795756674,4.87232339280936));
#27894=CARTESIAN_POINT('Ctrl Pts',(-45.6768352591707,4.19479621124706,4.17345045262303));
#27895=CARTESIAN_POINT('Ctrl Pts',(-45.7232548071983,4.89011284682673,3.47457751243669));
#27896=CARTESIAN_POINT('Ctrl Pts',(-45.769674355226,5.40698050394668,2.59816365430878));
#27897=CARTESIAN_POINT('Ctrl Pts',(-45.8160939032536,5.68212728628449,1.65149430421464));
#27898=CARTESIAN_POINT('Ctrl Pts',(-45.8625134512812,5.9572740686223,0.7048249541205));
#27899=CARTESIAN_POINT('Ctrl Pts',(-45.9089329993088,5.99069997617795,-0.312099887939838));
#27900=CARTESIAN_POINT('Ctrl Pts',(-45.9553525473364,5.77831320609204,-1.27479426837995));
#27901=CARTESIAN_POINT('Ctrl Pts',(-46.001772095364,5.56592643600614,-2.23748864882004));
#27902=CARTESIAN_POINT('Ctrl Pts',(-46.0481916433916,5.10772698827866,-3.14595256763994));
#27903=CARTESIAN_POINT('Ctrl Pts',(-46.0946111914192,4.45980494235696,-3.88897721907965));
#27904=CARTESIAN_POINT('Ctrl Pts',(-46.1410307394469,3.81188289643525,-4.63200187051937));
#27905=CARTESIAN_POINT('Ctrl Pts',(-46.1874502874745,2.97423825231934,-5.2095872545789));
#27906=CARTESIAN_POINT('Ctrl Pts',(-46.2338698355021,2.04941053699924,-5.551028768186));
#27907=CARTESIAN_POINT('Ctrl Pts',(-46.2802893835297,1.12458282167914,-5.89247028179309));
#27908=CARTESIAN_POINT('Ctrl Pts',(-46.3267089315573,0.112572035154879,
-5.99776792494772));
#27909=CARTESIAN_POINT('Ctrl Pts',(-46.3731284795849,-0.8627374187419,-5.85403177995257));
#27910=CARTESIAN_POINT('Ctrl Pts',(-46.4195480276125,-1.83804687263868,
-5.71029563495742));
#27911=CARTESIAN_POINT('Ctrl Pts',(-46.4659675756401,-2.77665499390798,
-5.31752570181249));
#27912=CARTESIAN_POINT('Ctrl Pts',(-46.5123871236677,-3.56366290095356,
-4.72380256390541));
#27913=CARTESIAN_POINT('Ctrl Pts',(-46.5588066716953,-4.35067080799912,
-4.13007942599834));
#27914=CARTESIAN_POINT('Ctrl Pts',(-46.605226219723,-4.98607850082097,-3.33540308332912));
#27915=CARTESIAN_POINT('Ctrl Pts',(-46.6516457677506,-5.3921031096479,-2.43705313633443));
#27916=CARTESIAN_POINT('Ctrl Pts',(-46.6910554477654,-5.73681348689026,
-1.67436402244332));
#27917=CARTESIAN_POINT('Ctrl Pts',(-46.7304651277802,-5.91618863956524,
-0.836948828693407));
#27918=CARTESIAN_POINT('Ctrl Pts',(-46.7698748077951,-5.91699642112564,
0.00013125821292051));
#27919=CARTESIAN_POINT('Ctrl Pts',(-47.0216251922048,-5.91683542453774,
0.000151426803681578));
#27920=CARTESIAN_POINT('Ctrl Pts',(-46.9846545909571,-5.91601941875459,
-0.785183114085889));
#27921=CARTESIAN_POINT('Ctrl Pts',(-46.9476839897095,-5.75873029000744,
-1.5708346976774));
#27922=CARTESIAN_POINT('Ctrl Pts',(-46.9107133884618,-5.45426065261164,
-2.2945684927006));
#27923=CARTESIAN_POINT('Ctrl Pts',(-46.8642938404342,-5.07197466106503,
-3.20327418109923));
#27924=CARTESIAN_POINT('Ctrl Pts',(-46.8178742924066,-4.45766136885915,
-4.01436764165459));
#27925=CARTESIAN_POINT('Ctrl Pts',(-46.7714547443789,-3.68652139340255,
-4.62855958698894));
#27926=CARTESIAN_POINT('Ctrl Pts',(-46.7250351963513,-2.91538141794593,
-5.24275153232329));
#27927=CARTESIAN_POINT('Ctrl Pts',(-46.6786156483237,-1.98741475923859,
-5.66004196243661));
#27928=CARTESIAN_POINT('Ctrl Pts',(-46.6321961002961,-1.01621763366518,
-5.82934863902905));
#27929=CARTESIAN_POINT('Ctrl Pts',(-46.5857765522685,-0.045020508091773,
-5.99865531562148));
#27930=CARTESIAN_POINT('Ctrl Pts',(-46.5393570042409,0.969407084347734,
-5.91997823869303));
#27931=CARTESIAN_POINT('Ctrl Pts',(-46.4929374562133,1.90288488866676,-5.60294859291119));
#27932=CARTESIAN_POINT('Ctrl Pts',(-46.4465179081857,2.83636269298577,-5.28591894712936));
#27933=CARTESIAN_POINT('Ctrl Pts',(-46.4000983601581,3.6888907091843,-4.73053673249415));
#27934=CARTESIAN_POINT('Ctrl Pts',(-46.3536788121304,4.35610747546488,-4.00478857076387));
#27935=CARTESIAN_POINT('Ctrl Pts',(-46.3072592641028,5.02332424174547,-3.27904040903357));
#27936=CARTESIAN_POINT('Ctrl Pts',(-46.2608397160752,5.50522975810808,-2.38292630020819));
#27937=CARTESIAN_POINT('Ctrl Pts',(-46.2144201680476,5.74283198771603,-1.42614325899866));
#27938=CARTESIAN_POINT('Ctrl Pts',(-46.16800062002,5.98043421732399,-0.469360217789129));
#27939=CARTESIAN_POINT('Ctrl Pts',(-46.1215810719924,5.97373316017729,0.548091755804578));
#27940=CARTESIAN_POINT('Ctrl Pts',(-46.0751615239648,5.72354912024968,1.50166217985638));
#27941=CARTESIAN_POINT('Ctrl Pts',(-46.0287419759371,5.47336508032206,2.45523260390819));
#27942=CARTESIAN_POINT('Ctrl Pts',(-45.9823224279095,4.97969805761354,3.34492147841808));
#27943=CARTESIAN_POINT('Ctrl Pts',(-45.9359028798819,4.3029798633399,4.06181832804142));
#27944=CARTESIAN_POINT('Ctrl Pts',(-45.8894833318543,3.62626166906627,4.77871517766474));
#27945=CARTESIAN_POINT('Ctrl Pts',(-45.8430637838267,2.76649230322752,5.3228200024015));
#27946=CARTESIAN_POINT('Ctrl Pts',(-45.7966442357991,1.82891967102184,5.62752669218647));
#27947=CARTESIAN_POINT('Ctrl Pts',(-45.7502246877715,0.891347038816158,
5.93223338197144));
#27948=CARTESIAN_POINT('Ctrl Pts',(-45.7038051397438,-0.12402885975648,
5.99754193680463));
#27949=CARTESIAN_POINT('Ctrl Pts',(-45.6573855917162,-1.09291168365437,
5.81545766780686));
#27950=CARTESIAN_POINT('Ctrl Pts',(-45.6109660436886,-2.06179450755229,
5.63337339880909));
#27951=CARTESIAN_POINT('Ctrl Pts',(-45.564546495661,-2.98418425677548,5.20389630598036));
#27952=CARTESIAN_POINT('Ctrl Pts',(-45.5181269476334,-3.74716740737289,
4.57960044713992));
#27953=CARTESIAN_POINT('Ctrl Pts',(-45.4717073996058,-4.51015055797028,
3.95530458829949));
#27954=CARTESIAN_POINT('Ctrl Pts',(-45.4252878515782,-5.11372710994189,
3.13618996344739));
#27955=CARTESIAN_POINT('Ctrl Pts',(-45.3788683035506,-5.4840107744226,2.22252776368231));
#27956=CARTESIAN_POINT('Ctrl Pts',(-45.3431205997687,-5.76916630297845,
1.51891630985034));
#27957=CARTESIAN_POINT('Ctrl Pts',(-45.3073728959868,-5.91596647289002,
0.759233006693162));
#27958=CARTESIAN_POINT('Ctrl Pts',(-45.2716251922049,-5.91675241673656,
-0.000155248934938149));
#27959=CARTESIAN_POINT('Origin',(-29.75,0.,0.));
#27960=CARTESIAN_POINT('',(-43.2698748077951,-5.91658768614795,0.000149985469924119));
#27961=CARTESIAN_POINT('',(-43.5216251922048,-5.9164475069627,0.000129275767947919));
#27962=CARTESIAN_POINT('',(-29.75,-5.91675,-7.2459289488551E-16));
#27963=CARTESIAN_POINT('Ctrl Pts',(-43.2698748077951,-5.91658768614795,
0.000149985469924119));
#27964=CARTESIAN_POINT('Ctrl Pts',(-43.2830626417842,-5.91685444793391,
0.280321481177761));
#27965=CARTESIAN_POINT('Ctrl Pts',(-43.2962504757734,-5.89731610636416,
0.560456079724737));
#27966=CARTESIAN_POINT('Ctrl Pts',(-43.3094383097625,-5.85766495001964,
0.837714311506925));
#27967=CARTESIAN_POINT('Ctrl Pts',(-43.3558578577901,-5.71809777334743,
1.81362906876509));
#27968=CARTESIAN_POINT('Ctrl Pts',(-43.4022774058177,-5.32934225143748,
2.75390699038182));
#27969=CARTESIAN_POINT('Ctrl Pts',(-43.4486969538453,-4.73898754708268,
3.54344478763073));
#27970=CARTESIAN_POINT('Ctrl Pts',(-43.4951165018729,-4.14863284272788,
4.33298258487964));
#27971=CARTESIAN_POINT('Ctrl Pts',(-43.5415360499005,-3.35667895592823,
4.97178025776071));
#27972=CARTESIAN_POINT('Ctrl Pts',(-43.5879555979282,-2.4600722200971,5.3816399550972));
#27973=CARTESIAN_POINT('Ctrl Pts',(-43.6343751459558,-1.563465484266,5.79149965243368));
#27974=CARTESIAN_POINT('Ctrl Pts',(-43.6807946939834,-0.56220589940344,
5.97242137422558));
#27975=CARTESIAN_POINT('Ctrl Pts',(-43.727214242011,0.421138229485253,5.90225774818909));
#27976=CARTESIAN_POINT('Ctrl Pts',(-43.7736337900386,1.40448235837399,5.8320941221526));
#27977=CARTESIAN_POINT('Ctrl Pts',(-43.8200533380662,2.36991103128888,5.51084514828768));
#27978=CARTESIAN_POINT('Ctrl Pts',(-43.8664728860938,3.19924215256585,4.97783623511641));
#27979=CARTESIAN_POINT('Ctrl Pts',(-43.9128924341214,4.02857327384278,4.44482732194516));
#27980=CARTESIAN_POINT('Ctrl Pts',(-43.9593119821491,4.72180684348183,3.70005846946757));
#27981=CARTESIAN_POINT('Ctrl Pts',(-44.0057315301767,5.19408128823263,2.8346998969245));
#27982=CARTESIAN_POINT('Ctrl Pts',(-44.0521510782043,5.66635573298344,1.9693413243814));
#27983=CARTESIAN_POINT('Ctrl Pts',(-44.0985706262319,5.91767105284598,0.98339303177284));
#27984=CARTESIAN_POINT('Ctrl Pts',(-44.1449901742595,5.91726270559451,-0.00245099417194854));
#27985=CARTESIAN_POINT('Ctrl Pts',(-44.1914097222871,5.91685435834304,-0.988295020116738));
#27986=CARTESIAN_POINT('Ctrl Pts',(-44.2378292703147,5.66472234397756,-1.97403477939774));
#27987=CARTESIAN_POINT('Ctrl Pts',(-44.2842488183423,5.19173117965784,-2.83900181270824));
#27988=CARTESIAN_POINT('Ctrl Pts',(-44.3306683663699,4.71874001533813,-3.70396884601872));
#27989=CARTESIAN_POINT('Ctrl Pts',(-44.3770879143976,4.02488970106418,-4.4481631533587));
#27990=CARTESIAN_POINT('Ctrl Pts',(-44.4235074624252,3.19511730833444,-4.98048484792131));
#27991=CARTESIAN_POINT('Ctrl Pts',(-44.4699270104528,2.36534491560469,-5.51280654248393));
#27992=CARTESIAN_POINT('Ctrl Pts',(-44.5163465584804,1.3996504444191,-5.83325562426917));
#27993=CARTESIAN_POINT('Ctrl Pts',(-44.562766106508,0.416248527901588,-5.90260460283525));
#27994=CARTESIAN_POINT('Ctrl Pts',(-44.6091856545356,-0.567153388615943,
-5.97195358140132));
#27995=CARTESIAN_POINT('Ctrl Pts',(-44.6556052025633,-1.56826275046543,
-5.79020245674823));
#27996=CARTESIAN_POINT('Ctrl Pts',(-44.7020247505909,-2.4645296420586,-5.37960013177621));
#27997=CARTESIAN_POINT('Ctrl Pts',(-44.7484442986185,-3.36079653365177,
-4.96899780680419));
#27998=CARTESIAN_POINT('Ctrl Pts',(-44.7948638466461,-4.1522209549886,-4.32954428151325));
#27999=CARTESIAN_POINT('Ctrl Pts',(-44.8412833946737,-4.74192138670128,
-3.53951769267185));
#28000=CARTESIAN_POINT('Ctrl Pts',(-44.8877029427013,-5.33162181841396,
-2.74949110383044));
#28001=CARTESIAN_POINT('Ctrl Pts',(-44.9341224907289,-5.71959826050248,
-1.80889145143859));
#28002=CARTESIAN_POINT('Ctrl Pts',(-44.9805420387565,-5.85835692054005,
-0.832861408610456));
#28003=CARTESIAN_POINT('Ctrl Pts',(-44.9936529617694,-5.89754847208288,
-0.557187575204382));
#28004=CARTESIAN_POINT('Ctrl Pts',(-45.0067638847822,-5.91685877090054,
-0.278687296026193));
#28005=CARTESIAN_POINT('Ctrl Pts',(-45.0198748077951,-5.91659248732073,
-0.000150399349319874));
#28006=CARTESIAN_POINT('Ctrl Pts',(-45.2716251922049,-5.91675241673656,
-0.000155248934938149));
#28007=CARTESIAN_POINT('Ctrl Pts',(-45.2609533479592,-5.91698704636109,
-0.226857171819796));
#28008=CARTESIAN_POINT('Ctrl Pts',(-45.2502815037135,-5.90420866411302,
-0.453532799616136));
#28009=CARTESIAN_POINT('Ctrl Pts',(-45.2396096594678,-5.87821350079514,
-0.678682454017764));
#28010=CARTESIAN_POINT('Ctrl Pts',(-45.1931901114401,-5.76514178569715,
-1.65802069727473));
#28011=CARTESIAN_POINT('Ctrl Pts',(-45.1467705634125,-5.40200757851135,
-2.60848740911062));
#28012=CARTESIAN_POINT('Ctrl Pts',(-45.1003510153849,-4.83326363148813,
-3.41373204907123));
#28013=CARTESIAN_POINT('Ctrl Pts',(-45.0539314673573,-4.26451968446491,
-4.21897668903183));
#28014=CARTESIAN_POINT('Ctrl Pts',(-45.0075119193297,-3.49016599760425,
-4.87899925711716));
#28015=CARTESIAN_POINT('Ctrl Pts',(-44.9610923713021,-2.60499439143712,
-5.31300367540839));
#28016=CARTESIAN_POINT('Ctrl Pts',(-44.9146728232745,-1.71982278526999,
-5.74700809369961));
#28017=CARTESIAN_POINT('Ctrl Pts',(-44.8682532752468,-0.723833259796379,
-5.95499436219676));
#28018=CARTESIAN_POINT('Ctrl Pts',(-44.8218337272192,0.261051009629444,
-5.91150202610921));
#28019=CARTESIAN_POINT('Ctrl Pts',(-44.7754141791916,1.2459352790553,-5.86800969002166));
#28020=CARTESIAN_POINT('Ctrl Pts',(-44.728994631164,2.21971429243333,-5.57303874934939));
#28021=CARTESIAN_POINT('Ctrl Pts',(-44.6825750831364,3.06318375456983,-5.06269781046245));
#28022=CARTESIAN_POINT('Ctrl Pts',(-44.6361555351088,3.90665321670632,-4.55235687157551));
#28023=CARTESIAN_POINT('Ctrl Pts',(-44.5897359870811,4.61981312760129,-3.82664593447388));
#28024=CARTESIAN_POINT('Ctrl Pts',(-44.5433164390535,5.11536264859339,-2.97440226057227));
#28025=CARTESIAN_POINT('Ctrl Pts',(-44.4968968910259,5.6109121695855,-2.12215858667066));
#28026=CARTESIAN_POINT('Ctrl Pts',(-44.4504773429983,5.88885130067477,-1.14338217596907));
#28027=CARTESIAN_POINT('Ctrl Pts',(-44.4040577949707,5.91515636937177,-0.157889075627079));
#28028=CARTESIAN_POINT('Ctrl Pts',(-44.3576382469431,5.94146143806878,0.827604024714909));
#28029=CARTESIAN_POINT('Ctrl Pts',(-44.3112186989155,5.71613244437352,1.81981381469727));
#28030=CARTESIAN_POINT('Ctrl Pts',(-44.2647991508879,5.2667528374168,2.69727981193718));
#28031=CARTESIAN_POINT('Ctrl Pts',(-44.2183796028602,4.81737323046008,3.5747458091771));
#28032=CARTESIAN_POINT('Ctrl Pts',(-44.1719600548327,4.14394301024188,4.33746801367458));
#28033=CARTESIAN_POINT('Ctrl Pts',(-44.1255405068051,3.32889954053823,4.89207846250714));
#28034=CARTESIAN_POINT('Ctrl Pts',(-44.0791209587774,2.51385607083456,5.44668891133971));
#28035=CARTESIAN_POINT('Ctrl Pts',(-44.0327014107498,1.55719935164544,5.79318760450736));
#28036=CARTESIAN_POINT('Ctrl Pts',(-43.9862818627222,0.576037667691109,
5.88915821146986));
#28037=CARTESIAN_POINT('Ctrl Pts',(-43.9398623146946,-0.405124016263193,
5.98512881843235));
#28038=CARTESIAN_POINT('Ctrl Pts',(-43.893442766667,-1.41079066498267,5.8305713391897));
#28039=CARTESIAN_POINT('Ctrl Pts',(-43.8470232186394,-2.31785448664446,
5.4444057906317));
#28040=CARTESIAN_POINT('Ctrl Pts',(-43.8006036706118,-3.22491830830626,
5.05824024207369));
#28041=CARTESIAN_POINT('Ctrl Pts',(-43.7541841225842,-4.03337930291038,
4.44046662420031));
#28042=CARTESIAN_POINT('Ctrl Pts',(-43.7077645745565,-4.64427043406613,
3.66670914712104));
#28043=CARTESIAN_POINT('Ctrl Pts',(-43.6613450265289,-5.2551615652219,2.89295167004174));
#28044=CARTESIAN_POINT('Ctrl Pts',(-43.6149254785013,-5.66848283292931,
1.96321033375654));
#28045=CARTESIAN_POINT('Ctrl Pts',(-43.5685059304737,-5.83363788038793,
0.99129860023346));
#28046=CARTESIAN_POINT('Ctrl Pts',(-43.5528790177174,-5.8892365156086,0.664109290730965));
#28047=CARTESIAN_POINT('Ctrl Pts',(-43.5372521049611,-5.91671049438226,
0.332140813727917));
#28048=CARTESIAN_POINT('Ctrl Pts',(-43.5216251922048,-5.9164475069627,0.000129275767947919));
#28049=CARTESIAN_POINT('Origin',(-29.75,0.,0.));
#28050=CARTESIAN_POINT('',(-41.5198748077951,-5.91700124842561,-0.000130358588716351));
#28051=CARTESIAN_POINT('',(-41.7716251922048,-5.91713952097907,-9.42380742528296E-5));
#28052=CARTESIAN_POINT('',(-29.75,-5.91675,-7.2459289488551E-16));
#28053=CARTESIAN_POINT('Ctrl Pts',(-41.5198748077951,-5.91700124842561,
-0.000130358588716351));
#28054=CARTESIAN_POINT('Ctrl Pts',(-41.5593613987862,-5.91619546953019,
0.838581376832566));
#28055=CARTESIAN_POINT('Ctrl Pts',(-41.5988479897773,-5.73609840048565,
1.67762805962007));
#28056=CARTESIAN_POINT('Ctrl Pts',(-41.6383345807684,-5.39008235223998,
2.4415192340965));
#28057=CARTESIAN_POINT('Ctrl Pts',(-41.684754128796,-4.98331367034798,3.33953251332482));
#28058=CARTESIAN_POINT('Ctrl Pts',(-41.7311736768237,-4.3472478686121,4.13368219792937));
#28059=CARTESIAN_POINT('Ctrl Pts',(-41.7775932248513,-3.55974837862319,
4.72675315785388));
#28060=CARTESIAN_POINT('Ctrl Pts',(-41.8240127728789,-2.77224888863434,
5.31982411777835));
#28061=CARTESIAN_POINT('Ctrl Pts',(-41.8704323209065,-1.83331571039248,
5.7118163530228));
#28062=CARTESIAN_POINT('Ctrl Pts',(-41.9168518689341,-0.857887517055163,
5.85474448139908));
#28063=CARTESIAN_POINT('Ctrl Pts',(-41.9632714169617,0.11754067628218,5.99767260977537));
#28064=CARTESIAN_POINT('Ctrl Pts',(-42.0096909649893,1.12946388471498,5.89153663128348));
#28065=CARTESIAN_POINT('Ctrl Pts',(-42.0561105130169,2.05400842520608,5.54932908769831));
#28066=CARTESIAN_POINT('Ctrl Pts',(-42.1025300610446,2.97855296569718,5.20712154411313));
#28067=CARTESIAN_POINT('Ctrl Pts',(-42.1489496090722,3.81571883824659,4.62884243543466));
#28068=CARTESIAN_POINT('Ctrl Pts',(-42.1953691570998,4.46302512426135,3.88528128641982));
#28069=CARTESIAN_POINT('Ctrl Pts',(-42.2417887051274,5.11033141027611,3.14172013740498));
#28070=CARTESIAN_POINT('Ctrl Pts',(-42.288208253155,5.56777810975624,2.23287694805376));
#28071=CARTESIAN_POINT('Ctrl Pts',(-42.3346278011826,5.77936729026419,1.27000695219218));
#28072=CARTESIAN_POINT('Ctrl Pts',(-42.3810473492102,5.99095647077213,0.307136956330597));
#28073=CARTESIAN_POINT('Ctrl Pts',(-42.4274668972378,5.95668813230791,-0.709759846041339));
#28074=CARTESIAN_POINT('Ctrl Pts',(-42.4738864452654,5.68075720316425,-1.65620093379082));
#28075=CARTESIAN_POINT('Ctrl Pts',(-42.5203059932931,5.40482627402059,-2.60264202154027));
#28076=CARTESIAN_POINT('Ctrl Pts',(-42.5667255413207,4.88723275419751,-3.47862739466726));
#28077=CARTESIAN_POINT('Ctrl Pts',(-42.6131450893483,4.19133739585716,-4.17692407980818));
#28078=CARTESIAN_POINT('Ctrl Pts',(-42.6595646373759,3.49544203751678,-4.87522076494912));
#28079=CARTESIAN_POINT('Ctrl Pts',(-42.7059841854035,2.62124484065913,-5.39582876210398));
#28080=CARTESIAN_POINT('Ctrl Pts',(-42.7524037334311,1.67575988063407,-5.67501830453871));
#28081=CARTESIAN_POINT('Ctrl Pts',(-42.7988232814587,0.730274920609009,
-5.95420784697344));
#28082=CARTESIAN_POINT('Ctrl Pts',(-42.8452428294864,-0.286497802583452,
-5.99197893468805));
#28083=CARTESIAN_POINT('Ctrl Pts',(-42.891662377514,-1.25009095685333,-5.78370785344363));
#28084=CARTESIAN_POINT('Ctrl Pts',(-42.9380819255416,-2.21368411112319,
-5.57543677219922));
#28085=CARTESIAN_POINT('Ctrl Pts',(-42.9845014735692,-3.12409769647047,
-5.12112352199578));
#28086=CARTESIAN_POINT('Ctrl Pts',(-43.0309210215968,-3.8698842404346,-4.47638245685375));
#28087=CARTESIAN_POINT('Ctrl Pts',(-43.0773405696244,-4.61567078439876,
-3.8316413917117));
#28088=CARTESIAN_POINT('Ctrl Pts',(-43.123760117652,-5.19683028697976,-2.99647251163105));
#28089=CARTESIAN_POINT('Ctrl Pts',(-43.1701796656797,-5.54222062255303,
-2.07311227514093));
#28090=CARTESIAN_POINT('Ctrl Pts',(-43.2034113797181,-5.7894852632298,-1.41207948534963));
#28091=CARTESIAN_POINT('Ctrl Pts',(-43.2366430937566,-5.91591547937049,
-0.705847605549909));
#28092=CARTESIAN_POINT('Ctrl Pts',(-43.2698748077951,-5.91658768614795,
0.000149985469924119));
#28093=CARTESIAN_POINT('Ctrl Pts',(-43.5216251922048,-5.9164475069627,0.000129275767947919));
#28094=CARTESIAN_POINT('Ctrl Pts',(-43.4908325569335,-5.91592929355626,
-0.65409528884822));
#28095=CARTESIAN_POINT('Ctrl Pts',(-43.4600399216622,-5.80771341252565,
-1.30848705144103));
#28096=CARTESIAN_POINT('Ctrl Pts',(-43.4292472863909,-5.59476610119005,
-1.92680982644798));
#28097=CARTESIAN_POINT('Ctrl Pts',(-43.3828277383633,-5.27375044732369,
-2.85892438884555));
#28098=CARTESIAN_POINT('Ctrl Pts',(-43.3364081903356,-4.71473031238112,
-3.70907138287973));
#28099=CARTESIAN_POINT('Ctrl Pts',(-43.289988642308,-3.98613765091202,-4.37318081747182));
#28100=CARTESIAN_POINT('Ctrl Pts',(-43.2435690942804,-3.25754498944294,
-5.03729025206388));
#28101=CARTESIAN_POINT('Ctrl Pts',(-43.1971495462528,-2.35937980144735,
-5.51536212721385));
#28102=CARTESIAN_POINT('Ctrl Pts',(-43.1507299982252,-1.40159018267562,
-5.74887369787763));
#28103=CARTESIAN_POINT('Ctrl Pts',(-43.1043104501976,-0.443800563903852,
-5.98238526854141));
#28104=CARTESIAN_POINT('Ctrl Pts',(-43.05789090217,0.573613485644089,-5.97133653471901));
#28105=CARTESIAN_POINT('Ctrl Pts',(-43.0114713541424,1.52610612648058,-5.71708001737253));
#28106=CARTESIAN_POINT('Ctrl Pts',(-42.9650518061148,2.47859876731708,-5.46282350002606));
#28107=CARTESIAN_POINT('Ctrl Pts',(-42.9186322580871,3.36616999944212,-4.96535919915553));
#28108=CARTESIAN_POINT('Ctrl Pts',(-42.8722127100595,4.08016857682748,-4.2855837664187));
#28109=CARTESIAN_POINT('Ctrl Pts',(-42.8257931620319,4.79416715421282,-3.60580833368187));
#28110=CARTESIAN_POINT('Ctrl Pts',(-42.7793736140043,5.33459307685845,-2.74372176907874));
#28111=CARTESIAN_POINT('Ctrl Pts',(-42.7329540659767,5.63529058423927,-1.80485563564129));
#28112=CARTESIAN_POINT('Ctrl Pts',(-42.6865345179491,5.93598809162008,-0.865989502203833));
#28113=CARTESIAN_POINT('Ctrl Pts',(-42.6401149699215,5.99695718373608,0.149656200067966));
#28114=CARTESIAN_POINT('Ctrl Pts',(-42.5936954218938,5.81073438319206,1.1177521023516));
#28115=CARTESIAN_POINT('Ctrl Pts',(-42.5472758738662,5.62451158264803,2.08584800463521));
#28116=CARTESIAN_POINT('Ctrl Pts',(-42.5008563258386,5.19109688944399,3.00639410693068));
#28117=CARTESIAN_POINT('Ctrl Pts',(-42.454436777811,4.56354637926056,3.76670257369223));
#28118=CARTESIAN_POINT('Ctrl Pts',(-42.4080172297834,3.9359958690771,4.52701104045381));
#28119=CARTESIAN_POINT('Ctrl Pts',(-42.3615976817558,3.11430954191427,5.12708187168144));
#28120=CARTESIAN_POINT('Ctrl Pts',(-42.3151781337282,2.19907340153071,5.49345792820897));
#28121=CARTESIAN_POINT('Ctrl Pts',(-42.2687585857006,1.28383726114717,5.8598339847365));
#28122=CARTESIAN_POINT('Ctrl Pts',(-42.2223390376729,0.275051307542909,
5.99251526656391));
#28123=CARTESIAN_POINT('Ctrl Pts',(-42.1759194896453,-0.703794820515237,
5.87525971212658));
#28124=CARTESIAN_POINT('Ctrl Pts',(-42.1294999416177,-1.68264094857338,
5.75800415768925));
#28125=CARTESIAN_POINT('Ctrl Pts',(-42.0830803935901,-2.63154725108544,
5.39081176698717));
#28126=CARTESIAN_POINT('Ctrl Pts',(-42.0366608455625,-3.43435420372208,
4.81863207121049));
#28127=CARTESIAN_POINT('Ctrl Pts',(-41.9902412975349,-4.23716115635874,
4.2464523754338));
#28128=CARTESIAN_POINT('Ctrl Pts',(-41.9438217495072,-4.89386875911997,
3.46928537458253));
#28129=CARTESIAN_POINT('Ctrl Pts',(-41.8974022014796,-5.32408673263024,
2.58226727852723));
#28130=CARTESIAN_POINT('Ctrl Pts',(-41.8554765317214,-5.71265528721273,
1.78112143922053));
#28131=CARTESIAN_POINT('Ctrl Pts',(-41.8135508619631,-5.91646444995278,
0.890364337754753));
#28132=CARTESIAN_POINT('Ctrl Pts',(-41.7716251922048,-5.91713952097907,
-9.42380742528296E-5));
#28133=CARTESIAN_POINT('Origin',(-29.75,0.,0.));
#28134=CARTESIAN_POINT('',(-39.7698748077951,-5.91629469088874,7.39219476919573E-5));
#28135=CARTESIAN_POINT('',(-40.0216251922048,-5.91624628365206,2.79657000012922E-5));
#28136=CARTESIAN_POINT('',(-29.75,-5.91675,-7.2459289488551E-16));
#28137=CARTESIAN_POINT('Ctrl Pts',(-39.7698748077951,-5.91629469088874,
7.39219476919573E-5));
#28138=CARTESIAN_POINT('Ctrl Pts',(-39.7892406077606,-5.91647483503357,
0.411552807703675));
#28139=CARTESIAN_POINT('Ctrl Pts',(-39.808606407726,-5.87416701816864,0.822995174920484));
#28140=CARTESIAN_POINT('Ctrl Pts',(-39.8279722076915,-5.78899689027189,
1.22536481866197));
#28141=CARTESIAN_POINT('Ctrl Pts',(-39.8743917557191,-5.58484530089954,
2.18983915154763));
#28142=CARTESIAN_POINT('Ctrl Pts',(-39.9208113037468,-5.13442654398146,
3.10218577926745));
#28143=CARTESIAN_POINT('Ctrl Pts',(-39.9672308517744,-4.4928782325929,3.85072059769141));
#28144=CARTESIAN_POINT('Ctrl Pts',(-40.013650399802,-3.85132992120435,4.59925541611538));
#28145=CARTESIAN_POINT('Ctrl Pts',(-40.0600699478296,-3.01865205534533,
5.18397842524349));
#28146=CARTESIAN_POINT('Ctrl Pts',(-40.1064894958572,-2.09677615824598,
5.53331127595433));
#28147=CARTESIAN_POINT('Ctrl Pts',(-40.1529090438848,-1.17490026114667,
5.88264412666515));
#28148=CARTESIAN_POINT('Ctrl Pts',(-40.1993285919124,-0.163826332807044,
5.99658681895872));
#28149=CARTESIAN_POINT('Ctrl Pts',(-40.2457481399401,0.812675907605946,
5.86119115910656));
#28150=CARTESIAN_POINT('Ctrl Pts',(-40.2921676879677,1.78917814801902,5.72579549925439));
#28151=CARTESIAN_POINT('Ctrl Pts',(-40.3385872359953,2.73110870050545,5.34106148725645));
#28152=CARTESIAN_POINT('Ctrl Pts',(-40.3850067840229,3.52316197099507,4.75408599633264));
#28153=CARTESIAN_POINT('Ctrl Pts',(-40.4314263320505,4.31521524148466,4.16711050540887));
#28154=CARTESIAN_POINT('Ctrl Pts',(-40.4778458800781,4.95739122997746,3.37789353555927));
#28155=CARTESIAN_POINT('Ctrl Pts',(-40.5242654281057,5.37107853178416,2.48304638293356));
#28156=CARTESIAN_POINT('Ctrl Pts',(-40.5706849761334,5.78476583359088,1.5881992303078));
#28157=CARTESIAN_POINT('Ctrl Pts',(-40.617104524161,5.96996444871147,0.58772189490592));
#28158=CARTESIAN_POINT('Ctrl Pts',(-40.6635240721886,5.90400345275445,-0.395913076641409));
#28159=CARTESIAN_POINT('Ctrl Pts',(-40.7099436202162,5.83804245679743,-1.37954804818868));
#28160=CARTESIAN_POINT('Ctrl Pts',(-40.7563631682438,5.52092184976282,-2.34634065588141));
#28161=CARTESIAN_POINT('Ctrl Pts',(-40.8027827162714,4.99146166980471,-3.17794183918814));
#28162=CARTESIAN_POINT('Ctrl Pts',(-40.849202264299,4.46200148984657,-4.0095430224949));
#28163=CARTESIAN_POINT('Ctrl Pts',(-40.8956218123267,3.72020173696491,-4.70595278141567));
#28164=CARTESIAN_POINT('Ctrl Pts',(-40.9420413603543,2.85686917070408,-5.1819207323031));
#28165=CARTESIAN_POINT('Ctrl Pts',(-40.9884609083819,1.99353660444324,-5.65788868319053));
#28166=CARTESIAN_POINT('Ctrl Pts',(-41.0348804564094,1.00867122480323,-5.91341482604464));
#28167=CARTESIAN_POINT('Ctrl Pts',(-41.0813000044371,0.022834454681672,
-5.91721915447378));
#28168=CARTESIAN_POINT('Ctrl Pts',(-41.1277195524647,-0.963002315439857,
-5.92102348290293));
#28169=CARTESIAN_POINT('Ctrl Pts',(-41.1741391004923,-1.94981047604293,
-5.67310599690714));
#28170=CARTESIAN_POINT('Ctrl Pts',(-41.2205586485199,-2.81679078041956,
-5.20381529588968));
#28171=CARTESIAN_POINT('Ctrl Pts',(-41.2669781965476,-3.68377108479622,
-4.73452459487222));
#28172=CARTESIAN_POINT('Ctrl Pts',(-41.3133977445751,-4.43092353294642,
-4.04386067883307));
#28173=CARTESIAN_POINT('Ctrl Pts',(-41.3598172926028,-4.96678611987679,
-3.21637055915381));
#28174=CARTESIAN_POINT('Ctrl Pts',(-41.4062368406304,-5.50264870680715,
-2.38888043947455));
#28175=CARTESIAN_POINT('Ctrl Pts',(-41.452656388658,-5.82722143251769,-1.42456411615518));
#28176=CARTESIAN_POINT('Ctrl Pts',(-41.4990759366856,-5.90077201434889,
-0.441467517569472));
#28177=CARTESIAN_POINT('Ctrl Pts',(-41.5060088937221,-5.91175710674018,
-0.294637856999195));
#28178=CARTESIAN_POINT('Ctrl Pts',(-41.5129418507586,-5.9171427250718,-0.147389270582132));
#28179=CARTESIAN_POINT('Ctrl Pts',(-41.5198748077951,-5.91700124842561,
-0.000130358588716351));
#28180=CARTESIAN_POINT('Ctrl Pts',(-41.7716251922048,-5.91713952097907,
-9.42380742528296E-5));
#28181=CARTESIAN_POINT('Ctrl Pts',(-41.7671313139355,-5.91721187968038,
-0.0955396410157708));
#28182=CARTESIAN_POINT('Ctrl Pts',(-41.7626374356662,-5.91495042886566,
-0.1909816141934));
#28183=CARTESIAN_POINT('Ctrl Pts',(-41.7581435573968,-5.91033254064073,
-0.286309436388467));
#28184=CARTESIAN_POINT('Ctrl Pts',(-41.7117240093692,-5.86263203088166,
-1.27099886398967));
#28185=CARTESIAN_POINT('Ctrl Pts',(-41.6653044613416,-5.56350266710422,
-2.24350852793274));
#28186=CARTESIAN_POINT('Ctrl Pts',(-41.618884913314,-5.04956210535865,-3.08478951931048));
#28187=CARTESIAN_POINT('Ctrl Pts',(-41.5724653652863,-4.5356215436131,-3.92607051068819));
#28188=CARTESIAN_POINT('Ctrl Pts',(-41.5260458172587,-3.80686978389939,
-4.63612282950058));
#28189=CARTESIAN_POINT('Ctrl Pts',(-41.4796262692311,-2.9525163272383,-5.12802605021787));
#28190=CARTESIAN_POINT('Ctrl Pts',(-41.4332067212035,-2.09816287057719,
-5.61992927093518));
#28191=CARTESIAN_POINT('Ctrl Pts',(-41.3867871731759,-1.11820771696867,
-5.89368339355742));
#28192=CARTESIAN_POINT('Ctrl Pts',(-41.3403676251483,-0.132611208340943,
-5.9157770496989));
#28193=CARTESIAN_POINT('Ctrl Pts',(-41.2939480771207,0.852985300286781,
-5.93787070584039));
#28194=CARTESIAN_POINT('Ctrl Pts',(-41.2475285290931,1.84422316393366,-5.70830389550112));
#28195=CARTESIAN_POINT('Ctrl Pts',(-41.2011089810655,2.71976087771816,-5.25517883638184));
#28196=CARTESIAN_POINT('Ctrl Pts',(-41.1546894330379,3.59529859150262,-4.80205377726258));
#28197=CARTESIAN_POINT('Ctrl Pts',(-41.1082698850102,4.35513615542474,-4.1253704693633));
#28198=CARTESIAN_POINT('Ctrl Pts',(-41.0618503369826,4.90625872728235,-3.30796450030643));
#28199=CARTESIAN_POINT('Ctrl Pts',(-41.015430788955,5.45738129914,-2.49055853124952));
#28200=CARTESIAN_POINT('Ctrl Pts',(-40.9690112409274,5.79978887893315,-1.53242990103499));
#28201=CARTESIAN_POINT('Ctrl Pts',(-40.9225916928998,5.89156594614075,-0.5508670770672));
#28202=CARTESIAN_POINT('Ctrl Pts',(-40.8761721448722,5.98334301334835,0.430695746900592));
#28203=CARTESIAN_POINT('Ctrl Pts',(-40.8297525968445,5.82448956797039,1.4356927646216));
#28204=CARTESIAN_POINT('Ctrl Pts',(-40.7833330488169,5.43445151378507,2.34109815655837));
#28205=CARTESIAN_POINT('Ctrl Pts',(-40.7369135007893,5.04441345959976,3.24650354849512));
#28206=CARTESIAN_POINT('Ctrl Pts',(-40.6904939527617,4.42319079660706,4.05231731464766));
#28207=CARTESIAN_POINT('Ctrl Pts',(-40.6440744047341,3.64682994671907,4.65989647675084));
#28208=CARTESIAN_POINT('Ctrl Pts',(-40.5976548567065,2.87046909683105,5.26747563885403));
#28209=CARTESIAN_POINT('Ctrl Pts',(-40.5512353086789,1.93897006004773,5.67682019690788));
#28210=CARTESIAN_POINT('Ctrl Pts',(-40.5048157606513,0.966361465686305,
5.83782059950102));
#28211=CARTESIAN_POINT('Ctrl Pts',(-40.4583962126236,-0.00624712867508953,
5.99882100209416));
#28212=CARTESIAN_POINT('Ctrl Pts',(-40.411976664596,-1.01996528061453,5.91147724922659));
#28213=CARTESIAN_POINT('Ctrl Pts',(-40.3655571165684,-1.95069958067579,
5.58648144902255));
#28214=CARTESIAN_POINT('Ctrl Pts',(-40.3191375685408,-2.88143388073706,
5.26148564881852));
#28215=CARTESIAN_POINT('Ctrl Pts',(-40.2727180205132,-3.72918432892018,
4.69883780127797));
#28216=CARTESIAN_POINT('Ctrl Pts',(-40.2262984724856,-4.39017430518342,
3.96741394417436));
#28217=CARTESIAN_POINT('Ctrl Pts',(-40.179878924458,-5.05116428144667,3.23599008707073));
#28218=CARTESIAN_POINT('Ctrl Pts',(-40.1334593764304,-5.52539378579008,
2.33579022040401));
#28219=CARTESIAN_POINT('Ctrl Pts',(-40.0870398284027,-5.75481043358768,
1.37701151331141));
#28220=CARTESIAN_POINT('Ctrl Pts',(-40.0652349496701,-5.86257542478278,
0.926639755551992));
#28221=CARTESIAN_POINT('Ctrl Pts',(-40.0434300709375,-5.91632225961091,
0.463342528899467));
#28222=CARTESIAN_POINT('Ctrl Pts',(-40.0216251922048,-5.91624628365206,
2.79657000012922E-5));
#28223=CARTESIAN_POINT('Origin',(-29.75,0.,0.));
#28224=CARTESIAN_POINT('',(-38.0198748077951,-5.91725909577585,-1.71678216764892E-5));
#28225=CARTESIAN_POINT('',(-38.2716251922048,-5.91724351279131,3.79183957586531E-5));
#28226=CARTESIAN_POINT('',(-29.75,-5.91675,-7.2459289488551E-16));
#28227=CARTESIAN_POINT('Ctrl Pts',(-38.0198748077951,-5.91725909577585,
-1.71678216764892E-5));
#28228=CARTESIAN_POINT('Ctrl Pts',(-38.0655393647625,-5.91709852423039,
0.969794642514453));
#28229=CARTESIAN_POINT('Ctrl Pts',(-38.11120392173,-5.67381360263478,1.93968406368008));
#28230=CARTESIAN_POINT('Ctrl Pts',(-38.1568684786975,-5.21580439043804,
2.79452831352257));
#28231=CARTESIAN_POINT('Ctrl Pts',(-38.2032880267251,-4.75022272197246,
3.66350605790234));
#28232=CARTESIAN_POINT('Ctrl Pts',(-38.2497075747527,-4.06275781569343,
4.41360300385667));
#28233=CARTESIAN_POINT('Ctrl Pts',(-38.2961271227803,-3.2375650790368,4.9529966983023));
#28234=CARTESIAN_POINT('Ctrl Pts',(-38.342546670808,-2.41237234238023,5.49239039274791));
#28235=CARTESIAN_POINT('Ctrl Pts',(-38.3889662188356,-1.44945177534604,
5.82108083568479));
#28236=CARTESIAN_POINT('Ctrl Pts',(-38.4353857668632,-0.466678446039116,
5.89883167774726));
#28237=CARTESIAN_POINT('Ctrl Pts',(-38.4818053148908,0.516094883267838,
5.97658251980974));
#28238=CARTESIAN_POINT('Ctrl Pts',(-38.5282248629184,1.51872097484763,5.80339376099782));
#28239=CARTESIAN_POINT('Ctrl Pts',(-38.574644410946,2.41846424398577,5.40046614978322));
#28240=CARTESIAN_POINT('Ctrl Pts',(-38.6210639589736,3.31820751312388,4.99753853856864));
#28241=CARTESIAN_POINT('Ctrl Pts',(-38.6674835070012,4.11506795982038,4.36487207495137));
#28242=CARTESIAN_POINT('Ctrl Pts',(-38.7139030550289,4.7114986184791,3.57991406355817));
#28243=CARTESIAN_POINT('Ctrl Pts',(-38.7603226030565,5.30792927713784,2.79495605216495));
#28244=CARTESIAN_POINT('Ctrl Pts',(-38.8067421510841,5.70393014775882,1.85770649299578));
#28245=CARTESIAN_POINT('Ctrl Pts',(-38.8531616991117,5.85102513460574,0.882897960471064));
#28246=CARTESIAN_POINT('Ctrl Pts',(-38.8995812471393,5.99812012145267,-0.0919105720536834));
#28247=CARTESIAN_POINT('Ctrl Pts',(-38.9460007951669,5.89630922452556,-1.10427807793392));
#28248=CARTESIAN_POINT('Ctrl Pts',(-38.9924203431945,5.55805553457138,-2.03027648585422));
#28249=CARTESIAN_POINT('Ctrl Pts',(-39.0388398912221,5.21980184461722,-2.95627489377446));
#28250=CARTESIAN_POINT('Ctrl Pts',(-39.0852594392497,4.64510536163601,-3.79590420373472));
#28251=CARTESIAN_POINT('Ctrl Pts',(-39.1316789872773,3.904317046434,-4.4463819376339));
#28252=CARTESIAN_POINT('Ctrl Pts',(-39.178098535305,3.16352873123197,-5.09685967153309));
#28253=CARTESIAN_POINT('Ctrl Pts',(-39.2245180833326,2.25664858380911,-5.5581858293712));
#28254=CARTESIAN_POINT('Ctrl Pts',(-39.2709376313602,1.29469153395299,-5.77388757825284));
#28255=CARTESIAN_POINT('Ctrl Pts',(-39.3173571793878,0.332734484096863,
-5.98958932713449));
#28256=CARTESIAN_POINT('Ctrl Pts',(-39.3637767274154,-0.684299468192547,
-5.95966666705966));
#28257=CARTESIAN_POINT('Ctrl Pts',(-39.4101962754431,-1.63191101269678,
-5.68778255395115));
#28258=CARTESIAN_POINT('Ctrl Pts',(-39.4566158234707,-2.57952255720101,
-5.41589844084264));
#28259=CARTESIAN_POINT('Ctrl Pts',(-39.5030353714982,-3.45771169392008,
-4.90205287470045));
#28260=CARTESIAN_POINT('Ctrl Pts',(-39.5494549195259,-4.15897567772266,
-4.20914780525743));
#28261=CARTESIAN_POINT('Ctrl Pts',(-39.5958744675535,-4.86023966152524,
-3.51624273581441));
#28262=CARTESIAN_POINT('Ctrl Pts',(-39.6422940155811,-5.38457849241134,
-2.64427816307056));
#28263=CARTESIAN_POINT('Ctrl Pts',(-39.6887135636087,-5.66780569694108,
-1.69999485767289));
#28264=CARTESIAN_POINT('Ctrl Pts',(-39.7157673116709,-5.83287316875554,
-1.14965768876502));
#28265=CARTESIAN_POINT('Ctrl Pts',(-39.742821059733,-5.91604303207176,-0.574756249176902));
#28266=CARTESIAN_POINT('Ctrl Pts',(-39.7698748077951,-5.91629469088874,
7.39219476919573E-5));
#28267=CARTESIAN_POINT('Ctrl Pts',(-40.0216251922048,-5.91624628365206,
2.79657000012922E-5));
#28268=CARTESIAN_POINT('Ctrl Pts',(-39.9970105229098,-5.91616051738276,
-0.522989607226258));
#28269=CARTESIAN_POINT('Ctrl Pts',(-39.9723958536149,-5.84748692575974,
-1.04602927257089));
#28270=CARTESIAN_POINT('Ctrl Pts',(-39.9477811843199,-5.71050652059654,
-1.55052220640218));
#28271=CARTESIAN_POINT('Ctrl Pts',(-39.9013616362923,-5.452182168556,-2.50191967150481));
#28272=CARTESIAN_POINT('Ctrl Pts',(-39.8549420882647,-4.95092967322311,
-3.38735705419161));
#28273=CARTESIAN_POINT('Ctrl Pts',(-39.8085225402371,-4.26810941472458,
-4.09844432172273));
#28274=CARTESIAN_POINT('Ctrl Pts',(-39.7621029922095,-3.58528915622607,
-4.80953158925383));
#28275=CARTESIAN_POINT('Ctrl Pts',(-39.7156834441818,-2.72090113456196,
-5.34626874162926));
#28276=CARTESIAN_POINT('Ctrl Pts',(-39.6692638961542,-1.78075864359127,
-5.6429515758685));
#28277=CARTESIAN_POINT('Ctrl Pts',(-39.6228443481266,-0.840616152620568,
-5.93963441010775));
#28278=CARTESIAN_POINT('Ctrl Pts',(-39.576424800099,0.175280807656705,-5.99626292621078));
#28279=CARTESIAN_POINT('Ctrl Pts',(-39.5300052520714,1.14257211089189,-5.80590499454942));
#28280=CARTESIAN_POINT('Ctrl Pts',(-39.4835857040438,2.10986341412708,-5.61554706288806));
#28281=CARTESIAN_POINT('Ctrl Pts',(-39.4371661560162,3.02854906032023,-5.17820268346229));
#28282=CARTESIAN_POINT('Ctrl Pts',(-39.3907466079886,3.786168960011,-4.54740898101007));
#28283=CARTESIAN_POINT('Ctrl Pts',(-39.3443270599609,4.54378885970176,-3.91661527855786));
#28284=CARTESIAN_POINT('Ctrl Pts',(-39.2979075119333,5.14034301289013,-3.09237225307922));
#28285=CARTESIAN_POINT('Ctrl Pts',(-39.2514879639057,5.50280477143654,-2.17557888429198));
#28286=CARTESIAN_POINT('Ctrl Pts',(-39.2050684158781,5.86526652998294,-1.25878551550473));
#28287=CARTESIAN_POINT('Ctrl Pts',(-39.1586488678505,5.99363589388735,-0.249441803408889));
#28288=CARTESIAN_POINT('Ctrl Pts',(-39.1122293198229,5.87219864119747,0.728894335717105));
#28289=CARTESIAN_POINT('Ctrl Pts',(-39.0658097717953,5.75076138850759,1.7072304748431));
#28290=CARTESIAN_POINT('Ctrl Pts',(-39.0193902237677,5.37951751922341,2.65455904099929));
#28291=CARTESIAN_POINT('Ctrl Pts',(-38.97297067574,4.80391252269629,3.45491364705453));
#28292=CARTESIAN_POINT('Ctrl Pts',(-38.9265511277124,4.22830752616917,4.25526825310977));
#28293=CARTESIAN_POINT('Ctrl Pts',(-38.8801315796848,3.44834140239914,4.90864889906404));
#28294=CARTESIAN_POINT('Ctrl Pts',(-38.8337120316572,2.5594930134089,5.33507257201182));
#28295=CARTESIAN_POINT('Ctrl Pts',(-38.7872924836296,1.67064462441864,5.76149624495962));
#28296=CARTESIAN_POINT('Ctrl Pts',(-38.740872935602,0.672913970208175,5.96096294490088));
#28297=CARTESIAN_POINT('Ctrl Pts',(-38.6944533875744,-0.311562635136377,
5.90905513248174));
#28298=CARTESIAN_POINT('Ctrl Pts',(-38.6480338395467,-1.2960392404809,5.85714732006259));
#28299=CARTESIAN_POINT('Ctrl Pts',(-38.6016142915191,-2.26726179695949,
5.55386499528307));
#28300=CARTESIAN_POINT('Ctrl Pts',(-38.5551947434915,-3.10633895578493,
5.03633419523514));
#28301=CARTESIAN_POINT('Ctrl Pts',(-38.5087751954639,-3.94541611461034,
4.51880339518723));
#28302=CARTESIAN_POINT('Ctrl Pts',(-38.4623556474363,-4.65234787578258,
3.7870241198709));
#28303=CARTESIAN_POINT('Ctrl Pts',(-38.4159360994087,-5.14059581407073,
2.93057648094711));
#28304=CARTESIAN_POINT('Ctrl Pts',(-38.3695165513811,-5.6288437523589,2.0741288420233));
#28305=CARTESIAN_POINT('Ctrl Pts',(-38.3230970033535,-5.89840786776299,
1.09301283949197));
#28306=CARTESIAN_POINT('Ctrl Pts',(-38.2766774553259,-5.91628970791874,
0.107330919573857));
#28307=CARTESIAN_POINT('Ctrl Pts',(-38.2749933676188,-5.91693845588085,
0.0715706660839549));
#28308=CARTESIAN_POINT('Ctrl Pts',(-38.2733092799118,-5.91725593527694,
0.0358044028545749));
#28309=CARTESIAN_POINT('Ctrl Pts',(-38.2716251922048,-5.91724351279131,
3.7918395758653E-5));
#28310=CARTESIAN_POINT('Origin',(-29.75,0.,0.));
#28311=CARTESIAN_POINT('',(-36.2698748077951,-5.91625954349593,-4.60302636559606E-5));
#28312=CARTESIAN_POINT('',(-36.5216251922048,-5.91632433790914,-8.97973128488559E-5));
#28313=CARTESIAN_POINT('',(-29.75,-5.91675,-7.2459289488551E-16));
#28314=CARTESIAN_POINT('Ctrl Pts',(-36.2698748077951,-5.91625954349593,
-4.60302636559606E-5));
#28315=CARTESIAN_POINT('Ctrl Pts',(-36.2954185737369,-5.91611265376947,
0.542709703882021));
#28316=CARTESIAN_POINT('Ctrl Pts',(-36.3209623396788,-5.84208692011566,
1.0855047064104));
#28317=CARTESIAN_POINT('Ctrl Pts',(-36.3465061056206,-5.69470404581093,
1.60759129290275));
#28318=CARTESIAN_POINT('Ctrl Pts',(-36.3929256536482,-5.4268717133423,2.55635599077197));
#28319=CARTESIAN_POINT('Ctrl Pts',(-36.4393452016758,-4.91678348370265,
3.43673285534667));
#28320=CARTESIAN_POINT('Ctrl Pts',(-36.4857647497034,-4.22688135560573,
4.14095133272836));
#28321=CARTESIAN_POINT('Ctrl Pts',(-36.5321842977311,-3.53697922750878,
4.84516981011006));
#28322=CARTESIAN_POINT('Ctrl Pts',(-36.5786038457587,-2.66726320095454,
5.37322990029873));
#28323=CARTESIAN_POINT('Ctrl Pts',(-36.6250233937863,-1.72419879280033,
5.66048959519386));
#28324=CARTESIAN_POINT('Ctrl Pts',(-36.6714429418139,-0.781134384646113,
5.94774929008899));
#28325=CARTESIAN_POINT('Ctrl Pts',(-36.7178624898415,0.235278405108075,
5.99420858969058));
#28326=CARTESIAN_POINT('Ctrl Pts',(-36.7642820378691,1.20061630530521,5.79418021999897));
#28327=CARTESIAN_POINT('Ctrl Pts',(-36.8107015858967,2.16595420550232,5.59415185030736));
#28328=CARTESIAN_POINT('Ctrl Pts',(-36.8571211339243,3.08021721614238,5.14763581132257));
#28329=CARTESIAN_POINT('Ctrl Pts',(-36.903540681952,3.83148664077805,4.50929196836171));
#28330=CARTESIAN_POINT('Ctrl Pts',(-36.9499602299796,4.58275606541374,3.87094812540083));
#28331=CARTESIAN_POINT('Ctrl Pts',(-36.9963797780072,5.17103190404502,3.04077647846387));
#28332=CARTESIAN_POINT('Ctrl Pts',(-37.0427993260348,5.52430089107451,2.12040175421203));
#28333=CARTESIAN_POINT('Ctrl Pts',(-37.0892188740624,5.877569878104,1.20002702996018));
#28334=CARTESIAN_POINT('Ctrl Pts',(-37.13563842209,5.99583201353171,0.189449228393454));
#28335=CARTESIAN_POINT('Ctrl Pts',(-37.1820579701176,5.86461034282473,-0.787622664240537));
#28336=CARTESIAN_POINT('Ctrl Pts',(-37.2284775181453,5.73338867211774,-1.76469455687453));
#28337=CARTESIAN_POINT('Ctrl Pts',(-37.2748970661728,5.35268319527606,-2.70826054057578));
#28338=CARTESIAN_POINT('Ctrl Pts',(-37.3213166142005,4.76909763595757,-3.50281482141091));
#28339=CARTESIAN_POINT('Ctrl Pts',(-37.3677361622281,4.18551207663908,-4.29736910224604));
#28340=CARTESIAN_POINT('Ctrl Pts',(-37.4141557102557,3.39904643484378,-4.94291168021504));
#28341=CARTESIAN_POINT('Ctrl Pts',(-37.4605752582833,2.50597520533521,-5.36041903256053));
#28342=CARTESIAN_POINT('Ctrl Pts',(-37.5069948063109,1.61290397582666,-5.77792638490601));
#28343=CARTESIAN_POINT('Ctrl Pts',(-37.5534143543385,0.613227158604841,
-5.96739851162799));
#28344=CARTESIAN_POINT('Ctrl Pts',(-37.5998339023661,-0.370680694423386,
-5.90564135019846));
#28345=CARTESIAN_POINT('Ctrl Pts',(-37.6462534503937,-1.35458854745164,
-5.84388418876892));
#28346=CARTESIAN_POINT('Ctrl Pts',(-37.6926729984214,-2.3227274362863,-5.53089773918786));
#28347=CARTESIAN_POINT('Ctrl Pts',(-37.739092546449,-3.15658349658267,-5.00499596038738));
#28348=CARTESIAN_POINT('Ctrl Pts',(-37.7855120944766,-3.99043955687904,
-4.47909418158689));
#28349=CARTESIAN_POINT('Ctrl Pts',(-37.8319316425042,-4.69001278863712,
-3.74027707356698));
#28350=CARTESIAN_POINT('Ctrl Pts',(-37.8783511905318,-5.16966555448492,
-2.87898627804374));
#28351=CARTESIAN_POINT('Ctrl Pts',(-37.9247707385594,-5.64931832033271,
-2.01769548252052));
#28352=CARTESIAN_POINT('Ctrl Pts',(-37.971190286587,-5.90905062027022,-1.03393099949398));
#28353=CARTESIAN_POINT('Ctrl Pts',(-38.0176098346146,-5.91706755491295,
-0.0481194865781631));
#28354=CARTESIAN_POINT('Ctrl Pts',(-38.0183648256748,-5.91719794640193,
-0.032085748403995));
#28355=CARTESIAN_POINT('Ctrl Pts',(-38.0191198167349,-5.91726175057181,
-0.0160514687204437));
#28356=CARTESIAN_POINT('Ctrl Pts',(-38.0198748077951,-5.91725909577585,
-1.71678216764892E-5));
#28357=CARTESIAN_POINT('Ctrl Pts',(-38.2716251922048,-5.91724351279131,
3.7918395758653E-5));
#28358=CARTESIAN_POINT('Ctrl Pts',(-38.2268897318842,-5.91691352664454,
-0.95004926510235));
#28359=CARTESIAN_POINT('Ctrl Pts',(-38.1821542715636,-5.68379628383804,
-1.90029255378405));
#28360=CARTESIAN_POINT('Ctrl Pts',(-38.137418811243,-5.24350887576506,-2.74219228065701));
#28361=CARTESIAN_POINT('Ctrl Pts',(-38.0909992632154,-4.78664663854823,
-3.61578572366473));
#28362=CARTESIAN_POINT('Ctrl Pts',(-38.0445797151878,-4.10672259920717,
-4.37272477237521));
#28363=CARTESIAN_POINT('Ctrl Pts',(-37.9981601671602,-3.28696905663254,
-4.92034940375804));
#28364=CARTESIAN_POINT('Ctrl Pts',(-37.9517406191326,-2.46721551405795,
-5.46797403514083));
#28365=CARTESIAN_POINT('Ctrl Pts',(-37.9053210711049,-1.50763246824981,
-5.806284249196));
#28366=CARTESIAN_POINT('Ctrl Pts',(-37.8589015230773,-0.525686427608837,
-5.89386610079917));
#28367=CARTESIAN_POINT('Ctrl Pts',(-37.8124819750497,0.456259613032197,
-5.98144795240236));
#28368=CARTESIAN_POINT('Ctrl Pts',(-37.7660624270221,1.46056864850614,-5.81830144155351));
#28369=CARTESIAN_POINT('Ctrl Pts',(-37.7196428789945,2.36429907801261,-5.42439800383698));
#28370=CARTESIAN_POINT('Ctrl Pts',(-37.6732233309669,3.26802950751907,-5.03049456612045));
#28371=CARTESIAN_POINT('Ctrl Pts',(-37.6268037829393,4.07118133105807,-4.40583420153629));
#28372=CARTESIAN_POINT('Ctrl Pts',(-37.5803842349117,4.67543742971133,-3.62688415519109));
#28373=CARTESIAN_POINT('Ctrl Pts',(-37.533964686884,5.27969352836458,-2.84793410884589));
#28374=CARTESIAN_POINT('Ctrl Pts',(-37.4875451388564,5.68505390213202,-1.91469438073971));
#28375=CARTESIAN_POINT('Ctrl Pts',(-37.4411255908288,5.84189671999184,-0.941406685375875));
#28376=CARTESIAN_POINT('Ctrl Pts',(-37.3947060428012,5.99873953785166,0.0318810099879278));
#28377=CARTESIAN_POINT('Ctrl Pts',(-37.3482864947736,5.90706479980387,1.04521667260943));
#28378=CARTESIAN_POINT('Ctrl Pts',(-37.301866946746,5.57809478768647,1.97455371512322));
#28379=CARTESIAN_POINT('Ctrl Pts',(-37.2554473987184,5.24912477556906,2.90389075763703));
#28380=CARTESIAN_POINT('Ctrl Pts',(-37.2090278506908,4.68285948938204,3.74922918004318));
#28381=CARTESIAN_POINT('Ctrl Pts',(-37.1626083026632,3.94861779244578,4.40708762829858));
#28382=CARTESIAN_POINT('Ctrl Pts',(-37.1161887546355,3.21437609550952,5.06494607655399));
#28383=CARTESIAN_POINT('Ctrl Pts',(-37.0697692066079,2.31215798782404,5.53532455065863));
#28384=CARTESIAN_POINT('Ctrl Pts',(-37.0233496585803,1.35240769971278,5.76064208644136));
#28385=CARTESIAN_POINT('Ctrl Pts',(-36.9769301105527,0.39265741160152,5.98595962222409));
#28386=CARTESIAN_POINT('Ctrl Pts',(-36.9305105625251,-0.624625056935495,
5.96621621968489));
#28387=CARTESIAN_POINT('Ctrl Pts',(-36.8840910144975,-1.57490997378356,
5.70382874995375));
#28388=CARTESIAN_POINT('Ctrl Pts',(-36.8376714664699,-2.5251948906316,5.44144128022261));
#28389=CARTESIAN_POINT('Ctrl Pts',(-36.7912519184422,-3.40848225579067,
4.93640974329955));
#28390=CARTESIAN_POINT('Ctrl Pts',(-36.7448323704146,-4.11664522901183,
4.25055712733942));
#28391=CARTESIAN_POINT('Ctrl Pts',(-36.698412822387,-4.82480820223301,3.56470451137927));
#28392=CARTESIAN_POINT('Ctrl Pts',(-36.6519932743594,-5.35784678351626,
2.69803081638205));
#28393=CARTESIAN_POINT('Ctrl Pts',(-36.6055737263318,-5.65050952718447,
1.75662913488289));
#28394=CARTESIAN_POINT('Ctrl Pts',(-36.5775908816228,-5.82693382376107,
1.18912905826634));
#28395=CARTESIAN_POINT('Ctrl Pts',(-36.5496080369138,-5.91600614704412,
0.594473019777904));
#28396=CARTESIAN_POINT('Ctrl Pts',(-36.5216251922048,-5.91632433790914,
-8.97973128488559E-5));
#28397=CARTESIAN_POINT('Origin',(-29.75,0.,0.));
#28398=CARTESIAN_POINT('',(-34.5198748077951,-5.9170907741469,0.000109654298403733));
#28399=CARTESIAN_POINT('',(-34.7716251922048,-5.91694163414713,0.000140169273084226));
#28400=CARTESIAN_POINT('',(-29.75,-5.91675,-7.2459289488551E-16));
#28401=CARTESIAN_POINT('Ctrl Pts',(-34.5198748077951,-5.9170907741469,0.000109654298403733));
#28402=CARTESIAN_POINT('Ctrl Pts',(-34.5252977827113,-5.91718880965865,
0.11529087392914));
#28403=CARTESIAN_POINT('Ctrl Pts',(-34.5307207576275,-5.91389496019476,
0.230466490326725));
#28404=CARTESIAN_POINT('Ctrl Pts',(-34.5361437325437,-5.9071714106131,0.345441543574822));
#28405=CARTESIAN_POINT('Ctrl Pts',(-34.5825632805713,-5.849619211397,1.32960431192358));
#28406=CARTESIAN_POINT('Ctrl Pts',(-34.628982828599,-5.54077263440303,2.29907180368102));
#28407=CARTESIAN_POINT('Ctrl Pts',(-34.6754023766266,-5.0184388597283,3.13516751475276));
#28408=CARTESIAN_POINT('Ctrl Pts',(-34.7218219246542,-4.49610508505359,
3.97126322582447));
#28409=CARTESIAN_POINT('Ctrl Pts',(-34.7682414726818,-3.76028411269806,
4.67398715621054));
#28410=CARTESIAN_POINT('Ctrl Pts',(-34.8146610207094,-2.90105081508504,
5.1573159785577));
#28411=CARTESIAN_POINT('Ctrl Pts',(-34.861080568737,-2.04181751747196,5.64064480090488));
#28412=CARTESIAN_POINT('Ctrl Pts',(-34.9075001167646,-1.0591718946014,5.90457851521318));
#28413=CARTESIAN_POINT('Ctrl Pts',(-34.9539196647922,-0.0734036398125114,
5.91680790968021));
#28414=CARTESIAN_POINT('Ctrl Pts',(-35.0003392128198,0.912364614976294,
5.92903730414724));
#28415=CARTESIAN_POINT('Ctrl Pts',(-35.0467587608474,1.90125550168333,5.68956237877302));
#28416=CARTESIAN_POINT('Ctrl Pts',(-35.0931783088751,2.77221481852983,5.2276982443821));
#28417=CARTESIAN_POINT('Ctrl Pts',(-35.1395978569027,3.64317413537638,4.76583410999116));
#28418=CARTESIAN_POINT('Ctrl Pts',(-35.1860174049303,4.39620188236236,4.08158076658348));
#28419=CARTESIAN_POINT('Ctrl Pts',(-35.2324369529579,4.9391168349927,3.25870048097148));
#28420=CARTESIAN_POINT('Ctrl Pts',(-35.2788565009855,5.48203178762306,2.43582019535944));
#28421=CARTESIAN_POINT('Ctrl Pts',(-35.3252760490131,5.81483394589777,1.47431296754308));
#28422=CARTESIAN_POINT('Ctrl Pts',(-35.3716955970407,5.8967836284609,0.49188085295889));
#28423=CARTESIAN_POINT('Ctrl Pts',(-35.4181151450684,5.97873331102404,-0.490551261625275));
#28424=CARTESIAN_POINT('Ctrl Pts',(-35.464534693096,5.8098305178756,-1.49390826297733));
#28425=CARTESIAN_POINT('Ctrl Pts',(-35.5109542411236,5.41075133479782,-2.39536509271044));
#28426=CARTESIAN_POINT('Ctrl Pts',(-35.5573737891512,5.01167215172005,-3.29682192244353));
#28427=CARTESIAN_POINT('Ctrl Pts',(-35.6037933371788,4.38241657871295,-4.09637858055776));
#28428=CARTESIAN_POINT('Ctrl Pts',(-35.6502128852064,3.60001437925112,-4.69615804712504));
#28429=CARTESIAN_POINT('Ctrl Pts',(-35.696632433234,2.81761217978926,-5.29593751369234));
#28430=CARTESIAN_POINT('Ctrl Pts',(-35.7430519812617,1.88206335387267,-5.69593978871267));
#28431=CARTESIAN_POINT('Ctrl Pts',(-35.7894715292893,0.907892282167387,
-5.84719894807531));
#28432=CARTESIAN_POINT('Ctrl Pts',(-35.8358910773169,-0.0662787895378396,
-5.99845810743793));
#28433=CARTESIAN_POINT('Ctrl Pts',(-35.8823106253445,-1.07907210703174,
-5.90097415114289));
#28434=CARTESIAN_POINT('Ctrl Pts',(-35.9287301733721,-2.00650747364734,
-5.56668049133318));
#28435=CARTESIAN_POINT('Ctrl Pts',(-35.9751497213997,-2.93394284026303,
-5.23238683152344));
#28436=CARTESIAN_POINT('Ctrl Pts',(-36.0215692694273,-3.7760202560004,-4.661283468199));
#28437=CARTESIAN_POINT('Ctrl Pts',(-36.0679888174549,-4.42965756005859,
-3.92328151360667));
#28438=CARTESIAN_POINT('Ctrl Pts',(-36.1144083654825,-5.08329486411676,
-3.18527955901436));
#28439=CARTESIAN_POINT('Ctrl Pts',(-36.1608279135102,-5.54849205649576,
-2.28037901315418));
#28440=CARTESIAN_POINT('Ctrl Pts',(-36.2072474615378,-5.76830243503646,
-1.31935247464221));
#28441=CARTESIAN_POINT('Ctrl Pts',(-36.2281232436235,-5.86715547772177,
-0.887159972796121));
#28442=CARTESIAN_POINT('Ctrl Pts',(-36.2489990257093,-5.91637958992632,
-0.443616115333533));
#28443=CARTESIAN_POINT('Ctrl Pts',(-36.2698748077951,-5.91625954349593,
-4.60302636559606E-5));
#28444=CARTESIAN_POINT('Ctrl Pts',(-36.5216251922048,-5.91632433790914,
-8.97973128488559E-5));
#28445=CARTESIAN_POINT('Ctrl Pts',(-36.5031884888862,-5.91653398030391,
-0.391821888062817));
#28446=CARTESIAN_POINT('Ctrl Pts',(-36.4847517855676,-5.87821607271003,
-0.783513512054098));
#28447=CARTESIAN_POINT('Ctrl Pts',(-36.4663150822489,-5.80096959006355,
-1.16737125606198));
#28448=CARTESIAN_POINT('Ctrl Pts',(-36.4198955342213,-5.60648000322127,
-2.1338402975065));
#28449=CARTESIAN_POINT('Ctrl Pts',(-36.3734759861937,-5.16521392348355,
-3.05064871239451));
#28450=CARTESIAN_POINT('Ctrl Pts',(-36.3270564381661,-4.53118854705755,
-3.80556621087274));
#28451=CARTESIAN_POINT('Ctrl Pts',(-36.2806368901385,-3.89716317063153,
-4.560483709351));
#28452=CARTESIAN_POINT('Ctrl Pts',(-36.2342173421109,-3.07037849751719,
-5.1535102914195));
#28453=CARTESIAN_POINT('Ctrl Pts',(-36.1877977940833,-2.15204464097599,
-5.51205113343194));
#28454=CARTESIAN_POINT('Ctrl Pts',(-36.1413782460557,-1.23371078443479,
-5.87059197544438));
#28455=CARTESIAN_POINT('Ctrl Pts',(-36.0949586980281,-0.223827744466776,
-5.99464707740077));
#28456=CARTESIAN_POINT('Ctrl Pts',(-36.0485391500005,0.75398054130614,-5.86903034390295));
#28457=CARTESIAN_POINT('Ctrl Pts',(-36.0021196019729,1.73178882707903,-5.74341361040513));
#28458=CARTESIAN_POINT('Ctrl Pts',(-35.9557000539452,2.67752235865676,-5.36812504145309));
#28459=CARTESIAN_POINT('Ctrl Pts',(-35.9092805059176,3.47541000365299,-4.78910525472458));
#28460=CARTESIAN_POINT('Ctrl Pts',(-35.86286095789,4.27329764864928,-4.21008546799603));
#28461=CARTESIAN_POINT('Ctrl Pts',(-35.8164414098624,4.92333940706406,-3.42733446349096));
#28462=CARTESIAN_POINT('Ctrl Pts',(-35.7700218618348,5.34596099295176,-2.53667201194006));
#28463=CARTESIAN_POINT('Ctrl Pts',(-35.7236023138072,5.76858257883944,-1.64600956038922));
#28464=CARTESIAN_POINT('Ctrl Pts',(-35.6771827657796,5.96378399220007,-0.647435661792543));
#28465=CARTESIAN_POINT('Ctrl Pts',(-35.6307632177519,5.9076698249577,0.336810144749435));
#28466=CARTESIAN_POINT('Ctrl Pts',(-35.5843436697243,5.85155565771532,1.32105595129147));
#28467=CARTESIAN_POINT('Ctrl Pts',(-35.5379241216967,5.54412590986989,2.29097366577883));
#28468=CARTESIAN_POINT('Ctrl Pts',(-35.4915045736691,5.02301432163358,3.12783167050048));
#28469=CARTESIAN_POINT('Ctrl Pts',(-35.4450850256415,4.50190273339729,3.96468967522209));
#28470=CARTESIAN_POINT('Ctrl Pts',(-35.3986654776139,3.76710930477012,4.66848797017802));
#28471=CARTESIAN_POINT('Ctrl Pts',(-35.3522459295863,2.90858312232014,5.15307171062816));
#28472=CARTESIAN_POINT('Ctrl Pts',(-35.3058263815587,2.05005693987014,5.6376554510783));
#28473=CARTESIAN_POINT('Ctrl Pts',(-35.2594068335311,1.0677980035973,5.90302463702264));
#28474=CARTESIAN_POINT('Ctrl Pts',(-35.2129872855034,0.08204867094368,5.91669433467018));
#28475=CARTESIAN_POINT('Ctrl Pts',(-35.1665677374758,-0.903700661709968,
5.93036403231773));
#28476=CARTESIAN_POINT('Ctrl Pts',(-35.1201481894482,-1.89294039074434,
5.69233424166847));
#28477=CARTESIAN_POINT('Ctrl Pts',(-35.0737286414206,-2.7645736111563,5.23174316865995));
#28478=CARTESIAN_POINT('Ctrl Pts',(-35.027309093393,-3.63620683156822,4.77115209565145));
#28479=CARTESIAN_POINT('Ctrl Pts',(-34.9808895453654,-4.39023354335769,
4.0879997402837));
#28480=CARTESIAN_POINT('Ctrl Pts',(-34.9344699973377,-4.93435023463825,
3.26591359289361));
#28481=CARTESIAN_POINT('Ctrl Pts',(-34.8880504493101,-5.47846692591882,
2.4438274455035));
#28482=CARTESIAN_POINT('Ctrl Pts',(-34.8416309012825,-5.81267359669049,
1.48280750609104));
#28483=CARTESIAN_POINT('Ctrl Pts',(-34.7952113532549,-5.89605863344435,
0.500496179114509));
#28484=CARTESIAN_POINT('Ctrl Pts',(-34.7873492995716,-5.91018151191266,
0.334122642218592));
#28485=CARTESIAN_POINT('Ctrl Pts',(-34.7794872458882,-5.91710931766303,
0.167138340296805));
#28486=CARTESIAN_POINT('Ctrl Pts',(-34.7716251922048,-5.91694163414713,
0.000140169273084226));
#28487=CARTESIAN_POINT('Origin',(-29.75,0.,0.));
#28488=CARTESIAN_POINT('',(-32.7698748077951,-5.91649785403418,-0.000138834737503368));
#28489=CARTESIAN_POINT('',(-33.0216251922048,-5.91664686417118,-0.000153939560766411));
#28490=CARTESIAN_POINT('',(-29.75,-5.91675,-7.2459289488551E-16));
#28491=CARTESIAN_POINT('Ctrl Pts',(-32.7698748077951,-5.91649785403418,
-0.000138834737503368));
#28492=CARTESIAN_POINT('Ctrl Pts',(-32.8015965397133,-5.91591751325044,
0.673809007249405));
#28493=CARTESIAN_POINT('Ctrl Pts',(-32.8333182716315,-5.80093975986991,
1.34794980680733));
#28494=CARTESIAN_POINT('Ctrl Pts',(-32.8650400035497,-5.57520380049187,
1.98270182260802));
#28495=CARTESIAN_POINT('Ctrl Pts',(-32.9114595515773,-5.24487627502982,
2.91155721294634));
#28496=CARTESIAN_POINT('Ctrl Pts',(-32.9578790996049,-4.67737645971137,
3.75606735812451));
#28497=CARTESIAN_POINT('Ctrl Pts',(-33.0042986476325,-3.9421743416468,4.41285229692244));
#28498=CARTESIAN_POINT('Ctrl Pts',(-33.0507181956601,-3.20697222358221,
5.0696372357204));
#28499=CARTESIAN_POINT('Ctrl Pts',(-33.0971377436877,-2.30406780277147,
5.53869696813813));
#28500=CARTESIAN_POINT('Ctrl Pts',(-33.1435572917153,-1.34398932395124,
5.7626119625997));
#28501=CARTESIAN_POINT('Ctrl Pts',(-33.1899768397429,-0.383910845131006,
5.98652695706128));
#28502=CARTESIAN_POINT('Ctrl Pts',(-33.2363963877706,0.633341691698729,
5.96529721356671));
#28503=CARTESIAN_POINT('Ctrl Pts',(-33.2828159357982,1.58324221848665,5.70152155235719));
#28504=CARTESIAN_POINT('Ctrl Pts',(-33.3292354838258,2.53314274527455,5.43774589114768));
#28505=CARTESIAN_POINT('Ctrl Pts',(-33.3756550318534,3.41569126202065,4.93142431222322));
#28506=CARTESIAN_POINT('Ctrl Pts',(-33.422074579881,4.12285137394988,4.24453772308737));
#28507=CARTESIAN_POINT('Ctrl Pts',(-33.4684941279086,4.83001148587914,3.55765113395147));
#28508=CARTESIAN_POINT('Ctrl Pts',(-33.5149136759362,5.36178319299148,2.69019953460422));
#28509=CARTESIAN_POINT('Ctrl Pts',(-33.5613332239639,5.65307013288908,1.74837124405247));
#28510=CARTESIAN_POINT('Ctrl Pts',(-33.6077527719915,5.94435707278667,0.806542953500733));
#28511=CARTESIAN_POINT('Ctrl Pts',(-33.6541723200191,5.99515924546949,-0.209662028255445));
#28512=CARTESIAN_POINT('Ctrl Pts',(-33.7005918680467,5.79925774797727,-1.175845868691));
#28513=CARTESIAN_POINT('Ctrl Pts',(-33.7470114160743,5.60335625048504,-2.14202970912655));
#28514=CARTESIAN_POINT('Ctrl Pts',(-33.7934309641019,5.16075108281776,-3.0581924082415));
#28515=CARTESIAN_POINT('Ctrl Pts',(-33.8398505121295,4.52562336444508,-3.81218272090687));
#28516=CARTESIAN_POINT('Ctrl Pts',(-33.8862700601571,3.89049564607243,-4.56617303357221));
#28517=CARTESIAN_POINT('Ctrl Pts',(-33.9326896081848,3.06284537699438,-5.15799095978799));
#28518=CARTESIAN_POINT('Ctrl Pts',(-33.9791091562124,2.14398863163539,-5.51518963244332));
#28519=CARTESIAN_POINT('Ctrl Pts',(-34.02552870424,1.22513188627637,-5.87238830509866));
#28520=CARTESIAN_POINT('Ctrl Pts',(-34.0719482522676,0.215068664636392,
-5.99496772419353));
#28521=CARTESIAN_POINT('Ctrl Pts',(-34.1183678002952,-0.762555038882753,
-5.86792243873985));
#28522=CARTESIAN_POINT('Ctrl Pts',(-34.1647873483228,-1.7401787424019,-5.74087715328617));
#28523=CARTESIAN_POINT('Ctrl Pts',(-34.2112068963505,-2.68536292780023,
-5.36420716328394));
#28524=CARTESIAN_POINT('Ctrl Pts',(-34.2576264443781,-3.48240371041724,
-4.78402219184488));
#28525=CARTESIAN_POINT('Ctrl Pts',(-34.3040459924057,-4.27944449303424,
-4.20383722040583));
#28526=CARTESIAN_POINT('Ctrl Pts',(-34.3504655404333,-4.92834187286995,
-3.42013726752995));
#28527=CARTESIAN_POINT('Ctrl Pts',(-34.3968850884609,-5.34966165206868,
-2.528858268622));
#28528=CARTESIAN_POINT('Ctrl Pts',(-34.4378816615723,-5.72176064624512,
-1.74170315415062));
#28529=CARTESIAN_POINT('Ctrl Pts',(-34.4788782346837,-5.91634964587558,
-0.870636636180083));
#28530=CARTESIAN_POINT('Ctrl Pts',(-34.5198748077951,-5.9170907741469,0.000109654298403733));
#28531=CARTESIAN_POINT('Ctrl Pts',(-34.7716251922048,-5.91694163414713,
0.000140169273084226));
#28532=CARTESIAN_POINT('Ctrl Pts',(-34.7330676978606,-5.91611927188961,
-0.818860984124561));
#28533=CARTESIAN_POINT('Ctrl Pts',(-34.6945102035163,-5.74463840154745,
-1.63819571286224));
#28534=CARTESIAN_POINT('Ctrl Pts',(-34.6559527091721,-5.41424544436451,
-2.38745682735834));
#28535=CARTESIAN_POINT('Ctrl Pts',(-34.6095331611445,-5.01648381579477,
-3.28949579231404));
#28536=CARTESIAN_POINT('Ctrl Pts',(-34.5631136131169,-4.38839715591919,
-4.0899710076849));
#28537=CARTESIAN_POINT('Ctrl Pts',(-34.5166940650892,-3.60687213674706,
-4.69089300916996));
#28538=CARTESIAN_POINT('Ctrl Pts',(-34.4702745170616,-2.82534711757491,
-5.29181501065503));
#28539=CARTESIAN_POINT('Ctrl Pts',(-34.423854969034,-1.8903837391062,-5.69318379825433));
#28540=CARTESIAN_POINT('Ctrl Pts',(-34.3774354210064,-0.916434714976281,
-5.84586616743047));
#28541=CARTESIAN_POINT('Ctrl Pts',(-34.3310158729788,0.0575143091536082,
-5.9985485366066));
#28542=CARTESIAN_POINT('Ctrl Pts',(-34.2845963249512,1.07044897894464,-5.90254448735958));
#28543=CARTESIAN_POINT('Ctrl Pts',(-34.2381767769236,1.99837179421368,-5.56960627032226));
#28544=CARTESIAN_POINT('Ctrl Pts',(-34.1917572288959,2.92629460948271,-5.23666805328494));
#28545=CARTESIAN_POINT('Ctrl Pts',(-34.1453376808684,3.76920557022969,-4.66679566845733));
#28546=CARTESIAN_POINT('Ctrl Pts',(-34.0989181328408,4.42392047797994,-3.92974953894413));
#28547=CARTESIAN_POINT('Ctrl Pts',(-34.0524985848131,5.0786353857302,-3.19270340943091));
#28548=CARTESIAN_POINT('Ctrl Pts',(-34.0060790367855,5.54515424048372,-2.28848353523204));
#28549=CARTESIAN_POINT('Ctrl Pts',(-33.9596594887579,5.76636854995267,-1.32777919114536));
#28550=CARTESIAN_POINT('Ctrl Pts',(-33.9132399407303,5.98758285942162,-0.36707484705867));
#28551=CARTESIAN_POINT('Ctrl Pts',(-33.8668203927027,5.96349262360604,0.650113966915861));
#28552=CARTESIAN_POINT('Ctrl Pts',(-33.820400844675,5.69704682738031,1.59926898330386));
#28553=CARTESIAN_POINT('Ctrl Pts',(-33.7739812966474,5.43060103115459,2.54842399969182));
#28554=CARTESIAN_POINT('Ctrl Pts',(-33.7275617486198,4.92179967451871,3.42954521849328));
#28555=CARTESIAN_POINT('Ctrl Pts',(-33.6811422005922,4.23292722476782,4.13477096634641));
#28556=CARTESIAN_POINT('Ctrl Pts',(-33.6347226525646,3.54405477501693,4.83999671419954));
#28557=CARTESIAN_POINT('Ctrl Pts',(-33.588303104537,2.67511123215103,5.36932699110438));
#28558=CARTESIAN_POINT('Ctrl Pts',(-33.5418835565094,1.73246755012107,5.65796430017894));
#28559=CARTESIAN_POINT('Ctrl Pts',(-33.4954640084818,0.789823868091082,
5.9466016092535));
#28560=CARTESIAN_POINT('Ctrl Pts',(-33.4490444604542,-0.226519953102918,
5.99454595049775));
#28561=CARTESIAN_POINT('Ctrl Pts',(-33.4026249124266,-1.19214908502915,
5.79592825985502));
#28562=CARTESIAN_POINT('Ctrl Pts',(-33.3562053643989,-2.15777821695538,
5.59731056921229));
#28563=CARTESIAN_POINT('Ctrl Pts',(-33.3097858163713,-3.07269265961378,
5.15213084668259));
#28564=CARTESIAN_POINT('Ctrl Pts',(-33.2633662683437,-3.82489397208368,
4.5148853735881));
#28565=CARTESIAN_POINT('Ctrl Pts',(-33.2169467203161,-4.57709528455356,
3.87763990049363));
#28566=CARTESIAN_POINT('Ctrl Pts',(-33.1705271722885,-5.16658346683494,
3.04832867683433));
#28567=CARTESIAN_POINT('Ctrl Pts',(-33.1241076242609,-5.52119684535653,
2.12847110131826));
#28568=CARTESIAN_POINT('Ctrl Pts',(-33.0899468135755,-5.78216191298198,
1.45153472796112));
#28569=CARTESIAN_POINT('Ctrl Pts',(-33.0557860028902,-5.91592585562199,
0.72556117549773));
#28570=CARTESIAN_POINT('Ctrl Pts',(-33.0216251922048,-5.91664686417118,
-0.000153939560766411));
#28571=CARTESIAN_POINT('Origin',(-29.75,0.,0.));
#28572=CARTESIAN_POINT('',(-31.0198748077951,-5.91669010006987,0.000155330332996806));
#28573=CARTESIAN_POINT('',(-31.2716251922048,-5.91653587213954,0.000144386273298953));
#28574=CARTESIAN_POINT('',(-29.75,-5.91675,-7.2459289488551E-16));
#28575=CARTESIAN_POINT('Ctrl Pts',(-31.0198748077951,-5.91669010006987,
0.000155330332996806));
#28576=CARTESIAN_POINT('Ctrl Pts',(-31.0314757486877,-5.91694033579073,
0.246601513478828));
#28577=CARTESIAN_POINT('Ctrl Pts',(-31.0430766895802,-5.9018335866036,0.493017226461263));
#28578=CARTESIAN_POINT('Ctrl Pts',(-31.0546776304728,-5.87112738637305,
0.737473489267511));
#28579=CARTESIAN_POINT('Ctrl Pts',(-31.1010971785004,-5.74826080602,1.71563115225999));
#28580=CARTESIAN_POINT('Ctrl Pts',(-31.147516726528,-5.37563318085241,2.66241628028925));
#28581=CARTESIAN_POINT('Ctrl Pts',(-31.1939362745556,-4.79885939147213,
3.46192901072102));
#28582=CARTESIAN_POINT('Ctrl Pts',(-31.2403558225832,-4.22208560209187,
4.26144174115277));
#28583=CARTESIAN_POINT('Ctrl Pts',(-31.2867753706108,-3.44116564849892,
4.91368207398704));
#28584=CARTESIAN_POINT('Ctrl Pts',(-31.3331949186384,-2.5516951549488,5.33880658673855));
#28585=CARTESIAN_POINT('Ctrl Pts',(-31.3796144666661,-1.66222466139868,
5.76393109949005));
#28586=CARTESIAN_POINT('Ctrl Pts',(-31.4260340146937,-0.66420362789138,
5.9619397921588));
#28587=CARTESIAN_POINT('Ctrl Pts',(-31.4724535627213,0.320196084962679,
5.90859360605945));
#28588=CARTESIAN_POINT('Ctrl Pts',(-31.5188731107489,1.30459579781674,5.85524741996011));
#28589=CARTESIAN_POINT('Ctrl Pts',(-31.5652926587765,2.27537419001756,5.55054635509267));
#28590=CARTESIAN_POINT('Ctrl Pts',(-31.6117122068041,3.11369428475438,5.03179012236004));
#28591=CARTESIAN_POINT('Ctrl Pts',(-31.6581317548318,3.95201437949117,4.51303388962741));
#28592=CARTESIAN_POINT('Ctrl Pts',(-31.7045513028594,4.65787617676397,3.78022248902961));
#28593=CARTESIAN_POINT('Ctrl Pts',(-31.750970850887,5.14487223002471,2.92306237892945));
#28594=CARTESIAN_POINT('Ctrl Pts',(-31.7973903989146,5.63186828328546,2.06590226882927));
#28595=CARTESIAN_POINT('Ctrl Pts',(-31.8438099469422,5.89999859253413,1.08439344922673));
#28596=CARTESIAN_POINT('Ctrl Pts',(-31.8902294949698,5.9164402235167,0.0986864526962545));
#28597=CARTESIAN_POINT('Ctrl Pts',(-31.9366490429974,5.93288185449926,-0.887020543834223));
#28598=CARTESIAN_POINT('Ctrl Pts',(-31.983068591025,5.69763480721572,-1.87692571729264));
#28599=CARTESIAN_POINT('Ctrl Pts',(-32.0294881390526,5.23949664053988,-2.74985070288613));
#28600=CARTESIAN_POINT('Ctrl Pts',(-32.0759076870803,4.78135847386406,-3.62277568847961));
#28601=CARTESIAN_POINT('Ctrl Pts',(-32.1223272351079,4.10032918779596,-4.37872048620816));
#28602=CARTESIAN_POINT('Ctrl Pts',(-32.1687467831355,3.27977637902512,-4.92514678339447));
#28603=CARTESIAN_POINT('Ctrl Pts',(-32.2151663311631,2.45922357025426,-5.4715730805808));
#28604=CARTESIAN_POINT('Ctrl Pts',(-32.2615858791907,1.49914723878067,-5.80848087722487));
#28605=CARTESIAN_POINT('Ctrl Pts',(-32.3080054272183,0.517074278132762,
-5.8946279038872));
#28606=CARTESIAN_POINT('Ctrl Pts',(-32.3544249752459,-0.464998682515144,
-5.98077493054954));
#28607=CARTESIAN_POINT('Ctrl Pts',(-32.4008445232736,-1.46906827233735,
-5.81616118723014));
#28608=CARTESIAN_POINT('Ctrl Pts',(-32.4472640713012,-2.37222220206094,
-5.42093771947633));
#28609=CARTESIAN_POINT('Ctrl Pts',(-32.4936836193288,-3.27537613178452,
-5.02571425172252));
#28610=CARTESIAN_POINT('Ctrl Pts',(-32.5401031673564,-4.07761440140948,
-4.39988105953429));
#28611=CARTESIAN_POINT('Ctrl Pts',(-32.586522715384,-4.68073172391043,-3.62004895867039));
#28612=CARTESIAN_POINT('Ctrl Pts',(-32.6329422634116,-5.28384904641137,
-2.8402168578065));
#28613=CARTESIAN_POINT('Ctrl Pts',(-32.6793618114392,-5.6878454217883,-1.90638584826694));
#28614=CARTESIAN_POINT('Ctrl Pts',(-32.7257813594668,-5.84326599167394,
-0.932870025747903));
#28615=CARTESIAN_POINT('Ctrl Pts',(-32.7404791755762,-5.89247678869508,
-0.624625823747457));
#28616=CARTESIAN_POINT('Ctrl Pts',(-32.7551769916857,-5.91676674673342,
-0.312403041320129));
#28617=CARTESIAN_POINT('Ctrl Pts',(-32.7698748077951,-5.91649785403418,
-0.000138834737503368));
#28618=CARTESIAN_POINT('Ctrl Pts',(-33.0216251922048,-5.91664686417118,
-0.000153939560766411));
#28619=CARTESIAN_POINT('Ctrl Pts',(-33.0093664548626,-5.9169056008419,-0.260579579419119));
#28620=CARTESIAN_POINT('Ctrl Pts',(-32.9971077175203,-5.90003159228609,
-0.52097193872601));
#28621=CARTESIAN_POINT('Ctrl Pts',(-32.984848980178,-5.86575487809614,-0.779052979208239));
#28622=CARTESIAN_POINT('Ctrl Pts',(-32.9384294321504,-5.7359609575523,-1.75631555684574));
#28623=CARTESIAN_POINT('Ctrl Pts',(-32.8920098841228,-5.35663454170278,
-2.70043678474785));
#28624=CARTESIAN_POINT('Ctrl Pts',(-32.8455903360952,-4.77421053767591,
-3.49584289925422));
#28625=CARTESIAN_POINT('Ctrl Pts',(-32.7991707880676,-4.19178653364904,
-4.29124901376059));
#28626=CARTESIAN_POINT('Ctrl Pts',(-32.75275124004,-3.40626494144485,-4.93794001487121));
#28627=CARTESIAN_POINT('Ctrl Pts',(-32.7063316920124,-2.51380469083249,
-5.35675179662735));
#28628=CARTESIAN_POINT('Ctrl Pts',(-32.6599121439847,-1.62134444022013,
-5.77556357838349));
#28629=CARTESIAN_POINT('Ctrl Pts',(-32.6134925959571,-0.621945531199624,
-5.9664961407851));
#28630=CARTESIAN_POINT('Ctrl Pts',(-32.5670730479295,0.362051504208375,
-5.90617664336433));
#28631=CARTESIAN_POINT('Ctrl Pts',(-32.5206534999019,1.34604853961635,-5.84585714594356));
#28632=CARTESIAN_POINT('Ctrl Pts',(-32.4742339518743,2.31464370141184,-5.53428558870041));
#28633=CARTESIAN_POINT('Ctrl Pts',(-32.4278144038467,3.14926727099989,-5.009602727775));
#28634=CARTESIAN_POINT('Ctrl Pts',(-32.3813948558191,3.98389084058799,-4.48491986684956));
#28635=CARTESIAN_POINT('Ctrl Pts',(-32.3349753077914,4.68454281796865,-3.7471257022418));
#28636=CARTESIAN_POINT('Ctrl Pts',(-32.2885557597638,5.16545351208018,-2.88653665295634));
#28637=CARTESIAN_POINT('Ctrl Pts',(-32.2421362117362,5.64636420619168,-2.02594760367094));
#28638=CARTESIAN_POINT('Ctrl Pts',(-32.1957166637086,5.9075336170341,-1.04256366970781));
#28639=CARTESIAN_POINT('Ctrl Pts',(-32.149297115681,5.91699092256471,-0.0567649241045975));
#28640=CARTESIAN_POINT('Ctrl Pts',(-32.1028775676534,5.92644822809533,0.929033821498671));
#28641=CARTESIAN_POINT('Ctrl Pts',(-32.0564580196258,5.68419342831414,1.91724737874199));
#28642=CARTESIAN_POINT('Ctrl Pts',(-32.0100384715982,5.21988192990835,2.78690446053288));
#28643=CARTESIAN_POINT('Ctrl Pts',(-31.9636189235706,4.75557043150258,3.65656154232375));
#28644=CARTESIAN_POINT('Ctrl Pts',(-31.9171993755429,4.06920223447221,4.40766214866215));
#28645=CARTESIAN_POINT('Ctrl Pts',(-31.8707798275153,3.24479849356221,4.94826096426798));
#28646=CARTESIAN_POINT('Ctrl Pts',(-31.8243602794877,2.42039475265223,5.48885977987379));
#28647=CARTESIAN_POINT('Ctrl Pts',(-31.7779407314601,1.4579554678626,5.81895680474706));
#28648=CARTESIAN_POINT('Ctrl Pts',(-31.7315211834325,0.475296791558483,
5.89814350404057));
#28649=CARTESIAN_POINT('Ctrl Pts',(-31.6851016354049,-0.507361884745695,
5.97733020333409));
#28650=CARTESIAN_POINT('Ctrl Pts',(-31.6386820873773,-1.51023995256432,
5.80560657704785));
#28651=CARTESIAN_POINT('Ctrl Pts',(-31.5922625393497,-2.41057098173501,
5.40399402075344));
#28652=CARTESIAN_POINT('Ctrl Pts',(-31.5458429913221,-3.31090201090567,
5.00238146445905));
#28653=CARTESIAN_POINT('Ctrl Pts',(-31.4994234432944,-4.10868600142836,
4.3708799781565));
#28654=CARTESIAN_POINT('Ctrl Pts',(-31.4530038952668,-4.70626293290763,
3.5867942568067));
#28655=CARTESIAN_POINT('Ctrl Pts',(-31.4065843472392,-5.30383986438691,
2.80270853545689));
#28656=CARTESIAN_POINT('Ctrl Pts',(-31.3601647992116,-5.7012097368228,1.86603857905981));
#28657=CARTESIAN_POINT('Ctrl Pts',(-31.313745251184,-5.84972886933474,0.891446010476035));
#28658=CARTESIAN_POINT('Ctrl Pts',(-31.2997052315243,-5.89464984829539,
0.596671515580249));
#28659=CARTESIAN_POINT('Ctrl Pts',(-31.2856652118645,-5.91680557048392,
0.298427800523953));
#28660=CARTESIAN_POINT('Ctrl Pts',(-31.2716251922048,-5.91653587213954,
0.000144386273298953));
#28661=CARTESIAN_POINT('Origin',(-29.75,0.,0.));
#28662=CARTESIAN_POINT('',(-29.2698748077951,-5.91689808548129,-0.00014569106262019));
#28663=CARTESIAN_POINT('',(-29.5216251922048,-5.91705311546107,-0.000119369217152434));
#28664=CARTESIAN_POINT('',(-29.75,-5.91675,-7.2459289488551E-16));
#28665=CARTESIAN_POINT('Ctrl Pts',(-29.2698748077951,-5.91689808548129,
-0.00014569106262019));
#28666=CARTESIAN_POINT('Ctrl Pts',(-29.3077745056896,-5.91607341121319,
0.804900279929208));
#28667=CARTESIAN_POINT('Ctrl Pts',(-29.3456742035842,-5.7505552877361,1.61027491020334));
#28668=CARTESIAN_POINT('Ctrl Pts',(-29.3835739014787,-5.43102511781527,
2.34903599462667));
#28669=CARTESIAN_POINT('Ctrl Pts',(-29.4299934495063,-5.03966458216716,
3.25387053274719));
#28670=CARTESIAN_POINT('Ctrl Pts',(-29.4764129975339,-4.41726519851383,
4.05877576500959));
#28671=CARTESIAN_POINT('Ctrl Pts',(-29.5228325455616,-3.64001743598446,
4.66521993052002));
#28672=CARTESIAN_POINT('Ctrl Pts',(-29.5692520935892,-2.86276967345511,
5.27166409603043));
#28673=CARTESIAN_POINT('Ctrl Pts',(-29.6156716416168,-1.93067353204981,
5.67964719478885));
#28674=CARTESIAN_POINT('Ctrl Pts',(-29.6620911896444,-0.957830735118941,
5.83922633721742));
#28675=CARTESIAN_POINT('Ctrl Pts',(-29.708510737672,0.0150120618118707,
5.99880547964598));
#28676=CARTESIAN_POINT('Ctrl Pts',(-29.7549302856996,1.02860151426824,5.90998066574465));
#28677=CARTESIAN_POINT('Ctrl Pts',(-29.8013498337272,1.95885996742694,5.58362530641197));
#28678=CARTESIAN_POINT('Ctrl Pts',(-29.8477693817548,2.88911842058573,5.25726994707927));
#28679=CARTESIAN_POINT('Ctrl Pts',(-29.8941889297825,3.73604587444693,4.69338404231518));
#28680=CARTESIAN_POINT('Ctrl Pts',(-29.9406084778101,4.39596645508967,3.96099518557123));
#28681=CARTESIAN_POINT('Ctrl Pts',(-29.9870280258377,5.05588703573237,3.22860632882733));
#28682=CARTESIAN_POINT('Ctrl Pts',(-30.0334475738653,5.52880074315668,2.3277145201035));
#28683=CARTESIAN_POINT('Ctrl Pts',(-30.0798671218929,5.75681626485063,1.36860163201104));
#28684=CARTESIAN_POINT('Ctrl Pts',(-30.1262866699205,5.9848317865446,0.409488743918518));
#28685=CARTESIAN_POINT('Ctrl Pts',(-30.1727062179481,5.96794912250825,-0.607845223542657));
#28686=CARTESIAN_POINT('Ctrl Pts',(-30.2191257659758,5.70823494910223,-1.55886423406273));
#28687=CARTESIAN_POINT('Ctrl Pts',(-30.2655453140034,5.44852077569622,-2.50988324458275));
#28688=CARTESIAN_POINT('Ctrl Pts',(-30.311964862031,4.94597509292055,-3.3945872981616));
#28689=CARTESIAN_POINT('Ctrl Pts',(-30.3583844100586,4.26211658529701,-4.10467613189253));
#28690=CARTESIAN_POINT('Ctrl Pts',(-30.4048039580862,3.57825807767347,-4.81476496562346));
#28691=CARTESIAN_POINT('Ctrl Pts',(-30.4512235061138,2.71308674520206,-5.35023857950647));
#28692=CARTESIAN_POINT('Ctrl Pts',(-30.4976430541414,1.77251177004035,-5.64554744550611));
#28693=CARTESIAN_POINT('Ctrl Pts',(-30.544062602169,0.83193679487858,-5.94085631150576));
#28694=CARTESIAN_POINT('Ctrl Pts',(-30.5904821501966,-0.184041822973492,
-5.996000429622));
#28695=CARTESIAN_POINT('Ctrl Pts',(-30.6369016982243,-1.15105396112758,
-5.8042293814911));
#28696=CARTESIAN_POINT('Ctrl Pts',(-30.6833212462519,-2.11806609928161,
-5.61245833336021));
#28697=CARTESIAN_POINT('Ctrl Pts',(-30.7297407942795,-3.03611175773765,
-5.17377211898222));
#28698=CARTESIAN_POINT('Ctrl Pts',(-30.7761603423071,-3.79280919056725,
-4.54187212263189));
#28699=CARTESIAN_POINT('Ctrl Pts',(-30.8225798903347,-4.54950662339687,
-3.90997212628154));
#28700=CARTESIAN_POINT('Ctrl Pts',(-30.8689994383623,-5.14485583060003,
-3.08485834795886));
#28701=CARTESIAN_POINT('Ctrl Pts',(-30.9154189863899,-5.50597766643234,
-2.16753635981969));
#28702=CARTESIAN_POINT('Ctrl Pts',(-30.950237593525,-5.77684974218483,-1.4794668873992));
#28703=CARTESIAN_POINT('Ctrl Pts',(-30.9850562006601,-5.91593905243186,
-0.739518538394789));
#28704=CARTESIAN_POINT('Ctrl Pts',(-31.0198748077951,-5.91669010006987,
0.000155330332996806));
#28705=CARTESIAN_POINT('Ctrl Pts',(-31.2716251922048,-5.91653587213954,
0.000144386273298953));
#28706=CARTESIAN_POINT('Ctrl Pts',(-31.2392456638369,-5.91591388546114,
-0.687766065954424));
#28707=CARTESIAN_POINT('Ctrl Pts',(-31.206866135469,-5.79601778419154,-1.37588766634103));
#28708=CARTESIAN_POINT('Ctrl Pts',(-31.1744866071011,-5.56101605193026,
-2.02215338302906));
#28709=CARTESIAN_POINT('Ctrl Pts',(-31.1280670590735,-5.22411570942588,
-2.94864502717984));
#28710=CARTESIAN_POINT('Ctrl Pts',(-31.0816475110459,-4.65064663182914,
-3.78911313471092));
#28711=CARTESIAN_POINT('Ctrl Pts',(-31.0352279630183,-3.91080952820358,
-4.44067254685975));
#28712=CARTESIAN_POINT('Ctrl Pts',(-30.9888084149907,-3.170972424578,-5.0922319590086));
#28713=CARTESIAN_POINT('Ctrl Pts',(-30.9423888669631,-2.26476729492359,
-5.55488267577518));
#28714=CARTESIAN_POINT('Ctrl Pts',(-30.8959693189355,-1.30312643732579,
-5.77198971955638));
#28715=CARTESIAN_POINT('Ctrl Pts',(-30.8495497709079,-0.341485579728019,
-5.98909676333757));
#28716=CARTESIAN_POINT('Ctrl Pts',(-30.8031302228802,0.675591005813218,
-5.96066013413337));
#28717=CARTESIAN_POINT('Ctrl Pts',(-30.7567106748526,1.62359879016756,-5.69016087671414));
#28718=CARTESIAN_POINT('Ctrl Pts',(-30.710291126825,2.57160657452198,-5.41966161929489));
#28719=CARTESIAN_POINT('Ctrl Pts',(-30.6638715787974,3.45054555768951,-4.90709973366061));
#28720=CARTESIAN_POINT('Ctrl Pts',(-30.6174520307698,4.15282120275032,-4.21522002893198));
#28721=CARTESIAN_POINT('Ctrl Pts',(-30.5710324827422,4.85509684781106,-3.5233403242034));
#28722=CARTESIAN_POINT('Ctrl Pts',(-30.5246129347146,5.38070915476503,-2.65214280038055));
#28723=CARTESIAN_POINT('Ctrl Pts',(-30.4781933866869,5.66531575872777,-1.70827433049633));
#28724=CARTESIAN_POINT('Ctrl Pts',(-30.4317738386593,5.9499223626905,-0.764405860612103));
#28725=CARTESIAN_POINT('Ctrl Pts',(-30.3853542906317,5.99352326366199,0.25213355533349));
#28726=CARTESIAN_POINT('Ctrl Pts',(-30.3389347426041,5.79078109597846,1.2169051453504));
#28727=CARTESIAN_POINT('Ctrl Pts',(-30.2925151945765,5.58803892829493,2.18167673536735));
#28728=CARTESIAN_POINT('Ctrl Pts',(-30.2460956465489,5.13895369195636,3.09468049945561));
#28729=CARTESIAN_POINT('Ctrl Pts',(-30.1996760985213,4.49849975829773,3.84415189071883));
#28730=CARTESIAN_POINT('Ctrl Pts',(-30.1532565504937,3.8580458246391,4.59362328198205));
#28731=CARTESIAN_POINT('Ctrl Pts',(-30.1068370024661,3.02622319366041,5.17956230042023));
#28732=CARTESIAN_POINT('Ctrl Pts',(-30.0604174544384,2.10485869577162,5.53024174020959));
#28733=CARTESIAN_POINT('Ctrl Pts',(-30.0139979064108,1.18349419788286,5.88092117999895));
#28734=CARTESIAN_POINT('Ctrl Pts',(-29.9675783583832,0.172587833084095,
5.9963410411395));
#28735=CARTESIAN_POINT('Ctrl Pts',(-29.9211588103556,-0.804111191600269,
5.86237230358709));
#28736=CARTESIAN_POINT('Ctrl Pts',(-29.874739262328,-1.78081021628463,5.72840356603468));
#28737=CARTESIAN_POINT('Ctrl Pts',(-29.8283197143004,-2.7233019008546,5.34504622978926));
#28738=CARTESIAN_POINT('Ctrl Pts',(-29.7819001662728,-3.51621196075299,
4.75922864352822));
#28739=CARTESIAN_POINT('Ctrl Pts',(-29.7354806182452,-4.30912202065143,
4.17341105726715));
#28740=CARTESIAN_POINT('Ctrl Pts',(-29.6890610702175,-4.95245045587837,
3.38513322099041));
#28741=CARTESIAN_POINT('Ctrl Pts',(-29.6426415221899,-5.36744478599853,
2.49089146764347));
#28742=CARTESIAN_POINT('Ctrl Pts',(-29.6023027455282,-5.72807655235332,
1.71379173482464));
#28743=CARTESIAN_POINT('Ctrl Pts',(-29.5619639688665,-5.91627768814128,
0.856671432896323));
#28744=CARTESIAN_POINT('Ctrl Pts',(-29.5216251922048,-5.91705311546107,
-0.000119369217152434));
#28745=CARTESIAN_POINT('Origin',(-29.75,0.,0.));
#28746=CARTESIAN_POINT('',(-27.5198748077951,-5.91634884690258,0.000100288842562468));
#28747=CARTESIAN_POINT('',(-27.7716251922048,-5.91627280920936,5.84495287493138E-5));
#28748=CARTESIAN_POINT('',(-29.75,-5.91675,-7.2459289488551E-16));
#28749=CARTESIAN_POINT('Ctrl Pts',(-27.5198748077951,-5.91634884690258,
0.000100288842562468));
#28750=CARTESIAN_POINT('Ctrl Pts',(-27.537653714664,-5.91657582580226,0.377851435059495));
#28751=CARTESIAN_POINT('Ctrl Pts',(-27.5554326215329,-5.88096092710108,
0.755560324906384));
#28752=CARTESIAN_POINT('Ctrl Pts',(-27.5732115284019,-5.80909502975842,
1.12624103531533));
#28753=CARTESIAN_POINT('Ctrl Pts',(-27.6196310764295,-5.62145793272878,
2.09406381354322));
#28754=CARTESIAN_POINT('Ctrl Pts',(-27.6660506244571,-5.18669868205167,
3.01397566782382));
#28755=CARTESIAN_POINT('Ctrl Pts',(-27.7124701724847,-4.55803794621954,
3.77336640352018));
#28756=CARTESIAN_POINT('Ctrl Pts',(-27.7588897205123,-3.92937721038742,
4.53275713921654));
#28757=CARTESIAN_POINT('Ctrl Pts',(-27.8053092685399,-3.10681498940029,
5.13162675632866));
#28758=CARTESIAN_POINT('Ctrl Pts',(-27.8517288165675,-2.19104450878334,
5.49666516125209));
#28759=CARTESIAN_POINT('Ctrl Pts',(-27.8981483645951,-1.27527402816635,
5.86170356617553));
#28760=CARTESIAN_POINT('Ctrl Pts',(-27.9445679126228,-0.266295287919555,
5.99291075891027));
#28761=CARTESIAN_POINT('Ctrl Pts',(-27.9909874606504,0.712378473384235,
5.87422512720195));
#28762=CARTESIAN_POINT('Ctrl Pts',(-28.037407008678,1.69105223468803,5.75553949549364));
#28763=CARTESIAN_POINT('Ctrl Pts',(-28.0838265567056,2.63942101704879,5.38696103934229));
#28764=CARTESIAN_POINT('Ctrl Pts',(-28.1302461047332,3.44139109619033,4.813608963912));
#28765=CARTESIAN_POINT('Ctrl Pts',(-28.1766656527608,4.24336117533185,4.24025688848174));
#28766=CARTESIAN_POINT('Ctrl Pts',(-28.2230852007884,4.89893255125415,3.46213119377257));
#28767=CARTESIAN_POINT('Ctrl Pts',(-28.269504748816,5.32785403478351,2.57448544731431));
#28768=CARTESIAN_POINT('Ctrl Pts',(-28.3159242968437,5.75677551831288,1.68683970085604));
#28769=CARTESIAN_POINT('Ctrl Pts',(-28.3623438448712,5.9590471094493,0.689673902648605));
#28770=CARTESIAN_POINT('Ctrl Pts',(-28.4087633928988,5.90990791056824,-0.294944779568952));
#28771=CARTESIAN_POINT('Ctrl Pts',(-28.4551829409265,5.86076871168719,-1.27956346178651));
#28772=CARTESIAN_POINT('Ctrl Pts',(-28.5016024889541,5.56021872278872,-2.25163502801417));
#28773=CARTESIAN_POINT('Ctrl Pts',(-28.5480220369817,5.04504950448862,-3.09216419868856));
#28774=CARTESIAN_POINT('Ctrl Pts',(-28.5944415850093,4.52988028618852,-3.93269336936294));
#28775=CARTESIAN_POINT('Ctrl Pts',(-28.6408611330369,3.80009183848674,-4.641680144484));
#28776=CARTESIAN_POINT('Ctrl Pts',(-28.6872806810645,2.94502056764569,-5.13233453610888));
#28777=CARTESIAN_POINT('Ctrl Pts',(-28.7337002290922,2.08994929680464,-5.62298892773375));
#28778=CARTESIAN_POINT('Ctrl Pts',(-28.7801197771198,1.10959520282435,-5.89531093586248));
#28779=CARTESIAN_POINT('Ctrl Pts',(-28.8265393251474,0.123967463565065,
-5.91596450313635));
#28780=CARTESIAN_POINT('Ctrl Pts',(-28.872958873175,-0.861660275694191,
-5.93661807041022));
#28781=CARTESIAN_POINT('Ctrl Pts',(-28.9193784212026,-1.85256166023243,
-5.70560319682918));
#28782=CARTESIAN_POINT('Ctrl Pts',(-28.9657979692302,-2.72743637495993,
-5.25119936347283));
#28783=CARTESIAN_POINT('Ctrl Pts',(-29.0122175172578,-3.60231108968744,
-4.79679553011648));
#28784=CARTESIAN_POINT('Ctrl Pts',(-29.0586370652854,-4.36115913460428,
-4.1190027369848));
#28785=CARTESIAN_POINT('Ctrl Pts',(-29.105056613313,-4.9110867986007,-3.30079238835192));
#28786=CARTESIAN_POINT('Ctrl Pts',(-29.1514761613407,-5.46101446259712,
-2.48258203971906));
#28787=CARTESIAN_POINT('Ctrl Pts',(-29.1978957093683,-5.80202174567313,
-1.52395413558503));
#28788=CARTESIAN_POINT('Ctrl Pts',(-29.2443152573959,-5.89236454338969,
-0.54225826152871));
#28789=CARTESIAN_POINT('Ctrl Pts',(-29.2528351075289,-5.90894607272058,
-0.362077667822123));
#28790=CARTESIAN_POINT('Ctrl Pts',(-29.261354957662,-5.91708347221425,-0.181119983843553));
#28791=CARTESIAN_POINT('Ctrl Pts',(-29.2698748077951,-5.91689808548129,
-0.00014569106262019));
#28792=CARTESIAN_POINT('Ctrl Pts',(-29.5216251922048,-5.91705311546107,
-0.000119369217152434));
#28793=CARTESIAN_POINT('Ctrl Pts',(-29.5155444208389,-5.91717000537774,
-0.129274227327039));
#28794=CARTESIAN_POINT('Ctrl Pts',(-29.509463649473,-5.91302795979075,-0.258421598105164));
#28795=CARTESIAN_POINT('Ctrl Pts',(-29.5033828781071,-5.90457561496714,
-0.38728625260564));
#28796=CARTESIAN_POINT('Ctrl Pts',(-29.4569633300795,-5.84005188880219,
-1.37101654909073));
#28797=CARTESIAN_POINT('Ctrl Pts',(-29.4105437820519,-5.52434421145891,
-2.33827147164377));
#28798=CARTESIAN_POINT('Ctrl Pts',(-29.3641242340242,-4.99609965855499,
-3.17064536586931));
#28799=CARTESIAN_POINT('Ctrl Pts',(-29.3177046859966,-4.46785510565111,
-4.0030192600948));
#28800=CARTESIAN_POINT('Ctrl Pts',(-29.271285137969,-3.72707367718662,-4.70051212599278));
#28801=CARTESIAN_POINT('Ctrl Pts',(-29.2248655899414,-2.86443747542453,
-5.17774099233492));
#28802=CARTESIAN_POINT('Ctrl Pts',(-29.1784460419138,-2.00180127366234,
-5.65496985867711));
#28803=CARTESIAN_POINT('Ctrl Pts',(-29.1320264938862,-1.01731029860253,
-5.91193472546341));
#28804=CARTESIAN_POINT('Ctrl Pts',(-29.0856069458586,-0.0314801407377438,
-5.91717946618666));
#28805=CARTESIAN_POINT('Ctrl Pts',(-29.0391873978309,0.954350017126954,
-5.92242420690991));
#28806=CARTESIAN_POINT('Ctrl Pts',(-28.9927678498033,1.9415193577966,-5.67594882157016));
#28807=CARTESIAN_POINT('Ctrl Pts',(-28.9463483017757,2.80918442102537,-5.20792537609653));
#28808=CARTESIAN_POINT('Ctrl Pts',(-28.8999287537481,3.67684948425417,-4.73990193062289));
#28809=CARTESIAN_POINT('Ctrl Pts',(-28.8535092057205,4.42501027004205,-4.05033042501536));
#28810=CARTESIAN_POINT('Ctrl Pts',(-28.8070896576929,4.9620813386371,-3.22362414420033));
#28811=CARTESIAN_POINT('Ctrl Pts',(-28.7606701096653,5.49915240723215,-2.3969178633853));
#28812=CARTESIAN_POINT('Ctrl Pts',(-28.7142505616377,5.82513375863435,-1.43307680736279));
#28813=CARTESIAN_POINT('Ctrl Pts',(-28.6678310136101,5.90012067451813,-0.450088725081483));
#28814=CARTESIAN_POINT('Ctrl Pts',(-28.6214114655824,5.97510759040192,0.532899357199769));
#28815=CARTESIAN_POINT('Ctrl Pts',(-28.5749919175548,5.7991000707673,1.53503446573988));
#28816=CARTESIAN_POINT('Ctrl Pts',(-28.5285723695272,5.39364392019479,2.43364111907807));
#28817=CARTESIAN_POINT('Ctrl Pts',(-28.4821528214996,4.98818776962226,3.33224777241634));
#28818=CARTESIAN_POINT('Ctrl Pts',(-28.435733273472,4.35328298811181,4.12732597055274));
#28819=CARTESIAN_POINT('Ctrl Pts',(-28.3893137254444,3.56665088199201,4.72154692026962));
#28820=CARTESIAN_POINT('Ctrl Pts',(-28.3428941774168,2.78001877587223,5.31576786998648));
#28821=CARTESIAN_POINT('Ctrl Pts',(-28.2964746293892,1.84165934514321,5.7091315712838));
#28822=CARTESIAN_POINT('Ctrl Pts',(-28.2500550813615,0.866441028168872,
5.8534847551717));
#28823=CARTESIAN_POINT('Ctrl Pts',(-28.2036355333339,-0.10877728880544,
5.99783793905961));
#28824=CARTESIAN_POINT('Ctrl Pts',(-28.1572159853063,-1.12085449202507,
5.89318060553806));
#28825=CARTESIAN_POINT('Ctrl Pts',(-28.1107964372787,-2.04589804731732,
5.55232428936793));
#28826=CARTESIAN_POINT('Ctrl Pts',(-28.0643768892511,-2.97094160260959,
5.21146797319779));
#28827=CARTESIAN_POINT('Ctrl Pts',(-28.0179573412235,-3.80895150997454,
4.63441267437906));
#28828=CARTESIAN_POINT('Ctrl Pts',(-27.9715377931959,-4.45734352904509,
3.89179810606892));
#28829=CARTESIAN_POINT('Ctrl Pts',(-27.9251182451682,-5.10573554811564,
3.14918353775878));
#28830=CARTESIAN_POINT('Ctrl Pts',(-27.8786986971406,-5.56450967889178,
2.24100969995723));
#28831=CARTESIAN_POINT('Ctrl Pts',(-27.832279149113,-5.77750549260991,1.27844988841335));
#28832=CARTESIAN_POINT('Ctrl Pts',(-27.812061163477,-5.87027559669915,0.859207968348168));
#28833=CARTESIAN_POINT('Ctrl Pts',(-27.7918431778409,-5.91642084319709,
0.429648871767775));
#28834=CARTESIAN_POINT('Ctrl Pts',(-27.7716251922048,-5.91627280920936,
5.84495287493138E-5));
#28835=CARTESIAN_POINT('Origin',(-29.75,0.,0.));
#28836=CARTESIAN_POINT('',(-25.7698748077951,-5.91722620641212,-5.21401381919917E-5));
#28837=CARTESIAN_POINT('',(-26.0216251922048,-5.91726316729143,2.21583349696063E-6));
#28838=CARTESIAN_POINT('',(-29.75,-5.91675,-7.2459289488551E-16));
#28839=CARTESIAN_POINT('Ctrl Pts',(-25.7698748077951,-5.91722620641212,
-5.21401381919917E-5));
#28840=CARTESIAN_POINT('Ctrl Pts',(-25.813952471666,-5.91679392379654,0.936072799262249));
#28841=CARTESIAN_POINT('Ctrl Pts',(-25.8580301355369,-5.69073137008731,
1.8723991018519));
#28842=CARTESIAN_POINT('Ctrl Pts',(-25.9021077994078,-5.26280619948913,
2.70497224403705));
#28843=CARTESIAN_POINT('Ctrl Pts',(-25.9485273474354,-4.81214499686768,
3.58178071268355));
#28844=CARTESIAN_POINT('Ctrl Pts',(-25.994946895463,-4.13760107317096,4.34351814822099));
#28845=CARTESIAN_POINT('Ctrl Pts',(-26.0413664434906,-3.3217481251996,4.89693713734667));
#28846=CARTESIAN_POINT('Ctrl Pts',(-26.0877859915183,-2.50589517722821,
5.45035612647238));
#28847=CARTESIAN_POINT('Ctrl Pts',(-26.1342055395458,-1.54873320498214,
5.79545666918634));
#28848=CARTESIAN_POINT('Ctrl Pts',(-26.1806250875735,-0.56743234328704,
5.88999358829735));
#28849=CARTESIAN_POINT('Ctrl Pts',(-26.2270446356011,0.413868518408088,
5.98453050740837));
#28850=CARTESIAN_POINT('Ctrl Pts',(-26.2734641836287,1.4193082695522,5.82850380291644));
#28851=CARTESIAN_POINT('Ctrl Pts',(-26.3198837316563,2.32580689378816,5.44101334561858));
#28852=CARTESIAN_POINT('Ctrl Pts',(-26.3663032796839,3.23230551802405,5.05352288832076));
#28853=CARTESIAN_POINT('Ctrl Pts',(-26.4127228277115,4.03986301535175,4.43456867821703));
#28854=CARTESIAN_POINT('Ctrl Pts',(-26.4591423757391,4.64962295019926,3.65991944656879));
#28855=CARTESIAN_POINT('Ctrl Pts',(-26.5055619237667,5.25938288504676,2.88527021492055));
#28856=CARTESIAN_POINT('Ctrl Pts',(-26.5519814717944,5.67134525741409,1.95492596172779));
#28857=CARTESIAN_POINT('Ctrl Pts',(-26.598401019822,5.83508005846991,0.982773954497618));
#28858=CARTESIAN_POINT('Ctrl Pts',(-26.6448205678496,5.99881485952574,0.0106219472674482));
#28859=CARTESIAN_POINT('Ctrl Pts',(-26.6912401158772,5.91432208927007,-1.00333781400015));
#28860=CARTESIAN_POINT('Ctrl Pts',(-26.7376596639048,5.59194485531658,-1.93498234345703));
#28861=CARTESIAN_POINT('Ctrl Pts',(-26.7840792119324,5.26956762136309,-2.86662687291391));
#28862=CARTESIAN_POINT('Ctrl Pts',(-26.83049875996,4.70930592371177,-3.7159561705601));
#28863=CARTESIAN_POINT('Ctrl Pts',(-26.8769183079876,3.97974370171135,-4.37900034289573));
#28864=CARTESIAN_POINT('Ctrl Pts',(-26.9233378560153,3.25018147971088,-5.0420445152314));
#28865=CARTESIAN_POINT('Ctrl Pts',(-26.9697574040429,2.35131873336127,-5.5188035622565));
#28866=CARTESIAN_POINT('Ctrl Pts',(-27.0161769520705,1.3931889494008,-5.75091544761872));
#28867=CARTESIAN_POINT('Ctrl Pts',(-27.0625965000981,0.435059165440296,
-5.98302733298095));
#28868=CARTESIAN_POINT('Ctrl Pts',(-27.1090160481257,-0.582337656131013,
-5.9704920566803));
#28869=CARTESIAN_POINT('Ctrl Pts',(-27.1554355961533,-1.53445778477314,
-5.71484411345937));
#28870=CARTESIAN_POINT('Ctrl Pts',(-27.2018551441809,-2.4865779134152,-5.45919617023846));
#28871=CARTESIAN_POINT('Ctrl Pts',(-27.2482746922086,-3.37342134912802,
-4.9604355600973));
#28872=CARTESIAN_POINT('Ctrl Pts',(-27.2946942402362,-4.08642593843634,
-4.27961762124454));
#28873=CARTESIAN_POINT('Ctrl Pts',(-27.3411137882638,-4.79943052774466,
-3.59879968239178));
#28874=CARTESIAN_POINT('Ctrl Pts',(-27.3875333362914,-5.33859627064848,
-2.73592441482741));
#28875=CARTESIAN_POINT('Ctrl Pts',(-27.433952884319,-5.63792167040933,-1.79661992995765));
#28876=CARTESIAN_POINT('Ctrl Pts',(-27.4625935254777,-5.82260402360958,
-1.21707351399728));
#28877=CARTESIAN_POINT('Ctrl Pts',(-27.4912341666364,-5.91598319893197,
-0.608431782664779));
#28878=CARTESIAN_POINT('Ctrl Pts',(-27.5198748077951,-5.91634884690258,
0.000100288842562468));
#28879=CARTESIAN_POINT('Ctrl Pts',(-27.7716251922048,-5.91627280920936,
5.84495287493138E-5));
#28880=CARTESIAN_POINT('Ctrl Pts',(-27.7454236298133,-5.91608096409504,
-0.556670616052406));
#28881=CARTESIAN_POINT('Ctrl Pts',(-27.7192220674217,-5.83813980461213,
-1.11345229290792));
#28882=CARTESIAN_POINT('Ctrl Pts',(-27.6930205050302,-5.68317102369272,
-1.64789895011231));
#28883=CARTESIAN_POINT('Ctrl Pts',(-27.6466009570026,-5.40862324439725,
-2.59474219180798));
#28884=CARTESIAN_POINT('Ctrl Pts',(-27.600181408975,-4.89231018914614,-3.47148288991311));
#28885=CARTESIAN_POINT('Ctrl Pts',(-27.5537618609474,-4.19743586316544,
-4.17079560862606));
#28886=CARTESIAN_POINT('Ctrl Pts',(-27.5073423129197,-3.50256153718475,
-4.87010832733899));
#28887=CARTESIAN_POINT('Ctrl Pts',(-27.4609227648921,-2.62912594047447,
-5.39199306665975));
#28888=CARTESIAN_POINT('Ctrl Pts',(-27.4145032168645,-1.68404991777717,
-5.67256376859322));
#28889=CARTESIAN_POINT('Ctrl Pts',(-27.3680836688369,-0.738973895079876,
-5.95313447052669));
#28890=CARTESIAN_POINT('Ctrl Pts',(-27.3216641208093,0.27774255360444,-5.99239113507287));
#28891=CARTESIAN_POINT('Ctrl Pts',(-27.2752445727817,1.24163898497985,-5.78552819242116));
#28892=CARTESIAN_POINT('Ctrl Pts',(-27.2288250247541,2.20553541635532,-5.57866524976944));
#28893=CARTESIAN_POINT('Ctrl Pts',(-27.1824054767265,3.11661183042188,-5.1256826999198));
#28894=CARTESIAN_POINT('Ctrl Pts',(-27.1359859286988,3.86333961512852,-4.48203200038782));
#28895=CARTESIAN_POINT('Ctrl Pts',(-27.0895663806712,4.61006739983517,-3.83838130085584));
#28896=CARTESIAN_POINT('Ctrl Pts',(-27.0431468326436,5.19244655518189,-3.00406245164152));
#28897=CARTESIAN_POINT('Ctrl Pts',(-26.996727284616,5.53918565283136,-2.0812078554986));
#28898=CARTESIAN_POINT('Ctrl Pts',(-26.9503077365884,5.88592475048081,-1.15835325935572));
#28899=CARTESIAN_POINT('Ctrl Pts',(-26.9038881885608,5.99702379043304,-0.14696291628425));
#28900=CARTESIAN_POINT('Ctrl Pts',(-26.8574686405332,5.85888268214156,0.829154720919783));
#28901=CARTESIAN_POINT('Ctrl Pts',(-26.8110490925056,5.72074157385008,1.80527235812382));
#28902=CARTESIAN_POINT('Ctrl Pts',(-26.7646295444779,5.3333603173149,2.74611728946041));
#28903=CARTESIAN_POINT('Ctrl Pts',(-26.7182099964503,4.74415984585059,3.53651681621066));
#28904=CARTESIAN_POINT('Ctrl Pts',(-26.6717904484227,4.15495937438626,4.32691634296093));
#28905=CARTESIAN_POINT('Ctrl Pts',(-26.6253709003951,3.3639396879928,4.96687046512485));
#28906=CARTESIAN_POINT('Ctrl Pts',(-26.5789513523675,2.46793276076853,5.37803976581127));
#28907=CARTESIAN_POINT('Ctrl Pts',(-26.5325318043399,1.57192583354425,5.78920906649768));
#28908=CARTESIAN_POINT('Ctrl Pts',(-26.4861122563123,0.570931665489247,
5.97159354570657));
#28909=CARTESIAN_POINT('Ctrl Pts',(-26.4396927082847,-0.412513929154647,
5.90286676900091));
#28910=CARTESIAN_POINT('Ctrl Pts',(-26.3932731602571,-1.39595952379854,
5.83413999229525));
#28911=CARTESIAN_POINT('Ctrl Pts',(-26.3468536122294,-2.36185654503133,
5.51430195967498));
#28912=CARTESIAN_POINT('Ctrl Pts',(-26.3004340642018,-3.19196556474444,
4.98250536053977));
#28913=CARTESIAN_POINT('Ctrl Pts',(-26.2540145161742,-4.02207458445755,
4.45070876140456));
#28914=CARTESIAN_POINT('Ctrl Pts',(-26.2075949681466,-4.71639560265107,
3.70695359575438));
#28915=CARTESIAN_POINT('Ctrl Pts',(-26.161175420119,-5.18993392702325,2.84228599325523));
#28916=CARTESIAN_POINT('Ctrl Pts',(-26.1146586774809,-5.66446375982073,
1.97580792438233));
#28917=CARTESIAN_POINT('Ctrl Pts',(-26.0681419348428,-5.91728509811654,
0.987910548273195));
#28918=CARTESIAN_POINT('Ctrl Pts',(-26.0216251922048,-5.91726313461423,
2.21569239827814E-6));
#28919=CARTESIAN_POINT('Origin',(-29.75,0.,0.));
#28920=CARTESIAN_POINT('',(-24.0198748077951,-5.91624086672945,-1.49279102093503E-5));
#28921=CARTESIAN_POINT('',(-24.2716251922048,-5.91627733888446,-6.20456869606399E-5));
#28922=CARTESIAN_POINT('',(-29.75,-5.91675,-7.2459289488551E-16));
#28923=CARTESIAN_POINT('Ctrl Pts',(-24.0198748077951,-5.91624086672945,
-1.49279102093503E-5));
#28924=CARTESIAN_POINT('Ctrl Pts',(-24.0438316806403,-5.91619635734186,
0.509026985967046));
#28925=CARTESIAN_POINT('Ctrl Pts',(-24.0677885534856,-5.85118645077979,
1.01808005821168));
#28926=CARTESIAN_POINT('Ctrl Pts',(-24.0917454263309,-5.72134892474527,
1.51002331627965));
#28927=CARTESIAN_POINT('Ctrl Pts',(-24.1381649743585,-5.46977187984169,
2.46322717732729));
#28928=CARTESIAN_POINT('Ctrl Pts',(-24.1845845223861,-4.97480544970528,
3.35219380141024));
#28929=CARTESIAN_POINT('Ctrl Pts',(-24.2310040704138,-4.29704051136091,
4.06810112682996));
#28930=CARTESIAN_POINT('Ctrl Pts',(-24.2774236184414,-3.61927557301662,
4.7840084522496));
#28931=CARTESIAN_POINT('Ctrl Pts',(-24.323843166469,-2.75871212646441,5.32685647900603));
#28932=CARTESIAN_POINT('Ctrl Pts',(-24.3702627144966,-1.82069528358946,
5.63019294684535));
#28933=CARTESIAN_POINT('Ctrl Pts',(-24.4166822625242,-0.882678440714442,
5.93352941468469));
#28934=CARTESIAN_POINT('Ctrl Pts',(-24.4631018105518,0.132791798483318,
5.99735432360688));
#28935=CARTESIAN_POINT('Ctrl Pts',(-24.5095213585794,1.10140754433813,5.8138546039325));
#28936=CARTESIAN_POINT('Ctrl Pts',(-24.555940906607,2.07002329019295,5.63035488425812));
#28937=CARTESIAN_POINT('Ctrl Pts',(-24.6023604546346,2.9917845427048,5.19953053598718));
#28938=CARTESIAN_POINT('Ctrl Pts',(-24.6487800026623,3.75385471479075,4.57412054002027));
#28939=CARTESIAN_POINT('Ctrl Pts',(-24.6951995506899,4.51592488687675,3.94871054405332));
#28940=CARTESIAN_POINT('Ctrl Pts',(-24.7416190987175,5.11830397853682,3.12871490039038));
#28941=CARTESIAN_POINT('Ctrl Pts',(-24.7880386467451,5.48725228694898,2.21451264926738));
#28942=CARTESIAN_POINT('Ctrl Pts',(-24.8344581947727,5.85620059536113,1.3003103981444));
#28943=CARTESIAN_POINT('Ctrl Pts',(-24.8808777428003,5.99171812052539,0.291901539561299));
#28944=CARTESIAN_POINT('Ctrl Pts',(-24.9272972908279,5.87721560466181,-0.68727044946791));
#28945=CARTESIAN_POINT('Ctrl Pts',(-24.9737168388556,5.76271308879823,-1.66644243849709));
#28946=CARTESIAN_POINT('Ctrl Pts',(-25.0201363868831,5.39819053190684,-2.61637755797244));
#28947=CARTESIAN_POINT('Ctrl Pts',(-25.0665559349108,4.82827063983722,-3.42079034184762));
#28948=CARTESIAN_POINT('Ctrl Pts',(-25.1129754829384,4.2583507477676,-4.22520312572279));
#28949=CARTESIAN_POINT('Ctrl Pts',(-25.159395030966,3.48303352051976,-4.88409357399777));
#28950=CARTESIAN_POINT('Ctrl Pts',(-25.2058145789936,2.59722872956742,-5.31680419619734));
#28951=CARTESIAN_POINT('Ctrl Pts',(-25.2522341270212,1.71142393861504,-5.74951481839694));
#28952=CARTESIAN_POINT('Ctrl Pts',(-25.2986536750488,0.715131583958168,
-5.95604561452111));
#28953=CARTESIAN_POINT('Ctrl Pts',(-25.3450732230764,-0.269688088482717,
-5.91111430014025));
#28954=CARTESIAN_POINT('Ctrl Pts',(-25.391492771104,-1.25450776092355,-5.8661829857594));
#28955=CARTESIAN_POINT('Ctrl Pts',(-25.4379123191317,-2.22785475114838,
-5.56978956087356));
#28956=CARTESIAN_POINT('Ctrl Pts',(-25.4843318671593,-3.07057764969502,
-5.05821676399751));
#28957=CARTESIAN_POINT('Ctrl Pts',(-25.5307514151869,-3.91330054824167,
-4.54664396712146));
#28958=CARTESIAN_POINT('Ctrl Pts',(-25.5771709632145,-4.62539935511013,
-3.8198917982552));
#28959=CARTESIAN_POINT('Ctrl Pts',(-25.6235905112421,-5.11970312574842,
-2.96692498027738));
#28960=CARTESIAN_POINT('Ctrl Pts',(-25.6700100592697,-5.61400689638677,
-2.11395816229946));
#28961=CARTESIAN_POINT('Ctrl Pts',(-25.7164296072974,-5.89051563079491,
-1.13477669520995));
#28962=CARTESIAN_POINT('Ctrl Pts',(-25.762849155325,-5.91538075722584,-0.149246210787353));
#28963=CARTESIAN_POINT('Ctrl Pts',(-25.7651910394817,-5.91663521247405,
-0.099525816567977));
#28964=CARTESIAN_POINT('Ctrl Pts',(-25.7675329236384,-5.91724917395894,
-0.0497892625659706));
#28965=CARTESIAN_POINT('Ctrl Pts',(-25.7698748077951,-5.91722620641212,
-5.21401381919917E-5));
#28966=CARTESIAN_POINT('Ctrl Pts',(-26.0216251922048,-5.91726313461423,
2.21569239827814E-6));
#28967=CARTESIAN_POINT('Ctrl Pts',(-25.9753028387876,-5.91724126289539,
-0.983777738154382));
#28968=CARTESIAN_POINT('Ctrl Pts',(-25.9289804853705,-5.66661285648345,
-1.96756842312595));
#28969=CARTESIAN_POINT('Ctrl Pts',(-25.8826581319533,-5.19587372555123,
-2.83141308580155));
#28970=CARTESIAN_POINT('Ctrl Pts',(-25.8362385839257,-4.72414687911932,
-3.69707028690149));
#28971=CARTESIAN_POINT('Ctrl Pts',(-25.7898190358981,-4.03138465651247,
-4.44227759072061));
#28972=CARTESIAN_POINT('Ctrl Pts',(-25.7433994878705,-3.20239093145171,
-4.9758111053855));
#28973=CARTESIAN_POINT('Ctrl Pts',(-25.6969799398429,-2.37339720639091,
-5.50934462005042));
#28974=CARTESIAN_POINT('Ctrl Pts',(-25.6505603918153,-1.40817197887618,
-5.8312043455611));
#28975=CARTESIAN_POINT('Ctrl Pts',(-25.6041408437876,-0.424872439983136,
-5.90199010877387));
#28976=CARTESIAN_POINT('Ctrl Pts',(-25.55772129576,0.55842709890991,-5.97277587198664));
#28977=CARTESIAN_POINT('Ctrl Pts',(-25.5113017477324,1.55980094918128,-5.79248767290151));
#28978=CARTESIAN_POINT('Ctrl Pts',(-25.4648821997048,2.45666681812683,-5.3831953316814));
#28979=CARTESIAN_POINT('Ctrl Pts',(-25.4184626516772,3.35353268707233,-4.97390299046132));
#28980=CARTESIAN_POINT('Ctrl Pts',(-25.3720431036496,4.14589057469203,-4.3356065071063));
#28981=CARTESIAN_POINT('Ctrl Pts',(-25.325623555622,4.73674469217009,-3.54644238012129));
#28982=CARTESIAN_POINT('Ctrl Pts',(-25.2792040075944,5.32759880964815,-2.75727825313629));
#28983=CARTESIAN_POINT('Ctrl Pts',(-25.2327844595667,5.71694915698457,-1.8172464825213));
#28984=CARTESIAN_POINT('Ctrl Pts',(-25.1863649115391,5.85713375635887,-0.841420224645929));
#28985=CARTESIAN_POINT('Ctrl Pts',(-25.1399453635115,5.99731835573319,0.134406033229496));
#28986=CARTESIAN_POINT('Ctrl Pts',(-25.0935258154839,5.88833720714536,1.14602677836531));
#28987=CARTESIAN_POINT('Ctrl Pts',(-25.0471062674563,5.54353114134686,2.06960535350088));
#28988=CARTESIAN_POINT('Ctrl Pts',(-25.0006867194287,5.19872507554837,2.9931839286364));
#28989=CARTESIAN_POINT('Ctrl Pts',(-24.9542671714011,4.61809409253925,3.82872033377169));
#28990=CARTESIAN_POINT('Ctrl Pts',(-24.9078476233735,3.8727156196889,4.47393312012366));
#28991=CARTESIAN_POINT('Ctrl Pts',(-24.8614280753458,3.12733714683856,5.11914590647564));
#28992=CARTESIAN_POINT('Ctrl Pts',(-24.8150085273182,2.21721118414701,5.5740350740443));
#28993=CARTESIAN_POINT('Ctrl Pts',(-24.7685889792906,1.25374999500223,5.78291576839519));
#28994=CARTESIAN_POINT('Ctrl Pts',(-24.722169431263,0.290288805857399,5.99179646274609));
#28995=CARTESIAN_POINT('Ctrl Pts',(-24.6757498832354,-0.726507609740667,
5.9546686838792));
#28996=CARTESIAN_POINT('Ctrl Pts',(-24.6293303352078,-1.67216901941713,
5.67607739595078));
#28997=CARTESIAN_POINT('Ctrl Pts',(-24.5829107871802,-2.61783042909354,
5.39748610802238));
#28998=CARTESIAN_POINT('Ctrl Pts',(-24.5364912391526,-3.49235683284836,
4.87743131103248));
#28999=CARTESIAN_POINT('Ctrl Pts',(-24.4900716911249,-4.18869385576106,
4.17957505220703));
#29000=CARTESIAN_POINT('Ctrl Pts',(-24.4436521430973,-4.88503087867377,
3.48171879338158));
#29001=CARTESIAN_POINT('Ctrl Pts',(-24.3972325950697,-5.40317852074435,
2.60606107272057));
#29002=CARTESIAN_POINT('Ctrl Pts',(-24.3508130470421,-5.67970819742667,
1.6597947543013));
#29003=CARTESIAN_POINT('Ctrl Pts',(-24.3244170954297,-5.83695367428408,
1.12171110172871));
#29004=CARTESIAN_POINT('Ctrl Pts',(-24.2980211438172,-5.91607198801577,
0.560796160819298));
#29005=CARTESIAN_POINT('Ctrl Pts',(-24.2716251922048,-5.91627733888446,
-6.20456869606399E-5));
#29006=CARTESIAN_POINT('Origin',(-29.75,0.,0.));
#29007=CARTESIAN_POINT('',(-22.2698748077951,-5.91717032569028,8.22304250084477E-5));
#29008=CARTESIAN_POINT('',(-22.5216251922048,-5.91704156442688,0.000122038191318572));
#29009=CARTESIAN_POINT('',(-29.75,-5.91675,-7.2459289488551E-16));
#29010=CARTESIAN_POINT('Ctrl Pts',(-22.2698748077951,-5.91717032569028,
8.22304250084477E-5));
#29011=CARTESIAN_POINT('Ctrl Pts',(-22.2737108896147,-5.91722571336033,
0.0815554764548256));
#29012=CARTESIAN_POINT('Ctrl Pts',(-22.2775469714344,-5.91557804319747,
0.163026480149979));
#29013=CARTESIAN_POINT('Ctrl Pts',(-22.281383053254,-5.91221275274682,0.244426472890983));
#29014=CARTESIAN_POINT('Ctrl Pts',(-22.3278026012816,-5.87149014331214,
1.22942915274484));
#29015=CARTESIAN_POINT('Ctrl Pts',(-22.3742221493092,-5.57925869458383,
2.20403379364773));
#29016=CARTESIAN_POINT('Ctrl Pts',(-22.4206416973368,-5.0712916604527,3.04893503194394));
#29017=CARTESIAN_POINT('Ctrl Pts',(-22.4670612453645,-4.56332462632153,
3.89383627024019));
#29018=CARTESIAN_POINT('Ctrl Pts',(-22.5134807933921,-3.83962200678752,
4.60903410592975));
#29019=CARTESIAN_POINT('Ctrl Pts',(-22.5599003414197,-2.98877521684958,
5.1069782295931));
#29020=CARTESIAN_POINT('Ctrl Pts',(-22.6063198894473,-2.13792842691164,
5.60492235325644));
#29021=CARTESIAN_POINT('Ctrl Pts',(-22.6527394374749,-1.15993746656978,
5.88561276489358));
#29022=CARTESIAN_POINT('Ctrl Pts',(-22.6991589855025,-0.174522232773706,
5.91468899644434));
#29023=CARTESIAN_POINT('Ctrl Pts',(-22.7455785335302,0.810893001022308,
5.94376522799509));
#29024=CARTESIAN_POINT('Ctrl Pts',(-22.7919980815578,1.80373250827253,5.72122727945949));
#29025=CARTESIAN_POINT('Ctrl Pts',(-22.8384176295854,2.68245872031269,5.27431693664786));
#29026=CARTESIAN_POINT('Ctrl Pts',(-22.884837177613,3.56118493235285,4.82740659383624));
#29027=CARTESIAN_POINT('Ctrl Pts',(-22.9312567256406,4.32579784918294,4.1561238567486));
#29028=CARTESIAN_POINT('Ctrl Pts',(-22.9776762736682,4.88269805800541,3.34264320691608));
#29029=CARTESIAN_POINT('Ctrl Pts',(-23.0240958216958,5.43959826682792,2.52916255708353));
#29030=CARTESIAN_POINT('Ctrl Pts',(-23.0705153697234,5.7887857676428,1.57348399450608));
#29031=CARTESIAN_POINT('Ctrl Pts',(-23.1169349177511,5.88751508190382,0.592596063729021));
#29032=CARTESIAN_POINT('Ctrl Pts',(-23.1633544657787,5.98624439616484,-0.388291867047986));
#29033=CARTESIAN_POINT('Ctrl Pts',(-23.2097740138063,5.83451552387203,-1.39438916602461));
#29034=CARTESIAN_POINT('Ctrl Pts',(-23.2561935618339,5.45090222050147,-2.30253532370825));
#29035=CARTESIAN_POINT('Ctrl Pts',(-23.3026131098615,5.0672889171309,-3.2106814813919));
#29036=CARTESIAN_POINT('Ctrl Pts',(-23.3490326578891,4.45179118268257,-4.02087649778257));
#29037=CARTESIAN_POINT('Ctrl Pts',(-23.3954522059167,3.67975462701281,-4.63394106774891));
#29038=CARTESIAN_POINT('Ctrl Pts',(-23.4418717539443,2.907718071343,-5.24700563771528));
#29039=CARTESIAN_POINT('Ctrl Pts',(-23.4882913019719,1.97914269445174,-5.66293976125731));
#29040=CARTESIAN_POINT('Ctrl Pts',(-23.5347108499996,1.00769922842084,-5.83082723114243));
#29041=CARTESIAN_POINT('Ctrl Pts',(-23.5811303980272,0.0362557623899958,
-5.99871470102755));
#29042=CARTESIAN_POINT('Ctrl Pts',(-23.6275499460548,-0.978055792780479,
-5.9185555172558));
#29043=CARTESIAN_POINT('Ctrl Pts',(-23.6739694940824,-1.91106938670352,
-5.60016229529079));
#29044=CARTESIAN_POINT('Ctrl Pts',(-23.72038904211,-2.84408298062656,-5.28176907332579));
#29045=CARTESIAN_POINT('Ctrl Pts',(-23.7668085901376,-3.69579861330217,
-4.72514181316754));
#29046=CARTESIAN_POINT('Ctrl Pts',(-23.8132281381652,-4.36195427014207,
-3.99841954771901));
#29047=CARTESIAN_POINT('Ctrl Pts',(-23.8596476861928,-5.028109926982,-3.27169728227043));
#29048=CARTESIAN_POINT('Ctrl Pts',(-23.9060672342205,-5.5087056079862,-2.37488001153154));
#29049=CARTESIAN_POINT('Ctrl Pts',(-23.9524867822481,-5.74490961865291,
-1.41775082715593));
#29050=CARTESIAN_POINT('Ctrl Pts',(-23.9749494574304,-5.85921004150957,
-0.954590738579167));
#29051=CARTESIAN_POINT('Ctrl Pts',(-23.9974121326127,-5.91628260005259,
-0.477307738180849));
#29052=CARTESIAN_POINT('Ctrl Pts',(-24.0198748077951,-5.91624086672945,
-1.49279102093503E-5));
#29053=CARTESIAN_POINT('Ctrl Pts',(-24.2716251922048,-5.91627733888446,
-6.20456869606399E-5));
#29054=CARTESIAN_POINT('Ctrl Pts',(-24.2516015957896,-5.91643311515571,
-0.425521166771968));
#29055=CARTESIAN_POINT('Ctrl Pts',(-24.2315779993744,-5.87117822566273,
-0.850947639899966));
#29056=CARTESIAN_POINT('Ctrl Pts',(-24.2115544029593,-5.78016964510108,
-1.26635015227775));
#29057=CARTESIAN_POINT('Ctrl Pts',(-24.1651348549317,-5.56918970479912,
-2.22935382425988));
#29058=CARTESIAN_POINT('Ctrl Pts',(-24.118715306904,-5.11231811290117,-3.13848625204656));
#29059=CARTESIAN_POINT('Ctrl Pts',(-24.0722957588764,-4.46548240055963,
-3.88245679494493));
#29060=CARTESIAN_POINT('Ctrl Pts',(-24.0258762108488,-3.81864668821811,
-4.62642733784326));
#29061=CARTESIAN_POINT('Ctrl Pts',(-23.9794566628212,-2.98184685543302,
-5.20523599585329));
#29062=CARTESIAN_POINT('Ctrl Pts',(-23.9330371147936,-2.05751901236383,
-5.54802841990587));
#29063=CARTESIAN_POINT('Ctrl Pts',(-23.886617566766,-1.13319116929464,-5.89082084395845));
#29064=CARTESIAN_POINT('Ctrl Pts',(-23.8401980187383,-0.121335315941354,
-5.99759703405356));
#29065=CARTESIAN_POINT('Ctrl Pts',(-23.7937784707107,0.854183109871268,
-5.85528607748012));
#29066=CARTESIAN_POINT('Ctrl Pts',(-23.7473589226831,1.82970153568389,-5.71297512090667));
#29067=CARTESIAN_POINT('Ctrl Pts',(-23.7009393746556,2.76888253395585,-5.32157701766468));
#29068=CARTESIAN_POINT('Ctrl Pts',(-23.6545198266279,3.55675709486016,-4.72900441979956));
#29069=CARTESIAN_POINT('Ctrl Pts',(-23.6081002786003,4.34463165576448,-4.13643182193444));
#29070=CARTESIAN_POINT('Ctrl Pts',(-23.5616807305727,4.98119977930114,-3.3426847294462));
#29071=CARTESIAN_POINT('Ctrl Pts',(-23.515261182545,5.38853654260112,-2.44492898943387));
#29072=CARTESIAN_POINT('Ctrl Pts',(-23.4688416345174,5.79587330590112,-1.54717324942149));
#29073=CARTESIAN_POINT('Ctrl Pts',(-23.4224220864899,5.97397870896441,-0.545408861885016));
#29074=CARTESIAN_POINT('Ctrl Pts',(-23.3760025384623,5.90105013666917,0.437734073198114));
#29075=CARTESIAN_POINT('Ctrl Pts',(-23.3295829904347,5.82812156437394,1.42087700828124));
#29076=CARTESIAN_POINT('Ctrl Pts',(-23.283163442407,5.50415901672018,2.38539849091103));
#29077=CARTESIAN_POINT('Ctrl Pts',(-23.2367438943794,4.96882008196121,3.21322747831846));
#29078=CARTESIAN_POINT('Ctrl Pts',(-23.1903243463518,4.43348114720223,4.0410564657259));
#29079=CARTESIAN_POINT('Ctrl Pts',(-23.1439047983242,3.68676582533804,4.73219295791099));
#29080=CARTESIAN_POINT('Ctrl Pts',(-23.0974852502966,2.82008261093496,5.20203209350194));
#29081=CARTESIAN_POINT('Ctrl Pts',(-23.051065702269,1.95339939653199,5.67187122909283));
#29082=CARTESIAN_POINT('Ctrl Pts',(-23.0046461542413,0.966748289590168,
5.92041300808964));
#29083=CARTESIAN_POINT('Ctrl Pts',(-22.9582266062137,-0.0190906887673131,
5.91723240881446));
#29084=CARTESIAN_POINT('Ctrl Pts',(-22.9118070581861,-1.00492966712491,
5.91405180953929));
#29085=CARTESIAN_POINT('Ctrl Pts',(-22.8653875101585,-1.98995651689816,
5.65914883199208));
#29086=CARTESIAN_POINT('Ctrl Pts',(-22.8189679621309,-2.85359004896614,
5.18372719833551));
#29087=CARTESIAN_POINT('Ctrl Pts',(-22.7725484141033,-3.71722358103407,
4.70830556467896));
#29088=CARTESIAN_POINT('Ctrl Pts',(-22.7261288660757,-4.45946379539674,
4.01236527491309));
#29089=CARTESIAN_POINT('Ctrl Pts',(-22.679709318048,-4.98945001380782,3.18109924303455));
#29090=CARTESIAN_POINT('Ctrl Pts',(-22.6332897700204,-5.51943623221891,
2.349833211156));
#29091=CARTESIAN_POINT('Ctrl Pts',(-22.5868702219928,-5.83716845467843,
1.38324143716479));
#29092=CARTESIAN_POINT('Ctrl Pts',(-22.5404506739652,-5.90375177267192,
0.399648396712717));
#29093=CARTESIAN_POINT('Ctrl Pts',(-22.5341755133784,-5.91275274382662,
0.26668277030843));
#29094=CARTESIAN_POINT('Ctrl Pts',(-22.5279003527916,-5.91716406927873,
0.13340645256461));
#29095=CARTESIAN_POINT('Ctrl Pts',(-22.5216251922048,-5.91704156442688,
0.000122038191318572));
#29096=CARTESIAN_POINT('Origin',(-29.75,0.,0.));
#29097=CARTESIAN_POINT('',(-20.5198748077951,-5.91641453668928,-0.000121371007781868));
#29098=CARTESIAN_POINT('',(-20.7716251922048,-5.9165474513811,-0.000145824772724381));
#29099=CARTESIAN_POINT('',(-29.75,-5.91675,-7.2459289488551E-16));
#29100=CARTESIAN_POINT('Ctrl Pts',(-20.5198748077951,-5.91641453668928,
-0.000121371007781868));
#29101=CARTESIAN_POINT('Ctrl Pts',(-20.5500096466167,-5.91594204778621,
0.640137786987893));
#29102=CARTESIAN_POINT('Ctrl Pts',(-20.5801444854383,-5.81238320478607,
1.28054610164413));
#29103=CARTESIAN_POINT('Ctrl Pts',(-20.61027932426,-5.60827747628413,1.88712153381709));
#29104=CARTESIAN_POINT('Ctrl Pts',(-20.6566988722876,-5.29387408016884,
2.82148715537517));
#29105=CARTESIAN_POINT('Ctrl Pts',(-20.7031184203152,-4.74089142151915,
3.67557357075011));
#29106=CARTESIAN_POINT('Ctrl Pts',(-20.7495379683428,-4.01702238257332,
4.34482854808991));
#29107=CARTESIAN_POINT('Ctrl Pts',(-20.7959575163704,-3.2931533436275,5.0140835254297));
#29108=CARTESIAN_POINT('Ctrl Pts',(-20.842377064398,-2.39839792438554,5.49850706473436));
#29109=CARTESIAN_POINT('Ctrl Pts',(-20.8887966124256,-1.44228681677674,
5.73879888761961));
#29110=CARTESIAN_POINT('Ctrl Pts',(-20.9352161604533,-0.486175709167936,
5.97909071050486));
#29111=CARTESIAN_POINT('Ctrl Pts',(-20.9816357084809,0.531291086807709,
5.97525081697072));
#29112=CARTESIAN_POINT('Ctrl Pts',(-21.0280552565085,1.48556127475539,5.72774926418216));
#29113=CARTESIAN_POINT('Ctrl Pts',(-21.0744748045361,2.43983146270312,5.48024771139358));
#29114=CARTESIAN_POINT('Ctrl Pts',(-21.1208943525637,3.33090504262288,4.98908449935057));
#29115=CARTESIAN_POINT('Ctrl Pts',(-21.1673139005913,4.04970203168403,4.31438493750457));
#29116=CARTESIAN_POINT('Ctrl Pts',(-21.2137334486189,4.76849902074518,3.63968537565857));
#29117=CARTESIAN_POINT('Ctrl Pts',(-21.2601529966465,5.31501941894773,2.78144946400959));
#29118=CARTESIAN_POINT('Ctrl Pts',(-21.3065725446742,5.62236141594072,1.84473739131974));
#29119=CARTESIAN_POINT('Ctrl Pts',(-21.3529920927018,5.9297034129337,0.908025318629945));
#29120=CARTESIAN_POINT('Ctrl Pts',(-21.3994116407294,5.99786700871715,-0.10716291510071));
#29121=CARTESIAN_POINT('Ctrl Pts',(-21.445831188757,5.81850801710345,-1.07655394165592));
#29122=CARTESIAN_POINT('Ctrl Pts',(-21.4922507367846,5.63914902548975,-2.04594496821113));
#29123=CARTESIAN_POINT('Ctrl Pts',(-21.5386702848122,5.2122674464789,-2.9695387875909));
#29124=CARTESIAN_POINT('Ctrl Pts',(-21.5850898328398,4.59011961036565,-3.73427448066272));
#29125=CARTESIAN_POINT('Ctrl Pts',(-21.6315093808674,3.96797177425236,-4.49901017373458));
#29126=CARTESIAN_POINT('Ctrl Pts',(-21.677928928895,3.15055768103664,-5.10488774049848));
#29127=CARTESIAN_POINT('Ctrl Pts',(-21.7243484769227,2.23794035274358,-5.4777392154021));
#29128=CARTESIAN_POINT('Ctrl Pts',(-21.7707680249503,1.32532302445052,-5.85059069030572));
#29129=CARTESIAN_POINT('Ctrl Pts',(-21.8171875729779,0.317502461080135,
-5.99041607334905));
#29130=CARTESIAN_POINT('Ctrl Pts',(-21.8636071210055,-0.662149875990963,
-5.8800987641465));
#29131=CARTESIAN_POINT('Ctrl Pts',(-21.9100266690331,-1.64180221306201,
-5.76978145494396));
#29132=CARTESIAN_POINT('Ctrl Pts',(-21.9564462170607,-2.59328632383376,
-5.40932145349556));
#29133=CARTESIAN_POINT('Ctrl Pts',(-22.0028657650883,-3.40012712386265,
-4.84284415152558));
#29134=CARTESIAN_POINT('Ctrl Pts',(-22.0492853131159,-4.20696792389155,
-4.27636684955561));
#29135=CARTESIAN_POINT('Ctrl Pts',(-22.0957048611436,-4.86916541317758,
-3.50387224706406));
#29136=CARTESIAN_POINT('Ctrl Pts',(-22.1421244091712,-5.30565727275007,
-2.61992458641588));
#29137=CARTESIAN_POINT('Ctrl Pts',(-22.1847078753791,-5.70607772365798,
-1.80902579622443));
#29138=CARTESIAN_POINT('Ctrl Pts',(-22.2272913415871,-5.91655547984308,
-0.904333624679423));
#29139=CARTESIAN_POINT('Ctrl Pts',(-22.2698748077951,-5.91717032569028,
8.22304250084477E-5));
#29140=CARTESIAN_POINT('Ctrl Pts',(-22.5216251922048,-5.91704156442688,
0.000122038191318572));
#29141=CARTESIAN_POINT('Ctrl Pts',(-22.481480804764,-5.91625785823037,-0.852544773504149));
#29142=CARTESIAN_POINT('Ctrl Pts',(-22.4413364173232,-5.7299223214418,-1.70554294837803));
#29143=CARTESIAN_POINT('Ctrl Pts',(-22.4011920298824,-5.37264844600463,
-2.47964765843172));
#29144=CARTESIAN_POINT('Ctrl Pts',(-22.3547724818548,-4.95952738781642,
-3.37475636621097));
#29145=CARTESIAN_POINT('Ctrl Pts',(-22.3083529338272,-4.31785085791257,
-4.16437947485653));
#29146=CARTESIAN_POINT('Ctrl Pts',(-22.2619333857995,-3.52616912020172,
-4.75185597109779));
#29147=CARTESIAN_POINT('Ctrl Pts',(-22.2155138377719,-2.73448738249086,
-5.33933246733905));
#29148=CARTESIAN_POINT('Ctrl Pts',(-22.1690942897443,-1.79280043697301,
-5.72466235117601));
#29149=CARTESIAN_POINT('Ctrl Pts',(-22.1226747417167,-0.816384056787076,
-5.86067580626549));
#29150=CARTESIAN_POINT('Ctrl Pts',(-22.0762551936891,0.160032323398914,
-5.99668926135499));
#29151=CARTESIAN_POINT('Ctrl Pts',(-22.0298356456614,1.17117813825299,-5.88338628769699));
#29152=CARTESIAN_POINT('Ctrl Pts',(-21.9834160976338,2.09327486868419,-5.53463676842998));
#29153=CARTESIAN_POINT('Ctrl Pts',(-21.9369965496062,3.0153715991154,-5.18588724916296));
#29154=CARTESIAN_POINT('Ctrl Pts',(-21.8905770015786,3.84841924512373,-4.60169118428693));
#29155=CARTESIAN_POINT('Ctrl Pts',(-21.844157453551,4.49044101716969,-3.85356241750953));
#29156=CARTESIAN_POINT('Ctrl Pts',(-21.7977379055234,5.13246278921561,-3.10543365073218));
#29157=CARTESIAN_POINT('Ctrl Pts',(-21.7513183574958,5.58345868729917,-2.19337218205349));
#29158=CARTESIAN_POINT('Ctrl Pts',(-21.7048988094682,5.78822044812066,-1.22902720811207));
#29159=CARTESIAN_POINT('Ctrl Pts',(-21.6584792614406,5.99298220894214,-0.264682234170656));
#29160=CARTESIAN_POINT('Ctrl Pts',(-21.612059713413,5.95150983250155,0.751946245033478));
#29161=CARTESIAN_POINT('Ctrl Pts',(-21.5656401653854,5.66888012301801,1.69640855491039));
#29162=CARTESIAN_POINT('Ctrl Pts',(-21.5192206173577,5.38625041353447,2.6408708647873));
#29163=CARTESIAN_POINT('Ctrl Pts',(-21.4728010693301,4.86246337100797,3.51316700533699));
#29164=CARTESIAN_POINT('Ctrl Pts',(-21.4263815213025,4.1616379221952,4.20651561733327));
#29165=CARTESIAN_POINT('Ctrl Pts',(-21.3799619732749,3.46081247338243,4.89986422932954));
#29166=CARTESIAN_POINT('Ctrl Pts',(-21.3335424252473,2.58294861828339,5.41426531277241));
#29167=CARTESIAN_POINT('Ctrl Pts',(-21.2871228772197,1.63550928296806,5.68674891477082));
#29168=CARTESIAN_POINT('Ctrl Pts',(-21.2407033291921,0.68806994765268,5.95923251676925));
#29169=CARTESIAN_POINT('Ctrl Pts',(-21.1942837811644,-0.328944867879004,
5.98979863732319));
#29170=CARTESIAN_POINT('Ctrl Pts',(-21.1478642331368,-1.29103819601777,
5.77470555186539));
#29171=CARTESIAN_POINT('Ctrl Pts',(-21.1014446851092,-2.25313152415654,
5.55961246640759));
#29172=CARTESIAN_POINT('Ctrl Pts',(-21.0550251370816,-3.1603033649024,5.09886017493805));
#29173=CARTESIAN_POINT('Ctrl Pts',(-21.008605589054,-3.90150308108809,4.44885126100907));
#29174=CARTESIAN_POINT('Ctrl Pts',(-20.9621860410264,-4.6427027972737,3.79884234708015));
#29175=CARTESIAN_POINT('Ctrl Pts',(-20.9157664929988,-5.21793038889919,
2.95957681069184));
#29176=CARTESIAN_POINT('Ctrl Pts',(-20.8693469449712,-5.55676987996417,
2.03379259892567));
#29177=CARTESIAN_POINT('Ctrl Pts',(-20.8367730273824,-5.79454319157011,
1.38414347694089));
#29178=CARTESIAN_POINT('Ctrl Pts',(-20.8041991097936,-5.91591360793864,
0.691890584790816));
#29179=CARTESIAN_POINT('Ctrl Pts',(-20.7716251922048,-5.9165474513811,-0.000145824772724381));
#29180=CARTESIAN_POINT('Origin',(-29.75,0.,0.));
#29181=CARTESIAN_POINT('',(-18.7698748077951,-5.91679704493989,0.000153720370225236));
#29182=CARTESIAN_POINT('',(-19.0216251922048,-5.91663428088003,0.000153302805156978));
#29183=CARTESIAN_POINT('',(-29.75,-5.91675,-7.2459289488551E-16));
#29184=CARTESIAN_POINT('Ctrl Pts',(-18.7698748077951,-5.91679704493989,
0.000153720370225235));
#29185=CARTESIAN_POINT('Ctrl Pts',(-18.7798888555911,-5.91701835347429,
0.212877460640914));
#29186=CARTESIAN_POINT('Ctrl Pts',(-18.7899029033871,-5.90576990250038,
0.425577918591127));
#29187=CARTESIAN_POINT('Ctrl Pts',(-18.7999169511831,-5.88287455300957,
0.637017211654891));
#29188=CARTESIAN_POINT('Ctrl Pts',(-18.8463364992107,-5.77674446486252,
1.61713200831315));
#29189=CARTESIAN_POINT('Ctrl Pts',(-18.8927560472383,-5.42035360085787,
2.57014773627856));
#29190=CARTESIAN_POINT('Ctrl Pts',(-18.9391755952659,-4.85732923286482,
3.37940181954573));
#29191=CARTESIAN_POINT('Ctrl Pts',(-18.9855951432935,-4.29430486487177,
4.1886559028129));
#29192=CARTESIAN_POINT('Ctrl Pts',(-19.0320146913211,-3.52464699289032,
4.85414834138182));
#29193=CARTESIAN_POINT('Ctrl Pts',(-19.0784342393488,-2.64257260343326,
5.29441346798454));
#29194=CARTESIAN_POINT('Ctrl Pts',(-19.1248537873764,-1.76049821397624,
5.73467859458724));
#29195=CARTESIAN_POINT('Ctrl Pts',(-19.171273335404,-0.766007307043637,
5.94971640922375));
#29196=CARTESIAN_POINT('Ctrl Pts',(-19.2176928834316,0.219160394071264,
5.91320324833018));
#29197=CARTESIAN_POINT('Ctrl Pts',(-19.2641124314592,1.20432809518617,5.87669008743662));
#29198=CARTESIAN_POINT('Ctrl Pts',(-19.3105319794868,2.18017259048333,5.58862595101298));
#29199=CARTESIAN_POINT('Ctrl Pts',(-19.3569515275144,3.02723674062986,5.08427395510635));
#29200=CARTESIAN_POINT('Ctrl Pts',(-19.403371075542,3.87430089077639,4.57992195919972));
#29201=CARTESIAN_POINT('Ctrl Pts',(-19.4497906235696,4.59258469577225,3.85928210381012));
#29202=CARTESIAN_POINT('Ctrl Pts',(-19.4962101715973,5.09416007999938,3.01057087837719));
#29203=CARTESIAN_POINT('Ctrl Pts',(-19.5426297196249,5.59573546422651,2.16185965294427));
#29204=CARTESIAN_POINT('Ctrl Pts',(-19.5890492676525,5.88060242768489,1.18507705746804));
#29205=CARTESIAN_POINT('Ctrl Pts',(-19.6354688156801,5.91388923342342,0.199795067983714));
#29206=CARTESIAN_POINT('Ctrl Pts',(-19.6818883637077,5.94717603916195,-0.785486921500666));
#29207=CARTESIAN_POINT('Ctrl Pts',(-19.7283079117353,5.72888268718055,-1.77926830499326));
#29208=CARTESIAN_POINT('Ctrl Pts',(-19.7747274597629,5.28573136476298,-2.65989621488377));
#29209=CARTESIAN_POINT('Ctrl Pts',(-19.8211470077906,4.84258004234542,-3.54052412477423));
#29210=CARTESIAN_POINT('Ctrl Pts',(-19.8675665558182,4.17457074949172,-4.30799856106274));
#29211=CARTESIAN_POINT('Ctrl Pts',(-19.9139861038458,3.36347725195724,-4.86836982058248));
#29212=CARTESIAN_POINT('Ctrl Pts',(-19.9604056518734,2.55238375442275,-5.42874108010222));
#29213=CARTESIAN_POINT('Ctrl Pts',(-20.006825199901,1.59820605220752,-5.78200916285315));
#29214=CARTESIAN_POINT('Ctrl Pts',(-20.0532447479286,0.617748963365208,
-5.88492906946662));
#29215=CARTESIAN_POINT('Ctrl Pts',(-20.0996642959562,-0.362708125477101,
-5.98784897608009));
#29216=CARTESIAN_POINT('Ctrl Pts',(-20.1460838439838,-1.36944460094645,
-5.84042070655609));
#29217=CARTESIAN_POINT('Ctrl Pts',(-20.1925033920114,-2.27922170932619,
-5.4606915618929));
#29218=CARTESIAN_POINT('Ctrl Pts',(-20.2389229400391,-3.18899881770599,
-5.08096241722968));
#29219=CARTESIAN_POINT('Ctrl Pts',(-20.2853424880667,-4.00181655899615,
-4.46893239742725));
#29220=CARTESIAN_POINT('Ctrl Pts',(-20.3317620360943,-4.61817456952039,
-3.6995226151258));
#29221=CARTESIAN_POINT('Ctrl Pts',(-20.3781815841219,-5.23453258004463,
-2.93011283282435));
#29222=CARTESIAN_POINT('Ctrl Pts',(-20.4246011321495,-5.65443085980294,
-2.0033232880239));
#29223=CARTESIAN_POINT('Ctrl Pts',(-20.4710206801771,-5.82646793289164,
-1.03260610175302));
#29224=CARTESIAN_POINT('Ctrl Pts',(-20.4873053893831,-5.8868212501241,-0.692063210420498));
#29225=CARTESIAN_POINT('Ctrl Pts',(-20.5035900985891,-5.91666986722,-0.346114069563229));
#29226=CARTESIAN_POINT('Ctrl Pts',(-20.5198748077951,-5.91641453668928,
-0.000121371007781868));
#29227=CARTESIAN_POINT('Ctrl Pts',(-20.7716251922048,-5.9165474513811,-0.000145824772724381));
#29228=CARTESIAN_POINT('Ctrl Pts',(-20.757779561766,-5.9168168682247,-0.294297744047323));
#29229=CARTESIAN_POINT('Ctrl Pts',(-20.7439339313272,-5.8952728365774,-0.588410551463468));
#29230=CARTESIAN_POINT('Ctrl Pts',(-20.7300883008883,-5.85158255527674,
-0.87919590143652));
#29231=CARTESIAN_POINT('Ctrl Pts',(-20.6836687528607,-5.70510434901984,
-1.8540973028883));
#29232=CARTESIAN_POINT('Ctrl Pts',(-20.6372492048331,-5.30969654600157,
-2.79159721864773));
#29233=CARTESIAN_POINT('Ctrl Pts',(-20.5908296568055,-4.71376264211306,
-3.57693242711421));
#29234=CARTESIAN_POINT('Ctrl Pts',(-20.5444101087779,-4.11782873822455,
-4.3622676355807));
#29235=CARTESIAN_POINT('Ctrl Pts',(-20.4979905607502,-3.32136873346579,
-4.99543813675423));
#29236=CARTESIAN_POINT('Ctrl Pts',(-20.4515710127226,-2.4218805736879,-5.39893492469718));
#29237=CARTESIAN_POINT('Ctrl Pts',(-20.405151464695,-1.52239241391001,-5.80243171264014));
#29238=CARTESIAN_POINT('Ctrl Pts',(-20.3587319166674,-0.519876099112993,
-5.97625478735251));
#29239=CARTESIAN_POINT('Ctrl Pts',(-20.3123123686398,0.462946224216296,
-5.89912575114362));
#29240=CARTESIAN_POINT('Ctrl Pts',(-20.2658928206122,1.44576854754547,-5.82199671493473));
#29241=CARTESIAN_POINT('Ctrl Pts',(-20.2194732725846,2.40889687940692,-5.49391556780463));
#29242=CARTESIAN_POINT('Ctrl Pts',(-20.173053724557,3.2344307183487,-4.95504407271259));
#29243=CARTESIAN_POINT('Ctrl Pts',(-20.1266341765294,4.05996455729051,-4.41617257762052));
#29244=CARTESIAN_POINT('Ctrl Pts',(-20.0802146285017,4.74790390331264,-3.66651073456648));
#29245=CARTESIAN_POINT('Ctrl Pts',(-20.0337950804741,5.21403527085829,-2.79782773389776));
#29246=CARTESIAN_POINT('Ctrl Pts',(-19.9873755324465,5.68016663840395,-1.92914473322905));
#29247=CARTESIAN_POINT('Ctrl Pts',(-19.9409559844189,5.92449002747313,-0.941440574945666));
#29248=CARTESIAN_POINT('Ctrl Pts',(-19.8945364363913,5.91709680685361,0.0443758114821791));
#29249=CARTESIAN_POINT('Ctrl Pts',(-19.8481168883637,5.90970358623408,1.03019219791008));
#29250=CARTESIAN_POINT('Ctrl Pts',(-19.8016973403361,5.65059375592582,2.01412081248244));
#29251=CARTESIAN_POINT('Ctrl Pts',(-19.7552777923085,5.17148601624514,2.87571490556745));
#29252=CARTESIAN_POINT('Ctrl Pts',(-19.7088582442808,4.69237827656447,3.73730899865245));
#29253=CARTESIAN_POINT('Ctrl Pts',(-19.6624386962532,3.99327262751139,4.47656857025009));
#29254=CARTESIAN_POINT('Ctrl Pts',(-19.6160191482256,3.15974946773534,5.00299781485742));
#29255=CARTESIAN_POINT('Ctrl Pts',(-19.569599600198,2.32622630795928,5.52942705946474));
#29256=CARTESIAN_POINT('Ctrl Pts',(-19.5231800521704,1.35828563746025,5.84302597708174));
#29257=CARTESIAN_POINT('Ctrl Pts',(-19.4767605041428,0.374417055861,5.90540563404431));
#29258=CARTESIAN_POINT('Ctrl Pts',(-19.4303409561152,-0.609451525738141,
5.96778529100687));
#29259=CARTESIAN_POINT('Ctrl Pts',(-19.3839214080876,-1.6092480184375,5.77894568731507));
#29260=CARTESIAN_POINT('Ctrl Pts',(-19.33750186006,-2.50258322036267,5.36200345575057));
#29261=CARTESIAN_POINT('Ctrl Pts',(-19.2910823120323,-3.39591842228794,
4.94506122418602));
#29262=CARTESIAN_POINT('Ctrl Pts',(-19.2446627640047,-4.182792333439,4.30001636474871));
#29263=CARTESIAN_POINT('Ctrl Pts',(-19.1982432159771,-4.76688048112083,
3.50583147242293));
#29264=CARTESIAN_POINT('Ctrl Pts',(-19.1518236679495,-5.35096862880262,
2.7116465800972));
#29265=CARTESIAN_POINT('Ctrl Pts',(-19.1054041199219,-5.73227101301522,
1.76832165488302));
#29266=CARTESIAN_POINT('Ctrl Pts',(-19.0589845718943,-5.86411084021375,
0.791332981752648));
#29267=CARTESIAN_POINT('Ctrl Pts',(-19.0465314453311,-5.89947994921908,
0.529232980476941));
#29268=CARTESIAN_POINT('Ctrl Pts',(-19.034078318768,-5.91689509388119,0.264710179816106));
#29269=CARTESIAN_POINT('Ctrl Pts',(-19.0216251922048,-5.91663428088003,
0.000153302805156978));
#29270=CARTESIAN_POINT('Origin',(-29.75,0.,0.));
#29271=CARTESIAN_POINT('',(-17.0198748077951,-5.916790746513,-0.000154010032091534));
#29272=CARTESIAN_POINT('',(-17.2716251922048,-5.91695431715726,-0.000138309308396116));
#29273=CARTESIAN_POINT('',(-29.75,-5.91675,-7.2459289488551E-16));
#29274=CARTESIAN_POINT('Ctrl Pts',(-17.0198748077951,-5.916790746513,-0.000154010032091534));
#29275=CARTESIAN_POINT('Ctrl Pts',(-17.0561876125931,-5.91598848246282,
0.771224306268274));
#29276=CARTESIAN_POINT('Ctrl Pts',(-17.0925004173911,-5.76438952161292,
1.54290865794934));
#29277=CARTESIAN_POINT('Ctrl Pts',(-17.128813222189,-5.47038119103934,2.25586647634896));
#29278=CARTESIAN_POINT('Ctrl Pts',(-17.1752327702167,-5.09454313893885,
3.1672579228919));
#29279=CARTESIAN_POINT('Ctrl Pts',(-17.2216523182443,-4.48599200945246,
3.98268354702695));
#29280=CARTESIAN_POINT('Ctrl Pts',(-17.2680718662719,-3.71922304994449,
4.60232374340981));
#29281=CARTESIAN_POINT('Ctrl Pts',(-17.3144914142995,-2.95245409043648,
5.22196393979271));
#29282=CARTESIAN_POINT('Ctrl Pts',(-17.3609109623271,-2.02746730090685,
5.64581870842343));
#29283=CARTESIAN_POINT('Ctrl Pts',(-17.4073305103547,-1.05749411969492,
5.82200224331825));
#29284=CARTESIAN_POINT('Ctrl Pts',(-17.4537500583823,-0.087520938482929,
5.99818577821308));
#29285=CARTESIAN_POINT('Ctrl Pts',(-17.5001696064099,0.927438634411407,
5.926698079372));
#29286=CARTESIAN_POINT('Ctrl Pts',(-17.5465891544375,1.86313922208543,5.61629025011341));
#29287=CARTESIAN_POINT('Ctrl Pts',(-17.5930087024651,2.79883980975946,5.30588242085483));
#29288=CARTESIAN_POINT('Ctrl Pts',(-17.6394282504928,3.65528141221321,4.75655446117873));
#29289=CARTESIAN_POINT('Ctrl Pts',(-17.6858477985204,4.32762348945498,4.03555186658647));
#29290=CARTESIAN_POINT('Ctrl Pts',(-17.732267346548,4.99996556669675,3.31454927199422));
#29291=CARTESIAN_POINT('Ctrl Pts',(-17.7786868945756,5.48820811872651,2.42187204248595));
#29292=CARTESIAN_POINT('Ctrl Pts',(-17.8251064426032,5.73258336610087,1.46679647023563));
#29293=CARTESIAN_POINT('Ctrl Pts',(-17.8715259906308,5.97695861347522,0.511720897985363));
#29294=CARTESIAN_POINT('Ctrl Pts',(-17.9179455386584,5.97746655619411,-0.505753017006816));
#29295=CARTESIAN_POINT('Ctrl Pts',(-17.964365086686,5.73404501489963,-1.46107210687797));
#29296=CARTESIAN_POINT('Ctrl Pts',(-18.0107846347137,5.49062347360513,-2.41639119674918));
#29297=CARTESIAN_POINT('Ctrl Pts',(-18.0572041827413,5.00327244829723,-3.30955546149939));
#29298=CARTESIAN_POINT('Ctrl Pts',(-18.1036237307689,4.33165058296566,-4.03122898896668));
#29299=CARTESIAN_POINT('Ctrl Pts',(-18.1500432787965,3.66002871763409,-4.75290251643397));
#29300=CARTESIAN_POINT('Ctrl Pts',(-18.1964628268241,2.80413601227882,-5.30308530661837));
#29301=CARTESIAN_POINT('Ctrl Pts',(-18.2428823748517,1.86874581413954,-5.61442722069919));
#29302=CARTESIAN_POINT('Ctrl Pts',(-18.2893019228793,0.933355616000316,
-5.92576913477999));
#29303=CARTESIAN_POINT('Ctrl Pts',(-18.335721470907,-0.0815320749229426,
-5.99827017275724));
#29304=CARTESIAN_POINT('Ctrl Pts',(-18.3821410189346,-1.05168068109539,
-5.82305518429997));
#29305=CARTESIAN_POINT('Ctrl Pts',(-18.4285605669622,-2.02182928726785,
-5.6478401958427));
#29306=CARTESIAN_POINT('Ctrl Pts',(-18.4749801149898,-2.94723880868953,
-5.22490918095089));
#29307=CARTESIAN_POINT('Ctrl Pts',(-18.5213996630174,-3.71462605867108,
-4.60603486511271));
#29308=CARTESIAN_POINT('Ctrl Pts',(-18.567819211045,-4.48201330865264,-3.98716054927452));
#29309=CARTESIAN_POINT('Ctrl Pts',(-18.6142387590726,-5.0913782871941,-3.17234293248995));
#29310=CARTESIAN_POINT('Ctrl Pts',(-18.6606583071002,-5.46812612032009,
-2.26132719142216));
#29311=CARTESIAN_POINT('Ctrl Pts',(-18.6970638073319,-5.76359847860266,
-1.54684406563382));
#29312=CARTESIAN_POINT('Ctrl Pts',(-18.7334693075635,-5.9159924903717,-0.773191317866126));
#29313=CARTESIAN_POINT('Ctrl Pts',(-18.7698748077951,-5.91679704493989,
0.000153720370225235));
#29314=CARTESIAN_POINT('Ctrl Pts',(-19.0216251922048,-5.91663428088003,
0.000153302805156978));
#29315=CARTESIAN_POINT('Ctrl Pts',(-18.9876587707404,-5.91592290255459,
-0.721436599964167));
#29316=CARTESIAN_POINT('Ctrl Pts',(-18.9536923492759,-5.78371152898367,
-1.44328001317763));
#29317=CARTESIAN_POINT('Ctrl Pts',(-18.9197259278114,-5.52564133302854,
-2.11690616066192));
#29318=CARTESIAN_POINT('Ctrl Pts',(-18.8733063797838,-5.17295472846031,
-3.0375042088996));
#29319=CARTESIAN_POINT('Ctrl Pts',(-18.8268868317562,-4.58520424913938,
-3.86804788432833));
#29320=CARTESIAN_POINT('Ctrl Pts',(-18.7804672837286,-3.83433884926859,
-4.50686691874871));
#29321=CARTESIAN_POINT('Ctrl Pts',(-18.734047735701,-3.08347344939785,-5.14568595316904));
#29322=CARTESIAN_POINT('Ctrl Pts',(-18.6876281876734,-2.16949312897728,
-5.59278034658103));
#29323=CARTESIAN_POINT('Ctrl Pts',(-18.6412086396458,-1.20428197918144,
-5.79341943492276));
#29324=CARTESIAN_POINT('Ctrl Pts',(-18.5947890916182,-0.239070829385605,
-5.99405852326448));
#29325=CARTESIAN_POINT('Ctrl Pts',(-18.5483695435905,0.777371149785462,
-5.94824230653593));
#29326=CARTESIAN_POINT('Ctrl Pts',(-18.5019499955629,1.72061711397817,-5.66157933631661));
#29327=CARTESIAN_POINT('Ctrl Pts',(-18.4555304475353,2.66386307817093,-5.37491636609728));
#29328=CARTESIAN_POINT('Ctrl Pts',(-18.4091108995077,3.5339130273853,-4.84740664238717));
#29329=CARTESIAN_POINT('Ctrl Pts',(-18.3626913514801,4.22426056791737,-4.14362480066189));
#29330=CARTESIAN_POINT('Ctrl Pts',(-18.3162718034525,4.9146081084494,-3.43984295893665));
#29331=CARTESIAN_POINT('Ctrl Pts',(-18.2698522554248,5.42525324029921,-2.55978899919613));
#29332=CARTESIAN_POINT('Ctrl Pts',(-18.2234327073972,5.69368579206225,-1.61119394722993));
#29333=CARTESIAN_POINT('Ctrl Pts',(-18.1770131593696,5.9621183438253,-0.662598895263667));
#29334=CARTESIAN_POINT('Ctrl Pts',(-18.130593611342,5.98833831550164,0.354537248928418));
#29335=CARTESIAN_POINT('Ctrl Pts',(-18.0841740633144,5.76913601248835,1.31570266539666));
#29336=CARTESIAN_POINT('Ctrl Pts',(-18.0377545152868,5.54993370947507,2.27686808186486));
#29337=CARTESIAN_POINT('Ctrl Pts',(-17.9913349672592,5.08530913177228,3.18206277060904));
#29338=CARTESIAN_POINT('Ctrl Pts',(-17.9449154192316,4.43213888542068,3.9204781257729));
#29339=CARTESIAN_POINT('Ctrl Pts',(-17.898495871204,3.77896863906908,4.65889348093676));
#29340=CARTESIAN_POINT('Ctrl Pts',(-17.8520763231763,2.93725272406858,5.23052950252021));
#29341=CARTESIAN_POINT('Ctrl Pts',(-17.8056567751487,2.01002904842788,5.5654098733874));
#29342=CARTESIAN_POINT('Ctrl Pts',(-17.7592372271211,1.08280537278718,5.90029024425459));
#29343=CARTESIAN_POINT('Ctrl Pts',(-17.7128176790935,0.0700739365061698,
5.99841496440561));
#29344=CARTESIAN_POINT('Ctrl Pts',(-17.6663981310659,-0.904192638882054,
5.84777218315773));
#29345=CARTESIAN_POINT('Ctrl Pts',(-17.6199785830383,-1.87845921427028,
5.69712940190986));
#29346=CARTESIAN_POINT('Ctrl Pts',(-17.5735590350107,-2.81426092876568,
5.29771911926308));
#29347=CARTESIAN_POINT('Ctrl Pts',(-17.5271394869831,-3.59704244457092,
4.69843479110619));
#29348=CARTESIAN_POINT('Ctrl Pts',(-17.4807199389554,-4.3798239603762,4.09915046294928));
#29349=CARTESIAN_POINT('Ctrl Pts',(-17.4343003909278,-5.00958527749128,
3.29999208928225));
#29350=CARTESIAN_POINT('Ctrl Pts',(-17.3878808429002,-5.40923472222464,
2.39878793439545));
#29351=CARTESIAN_POINT('Ctrl Pts',(-17.3491289593351,-5.74286935261707,
1.64644630328328));
#29352=CARTESIAN_POINT('Ctrl Pts',(-17.31037707577,-5.91613408823061,0.822986780567107));
#29353=CARTESIAN_POINT('Ctrl Pts',(-17.2716251922048,-5.91695431715726,
-0.000138309308396116));
#29354=CARTESIAN_POINT('Origin',(-29.75,0.,0.));
#29355=CARTESIAN_POINT('',(-15.2698748077951,-5.91641904191932,0.000122539150512468));
#29356=CARTESIAN_POINT('',(-15.5216251922048,-5.91631764548591,8.65724823460925E-5));
#29357=CARTESIAN_POINT('',(-29.75,-5.91675,-7.2459289488551E-16));
#29358=CARTESIAN_POINT('Ctrl Pts',(-15.2698748077951,-5.91641904191932,
0.000122539150512468));
#29359=CARTESIAN_POINT('Ctrl Pts',(-15.2860668215674,-5.91667562844659,
0.344145035781405));
#29360=CARTESIAN_POINT('Ctrl Pts',(-15.3022588353398,-5.88716769234933,
0.688124008340338));
#29361=CARTESIAN_POINT('Ctrl Pts',(-15.3184508491121,-5.82749602249077,
1.02678821684237));
#29362=CARTESIAN_POINT('Ctrl Pts',(-15.3648703971398,-5.65642823661614,
1.99767668771552));
#29363=CARTESIAN_POINT('Ctrl Pts',(-15.4112899451674,-5.23745550856503,
2.92488501319836));
#29364=CARTESIAN_POINT('Ctrl Pts',(-15.457709493195,-4.62186601364884,3.6949098075961));
#29365=CARTESIAN_POINT('Ctrl Pts',(-15.5041290412226,-4.00627651873265,
4.46493460199384));
#29366=CARTESIAN_POINT('Ctrl Pts',(-15.5505485892502,-3.1940702569514,5.07777586530647));
#29367=CARTESIAN_POINT('Ctrl Pts',(-15.5969681372778,-2.28467273825905,
5.45841317723823));
#29368=CARTESIAN_POINT('Ctrl Pts',(-15.6433876853054,-1.37527521956669,
5.83905048916999));
#29369=CARTESIAN_POINT('Ctrl Pts',(-15.689807233333,-0.368686443963233,
5.98748384972087));
#29370=CARTESIAN_POINT('Ctrl Pts',(-15.7362267813607,0.611872915382893,
5.88554292056501));
#29371=CARTESIAN_POINT('Ctrl Pts',(-15.7826463293883,1.59243227472908,5.78360199140914));
#29372=CARTESIAN_POINT('Ctrl Pts',(-15.8290658774159,2.54696221781793,5.43128677254651));
#29373=CARTESIAN_POINT('Ctrl Pts',(-15.8754854254435,3.35861480734123,4.8717256193571));
#29374=CARTESIAN_POINT('Ctrl Pts',(-15.9219049734711,4.1702673968645,4.31216446616772));
#29375=CARTESIAN_POINT('Ctrl Pts',(-15.9683245214987,4.83904263282224,3.5453573786516));
#29376=CARTESIAN_POINT('Ctrl Pts',(-16.0147440695263,5.28307298721258,2.66517236706686));
#29377=CARTESIAN_POINT('Ctrl Pts',(-16.0611636175539,5.72710334160293,1.78498735548211));
#29378=CARTESIAN_POINT('Ctrl Pts',(-16.1075831655815,5.94638881442588,0.791424419828757));
#29379=CARTESIAN_POINT('Ctrl Pts',(-16.1540027136092,5.9140857688039,-0.193890313381902));
#29380=CARTESIAN_POINT('Ctrl Pts',(-16.2004222616368,5.88178272318191,-1.17920504659262));
#29381=CARTESIAN_POINT('Ctrl Pts',(-16.2468418096644,5.59789115911495,-2.15627157736063));
#29382=CARTESIAN_POINT('Ctrl Pts',(-16.293261357692,5.09716341090182,-3.00548317196351));
#29383=CARTESIAN_POINT('Ctrl Pts',(-16.3396809057196,4.59643566268871,-3.85469476656634));
#29384=CARTESIAN_POINT('Ctrl Pts',(-16.3861004537472,3.87887173032945,-4.57605142500404));
#29385=CARTESIAN_POINT('Ctrl Pts',(-16.4325200017748,3.03231156687109,-5.08124891102688));
#29386=CARTESIAN_POINT('Ctrl Pts',(-16.4789395498025,2.18575140341273,-5.58644639704972));
#29387=CARTESIAN_POINT('Ctrl Pts',(-16.5253590978301,1.21019500885526,-5.87548471065769));
#29388=CARTESIAN_POINT('Ctrl Pts',(-16.5717786458577,0.225064254934827,
-5.91298148276677));
#29389=CARTESIAN_POINT('Ctrl Pts',(-16.6181981938853,-0.760066498985666,
-5.95047825487585));
#29390=CARTESIAN_POINT('Ctrl Pts',(-16.6646177419129,-1.75477161226913,
-5.736433485486));
#29391=CARTESIAN_POINT('Ctrl Pts',(-16.7110372899405,-2.63728513974157,
-5.29704927540705));
#29392=CARTESIAN_POINT('Ctrl Pts',(-16.7574568379681,-3.51979866721402,
-4.8576650653281));
#29393=CARTESIAN_POINT('Ctrl Pts',(-16.8038763859957,-4.29012060887544,
-4.19294141456005));
#29394=CARTESIAN_POINT('Ctrl Pts',(-16.8502959340234,-4.85395268671152,
-3.38424987989334));
#29395=CARTESIAN_POINT('Ctrl Pts',(-16.896715482051,-5.4177847645476,-2.57555834522663));
#29396=CARTESIAN_POINT('Ctrl Pts',(-16.9431350300786,-5.77512697855834,
-1.62289892666125));
#29397=CARTESIAN_POINT('Ctrl Pts',(-16.9895545781062,-5.8822355982064,-0.642890582903073));
#29398=CARTESIAN_POINT('Ctrl Pts',(-16.9996613213358,-5.90555593117947,
-0.429517271138596));
#29399=CARTESIAN_POINT('Ctrl Pts',(-17.0097680645655,-5.91701403625343,
-0.214847494028373));
#29400=CARTESIAN_POINT('Ctrl Pts',(-17.0198748077951,-5.916790746513,-0.000154010032091534));
#29401=CARTESIAN_POINT('Ctrl Pts',(-17.2716251922048,-5.91695431715726,
-0.000138309308396116));
#29402=CARTESIAN_POINT('Ctrl Pts',(-17.2639575277424,-5.9171166122411,-0.163006444200649));
#29403=CARTESIAN_POINT('Ctrl Pts',(-17.2562898632799,-5.91052756808586,
-0.325861485781881));
#29404=CARTESIAN_POINT('Ctrl Pts',(-17.2486221988174,-5.89709364756359,
-0.488149921834486));
#29405=CARTESIAN_POINT('Ctrl Pts',(-17.2022026507898,-5.81576555581756,
-1.47063368707121));
#29406=CARTESIAN_POINT('Ctrl Pts',(-17.1557831027622,-5.48357179997386,
-2.43235128143819));
#29407=CARTESIAN_POINT('Ctrl Pts',(-17.1093635547345,-4.94117758434384,
-3.25557489766398));
#29408=CARTESIAN_POINT('Ctrl Pts',(-17.0629440067069,-4.39878336871378,
-4.07879851388981));
#29409=CARTESIAN_POINT('Ctrl Pts',(-17.0165244586793,-3.64618869329736,
-4.76352815197446));
#29410=CARTESIAN_POINT('Ctrl Pts',(-16.9701049106517,-2.77552176851717,
-5.2259432399146));
#29411=CARTESIAN_POINT('Ctrl Pts',(-16.9236853626241,-1.90485484373698,
-5.68835832785475));
#29412=CARTESIAN_POINT('Ctrl Pts',(-16.8772658145965,-0.916115669593002,
-5.92845886565041));
#29413=CARTESIAN_POINT('Ctrl Pts',(-16.8308462665689,0.0696601238949256,
-5.9168531586867));
#29414=CARTESIAN_POINT('Ctrl Pts',(-16.7844267185412,1.05543591738285,-5.905247451723));
#29415=CARTESIAN_POINT('Ctrl Pts',(-16.7380071705136,2.03824833021476,-5.64193549999993));
#29416=CARTESIAN_POINT('Ctrl Pts',(-16.691587622486,2.89778725160595,-5.15915040280392));
#29417=CARTESIAN_POINT('Ctrl Pts',(-16.6451680744584,3.75732617299704,-4.67636530560797));
#29418=CARTESIAN_POINT('Ctrl Pts',(-16.5987485264308,4.49359160294746,-3.97410706293911));
#29419=CARTESIAN_POINT('Ctrl Pts',(-16.5523289784032,5.01645426115131,-3.13834199540119));
#29420=CARTESIAN_POINT('Ctrl Pts',(-16.5059094303756,5.53931691935521,-2.30257692786317));
#29421=CARTESIAN_POINT('Ctrl Pts',(-16.459489882348,5.84877680581247,-1.3333050354562));
#29422=CARTESIAN_POINT('Ctrl Pts',(-16.4130703343204,5.90695166269147,-0.349178878153185));
#29423=CARTESIAN_POINT('Ctrl Pts',(-16.3666507862928,5.96512651957047,0.634947279149776));
#29424=CARTESIAN_POINT('Ctrl Pts',(-16.3202312382651,5.77201634687118,1.63392770134863));
#29425=CARTESIAN_POINT('Ctrl Pts',(-16.2738116902375,5.35126055529678,2.52547308511626));
#29426=CARTESIAN_POINT('Ctrl Pts',(-16.2273921422099,4.93050476372235,3.41701846888394));
#29427=CARTESIAN_POINT('Ctrl Pts',(-16.1809725941823,4.28210335327276,4.2011288142204));
#29428=CARTESIAN_POINT('Ctrl Pts',(-16.1345530461547,3.48542980815072,4.78181794789139));
#29429=CARTESIAN_POINT('Ctrl Pts',(-16.0881334981271,2.68875626302869,5.36250708156239));
#29430=CARTESIAN_POINT('Ctrl Pts',(-16.0417139500994,1.74381058323418,5.73977500356793));
#29431=CARTESIAN_POINT('Ctrl Pts',(-15.9952944020718,0.76626745697552,5.86743879547986));
#29432=CARTESIAN_POINT('Ctrl Pts',(-15.9488748540442,-0.211275669283083,
5.99510258739178));
#29433=CARTESIAN_POINT('Ctrl Pts',(-15.9024553060166,-1.22141624200586,
5.87316224921013));
#29434=CARTESIAN_POINT('Ctrl Pts',(-15.856035757989,-2.14049879792674,5.51654499939918));
#29435=CARTESIAN_POINT('Ctrl Pts',(-15.8096162099614,-3.05958135384761,
5.15992774958823));
#29436=CARTESIAN_POINT('Ctrl Pts',(-15.7631966619338,-3.88760589296661,
4.56863358814798));
#29437=CARTESIAN_POINT('Ctrl Pts',(-15.7167771139062,-4.52321052492381,
3.81504526598837));
#29438=CARTESIAN_POINT('Ctrl Pts',(-15.6703575658785,-5.15881515688104,
3.06145694382872));
#29439=CARTESIAN_POINT('Ctrl Pts',(-15.6239380178509,-5.60199988167648,
2.14557446094968));
#29440=CARTESIAN_POINT('Ctrl Pts',(-15.5775184698233,-5.79851263386804,
1.17951476005797));
#29441=CARTESIAN_POINT('Ctrl Pts',(-15.5588873772838,-5.87738559637715,
0.791774067811633));
#29442=CARTESIAN_POINT('Ctrl Pts',(-15.5402562847443,-5.91652159902753,
0.395950211203544));
#29443=CARTESIAN_POINT('Ctrl Pts',(-15.5216251922048,-5.91631764548591,
8.65724823460925E-5));
#29444=CARTESIAN_POINT('Origin',(-29.75,0.,0.));
#29445=CARTESIAN_POINT('',(-13.5198748077951,-5.91716619296352,-8.39733533108955E-5));
#29446=CARTESIAN_POINT('',(-13.7716251922048,-5.91724766713751,-3.36308197105027E-5));
#29447=CARTESIAN_POINT('',(-29.75,-5.91675,-7.2459289488551E-16));
#29448=CARTESIAN_POINT('Ctrl Pts',(-13.5198748077951,-5.91716619296352,
-8.39733533108955E-5));
#29449=CARTESIAN_POINT('Ctrl Pts',(-13.5623655785694,-5.91654215140973,
0.9023649832068));
#29450=CARTESIAN_POINT('Ctrl Pts',(-13.6048563493438,-5.7070112106254,1.8050937555527));
#29451=CARTESIAN_POINT('Ctrl Pts',(-13.6473471201181,-5.30827046191485,
2.61462590776469));
#29452=CARTESIAN_POINT('Ctrl Pts',(-13.6937666681457,-4.87266138733159,
3.49900893811922));
#29453=CARTESIAN_POINT('Ctrl Pts',(-13.7401862161733,-4.21123551650526,
4.27216431907237));
#29454=CARTESIAN_POINT('Ctrl Pts',(-13.7866057642009,-3.40496071141642,
4.83944691964926));
#29455=CARTESIAN_POINT('Ctrl Pts',(-13.8330253122285,-2.59868590632748,
5.40672952022621));
#29456=CARTESIAN_POINT('Ctrl Pts',(-13.8794448602561,-1.64756216697599,
5.76813934042686));
#29457=CARTESIAN_POINT('Ctrl Pts',(-13.9258644082838,-0.668020463257402,
5.87943471730586));
#29458=CARTESIAN_POINT('Ctrl Pts',(-13.9722839563114,0.311521240461189,
5.99073009418486));
#29459=CARTESIAN_POINT('Ctrl Pts',(-14.018703504339,1.31948090854688,5.85191102774222));
#29460=CARTESIAN_POINT('Ctrl Pts',(-14.0651230523666,2.23247005124256,5.4799709310084));
#29461=CARTESIAN_POINT('Ctrl Pts',(-14.1115426003942,3.1454591939382,5.10803083427462));
#29462=CARTESIAN_POINT('Ctrl Pts',(-14.1579621484218,3.96347781124383,4.50296970724969));
#29463=CARTESIAN_POINT('Ctrl Pts',(-14.2043816964494,4.58638887885351,3.73885557173862));
#29464=CARTESIAN_POINT('Ctrl Pts',(-14.250801244477,5.20929994646318,2.97474143622756));
#29465=CARTESIAN_POINT('Ctrl Pts',(-14.2972207925047,5.6371034643769,2.05157429223036));
#29466=CARTESIAN_POINT('Ctrl Pts',(-14.3436403405323,5.81743024396591,1.08236282779058));
#29467=CARTESIAN_POINT('Ctrl Pts',(-14.3900598885599,5.99775702355493,0.113151363350743));
#29468=CARTESIAN_POINT('Ctrl Pts',(-14.4364794365875,5.93060706481922,-0.902104421531676));
#29469=CARTESIAN_POINT('Ctrl Pts',(-14.4828989846151,5.62420047046525,-1.83912288942596));
#29470=CARTESIAN_POINT('Ctrl Pts',(-14.5293185326427,5.31779387611128,-2.77614135732025));
#29471=CARTESIAN_POINT('Ctrl Pts',(-14.5757380806703,4.77213064613906,-3.63492250822641));
#29472=CARTESIAN_POINT('Ctrl Pts',(-14.6221576286979,4.05400766141003,-4.31033940840172));
#29473=CARTESIAN_POINT('Ctrl Pts',(-14.6685771767256,3.33588467668099,-4.98575630857702));
#29474=CARTESIAN_POINT('Ctrl Pts',(-14.7149967247532,2.44530193719514,-5.47780895802147));
#29475=CARTESIAN_POINT('Ctrl Pts',(-14.7614162727808,1.49127933998626,-5.72626316759213));
#29476=CARTESIAN_POINT('Ctrl Pts',(-14.8078358208084,0.53725674277749,-5.97471737716275));
#29477=CARTESIAN_POINT('Ctrl Pts',(-14.854255368836,-0.480205712154302,
-5.97957314685963));
#29478=CARTESIAN_POINT('Ctrl Pts',(-14.9006749168636,-1.43655625981935,
-5.74023606193734));
#29479=CARTESIAN_POINT('Ctrl Pts',(-14.9470944648912,-2.3929068074845,-5.50089897701502));
#29480=CARTESIAN_POINT('Ctrl Pts',(-14.9935140129189,-3.2881454478829,-5.01736903747348));
#29481=CARTESIAN_POINT('Ctrl Pts',(-15.0399335609465,-4.01268233599549,
-4.34883713247367));
#29482=CARTESIAN_POINT('Ctrl Pts',(-15.0863531089741,-4.73721922410796,
-3.68030522747397));
#29483=CARTESIAN_POINT('Ctrl Pts',(-15.1327726570017,-5.29105435993469,
-2.82677135701607));
#29484=CARTESIAN_POINT('Ctrl Pts',(-15.1791922050293,-5.60639050599904,
-1.89272011365545));
#29485=CARTESIAN_POINT('Ctrl Pts',(-15.2094197392846,-5.81173145743218,
-1.28448355913171));
#29486=CARTESIAN_POINT('Ctrl Pts',(-15.2396472735398,-5.91594004170654,
-0.642104669132373));
#29487=CARTESIAN_POINT('Ctrl Pts',(-15.2698748077951,-5.91641904191932,
0.000122539150512468));
#29488=CARTESIAN_POINT('Ctrl Pts',(-15.5216251922048,-5.91631764548591,
8.65724823460925E-5));
#29489=CARTESIAN_POINT('Ctrl Pts',(-15.4938367367167,-5.91601344679757,
-0.59034788972918));
#29490=CARTESIAN_POINT('Ctrl Pts',(-15.4660482812286,-5.82819353340298,
-1.18087085127824));
#29491=CARTESIAN_POINT('Ctrl Pts',(-15.4382598257405,-5.65417516915888,
-1.74479425457244));
#29492=CARTESIAN_POINT('Ctrl Pts',(-15.3918402777129,-5.36348417267047,
-2.68680664940669));
#29493=CARTESIAN_POINT('Ctrl Pts',(-15.3454207296853,-4.83226140010595,
-3.55459452017086));
#29494=CARTESIAN_POINT('Ctrl Pts',(-15.2990011816577,-4.12553601652687,
-4.2419283834904));
#29495=CARTESIAN_POINT('Ctrl Pts',(-15.25258163363,-3.41881063294774,-4.92926224680999));
#29496=CARTESIAN_POINT('Ctrl Pts',(-15.2061620856024,-2.53658263835401,
-5.43614210268493));
#29497=CARTESIAN_POINT('Ctrl Pts',(-15.1597425375748,-1.58684919108548,
-5.7005187026334));
#29498=CARTESIAN_POINT('Ctrl Pts',(-15.1133229895472,-0.6371157438171,-5.96489530258183));
#29499=CARTESIAN_POINT('Ctrl Pts',(-15.0669034415196,0.380123156126065,
-5.98676864660388));
#29500=CARTESIAN_POINT('Ctrl Pts',(-15.020483893492,1.34034311004015,-5.76346112866998));
#29501=CARTESIAN_POINT('Ctrl Pts',(-14.9740643454644,2.30056306395439,-5.54015361073604));
#29502=CARTESIAN_POINT('Ctrl Pts',(-14.9276447974368,3.20376407183954,-5.07166523084607));
#29503=CARTESIAN_POINT('Ctrl Pts',(-14.8812252494091,3.93938158251497,-4.4153455789625));
#29504=CARTESIAN_POINT('Ctrl Pts',(-14.8348057013815,4.67499909319041,-3.75902592707893));
#29505=CARTESIAN_POINT('Ctrl Pts',(-14.7883861533539,5.24303310665613,-2.91487500320176));
#29506=CARTESIAN_POINT('Ctrl Pts',(-14.7419666053263,5.57394824240897,-1.98622879479375));
#29507=CARTESIAN_POINT('Ctrl Pts',(-14.6955470572987,5.9048633781618,-1.05758258638574));
#29508=CARTESIAN_POINT('Ctrl Pts',(-14.6491275092711,5.99865963620174,-0.0444410934468829));
#29509=CARTESIAN_POINT('Ctrl Pts',(-14.6027079612435,5.84385503070052,0.929172865767193));
#29510=CARTESIAN_POINT('Ctrl Pts',(-14.5562884132158,5.68905042519931,1.90278682498127));
#29511=CARTESIAN_POINT('Ctrl Pts',(-14.5098688651882,5.28564495615694,2.83687325047057));
#29512=CARTESIAN_POINT('Ctrl Pts',(-14.4634493171606,4.68302114666527,3.6170867800217));
#29513=CARTESIAN_POINT('Ctrl Pts',(-14.417029769133,4.08039733717367,4.39730030957275));
#29514=CARTESIAN_POINT('Ctrl Pts',(-14.3706102211054,3.27855518723281,5.02364094318566));
#29515=CARTESIAN_POINT('Ctrl Pts',(-14.3241906730778,2.37565149322788,5.41943574710928));
#29516=CARTESIAN_POINT('Ctrl Pts',(-14.2777711250502,1.47274779922286,5.81523055103295));
#29517=CARTESIAN_POINT('Ctrl Pts',(-14.2313515770226,0.468782561153745,
5.98047952526726));
#29518=CARTESIAN_POINT('Ctrl Pts',(-14.1849320289949,-0.513344705833924,
5.89495386303524));
#29519=CARTESIAN_POINT('Ctrl Pts',(-14.1385124809673,-1.49547197282154,
5.80942820080323));
#29520=CARTESIAN_POINT('Ctrl Pts',(-14.0920929329397,-2.45576126872771,
5.47312790210493));
#29521=CARTESIAN_POINT('Ctrl Pts',(-14.0456733849121,-3.27665963017168,
4.92722087005698));
#29522=CARTESIAN_POINT('Ctrl Pts',(-13.9992538368845,-4.09755799161564,
4.38131383800903));
#29523=CARTESIAN_POINT('Ctrl Pts',(-13.9528342888569,-4.77906541859739,
3.62580007261144));
#29524=CARTESIAN_POINT('Ctrl Pts',(-13.9064147408293,-5.23775578323106,
2.75316512210063));
#29525=CARTESIAN_POINT('Ctrl Pts',(-13.8614848912878,-5.68172583345341,
1.90853481661455));
#29526=CARTESIAN_POINT('Ctrl Pts',(-13.8165550417463,-5.91695065499682,
0.954180020948209));
#29527=CARTESIAN_POINT('Ctrl Pts',(-13.7716251922048,-5.91724766713751,
-3.36308197105027E-5));
#29528=CARTESIAN_POINT('Origin',(-29.75,0.,0.));
#29529=CARTESIAN_POINT('',(-11.7698748077951,-5.91624143118648,1.67735000153324E-5));
#29530=CARTESIAN_POINT('',(-12.0216251922048,-5.916248517546,-3.1785587739037E-5));
#29531=CARTESIAN_POINT('',(-29.75,-5.91675,-7.2459289488551E-16));
#29532=CARTESIAN_POINT('Ctrl Pts',(-11.7698748077951,-5.91624143118648,
1.67735000153324E-5));
#29533=CARTESIAN_POINT('Ctrl Pts',(-11.7922447875438,-5.91628813593339,
0.47533983721482));
#29534=CARTESIAN_POINT('Ctrl Pts',(-11.8146147672925,-5.85969045278836,
0.950651967737993));
#29535=CARTESIAN_POINT('Ctrl Pts',(-11.8369847470412,-5.74632229224677,
1.41201418123897));
#29536=CARTESIAN_POINT('Ctrl Pts',(-11.8834042950688,-5.51107403399256,
2.36937872373404));
#29537=CARTESIAN_POINT('Ctrl Pts',(-11.9298238430964,-5.0313740094756,3.26667539272024));
#29538=CARTESIAN_POINT('Ctrl Pts',(-11.976243391124,-4.36594427220227,3.99406241143229));
#29539=CARTESIAN_POINT('Ctrl Pts',(-12.0226629391517,-3.70051453492894,
4.72144943014433));
#29540=CARTESIAN_POINT('Ctrl Pts',(-12.0690824871793,-2.84935508489923,
5.27892679858222));
#29541=CARTESIAN_POINT('Ctrl Pts',(-12.1155020352069,-1.91665985209559,
5.59825141859108));
#29542=CARTESIAN_POINT('Ctrl Pts',(-12.1619215832345,-0.983964619291893,
5.91757603859996));
#29543=CARTESIAN_POINT('Ctrl Pts',(-12.2083411312621,0.0302663962857454,
5.9987479101798));
#29544=CARTESIAN_POINT('Ctrl Pts',(-12.2547606792897,1.00187700343316,5.83183045058615));
#29545=CARTESIAN_POINT('Ctrl Pts',(-12.3011802273173,1.97348761058057,5.6649129909925));
#29546=CARTESIAN_POINT('Ctrl Pts',(-12.3475997753449,2.90247780929775,5.24990620022537));
#29547=CARTESIAN_POINT('Ctrl Pts',(-12.3940193233726,3.67512608745658,4.63761276689723));
#29548=CARTESIAN_POINT('Ctrl Pts',(-12.4404388714002,4.44777436561531,4.02531933356917));
#29549=CARTESIAN_POINT('Ctrl Pts',(-12.4868584194278,5.06408072321573,3.21573925768014));
#29550=CARTESIAN_POINT('Ctrl Pts',(-12.5332779674554,5.44860056351477,2.30797656696481));
#29551=CARTESIAN_POINT('Ctrl Pts',(-12.579697515483,5.83312040381384,1.40021387624937));
#29552=CARTESIAN_POINT('Ctrl Pts',(-12.6261170635106,5.98585372681148,0.394268570707601));
#29553=CARTESIAN_POINT('Ctrl Pts',(-12.6725366115382,5.88810381808847,-0.586717446309564));
#29554=CARTESIAN_POINT('Ctrl Pts',(-12.7189561595658,5.79035390936548,-1.56770346332667));
#29555=CARTESIAN_POINT('Ctrl Pts',(-12.7653757075934,5.44212076892188,-2.52373019181918));
#29556=CARTESIAN_POINT('Ctrl Pts',(-12.8117952556211,4.88603304812455,-3.3377664668198));
#29557=CARTESIAN_POINT('Ctrl Pts',(-12.8582148036487,4.32994532732723,-4.15180274182043));
#29558=CARTESIAN_POINT('Ctrl Pts',(-12.9046343516763,3.56600302617619,-4.82384856332916));
#29559=CARTESIAN_POINT('Ctrl Pts',(-12.9510538997039,2.68772346464476,-5.27163603751151));
#29560=CARTESIAN_POINT('Ctrl Pts',(-12.9974734477315,1.80944390311323,-5.71942351169391));
#29561=CARTESIAN_POINT('Ctrl Pts',(-13.0438929957591,0.816827081201296,
-5.94295263854987));
#29562=CARTESIAN_POINT('Ctrl Pts',(-13.0903125437867,-0.168616692255152,
-5.91486029805312));
#29563=CARTESIAN_POINT('Ctrl Pts',(-13.1367320918144,-1.15406046571149,
-5.88676795755636));
#29564=CARTESIAN_POINT('Ctrl Pts',(-13.183151639842,-2.13233119071233,-5.60705414970694));
#29565=CARTESIAN_POINT('Ctrl Pts',(-13.2295711878696,-2.98367472316512,
-5.10995979247759));
#29566=CARTESIAN_POINT('Ctrl Pts',(-13.2759907358972,-3.8350182556179,-4.61286543524824));
#29567=CARTESIAN_POINT('Ctrl Pts',(-13.3224102839248,-4.55943459552262,
-3.89839052863896));
#29568=CARTESIAN_POINT('Ctrl Pts',(-13.3688298319524,-5.06824495843351,
-3.05399688534637));
#29569=CARTESIAN_POINT('Ctrl Pts',(-13.41524937998,-5.5770553213444,-2.20960324205378));
#29570=CARTESIAN_POINT('Ctrl Pts',(-13.4616689280076,-5.87025970726146,
-1.23529086207788));
#29571=CARTESIAN_POINT('Ctrl Pts',(-13.5080884760353,-5.91196576104991,
-0.250329332211946));
#29572=CARTESIAN_POINT('Ctrl Pts',(-13.5120172532885,-5.91549560574704,
-0.166965865346676));
#29573=CARTESIAN_POINT('Ctrl Pts',(-13.5159460305418,-5.91722389302913,
-0.0835261154508764));
#29574=CARTESIAN_POINT('Ctrl Pts',(-13.5198748077951,-5.91716619296352,
-8.39733533108955E-5));
#29575=CARTESIAN_POINT('Ctrl Pts',(-13.7716251922048,-5.91724766713751,
-3.36308197105027E-5));
#29576=CARTESIAN_POINT('Ctrl Pts',(-13.7701354937187,-5.9172575149011,-0.0316716319925286));
#29577=CARTESIAN_POINT('Ctrl Pts',(-13.7686457952326,-5.91700910022253,
-0.0633094780020733));
#29578=CARTESIAN_POINT('Ctrl Pts',(-13.7671560967464,-5.91650146876277,
-0.0949431643132593));
#29579=CARTESIAN_POINT('Ctrl Pts',(-13.7207365487188,-5.90068348737519,
-1.08066036459218));
#29580=CARTESIAN_POINT('Ctrl Pts',(-13.6743170006912,-5.63317422231444,
-2.06233862952592));
#29581=CARTESIAN_POINT('Ctrl Pts',(-13.6278974526636,-5.14672058326051,
-2.91980668403996));
#29582=CARTESIAN_POINT('Ctrl Pts',(-13.581477904636,-4.66026694420664,-3.7772747385539));
#29583=CARTESIAN_POINT('Ctrl Pts',(-13.5350583566084,-3.95486893115965,
-4.51053258264816));
#29584=CARTESIAN_POINT('Ctrl Pts',(-13.4886388085808,-3.11687721693247,
-5.02981910697483));
#29585=CARTESIAN_POINT('Ctrl Pts',(-13.4422192605532,-2.27888550270521,
-5.54910563130157));
#29586=CARTESIAN_POINT('Ctrl Pts',(-13.3957997125255,-1.30830008729773,
-5.85442083586066));
#29587=CARTESIAN_POINT('Ctrl Pts',(-13.3493801644979,-0.323934324437635,
-5.90838983038297));
#29588=CARTESIAN_POINT('Ctrl Pts',(-13.3029606164703,0.660431438422463,
-5.96235882490529));
#29589=CARTESIAN_POINT('Ctrl Pts',(-13.2565410684427,1.65857754873518,-5.76498160939082));
#29590=CARTESIAN_POINT('Ctrl Pts',(-13.2101215204151,2.54831683472379,-5.34041994080851));
#29591=CARTESIAN_POINT('Ctrl Pts',(-13.1637019723875,3.43805612071233,-4.91585827222623));
#29592=CARTESIAN_POINT('Ctrl Pts',(-13.1172824243599,4.21938858237678,-4.26411215057615));
#29593=CARTESIAN_POINT('Ctrl Pts',(-13.0708628763323,4.79666809865151,-3.46496449991928));
#29594=CARTESIAN_POINT('Ctrl Pts',(-13.0244433283046,5.37394761492623,-2.6658168492624));
#29595=CARTESIAN_POINT('Ctrl Pts',(-12.978023780277,5.74717418581124,-1.71926766959874));
#29596=CARTESIAN_POINT('Ctrl Pts',(-12.9316042322494,5.87065961129535,-0.741187940152418));
#29597=CARTESIAN_POINT('Ctrl Pts',(-12.8851846842218,5.99414503677946,0.236891789293961));
#29598=CARTESIAN_POINT('Ctrl Pts',(-12.8387651361942,5.86788931686263,1.24650206852301));
#29599=CARTESIAN_POINT('Ctrl Pts',(-12.7923455881666,5.50734793364101,2.16405234967687));
#29600=CARTESIAN_POINT('Ctrl Pts',(-12.745926040139,5.14680655041941,3.08160263083068));
#29601=CARTESIAN_POINT('Ctrl Pts',(-12.6995064921114,4.55197950389303,3.90709291390932));
#29602=CARTESIAN_POINT('Ctrl Pts',(-12.6530869440837,3.79568201996964,4.53947153726081));
#29603=CARTESIAN_POINT('Ctrl Pts',(-12.6066673960561,3.03938453604625,5.17185016061231));
#29604=CARTESIAN_POINT('Ctrl Pts',(-12.5602478480285,2.12161661472584,5.61111712423666));
#29605=CARTESIAN_POINT('Ctrl Pts',(-12.5138283000009,1.15472600299149,5.8034999519546));
#29606=CARTESIAN_POINT('Ctrl Pts',(-12.4674087519733,0.187835391257087,
5.99588277967256));
#29607=CARTESIAN_POINT('Ctrl Pts',(-12.4209892039457,-0.828177910891272,
5.9413814714841));
#29608=CARTESIAN_POINT('Ctrl Pts',(-12.3745696559181,-1.76893953521789,
5.64666775674512));
#29609=CARTESIAN_POINT('Ctrl Pts',(-12.3281501078905,-2.70970115954445,
5.35195404200617));
#29610=CARTESIAN_POINT('Ctrl Pts',(-12.2817305598628,-3.57521110604927,
4.81702792071674));
#29611=CARTESIAN_POINT('Ctrl Pts',(-12.2353110118352,-4.25951874143788,
4.10737190009151));
#29612=CARTESIAN_POINT('Ctrl Pts',(-12.1888914638076,-4.94382637682645,
3.39771587946632));
#29613=CARTESIAN_POINT('Ctrl Pts',(-12.14247191578,-5.44693170109882,2.51332995950535));
#29614=CARTESIAN_POINT('Ctrl Pts',(-12.0960523677524,-5.70724752171524,
1.56247545907036));
#29615=CARTESIAN_POINT('Ctrl Pts',(-12.0712433092366,-5.8463740470841,1.05428858643384));
#29616=CARTESIAN_POINT('Ctrl Pts',(-12.0464342507207,-5.91615022215936,
0.527115640388131));
#29617=CARTESIAN_POINT('Ctrl Pts',(-12.0216251922048,-5.916248517546,-3.1785587739037E-5));
#29618=CARTESIAN_POINT('Origin',(-29.75,0.,0.));
#29619=CARTESIAN_POINT('',(-10.0198748077951,-5.91722893930563,5.01660477857623E-5));
#29620=CARTESIAN_POINT('',(-10.2716251922049,-5.91712979830057,9.76190556973378E-5));
#29621=CARTESIAN_POINT('',(-29.75,-5.91675,-7.2459289488551E-16));
#29622=CARTESIAN_POINT('Ctrl Pts',(-10.0198748077951,-5.91722893930563,
5.01660477857623E-5));
#29623=CARTESIAN_POINT('Ctrl Pts',(-10.0221239965182,-5.91725026066663,
0.0478185513098333));
#29624=CARTESIAN_POINT('Ctrl Pts',(-10.0243731852412,-5.91668394546353,
0.0955864297295038));
#29625=CARTESIAN_POINT('Ctrl Pts',(-10.0266223739643,-5.91552682193497,
0.143339992186572));
#29626=CARTESIAN_POINT('Ctrl Pts',(-10.0730419219919,-5.89164569952976,
1.12889481168223));
#29627=CARTESIAN_POINT('Ctrl Pts',(-10.1194614700195,-5.61611475547292,
2.10835186768951));
#29628=CARTESIAN_POINT('Ctrl Pts',(-10.1658810180471,-5.12266286617188,
2.96181179245674));
#29629=CARTESIAN_POINT('Ctrl Pts',(-10.2123005660748,-4.62921097687081,
3.81527171722401));
#29630=CARTESIAN_POINT('Ctrl Pts',(-10.2587201141024,-3.91783814232551,
4.54273451075121));
#29631=CARTESIAN_POINT('Ctrl Pts',(-10.30513966213,-3.0756264378292,5.0551484596714));
#29632=CARTESIAN_POINT('Ctrl Pts',(-10.3515592101576,-2.23341473333289,
5.56756240859159));
#29633=CARTESIAN_POINT('Ctrl Pts',(-10.3979787581852,-1.26036415888558,
5.86492751290477));
#29634=CARTESIAN_POINT('Ctrl Pts',(-10.4443983062128,-0.275589838474683,
5.91084208681991));
#29635=CARTESIAN_POINT('Ctrl Pts',(-10.4908178542404,0.709184481936216,
5.95675666073506));
#29636=CARTESIAN_POINT('Ctrl Pts',(-10.537237402268,1.7056825483107,5.75122070425218));
#29637=CARTESIAN_POINT('Ctrl Pts',(-10.5836569502957,2.59191893271063,5.31939471938756));
#29638=CARTESIAN_POINT('Ctrl Pts',(-10.6300764983233,3.47815531711046,4.88756873452299));
#29639=CARTESIAN_POINT('Ctrl Pts',(-10.6764960463509,4.25413001953575,4.22945272127673));
#29640=CARTESIAN_POINT('Ctrl Pts',(-10.7229155943785,4.82485278427143,3.42560936834607));
#29641=CARTESIAN_POINT('Ctrl Pts',(-10.7693351424061,5.39557554900716,2.62176601541532));
#29642=CARTESIAN_POINT('Ctrl Pts',(-10.8157546904337,5.76104637605323,1.67219532280013));
#29643=CARTESIAN_POINT('Ctrl Pts',(-10.8621742384613,5.87652647790919,0.693138145555667));
#29644=CARTESIAN_POINT('Ctrl Pts',(-10.908593786489,5.99200657976514,-0.285919031688796));
#29645=CARTESIAN_POINT('Ctrl Pts',(-10.9550133345166,5.857495956431,-1.29446269356253));
#29646=CARTESIAN_POINT('Ctrl Pts',(-11.0014328825442,5.48946060669121,-2.20903286122626));
#29647=CARTESIAN_POINT('Ctrl Pts',(-11.0478524305718,5.12142525695144,-3.12360302888994));
#29648=CARTESIAN_POINT('Ctrl Pts',(-11.0942719785994,4.51986518080605,-3.94419970234363));
#29649=CARTESIAN_POINT('Ctrl Pts',(-11.140691526627,3.75841982201842,-4.57037026682205));
#29650=CARTESIAN_POINT('Ctrl Pts',(-11.1871110746546,2.99697446323079,-5.19654083130047));
#29651=CARTESIAN_POINT('Ctrl Pts',(-11.2335306226822,2.07564382180092,-5.62828528680363));
#29652=CARTESIAN_POINT('Ctrl Pts',(-11.2799501707098,1.10721177193765,-5.81275201831927));
#29653=CARTESIAN_POINT('Ctrl Pts',(-11.3263697187375,0.138779722074373,
-5.99721874983492));
#29654=CARTESIAN_POINT('Ctrl Pts',(-11.3727892667651,-0.8767537362223,-5.93440775736305));
#29655=CARTESIAN_POINT('Ctrl Pts',(-11.4192088147927,-1.81507297437667,
-5.63200799289912));
#29656=CARTESIAN_POINT('Ctrl Pts',(-11.4656283628203,-2.75339221253104,
-5.32960822843518));
#29657=CARTESIAN_POINT('Ctrl Pts',(-11.5120479108479,-3.61449723054312,
-4.78761969197916));
#29658=CARTESIAN_POINT('Ctrl Pts',(-11.5584674588755,-4.29297662053726,
-4.07238943004136));
#29659=CARTESIAN_POINT('Ctrl Pts',(-11.6048870069031,-4.97145601053144,
-3.35715916810351));
#29660=CARTESIAN_POINT('Ctrl Pts',(-11.6513065549308,-5.46730977250767,
-2.46868718068385));
#29661=CARTESIAN_POINT('Ctrl Pts',(-11.6977261029584,-5.71983840750006,
-1.51573497897201));
#29662=CARTESIAN_POINT('Ctrl Pts',(-11.7217756712373,-5.85067131966066,
-1.02201864575865));
#29663=CARTESIAN_POINT('Ctrl Pts',(-11.7458252395162,-5.91619121974183,
-0.510994617827731));
#29664=CARTESIAN_POINT('Ctrl Pts',(-11.7698748077951,-5.91624143118648,
1.67735000153324E-5));
#29665=CARTESIAN_POINT('Ctrl Pts',(-12.0216251922048,-5.916248517546,-3.1785587739037E-5));
#29666=CARTESIAN_POINT('Ctrl Pts',(-12.0000147026931,-5.9163341399577,-0.459215430663503));
#29667=CARTESIAN_POINT('Ctrl Pts',(-11.9784042131813,-5.86355046136694,
-0.918379711943183));
#29668=CARTESIAN_POINT('Ctrl Pts',(-11.9567937236695,-5.75768100403336,
-1.36495908001494));
#29669=CARTESIAN_POINT('Ctrl Pts',(-11.9103741756419,-5.53027234877463,
-2.32421603775583));
#29670=CARTESIAN_POINT('Ctrl Pts',(-11.8639546276143,-5.05792872129679,
-3.22540687232847));
#29671=CARTESIAN_POINT('Ctrl Pts',(-11.8175350795867,-4.39847164828013,
-3.95821310613738));
#29672=CARTESIAN_POINT('Ctrl Pts',(-11.7711155315591,-3.73901457526351,
-4.69101933994624));
#29673=CARTESIAN_POINT('Ctrl Pts',(-11.7246959835315,-2.89244405670809,
-5.25544097299139));
#29674=CARTESIAN_POINT('Ctrl Pts',(-11.6782764355039,-1.9623922726155,-5.5823848311184));
#29675=CARTESIAN_POINT('Ctrl Pts',(-11.6318568874763,-1.03234048852291,
-5.90932868924541));
#29676=CARTESIAN_POINT('Ctrl Pts',(-11.5854373394486,-0.0188074388931536,
-5.99879477245428));
#29677=CARTESIAN_POINT('Ctrl Pts',(-11.539017791421,0.954136125952757,-5.83983116943235));
#29678=CARTESIAN_POINT('Ctrl Pts',(-11.4925982433934,1.92707969079872,-5.68086756641042));
#29679=CARTESIAN_POINT('Ctrl Pts',(-11.4461786953658,2.85943377086084,-5.27347427715765));
#29680=CARTESIAN_POINT('Ctrl Pts',(-11.3997591473382,3.63706506745639,-4.66752199024389));
#29681=CARTESIAN_POINT('Ctrl Pts',(-11.3533395993106,4.41469636405186,-4.06156970333021));
#29682=CARTESIAN_POINT('Ctrl Pts',(-11.306920051283,5.03760487718081,-3.25705841875559));
#29683=CARTESIAN_POINT('Ctrl Pts',(-11.2605005032554,5.42953781308038,-2.35247167265668));
#29684=CARTESIAN_POINT('Ctrl Pts',(-11.2140809552277,5.82147074898,-1.44788492655767));
#29685=CARTESIAN_POINT('Ctrl Pts',(-11.1676614072001,5.9824281076502,-0.44322271893434));
#29686=CARTESIAN_POINT('Ctrl Pts',(-11.1212418591725,5.89270643663109,0.538530116157276));
#29687=CARTESIAN_POINT('Ctrl Pts',(-11.0748223111449,5.80298476561198,1.52028295124889));
#29688=CARTESIAN_POINT('Ctrl Pts',(-11.0284027631173,5.46258406490356,2.4791264138088));
#29689=CARTESIAN_POINT('Ctrl Pts',(-10.9819832150897,4.91317418470176,3.29768453086436));
#29690=CARTESIAN_POINT('Ctrl Pts',(-10.9355636670621,4.36376430449999,4.11624264791987));
#29691=CARTESIAN_POINT('Ctrl Pts',(-10.8891441190345,3.60534524480486,4.79451541947105));
#29692=CARTESIAN_POINT('Ctrl Pts',(-10.8427245710069,2.73075820288027,5.24947268511076));
#29693=CARTESIAN_POINT('Ctrl Pts',(-10.7963050229792,1.85617116095567,5.70442995075048));
#29694=CARTESIAN_POINT('Ctrl Pts',(-10.7498854749516,0.865416136801603,
5.93607171047874));
#29695=CARTESIAN_POINT('Ctrl Pts',(-10.703465926924,-0.120224471069116,
5.91604174350367));
#29696=CARTESIAN_POINT('Ctrl Pts',(-10.6570463788964,-1.10586507893989,
5.8960117765286));
#29697=CARTESIAN_POINT('Ctrl Pts',(-10.6106268308688,-2.08639127052732,
5.62431008285018));
#29698=CARTESIAN_POINT('Ctrl Pts',(-10.5642072828412,-2.94177280079486,
5.13419678458329));
#29699=CARTESIAN_POINT('Ctrl Pts',(-10.5177877348136,-3.79715433106241,
4.64408348631641));
#29700=CARTESIAN_POINT('Ctrl Pts',(-10.471368186786,-4.52739120001007,3.93555858346107));
#29701=CARTESIAN_POINT('Ctrl Pts',(-10.4249486387583,-5.04309210828604,
3.09535552427583));
#29702=CARTESIAN_POINT('Ctrl Pts',(-10.3785290907307,-5.55879301656195,
2.25515246509068));
#29703=CARTESIAN_POINT('Ctrl Pts',(-10.3321095427031,-5.85995796416621,
1.28327124957567));
#29704=CARTESIAN_POINT('Ctrl Pts',(-10.2856899946755,-5.90972011085785,
0.298683855680485));
#29705=CARTESIAN_POINT('Ctrl Pts',(-10.2810017271853,-5.91474597311827,
0.199242795476116));
#29706=CARTESIAN_POINT('Ctrl Pts',(-10.2763134596951,-5.91720739231159,
0.0996721254546018));
#29707=CARTESIAN_POINT('Ctrl Pts',(-10.2716251922049,-5.91712979830057,
9.76190556973378E-5));
#29708=CARTESIAN_POINT('Origin',(-29.75,0.,0.));
#29709=CARTESIAN_POINT('',(-8.26987480779513,-5.91634522401586,-9.88515524452672E-5));
#29710=CARTESIAN_POINT('',(-8.52162519220486,-5.9164576885749,-0.000131435617752113));
#29711=CARTESIAN_POINT('',(-29.75,-5.91675,-7.2459289488551E-16));
#29712=CARTESIAN_POINT('Ctrl Pts',(-8.26987480779513,-5.91634522401586,
-9.88515524452672E-5));
#29713=CARTESIAN_POINT('Ctrl Pts',(-8.29842275352017,-5.91598626571606,
0.606464769270553));
#29714=CARTESIAN_POINT('Ctrl Pts',(-8.32697069924521,-5.82322044315546,
1.21313569281818));
#29715=CARTESIAN_POINT('Ctrl Pts',(-8.35551864497026,-5.63971267484951,
1.7909899160894));
#29716=CARTESIAN_POINT('Ctrl Pts',(-8.40193819299787,-5.34132526209617,
2.73059279079175));
#29717=CARTESIAN_POINT('Ctrl Pts',(-8.4483577410255,-4.80302131586862,3.59400595212951));
#29718=CARTESIAN_POINT('Ctrl Pts',(-8.49477728905311,-4.0906968368287,4.27553544290674));
#29719=CARTESIAN_POINT('Ctrl Pts',(-8.54119683708072,-3.37837235778882,
4.95706493368393));
#29720=CARTESIAN_POINT('Ctrl Pts',(-8.58761638510832,-2.49202734593661,
5.45671075390062));
#29721=CARTESIAN_POINT('Ctrl Pts',(-8.63403593313593,-1.54016294063202,
5.71330920314101));
#29722=CARTESIAN_POINT('Ctrl Pts',(-8.68045548116354,-0.588298535327425,
5.96990765238141));
#29723=CARTESIAN_POINT('Ctrl Pts',(-8.72687502919116,0.429085263429556,
5.98345873064552));
#29724=CARTESIAN_POINT('Ctrl Pts',(-8.77329457721878,1.3874463192751,5.75230359469335));
#29725=CARTESIAN_POINT('Ctrl Pts',(-8.81971412524639,2.34580737512064,5.52114845874118));
#29726=CARTESIAN_POINT('Ctrl Pts',(-8.86613367327399,3.24514568805474,5.04528710857274));
#29727=CARTESIAN_POINT('Ctrl Pts',(-8.91255322130161,3.97536955527705,4.38297168977492));
#29728=CARTESIAN_POINT('Ctrl Pts',(-8.95897276932922,4.70559342249941,3.72065627097706));
#29729=CARTESIAN_POINT('Ctrl Pts',(-9.00539231735684,5.26670284400996,2.8718867835498));
#29730=CARTESIAN_POINT('Ctrl Pts',(-9.05181186538445,5.5900101070948,1.94056459232104));
#29731=CARTESIAN_POINT('Ctrl Pts',(-9.09823141341206,5.91331737017962,1.00924240109232));
#29732=CARTESIAN_POINT('Ctrl Pts',(-9.14465096143967,5.99882247483874,-0.00463249393789208));
#29733=CARTESIAN_POINT('Ctrl Pts',(-9.19107050946728,5.83605838943942,-0.976947495746754));
#29734=CARTESIAN_POINT('Ctrl Pts',(-9.23749005749489,5.67329430404009,-1.94926249755562));
#29735=CARTESIAN_POINT('Ctrl Pts',(-9.28390960552251,5.26226102858231,-2.88001760614312));
#29736=CARTESIAN_POINT('Ctrl Pts',(-9.33032915355012,4.65327483732233,-3.65527525950303));
#29737=CARTESIAN_POINT('Ctrl Pts',(-9.37674870157774,4.04428864606231,-4.43053291286298));
#29738=CARTESIAN_POINT('Ctrl Pts',(-9.42316824960535,3.23734953900007,-5.05029311099531));
#29739=CARTESIAN_POINT('Ctrl Pts',(-9.46958779763296,2.33123825201114,-5.43868845832818));
#29740=CARTESIAN_POINT('Ctrl Pts',(-9.51600734566057,1.42512696502221,-5.82708380566105));
#29741=CARTESIAN_POINT('Ctrl Pts',(-9.56242689368819,0.419843498106589,
-5.98411430219445));
#29742=CARTESIAN_POINT('Ctrl Pts',(-9.6088464417158,-0.561551263773847,
-5.89055719881796));
#29743=CARTESIAN_POINT('Ctrl Pts',(-9.65526598974341,-1.54294602565423,
-5.79700009544146));
#29744=CARTESIAN_POINT('Ctrl Pts',(-9.70168553777102,-2.50045208249942,
-5.45285539215509));
#29745=CARTESIAN_POINT('Ctrl Pts',(-9.74810508579863,-3.31685717867248,
-4.90025125791331));
#29746=CARTESIAN_POINT('Ctrl Pts',(-9.79452463382625,-4.13326227484553,
-4.34764712367153));
#29747=CARTESIAN_POINT('Ctrl Pts',(-9.84094418185386,-4.80856641034645,
-3.58658355847433));
#29748=CARTESIAN_POINT('Ctrl Pts',(-9.88736372988147,-5.26010282772011,
-2.71022548438372));
#29749=CARTESIAN_POINT('Ctrl Pts',(-9.93153408918603,-5.68976073353647,
-1.87633001023987));
#29750=CARTESIAN_POINT('Ctrl Pts',(-9.97570444849058,-5.91681022291855,
-0.938042186448962));
#29751=CARTESIAN_POINT('Ctrl Pts',(-10.0198748077951,-5.91722893930563,
5.01660477857623E-5));
#29752=CARTESIAN_POINT('Ctrl Pts',(-10.2716251922049,-5.91712979830057,
9.76190556973378E-5));
#29753=CARTESIAN_POINT('Ctrl Pts',(-10.2298939116675,-5.91643911726574,
-0.886236548007039));
#29754=CARTESIAN_POINT('Ctrl Pts',(-10.1881626311301,-5.71457825033594,
-1.7728746775507));
#29755=CARTESIAN_POINT('Ctrl Pts',(-10.1464313505927,-5.3294818102357,-2.5711140520577));
#29756=CARTESIAN_POINT('Ctrl Pts',(-10.1000118025651,-4.90112201714299,
-3.45903099362507));
#29757=CARTESIAN_POINT('Ctrl Pts',(-10.0535922545374,-4.24604308517861,
-4.2375713044844));
#29758=CARTESIAN_POINT('Ctrl Pts',(-10.0071727065098,-3.44443592142545,
-4.81143066223716));
#29759=CARTESIAN_POINT('Ctrl Pts',(-9.96075315848222,-2.64282875767234,
-5.38529001998988));
#29760=CARTESIAN_POINT('Ctrl Pts',(-9.91433361045461,-1.69469336213048,
-5.75446842463606));
#29761=CARTESIAN_POINT('Ctrl Pts',(-9.867914062427,-0.716094889235394,-5.87377322884811));
#29762=CARTESIAN_POINT('Ctrl Pts',(-9.82149451439938,0.26250358365986,-5.99307803306019));
#29763=CARTESIAN_POINT('Ctrl Pts',(-9.77507496637177,1.27156513390835,-5.86250923683805));
#29764=CARTESIAN_POINT('Ctrl Pts',(-9.72865541834415,2.18756638582422,-5.49805030369255));
#29765=CARTESIAN_POINT('Ctrl Pts',(-9.68223587031654,3.10356763774005,-5.13359137054708));
#29766=CARTESIAN_POINT('Ctrl Pts',(-9.63581632228892,3.92650859132326,-4.53524230047826));
#29767=CARTESIAN_POINT('Ctrl Pts',(-9.58939677426131,4.55564965883346,-3.77624946478545));
#29768=CARTESIAN_POINT('Ctrl Pts',(-9.5429772262337,5.18479072634363,-3.01725662909268));
#29769=CARTESIAN_POINT('Ctrl Pts',(-9.49655767820609,5.62013190778081,-2.09762002777593));
#29770=CARTESIAN_POINT('Ctrl Pts',(-9.45013813017848,5.80838129811409,-1.12991616062445));
#29771=CARTESIAN_POINT('Ctrl Pts',(-9.40371858215087,5.99663068844738,-0.162212293472971));
#29772=CARTESIAN_POINT('Ctrl Pts',(-9.35729903412325,5.93778828767677,0.853558839513239));
#29773=CARTESIAN_POINT('Ctrl Pts',(-9.31087948609563,5.63905723616061,1.79305251502193));
#29774=CARTESIAN_POINT('Ctrl Pts',(-9.26445993806802,5.34032618464443,2.73254619053068));
#29775=CARTESIAN_POINT('Ctrl Pts',(-9.21804039004041,4.80170648238268,3.5957624085619));
#29776=CARTESIAN_POINT('Ctrl Pts',(-9.1716208420128,4.08913278303239,4.27703132056005));
#29777=CARTESIAN_POINT('Ctrl Pts',(-9.12520129398519,3.37655908368215,4.95830023255815));
#29778=CARTESIAN_POINT('Ctrl Pts',(-9.07878174595758,2.49003138724338,5.45762183852321));
#29779=CARTESIAN_POINT('Ctrl Pts',(-9.03236219792996,1.53807319624787,5.7138721264398));
#29780=CARTESIAN_POINT('Ctrl Pts',(-8.98594264990235,0.586115005252362,
5.9701224143564));
#29781=CARTESIAN_POINT('Ctrl Pts',(-8.93952310187473,-0.431273680299897,
5.98330138422453));
#29782=CARTESIAN_POINT('Ctrl Pts',(-8.89310355384712,-1.38955012583237,
5.75179574412384));
#29783=CARTESIAN_POINT('Ctrl Pts',(-8.84668400581951,-2.3478265713649,5.52029010402313));
#29784=CARTESIAN_POINT('Ctrl Pts',(-8.8002644577919,-3.24699077687763,5.04409985395356));
#29785=CARTESIAN_POINT('Ctrl Pts',(-8.75384490976429,-3.97697235277594,
4.38151740149205));
#29786=CARTESIAN_POINT('Ctrl Pts',(-8.70742536173668,-4.70695392867421,
3.71893494903058));
#29787=CARTESIAN_POINT('Ctrl Pts',(-8.66100581370906,-5.26775287495808,
2.86996029417718));
#29788=CARTESIAN_POINT('Ctrl Pts',(-8.61458626568145,-5.59071948546345,
1.93851991714843));
#29789=CARTESIAN_POINT('Ctrl Pts',(-8.58359924118925,-5.80631344738524,
1.31674381198596));
#29790=CARTESIAN_POINT('Ctrl Pts',(-8.55261221669705,-5.91592620827154,
0.658219901896991));
#29791=CARTESIAN_POINT('Ctrl Pts',(-8.52162519220486,-5.9164576885749,-0.000131435617752112));
#29792=CARTESIAN_POINT('Origin',(-29.75,0.,0.));
#29793=CARTESIAN_POINT('',(-6.51987480779513,-5.91690427471314,0.000144985681112611));
#29794=CARTESIAN_POINT('',(-6.77162519220487,-5.916739287675,0.000155466350801038));
#29795=CARTESIAN_POINT('',(-29.75,-5.91675,-7.2459289488551E-16));
#29796=CARTESIAN_POINT('Ctrl Pts',(-6.51987480779513,-5.91690427471314,
0.000144985681112611));
#29797=CARTESIAN_POINT('Ctrl Pts',(-6.52830196249454,-5.91708722319681,
0.179149749583483));
#29798=CARTESIAN_POINT('Ctrl Pts',(-6.53672911719395,-5.9091261911554,0.35813830044998));
#29799=CARTESIAN_POINT('Ctrl Pts',(-6.54515627189336,-5.89290301795475,
0.536374827309976));
#29800=CARTESIAN_POINT('Ctrl Pts',(-6.59157581992097,-5.80354042827781,
1.51816041378229));
#29801=CARTESIAN_POINT('Ctrl Pts',(-6.63799536794859,-5.46349044623204,
2.47712831491668));
#29802=CARTESIAN_POINT('Ctrl Pts',(-6.68441491597621,-4.91437998909899,
3.29588732470264));
#29803=CARTESIAN_POINT('Ctrl Pts',(-6.73083446400383,-4.36526953196594,
4.1146463344886));
#29804=CARTESIAN_POINT('Ctrl Pts',(-6.77725401203144,-3.60709859974563,
4.79319645292615));
#29805=CARTESIAN_POINT('Ctrl Pts',(-6.82367356005905,-2.73267801539693,
5.24847356843477));
#29806=CARTESIAN_POINT('Ctrl Pts',(-6.87009310808666,-1.85825743104829,
5.70375068394336));
#29807=CARTESIAN_POINT('Ctrl Pts',(-6.91651265611427,-0.867587194571285,
5.93575479652306));
#29808=CARTESIAN_POINT('Ctrl Pts',(-6.96293220414188,0.118060674729629,
5.9160853282787));
#29809=CARTESIAN_POINT('Ctrl Pts',(-7.00935175216949,1.10370854403049,5.89641586003434));
#29810=CARTESIAN_POINT('Ctrl Pts',(-7.0557713001971,2.08433404615525,5.62507281096596));
#29811=CARTESIAN_POINT('Ctrl Pts',(-7.10219084822471,2.93989477905598,5.13527240002626));
#29812=CARTESIAN_POINT('Ctrl Pts',(-7.14861039625233,3.79545551195686,4.64547198908647));
#29813=CARTESIAN_POINT('Ctrl Pts',(-7.19502994427994,4.52595147563366,3.93721421627529));
#29814=CARTESIAN_POINT('Ctrl Pts',(-7.24144949230756,5.04195965388283,3.09719982936359));
#29815=CARTESIAN_POINT('Ctrl Pts',(-7.28786904033517,5.55796783213196,2.25718544245194));
#29816=CARTESIAN_POINT('Ctrl Pts',(-7.33428858836279,5.8594882249535,1.28541444143978));
#29817=CARTESIAN_POINT('Ctrl Pts',(-7.3807081363904,5.90961048059508,0.300845312466115));
#29818=CARTESIAN_POINT('Ctrl Pts',(-7.42712768441801,5.95973273623666,-0.683723816507492));
#29819=CARTESIAN_POINT('Ctrl Pts',(-7.47354723244562,5.75845685469833,-1.6810910734426));
#29820=CARTESIAN_POINT('Ctrl Pts',(-7.51996678047324,5.33042184469627,-2.56916462920867));
#29821=CARTESIAN_POINT('Ctrl Pts',(-7.56638632850085,4.90238683469421,-3.45723818497473));
#29822=CARTESIAN_POINT('Ctrl Pts',(-7.61280587652846,4.24759269622844,-4.23601803957176));
#29823=CARTESIAN_POINT('Ctrl Pts',(-7.65922542455607,3.44619547363803,-4.81017054706679));
#29824=CARTESIAN_POINT('Ctrl Pts',(-7.70564497258368,2.64479825104767,-5.38432305456179));
#29825=CARTESIAN_POINT('Ctrl Pts',(-7.75206452061129,1.6967979443327,-5.75384821495482));
#29826=CARTESIAN_POINT('Ctrl Pts',(-7.79848406863889,0.718243171149578,
-5.87351093312076));
#29827=CARTESIAN_POINT('Ctrl Pts',(-7.84490361666651,-0.260311602033657,
-5.99317365128671));
#29828=CARTESIAN_POINT('Ctrl Pts',(-7.89132316469413,-1.26942084168505,
-5.86297392722552));
#29829=CARTESIAN_POINT('Ctrl Pts',(-7.93774271272174,-2.18555533426276,
-5.49885004480643));
#29830=CARTESIAN_POINT('Ctrl Pts',(-7.98416226074936,-3.10168982684046,
-5.13472616238734));
#29831=CARTESIAN_POINT('Ctrl Pts',(-8.03058180877697,-3.92484957234447,
-4.53667812161035));
#29832=CARTESIAN_POINT('Ctrl Pts',(-8.07700135680458,-4.55426819981524,
-3.77791544354075));
#29833=CARTESIAN_POINT('Ctrl Pts',(-8.1234209048322,-5.18368682728602,-3.01915276547114));
#29834=CARTESIAN_POINT('Ctrl Pts',(-8.16984045285981,-5.61936433672356,
-2.09967545010891));
#29835=CARTESIAN_POINT('Ctrl Pts',(-8.21626000088743,-5.80796765180276,
-1.13204049839432));
#29836=CARTESIAN_POINT('Ctrl Pts',(-8.23413160319,-5.88058023816478,-0.75949945122988));
#29837=CARTESIAN_POINT('Ctrl Pts',(-8.25200320549256,-5.91656993930847,
-0.379820177456627));
#29838=CARTESIAN_POINT('Ctrl Pts',(-8.26987480779513,-5.91634522401586,
-9.88515524452672E-5));
#29839=CARTESIAN_POINT('Ctrl Pts',(-8.52162519220486,-5.9164576885749,-0.000131435617752112));
#29840=CARTESIAN_POINT('Ctrl Pts',(-8.50619266866945,-5.91672238266621,
-0.328011336229925));
#29841=CARTESIAN_POINT('Ctrl Pts',(-8.49076014513403,-5.88993102800002,
-0.655848432687641));
#29842=CARTESIAN_POINT('Ctrl Pts',(-8.47532762159862,-5.83570067282893,
-0.979081963609703));
#29843=CARTESIAN_POINT('Ctrl Pts',(-8.42890807357101,-5.67258097496215,
-1.95133736813505));
#29844=CARTESIAN_POINT('Ctrl Pts',(-8.38248852554339,-5.26120730450169,
-2.88194207798159));
#29845=CARTESIAN_POINT('Ctrl Pts',(-8.33606897751578,-4.65193760485649,
-3.65697694207167));
#29846=CARTESIAN_POINT('Ctrl Pts',(-8.28964942948816,-4.04266790521129,
-4.43201180616177));
#29847=CARTESIAN_POINT('Ctrl Pts',(-8.24322988146054,-3.23550217638136,
-5.05147682449541));
#29848=CARTESIAN_POINT('Ctrl Pts',(-8.19681033343293,-2.32924889594513,
-5.43954073567431));
#29849=CARTESIAN_POINT('Ctrl Pts',(-8.15039078540532,-1.42299561550895,
-5.82760464685319));
#29850=CARTESIAN_POINT('Ctrl Pts',(-8.10397123737771,-0.417654783466492,
-5.98426745087736));
#29851=CARTESIAN_POINT('Ctrl Pts',(-8.0575516893501,0.563705692919205,-5.89035140938912));
#29852=CARTESIAN_POINT('Ctrl Pts',(-8.01113214132249,1.5450661693049,-5.79643536790087));
#29853=CARTESIAN_POINT('Ctrl Pts',(-7.96471259329487,2.50244629003383,-5.45194048090022));
#29854=CARTESIAN_POINT('Ctrl Pts',(-7.91829304526726,3.31864921582715,-4.89903778477077));
#29855=CARTESIAN_POINT('Ctrl Pts',(-7.87187349723965,4.13485214162051,-4.34613508864129));
#29856=CARTESIAN_POINT('Ctrl Pts',(-7.82545394921204,4.80987787247824,-3.58482458338298));
#29857=CARTESIAN_POINT('Ctrl Pts',(-7.77903440118442,5.26109373160295,-2.70830142000666));
#29858=CARTESIAN_POINT('Ctrl Pts',(-7.73261485315681,5.71230959072763,-1.83177825663038));
#29859=CARTESIAN_POINT('Ctrl Pts',(-7.6861953051292,5.93971557811932,-0.840042435136087));
#29860=CARTESIAN_POINT('Ctrl Pts',(-7.63977575710159,5.91547399130399,0.145503582525929));
#29861=CARTESIAN_POINT('Ctrl Pts',(-7.59335620907397,5.89123240448867,1.13104960018795));
#29862=CARTESIAN_POINT('Ctrl Pts',(-7.54693666104636,5.61534324346633,2.11040581401769));
#29863=CARTESIAN_POINT('Ctrl Pts',(-7.50051711301874,5.12157923545686,2.9636852007693));
#29864=CARTESIAN_POINT('Ctrl Pts',(-7.45409756499113,4.62781522744736,3.81696458752096));
#29865=CARTESIAN_POINT('Ctrl Pts',(-7.40767801696354,3.91617637245083,4.54416714719437));
#29866=CARTESIAN_POINT('Ctrl Pts',(-7.36125846893592,3.07377731041813,5.05627302271945));
#29867=CARTESIAN_POINT('Ctrl Pts',(-7.31483892090831,2.23137824838549,5.56837889824451));
#29868=CARTESIAN_POINT('Ctrl Pts',(-7.26841937288069,1.25821897931661,5.86538808962119));
#29869=CARTESIAN_POINT('Ctrl Pts',(-7.22199982485307,0.273427932955036,
5.91094247982517));
#29870=CARTESIAN_POINT('Ctrl Pts',(-7.17558027682546,-0.71136311340654,
5.95649687002916));
#29871=CARTESIAN_POINT('Ctrl Pts',(-7.12916072879785,-1.70778593706098,
5.75059645906052));
#29872=CARTESIAN_POINT('Ctrl Pts',(-7.08274118077024,-2.59386432084106,
5.31844636330852));
#29873=CARTESIAN_POINT('Ctrl Pts',(-7.03632163274263,-3.47994270462119,
4.88629626755649));
#29874=CARTESIAN_POINT('Ctrl Pts',(-6.98990208471501,-4.25567664852695,
4.22789648702108));
#29875=CARTESIAN_POINT('Ctrl Pts',(-6.9434825366874,-4.82610536908409,3.42384444752088));
#29876=CARTESIAN_POINT('Ctrl Pts',(-6.89706298865978,-5.39653408964123,
2.61979240802068));
#29877=CARTESIAN_POINT('Ctrl Pts',(-6.85064344063217,-5.76165758684977,
1.67008810955569));
#29878=CARTESIAN_POINT('Ctrl Pts',(-6.80422389260456,-5.87677959128358,
0.690988762422807));
#29879=CARTESIAN_POINT('Ctrl Pts',(-6.793357659138,-5.90372820734017,0.46179389635958));
#29880=CARTESIAN_POINT('Ctrl Pts',(-6.78249142567143,-5.9169775084423,0.23098827179514));
#29881=CARTESIAN_POINT('Ctrl Pts',(-6.77162519220487,-5.916739287675,0.000155466350801038));
#29882=CARTESIAN_POINT('Origin',(-29.75,0.,0.));
#29883=CARTESIAN_POINT('',(-4.76987480779513,-5.91668395451438,-0.000155206356347026));
#29884=CARTESIAN_POINT('',(-5.02162519220488,-5.91684860187072,-0.000150428407648674));
#29885=CARTESIAN_POINT('',(-29.75,-5.91675,-7.2459289488551E-16));
#29886=CARTESIAN_POINT('Ctrl Pts',(-4.76987480779513,-5.91668395451438,
-0.000155206356347026));
#29887=CARTESIAN_POINT('Ctrl Pts',(-4.80460071949653,-5.9159368893773,0.737551676700471));
#29888=CARTESIAN_POINT('Ctrl Pts',(-4.83932663119792,-5.77760472280962,
1.47553084454169));
#29889=CARTESIAN_POINT('Ctrl Pts',(-4.87405254289932,-5.50813907390267,
2.16203789905239));
#29890=CARTESIAN_POINT('Ctrl Pts',(-4.92047209092693,-5.14793330770747,
3.07971998792533));
#29891=CARTESIAN_POINT('Ctrl Pts',(-4.96689163895454,-4.553408222658,3.90542777458002));
#29892=CARTESIAN_POINT('Ctrl Pts',(-5.01331118698216,-3.79734208031535,
4.53808297185698));
#29893=CARTESIAN_POINT('Ctrl Pts',(-5.05973073500977,-3.04127593797266,
5.17073816913398));
#29894=CARTESIAN_POINT('Ctrl Pts',(-5.10615028303738,-2.12366873833678,
5.61034077703322));
#29895=CARTESIAN_POINT('Ctrl Pts',(-5.15256983106499,-1.15684855378816,
5.80307723177887));
#29896=CARTESIAN_POINT('Ctrl Pts',(-5.1989893790926,-0.190028369239583,
5.99581368652452));
#29897=CARTESIAN_POINT('Ctrl Pts',(-5.24540892712022,0.826004800221705,
5.94168398811661));
#29898=CARTESIAN_POINT('Ctrl Pts',(-5.29182847514783,1.76687415432054,5.64731437562902));
#29899=CARTESIAN_POINT('Ctrl Pts',(-5.33824802317544,2.70774350841938,5.35294476314143));
#29900=CARTESIAN_POINT('Ctrl Pts',(-5.38466757120306,3.57344904715588,4.81833523657406));
#29901=CARTESIAN_POINT('Ctrl Pts',(-5.43108711923068,4.25801619398554,4.10892954747936));
#29902=CARTESIAN_POINT('Ctrl Pts',(-5.47750666725829,4.94258334081521,3.39952385838465));
#29903=CARTESIAN_POINT('Ctrl Pts',(-5.5239262152859,5.44601209573819,2.51532200676252));
#29904=CARTESIAN_POINT('Ctrl Pts',(-5.5703457633135,5.70667567373816,1.56456277891212));
#29905=CARTESIAN_POINT('Ctrl Pts',(-5.61676531134112,5.96733925173814,0.613803551061655));
#29906=CARTESIAN_POINT('Ctrl Pts',(-5.66318485936872,5.9852376528151,-0.403513053016923));
#29907=CARTESIAN_POINT('Ctrl Pts',(-5.70960440739634,5.75817986005846,-1.36285312253713));
#29908=CARTESIAN_POINT('Ctrl Pts',(-5.75602395542395,5.53112206730183,-2.32219319205729));
#29909=CARTESIAN_POINT('Ctrl Pts',(-5.80244350345158,5.05910808071154,-3.22355672701905));
#29910=CARTESIAN_POINT('Ctrl Pts',(-5.84886305147919,4.39991907427081,-3.95660410886154));
#29911=CARTESIAN_POINT('Ctrl Pts',(-5.89528259950681,3.74073006782999,-4.68965149070412));
#29912=CARTESIAN_POINT('Ctrl Pts',(-5.94170214753442,2.89436604153866,-5.25438271942753));
#29913=CARTESIAN_POINT('Ctrl Pts',(-5.98812169556203,1.96443389783085,-5.58166672199668));
#29914=CARTESIAN_POINT('Ctrl Pts',(-6.03454124358964,1.03450175412321,-5.90895072456578));
#29915=CARTESIAN_POINT('Ctrl Pts',(-6.08096079161725,0.0210014929991525,
-5.99878750098069));
#29916=CARTESIAN_POINT('Ctrl Pts',(-6.12738033964486,-0.952000148996213,
-5.84017976184837));
#29917=CARTESIAN_POINT('Ctrl Pts',(-6.17379988767247,-1.92500179099163,
-5.68157202271603));
#29918=CARTESIAN_POINT('Ctrl Pts',(-6.22021943570009,-2.85750481385833,
-5.27451976803642));
#29919=CARTESIAN_POINT('Ctrl Pts',(-6.2666389837277,-3.63535768621217,-4.66885193893426));
#29920=CARTESIAN_POINT('Ctrl Pts',(-6.31305853175531,-4.41321055856602,
-4.06318410983209));
#29921=CARTESIAN_POINT('Ctrl Pts',(-6.35947807978292,-5.03641328040699,
-3.25890070630738));
#29922=CARTESIAN_POINT('Ctrl Pts',(-6.40589762781053,-5.42867704267341,
-2.35445736863992));
#29923=CARTESIAN_POINT('Ctrl Pts',(-6.44389002113873,-5.74972797439643,
-1.61420959614342));
#29924=CARTESIAN_POINT('Ctrl Pts',(-6.48188241446693,-5.91607948259785,
-0.806867539943621));
#29925=CARTESIAN_POINT('Ctrl Pts',(-6.51987480779513,-5.91690427471314,
0.000144985681112611));
#29926=CARTESIAN_POINT('Ctrl Pts',(-6.77162519220487,-5.916739287675,0.000155466350801038));
#29927=CARTESIAN_POINT('Ctrl Pts',(-6.73607187764382,-5.91595985127682,
-0.755108201434952));
#29928=CARTESIAN_POINT('Ctrl Pts',(-6.70051856308277,-5.77079135495242,
-1.51066285089507));
#29929=CARTESIAN_POINT('Ctrl Pts',(-6.66496524852172,-5.48865227932844,
-2.21104047700275));
#29930=CARTESIAN_POINT('Ctrl Pts',(-6.61854570049411,-5.12028245128035,
-3.12547597349477));
#29931=CARTESIAN_POINT('Ctrl Pts',(-6.5721261524665,-4.51842228352505,-3.9458525706781));
#29932=CARTESIAN_POINT('Ctrl Pts',(-6.52570660443889,-3.75674795527445,
-4.57174459422911));
#29933=CARTESIAN_POINT('Ctrl Pts',(-6.47928705641128,-2.9950736270239,-5.19763661778009));
#29934=CARTESIAN_POINT('Ctrl Pts',(-6.43286750838367,-2.07358513827807,
-5.62904406769878));
#29935=CARTESIAN_POINT('Ctrl Pts',(-6.38644796035606,-1.10508568598514,
-5.813156583213));
#29936=CARTESIAN_POINT('Ctrl Pts',(-6.34002841232845,-0.13658623369216,
-5.99726909872722));
#29937=CARTESIAN_POINT('Ctrl Pts',(-6.29360886430083,0.878924182148105,
-5.93408667983692));
#29938=CARTESIAN_POINT('Ctrl Pts',(-6.24718931627322,1.8171327536815,-5.63134374637349));
#29939=CARTESIAN_POINT('Ctrl Pts',(-6.2007697682456,2.75534132521499,-5.32860081291002));
#29940=CARTESIAN_POINT('Ctrl Pts',(-6.15435022021799,3.61624805244166,-4.78629736487347));
#29941=CARTESIAN_POINT('Ctrl Pts',(-6.10793067219037,4.29446580107692,-4.0708189983961));
#29942=CARTESIAN_POINT('Ctrl Pts',(-6.06151112416276,4.97268354971214,-3.35534063191877));
#29943=CARTESIAN_POINT('Ctrl Pts',(-6.01509157613515,5.46821231975582,-2.46668734700071));
#29944=CARTESIAN_POINT('Ctrl Pts',(-5.96867202810754,5.72039239584158,-1.51364284820421));
#29945=CARTESIAN_POINT('Ctrl Pts',(-5.92225248007992,5.97257247192732,-0.560598349407762));
#29946=CARTESIAN_POINT('Ctrl Pts',(-5.87583293205231,5.98140385405515,0.456837363267123));
#29947=CARTESIAN_POINT('Ctrl Pts',(-5.8294133840247,5.74580545640615,1.41411579846036));
#29948=CARTESIAN_POINT('Ctrl Pts',(-5.78299383599708,5.51020705875715,2.37139423365359));
#29949=CARTESIAN_POINT('Ctrl Pts',(-5.73657428796947,5.03017888133132,3.26851539136518));
#29950=CARTESIAN_POINT('Ctrl Pts',(-5.69015473994186,4.36448314818263,3.99565897988701));
#29951=CARTESIAN_POINT('Ctrl Pts',(-5.64373519191425,3.6987874150339,4.72280256840889));
#29952=CARTESIAN_POINT('Ctrl Pts',(-5.59731564388664,2.84742412616229,5.27996858774099));
#29953=CARTESIAN_POINT('Ctrl Pts',(-5.55089609585902,1.9146121643015,5.59895205325341));
#29954=CARTESIAN_POINT('Ctrl Pts',(-5.50447654783141,0.981800202440707,
5.91793551876582));
#29955=CARTESIAN_POINT('Ctrl Pts',(-5.45805699980379,-0.0324604324092743,
5.99873643045854));
#29956=CARTESIAN_POINT('Ctrl Pts',(-5.41163745177617,-1.00400992322729,
5.83146361631306));
#29957=CARTESIAN_POINT('Ctrl Pts',(-5.36521790374857,-1.97555941404519,
5.66419080216759));
#29958=CARTESIAN_POINT('Ctrl Pts',(-5.31879835572096,-2.90439776083114,
5.24884426218397));
#29959=CARTESIAN_POINT('Ctrl Pts',(-5.27237880769335,-3.67682204027665,
4.636268275074));
#29960=CARTESIAN_POINT('Ctrl Pts',(-5.22595925966574,-4.44924631972226,
4.02369228796397));
#29961=CARTESIAN_POINT('Ctrl Pts',(-5.17953971163812,-5.06525653182739,
3.21388685372754));
#29962=CARTESIAN_POINT('Ctrl Pts',(-5.13312016361051,-5.44944433223741,
2.30598358714182));
#29963=CARTESIAN_POINT('Ctrl Pts',(-5.09595517314197,-5.75703750250859,
1.57908688773953));
#29964=CARTESIAN_POINT('Ctrl Pts',(-5.05879018267342,-5.91602969878726,
0.78930828952916));
#29965=CARTESIAN_POINT('Ctrl Pts',(-5.02162519220488,-5.91684860187072,
-0.000150428407648674));
#29966=CARTESIAN_POINT('Origin',(-29.75,0.,0.));
#29967=CARTESIAN_POINT('',(-3.01987480779514,-5.9165030994658,0.000139679809713911));
#29968=CARTESIAN_POINT('',(-3.27162519220487,-5.91637946298814,0.000111165658334626));
#29969=CARTESIAN_POINT('',(-29.75,-5.91675,-7.2459289488551E-16));
#29970=CARTESIAN_POINT('Ctrl Pts',(-3.01987480779514,-5.9165030994658,0.000139679809713911));
#29971=CARTESIAN_POINT('Ctrl Pts',(-3.03447992847091,-5.91677227233095,
0.310433725540576));
#29972=CARTESIAN_POINT('Ctrl Pts',(-3.04908504914667,-5.89278908313743,
0.620686564004424));
#29973=CARTESIAN_POINT('Ctrl Pts',(-3.06369016982243,-5.84419449252714,
0.927035418652865));
#29974=CARTESIAN_POINT('Ctrl Pts',(-3.11010971785004,-5.68974599581187,
1.90070593375919));
#29975=CARTESIAN_POINT('Ctrl Pts',(-3.15652926587766,-5.28668219474421,
2.83493984352893));
#29976=CARTESIAN_POINT('Ctrl Pts',(-3.20294881390527,-4.68434378731049,
3.61537373131302));
#29977=CARTESIAN_POINT('Ctrl Pts',(-3.24936836193289,-4.08200537987681,
4.39580761909706));
#29978=CARTESIAN_POINT('Ctrl Pts',(-3.29578790996049,-3.28039236607707,
5.02244148489549));
#29979=CARTESIAN_POINT('Ctrl Pts',(-3.3422074579881,-2.3776334928619,5.41856649934147));
#29980=CARTESIAN_POINT('Ctrl Pts',(-3.38862700601571,-1.47487461964673,
5.81469151378745));
#29981=CARTESIAN_POINT('Ctrl Pts',(-3.43504655404332,-0.4709698870161,5.98030767688098));
#29982=CARTESIAN_POINT('Ctrl Pts',(-3.48146610207094,0.511188596636436,
5.89514123267316));
#29983=CARTESIAN_POINT('Ctrl Pts',(-3.52788565009856,1.49334708028909,5.80997478846532));
#29984=CARTESIAN_POINT('Ctrl Pts',(-3.57430519812617,2.45375931496351,5.47402573695612));
#29985=CARTESIAN_POINT('Ctrl Pts',(-3.62072474615379,3.27485728782222,4.92841898368611));
#29986=CARTESIAN_POINT('Ctrl Pts',(-3.6671442941814,4.09595526068089,4.38281223041613));
#29987=CARTESIAN_POINT('Ctrl Pts',(-3.71356384220902,4.77773897172381,3.62754777538526));
#29988=CARTESIAN_POINT('Ctrl Pts',(-3.75998339023663,5.23674847200481,2.75508064770333));
#29989=CARTESIAN_POINT('Ctrl Pts',(-3.80640293826424,5.69575797228578,1.88261352002145));
#29990=CARTESIAN_POINT('Ctrl Pts',(-3.85282248629185,5.93199326180497,0.892943719688536));
#29991=CARTESIAN_POINT('Ctrl Pts',(-3.89924203431946,5.91653580688652,-0.0927792014856135));
#29992=CARTESIAN_POINT('Ctrl Pts',(-3.94566158234707,5.90107835196807,-1.07850212265976));
#29993=CARTESIAN_POINT('Ctrl Pts',(-3.99208113037469,5.63392815261194,-2.06027816467504));
#29994=CARTESIAN_POINT('Ctrl Pts',(-4.0385006784023,5.14778816379024,-2.91792408316712));
#29995=CARTESIAN_POINT('Ctrl Pts',(-4.08492022642991,4.66164817496857,-3.77557000165915));
#29996=CARTESIAN_POINT('Ctrl Pts',(-4.13133977445751,3.95651839668135,-4.50908579662804));
#29997=CARTESIAN_POINT('Ctrl Pts',(-4.17775932248512,3.11871666601992,-5.02867878189548));
#29998=CARTESIAN_POINT('Ctrl Pts',(-4.22417887051273,2.2809149353584,-5.54827176716297));
#29999=CARTESIAN_POINT('Ctrl Pts',(-4.27059841854035,1.31044125232261,-5.85394194272899));
#30000=CARTESIAN_POINT('Ctrl Pts',(-4.31701796656796,0.326095293021471,
-5.90827096486437));
#30001=CARTESIAN_POINT('Ctrl Pts',(-4.36343751459558,-0.658250666279667,
-5.96259998699975));
#30002=CARTESIAN_POINT('Ctrl Pts',(-4.40985706262319,-1.65646890184619,
-5.76558785570449));
#30003=CARTESIAN_POINT('Ctrl Pts',(-4.45627661065081,-2.54636341275257,
-5.34135163648564));
#30004=CARTESIAN_POINT('Ctrl Pts',(-4.50269615867842,-3.4362579236589,-4.91711541726682));
#30005=CARTESIAN_POINT('Ctrl Pts',(-4.54911570670603,-4.21782870990514,
-4.2656551101244));
#30006=CARTESIAN_POINT('Ctrl Pts',(-4.59553525473364,-4.79540047613297,
-3.46671865139005));
#30007=CARTESIAN_POINT('Ctrl Pts',(-4.64195480276126,-5.37297224236086,
-2.66778219265561));
#30008=CARTESIAN_POINT('Ctrl Pts',(-4.68837435078887,-5.74654498857032,
-1.72136958232917));
#30009=CARTESIAN_POINT('Ctrl Pts',(-4.73479389881649,-5.87038813800455,
-0.743335081620309));
#30010=CARTESIAN_POINT('Ctrl Pts',(-4.7464875351427,-5.90158570050807,-0.496956556801938));
#30011=CARTESIAN_POINT('Ctrl Pts',(-4.75818117146892,-5.9169355219347,-0.248571319372749));
#30012=CARTESIAN_POINT('Ctrl Pts',(-4.76987480779513,-5.91668395451438,
-0.000155206356347026));
#30013=CARTESIAN_POINT('Ctrl Pts',(-5.02162519220488,-5.91684860187072,
-0.000150428407648674));
#30014=CARTESIAN_POINT('Ctrl Pts',(-5.01237063464581,-5.91705251920329,
-0.196735737687811));
#30015=CARTESIAN_POINT('Ctrl Pts',(-5.00311607708674,-5.90744852755087,
-0.393301212035374));
#30016=CARTESIAN_POINT('Ctrl Pts',(-4.99386151952768,-5.88788882431215,
-0.588870976413262));
#30017=CARTESIAN_POINT('Ctrl Pts',(-4.94744197150006,-5.78978012726201,
-1.56982117444776));
#30018=CARTESIAN_POINT('Ctrl Pts',(-4.90102242347245,-5.44119734444683,
-2.5257204715818));
#30019=CARTESIAN_POINT('Ctrl Pts',(-4.85460287544484,-4.88481192839464,
-3.33955330224496));
#30020=CARTESIAN_POINT('Ctrl Pts',(-4.80818332741722,-4.32842651234242,
-4.15338613290818));
#30021=CARTESIAN_POINT('Ctrl Pts',(-4.76176377938962,-3.56423846305318,
-4.82515249710048));
#30022=CARTESIAN_POINT('Ctrl Pts',(-4.715344231362,-2.68579518354086,-5.27261871050719));
#30023=CARTESIAN_POINT('Ctrl Pts',(-4.66892468333439,-1.80735190402854,
-5.72008492391391));
#30024=CARTESIAN_POINT('Ctrl Pts',(-4.62250513530677,-0.814653394293164,
-5.94325098653501));
#30025=CARTESIAN_POINT('Ctrl Pts',(-4.57608558727915,0.170780037086872,
-5.91479822253088));
#30026=CARTESIAN_POINT('Ctrl Pts',(-4.52966603925154,1.1562134684668,-5.88634545852675));
#30027=CARTESIAN_POINT('Ctrl Pts',(-4.48324649122394,2.13438182149134,-5.60627386789744));
#30028=CARTESIAN_POINT('Ctrl Pts',(-4.43682694319633,2.98554348384278,-5.1088681662777));
#30029=CARTESIAN_POINT('Ctrl Pts',(-4.39040739516872,3.83670514619431,-4.61146246465791));
#30030=CARTESIAN_POINT('Ctrl Pts',(-4.3439878471411,4.56086011787267,-3.89672265204767));
#30031=CARTESIAN_POINT('Ctrl Pts',(-4.29756829911349,5.06936160959196,-3.05214296937695));
#30032=CARTESIAN_POINT('Ctrl Pts',(-4.25114875108587,5.57786310131125,-2.20756328670622));
#30033=CARTESIAN_POINT('Ctrl Pts',(-4.20472920305825,5.87071111307149,-1.23314373397488));
#30034=CARTESIAN_POINT('Ctrl Pts',(-4.15830965503064,5.9120569149645,-0.248167017434493));
#30035=CARTESIAN_POINT('Ctrl Pts',(-4.11189010700303,5.9534027168575,0.736809699105835));
#30036=CARTESIAN_POINT('Ctrl Pts',(-4.06547055897542,5.74324630888342,1.73234357945519));
#30037=CARTESIAN_POINT('Ctrl Pts',(-4.01905101094781,5.30731380153418,2.61656722565398));
#30038=CARTESIAN_POINT('Ctrl Pts',(-3.9726314629202,4.87138129418494,3.50079087185276));
#30039=CARTESIAN_POINT('Ctrl Pts',(-3.92621191489259,4.20967268746058,4.27370428390081));
#30040=CARTESIAN_POINT('Ctrl Pts',(-3.87979236686498,3.40319045420619,4.84069195123201));
#30041=CARTESIAN_POINT('Ctrl Pts',(-3.83337281883736,2.59670822095181,5.40767961856321));
#30042=CARTESIAN_POINT('Ctrl Pts',(-3.78695327080975,1.64545236116725,5.7687415411776));
#30043=CARTESIAN_POINT('Ctrl Pts',(-3.74053372278213,0.66587001815382,5.87967864370526));
#30044=CARTESIAN_POINT('Ctrl Pts',(-3.69411417475452,-0.31371232485961,
5.99061574623291));
#30045=CARTESIAN_POINT('Ctrl Pts',(-3.64769462672691,-1.32162115110204,
5.8514280286739));
#30046=CARTESIAN_POINT('Ctrl Pts',(-3.6012750786993,-2.23447419457524,5.47915403215709));
#30047=CARTESIAN_POINT('Ctrl Pts',(-3.55485553067169,-3.14732723804844,
5.10688003564028));
#30048=CARTESIAN_POINT('Ctrl Pts',(-3.50843598264408,-3.96512449875239,
4.50151976016569));
#30049=CARTESIAN_POINT('Ctrl Pts',(-3.46201643461646,-4.58775604955412,
3.73717784753347));
#30050=CARTESIAN_POINT('Ctrl Pts',(-3.41559688658885,-5.21038760035589,
2.97283593490122));
#30051=CARTESIAN_POINT('Ctrl Pts',(-3.36917733856124,-5.6378534412554,2.04951238511135));
#30052=CARTESIAN_POINT('Ctrl Pts',(-3.32275779053362,-5.81782572005508,
1.08023503247858));
#30053=CARTESIAN_POINT('Ctrl Pts',(-3.3057135910907,-5.88390743658177,0.724338492858101));
#30054=CARTESIAN_POINT('Ctrl Pts',(-3.28866939164779,-5.91662229564017,
0.36224650323652));
#30055=CARTESIAN_POINT('Ctrl Pts',(-3.27162519220487,-5.91637946298814,
0.000111165658334626));
#30056=CARTESIAN_POINT('Origin',(-29.75,0.,0.));
#30057=CARTESIAN_POINT('',(-1.26987480779516,-5.91708582682028,-0.000110601437552926));
#30058=CARTESIAN_POINT('',(-1.52162519220488,-5.91720137462112,-6.73836950611244E-5));
#30059=CARTESIAN_POINT('',(-29.75,-5.91675,-7.2459289488551E-16));
#30060=CARTESIAN_POINT('Ctrl Pts',(-1.26987480779516,-5.91708582682028,
-0.000110601437552926));
#30061=CARTESIAN_POINT('Ctrl Pts',(-1.3107786854729,-5.91633930945087,0.868669186826611));
#30062=CARTESIAN_POINT('Ctrl Pts',(-1.35168256315065,-5.72265720390265,
1.73777006268092));
#30063=CARTESIAN_POINT('Ctrl Pts',(-1.39258644082839,-5.35218380498871,
2.52351549592291));
#30064=CARTESIAN_POINT('Ctrl Pts',(-1.439005988856,-4.93175403866376,3.41521452170255));
#30065=CARTESIAN_POINT('Ctrl Pts',(-1.4854255368836,-4.28363963608922,4.19956236932577));
#30066=CARTESIAN_POINT('Ctrl Pts',(-1.53184508491121,-3.48717857307409,
4.78054294561178));
#30067=CARTESIAN_POINT('Ctrl Pts',(-1.57826463293882,-2.69071751005887,
5.36152352189784));
#30068=CARTESIAN_POINT('Ctrl Pts',(-1.62468418096643,-1.74590978660303,
5.73913682684664));
#30069=CARTESIAN_POINT('Ctrl Pts',(-1.67110372899405,-0.768413395098483,
5.86715809605289));
#30070=CARTESIAN_POINT('Ctrl Pts',(-1.71752327702166,0.209082996406062,
5.99517936525915));
#30071=CARTESIAN_POINT('Ctrl Pts',(-1.76394282504928,1.2192680559593,5.87360859872287));
#30072=CARTESIAN_POINT('Ctrl Pts',(-1.8103623730769,2.13848097288002,5.51732755179846));
#30073=CARTESIAN_POINT('Ctrl Pts',(-1.85678192110451,3.05769388980073,5.16104650487406));
#30074=CARTESIAN_POINT('Ctrl Pts',(-1.90320146913213,3.88593466408892,4.57005517756153));
#30075=CARTESIAN_POINT('Ctrl Pts',(-1.94962101715974,4.52181488471369,3.81669936354943));
#30076=CARTESIAN_POINT('Ctrl Pts',(-1.99604056518734,5.15769510533839,3.06334354953742));
#30077=CARTESIAN_POINT('Ctrl Pts',(-2.04246011321495,5.60121477229972,2.14762324882588));
#30078=CARTESIAN_POINT('Ctrl Pts',(-2.08887966124256,5.79808084435675,1.1816354923312));
#30079=CARTESIAN_POINT('Ctrl Pts',(-2.13529920927017,5.99494691641379,0.215647735836411));
#30080=CARTESIAN_POINT('Ctrl Pts',(-2.18171875729779,5.94515939356647,-0.800607476441526));
#30081=CARTESIAN_POINT('Ctrl Pts',(-2.22813830532541,5.65481295806546,-1.74272613311839));
#30082=CARTESIAN_POINT('Ctrl Pts',(-2.27455785335302,5.36446652256445,-2.68484478979524));
#30083=CARTESIAN_POINT('Ctrl Pts',(-2.32097740138064,4.83356117440976,-3.55282689087102));
#30084=CARTESIAN_POINT('Ctrl Pts',(-2.36739694940825,4.12708722822561,-4.2404191917822));
#30085=CARTESIAN_POINT('Ctrl Pts',(-2.41381649743586,3.42061328204151,-4.92801149269334));
#30086=CARTESIAN_POINT('Ctrl Pts',(-2.46023604546347,2.53857073782799,-5.43521399343989));
#30087=CARTESIAN_POINT('Ctrl Pts',(-2.50665559349108,1.58893404870036,-5.69993794139027));
#30088=CARTESIAN_POINT('Ctrl Pts',(-2.55307514151869,0.639297359572737,
-5.96466188934065));
#30089=CARTESIAN_POINT('Ctrl Pts',(-2.59949468954631,-0.37793347446899,
-5.98690728449486));
#30090=CARTESIAN_POINT('Ctrl Pts',(-2.64591423757392,-1.33823504031722,
-5.76395098054405));
#30091=CARTESIAN_POINT('Ctrl Pts',(-2.69233378560153,-2.29853660616546,
-5.54099467659324));
#30092=CARTESIAN_POINT('Ctrl Pts',(-2.73875333362914,-3.2019089038202,-5.07283667353741));
#30093=CARTESIAN_POINT('Ctrl Pts',(-2.78517288165675,-3.93776641472978,
-4.41678611648578));
#30094=CARTESIAN_POINT('Ctrl Pts',(-2.83159242968436,-4.67362392563931,
-3.76073555943419));
#30095=CARTESIAN_POINT('Ctrl Pts',(-2.87801197771197,-5.24196664980369,
-2.91679244838682));
#30096=CARTESIAN_POINT('Ctrl Pts',(-2.92443152573957,-5.57322141570446,
-1.98826733264174));
#30097=CARTESIAN_POINT('Ctrl Pts',(-2.95624595309143,-5.80025250783052,
-1.35188684005969));
#30098=CARTESIAN_POINT('Ctrl Pts',(-2.98806038044329,-5.91591675849993,
-0.675775815500215));
#30099=CARTESIAN_POINT('Ctrl Pts',(-3.01987480779514,-5.9165030994658,0.000139679809713911));
#30100=CARTESIAN_POINT('Ctrl Pts',(-3.27162519220487,-5.91637946298814,
0.000111165658334626));
#30101=CARTESIAN_POINT('Ctrl Pts',(-3.24224984362017,-5.91596094560191,
-0.624022095151271));
#30102=CARTESIAN_POINT('Ctrl Pts',(-3.21287449503547,-5.81764537263417,
-1.24828411611053));
#30103=CARTESIAN_POINT('Ctrl Pts',(-3.18349914645077,-5.62352742823134,
-1.84117981149419));
#30104=CARTESIAN_POINT('Ctrl Pts',(-3.13707959842316,-5.31677814090809,
-2.77808614735848));
#30105=CARTESIAN_POINT('Ctrl Pts',(-3.09066005039555,-4.77080084956173,
-3.63666766361148));
#30106=CARTESIAN_POINT('Ctrl Pts',(-3.04424050236794,-4.0524308805934,-4.31182186463013));
#30107=CARTESIAN_POINT('Ctrl Pts',(-2.99782095434033,-3.33406091162508,
-4.98697606564878));
#30108=CARTESIAN_POINT('Ctrl Pts',(-2.95140140631272,-2.44329826503476,
-5.4787029514331));
#30109=CARTESIAN_POINT('Ctrl Pts',(-2.90498185828511,-1.48918486103517,
-5.72680821087003));
#30110=CARTESIAN_POINT('Ctrl Pts',(-2.8585623102575,-0.535071457035527,
-5.97491347030698));
#30111=CARTESIAN_POINT('Ctrl Pts',(-2.81214276222989,0.482392704373251,
-5.97939710339653));
#30112=CARTESIAN_POINT('Ctrl Pts',(-2.76572321420227,1.43865564932456,-5.73971025024428));
#30113=CARTESIAN_POINT('Ctrl Pts',(-2.71930366617466,2.39491859427582,-5.50002339709204));
#30114=CARTESIAN_POINT('Ctrl Pts',(-2.67288411814704,3.2899803227696,-5.01616605769791));
#30115=CARTESIAN_POINT('Ctrl Pts',(-2.62646457011943,4.01427264626211,-4.34736919943388));
#30116=CARTESIAN_POINT('Ctrl Pts',(-2.58004502209182,4.73856496975463,-3.67857234116986));
#30117=CARTESIAN_POINT('Ctrl Pts',(-2.53362547406421,5.29208788824606,-2.82483596403585));
#30118=CARTESIAN_POINT('Ctrl Pts',(-2.4872059260366,5.60708238414337,-1.89066945055927));
#30119=CARTESIAN_POINT('Ctrl Pts',(-2.44078637800898,5.92207688004071,-0.956502937082576));
#30120=CARTESIAN_POINT('Ctrl Pts',(-2.39436682998137,5.99854295334388,0.0580937127365762));
#30121=CARTESIAN_POINT('Ctrl Pts',(-2.34794728195375,5.82712007728882,1.02891954948094));
#30122=CARTESIAN_POINT('Ctrl Pts',(-2.30152773392615,5.65569720123378,1.99974538622514));
#30123=CARTESIAN_POINT('Ctrl Pts',(-2.25510818589853,5.23638537582048,2.92680040989459));
#30124=CARTESIAN_POINT('Ctrl Pts',(-2.20868863787092,4.62051428694949,3.69659999997161));
#30125=CARTESIAN_POINT('Ctrl Pts',(-2.16226908984331,4.00464319807843,4.46639959004873));
#30126=CARTESIAN_POINT('Ctrl Pts',(-2.1158495418157,3.19221284574972,5.07894374653346));
#30127=CARTESIAN_POINT('Ctrl Pts',(-2.06942999378809,2.28267617120534,5.4592484214001));
#30128=CARTESIAN_POINT('Ctrl Pts',(-2.02301044576047,1.37313949666091,5.83955309626675));
#30129=CARTESIAN_POINT('Ctrl Pts',(-1.97659089773286,0.366496499900915,
5.98761828951517));
#30130=CARTESIAN_POINT('Ctrl Pts',(-1.93017134970524,-0.614025507383721,
5.88531872740078));
#30131=CARTESIAN_POINT('Ctrl Pts',(-1.88375180167762,-1.59454751466825,
5.78301916528641));
#30132=CARTESIAN_POINT('Ctrl Pts',(-1.83733225365001,-2.54894853247744,
5.43035484780929));
#30133=CARTESIAN_POINT('Ctrl Pts',(-1.7909127056224,-3.36039640789849,4.87049687332077));
#30134=CARTESIAN_POINT('Ctrl Pts',(-1.74449315759478,-4.17184428331958,
4.31063889883221));
#30135=CARTESIAN_POINT('Ctrl Pts',(-1.69807360956717,-4.84033901635253,
3.54358726733221));
#30136=CARTESIAN_POINT('Ctrl Pts',(-1.65165406153956,-5.28404741237419,
2.66323990838002));
#30137=CARTESIAN_POINT('Ctrl Pts',(-1.60831110509467,-5.69834773411708,
1.84124015058956));
#30138=CARTESIAN_POINT('Ctrl Pts',(-1.56496814864977,-5.91667103198986,
0.920464996667376));
#30139=CARTESIAN_POINT('Ctrl Pts',(-1.52162519220488,-5.91720137462112,
-6.73836950611244E-5));
#30140=CARTESIAN_POINT('Origin',(-62.8183905640093,0.,0.));
#30141=CARTESIAN_POINT('',(-0.69339056400935,-4.91852915329511,-9.19365388711588E-5));
#30142=CARTESIAN_POINT('',(-0.348109435990813,-4.91783243427629,2.96545098249501E-5));
#30143=CARTESIAN_POINT('',(-62.8183905640093,-4.91825,1.40632325245411E-12));
#30144=CARTESIAN_POINT('',(-3.12250225675825E-15,3.9094845766438,-2.98454410297281));
#30145=CARTESIAN_POINT('Ctrl Pts',(-0.69339056400935,-4.91852915329511,
-9.19365388716252E-5));
#30146=CARTESIAN_POINT('Ctrl Pts',(-0.687874893659468,-4.91861282933523,
-0.0974721923576648));
#30147=CARTESIAN_POINT('Ctrl Pts',(-0.635939675281974,-4.89194258344,-1.01435309429727));
#30148=CARTESIAN_POINT('Ctrl Pts',(-0.537584908876869,-4.34627971767338,
-2.721289900206));
#30149=CARTESIAN_POINT('Ctrl Pts',(-0.398326264794041,-2.50959877852527,
-4.47185006834336));
#30150=CARTESIAN_POINT('Ctrl Pts',(-0.259067620711191,-0.0584880437401866,
-5.12759583452146));
#30151=CARTESIAN_POINT('Ctrl Pts',(-0.12629219911318,2.29214640132989,-4.55583897742123));
#30152=CARTESIAN_POINT('Ctrl Pts',(-0.0399363255427856,3.48109416590671,
-3.54459219221265));
#30153=CARTESIAN_POINT('Ctrl Pts',(-3.25477492180148E-15,3.9094845766438,
-2.98454410297281));
#30154=CARTESIAN_POINT('',(0.,-1.55153804394499,-4.66710967952236));
#30155=CARTESIAN_POINT('Origin',(0.,0.,0.));
#30156=CARTESIAN_POINT('Ctrl Pts',(-0.348109435990813,-4.91783243427629,
2.96545098246725E-5));
#30157=CARTESIAN_POINT('Ctrl Pts',(-0.324912053382433,-4.91783717729381,
-0.409677115258361));
#30158=CARTESIAN_POINT('Ctrl Pts',(-0.255295122746436,-4.76590055786429,
-1.63925672502214));
#30159=CARTESIAN_POINT('Ctrl Pts',(-0.139258644082833,-3.75247085555401,
-3.49516562013044));
#30160=CARTESIAN_POINT('Ctrl Pts',(-0.0464195480276115,-2.32937887075175,
-4.40852359138744));
#30161=CARTESIAN_POINT('Ctrl Pts',(0.,-1.55153804394499,-4.66710967952236));
#30162=CARTESIAN_POINT('Origin',(-62.8183905640093,0.,0.));
#30163=CARTESIAN_POINT('',(-2.44339056400933,-4.91804476595219,0.000116107698993155));
#30164=CARTESIAN_POINT('',(-2.0981094359908,-4.91862520145862,-5.60121431075755E-5));
#30165=CARTESIAN_POINT('',(-62.8183905640093,-4.91825,1.40632325245411E-12));
#30166=CARTESIAN_POINT('Ctrl Pts',(-2.44339056400934,-4.9180447659522,0.000116107698993062));
#30167=CARTESIAN_POINT('Ctrl Pts',(-2.41157613665747,-4.91755737482448,
-0.561733114392291));
#30168=CARTESIAN_POINT('Ctrl Pts',(-2.333342161278,-4.68112996827926,-1.94376062201184));
#30169=CARTESIAN_POINT('Ctrl Pts',(-2.20868863787092,-3.41248139082355,
-3.82760144861539));
#30170=CARTESIAN_POINT('Ctrl Pts',(-2.06942999378809,-1.15971890993101,
-4.99505897100328));
#30171=CARTESIAN_POINT('Ctrl Pts',(-1.93017134970524,1.37697549976642,-4.93958506317368));
#30172=CARTESIAN_POINT('Ctrl Pts',(-1.79091270562242,3.57654743186344,-3.67476128358358));
#30173=CARTESIAN_POINT('Ctrl Pts',(-1.65165406153958,4.90047960504737,-1.51025223624387));
#30174=CARTESIAN_POINT('Ctrl Pts',(-1.51239541745672,5.02463601739066,1.02400924064084));
#30175=CARTESIAN_POINT('Ctrl Pts',(-1.3731367733739,3.91861974053298,3.3075642508956));
#30176=CARTESIAN_POINT('Ctrl Pts',(-1.23387812929106,1.85321465084221,4.7813343589219));
#30177=CARTESIAN_POINT('Ctrl Pts',(-1.09461948520821,-0.665909531765221,
5.08449847225302));
#30178=CARTESIAN_POINT('Ctrl Pts',(-0.955360841125384,-3.0220005881154,
4.1428345670361));
#30179=CARTESIAN_POINT('Ctrl Pts',(-0.821617867392433,-4.57420574358984,
2.26435637255426));
#30180=CARTESIAN_POINT('Ctrl Pts',(-0.734294441687084,-4.91790861684306,
0.722074150186002));
#30181=CARTESIAN_POINT('Ctrl Pts',(-0.69339056400935,-4.91852915329511,
-9.19365388716252E-5));
#30182=CARTESIAN_POINT('Ctrl Pts',(-2.0981094359908,-4.91862520145862,-5.60121431077924E-5));
#30183=CARTESIAN_POINT('Ctrl Pts',(-2.09503284440806,-4.9186564935966,-0.054370759900058));
#30184=CARTESIAN_POINT('Ctrl Pts',(-2.0455367047977,-4.90448501505777,-0.928168902546578));
#30185=CARTESIAN_POINT('Ctrl Pts',(-1.94962101715972,-4.41626575409672,
-2.60617701967216));
#30186=CARTESIAN_POINT('Ctrl Pts',(-1.8103623730769,-2.62620047284534,-4.40438801630634));
#30187=CARTESIAN_POINT('Ctrl Pts',(-1.67110372899405,-0.193167284512309,
-5.12428009940892));
#30188=CARTESIAN_POINT('Ctrl Pts',(-1.53184508491121,2.28715890535059,-4.58960454528829));
#30189=CARTESIAN_POINT('Ctrl Pts',(-1.39258644082838,4.20752364775137,-2.93126272184108));
#30190=CARTESIAN_POINT('Ctrl Pts',(-1.25332779674554,5.0977685824936,-0.555268006901366));
#30191=CARTESIAN_POINT('Ctrl Pts',(-1.1140691526627,4.73993440187225,1.95667777727522));
#30192=CARTESIAN_POINT('Ctrl Pts',(-0.974810508579856,3.22163334032844,
3.98956232001804));
#30193=CARTESIAN_POINT('Ctrl Pts',(-0.835551864497027,0.914579917925479,
5.04571140862161));
#30194=CARTESIAN_POINT('Ctrl Pts',(-0.696293220414185,-1.61637760332782,
4.86648495952254));
#30195=CARTESIAN_POINT('Ctrl Pts',(-0.55703457633135,-3.75162148741517,
3.49588943240163));
#30196=CARTESIAN_POINT('Ctrl Pts',(-0.440973314856899,-4.7656461069887,
1.64014823529778));
#30197=CARTESIAN_POINT('Ctrl Pts',(-0.371331601410049,-4.91782768619158,
0.410174132512313));
#30198=CARTESIAN_POINT('Ctrl Pts',(-0.348109435990813,-4.91783243427629,
2.96545098246725E-5));
#30199=CARTESIAN_POINT('Origin',(-62.8183905640093,0.,0.));
#30200=CARTESIAN_POINT('',(-4.19339056400932,-4.91819510023076,-0.000129014012458647));
#30201=CARTESIAN_POINT('',(-3.84810943599078,-4.91794199414229,9.24055450682304E-5));
#30202=CARTESIAN_POINT('',(-62.8183905640093,-4.91825,1.40632325245411E-12));
#30203=CARTESIAN_POINT('Ctrl Pts',(-4.19339056400932,-4.91819510023076,
-0.000129014012458656));
#30204=CARTESIAN_POINT('Ctrl Pts',(-4.1816969276831,-4.91840421358947,-0.206622874297924));
#30205=CARTESIAN_POINT('Ctrl Pts',(-4.12358374332926,-4.85499449889969,
-1.23269585591806));
#30206=CARTESIAN_POINT('Ctrl Pts',(-4.01905101094782,-4.15570990356999,
-3.0042698423568));
#30207=CARTESIAN_POINT('Ctrl Pts',(-3.87979236686497,-2.20668695036655,
-4.62883298374532));
#30208=CARTESIAN_POINT('Ctrl Pts',(-3.74053372278213,0.28259525882338,-5.12012714764091));
#30209=CARTESIAN_POINT('Ctrl Pts',(-3.60127507869929,2.70269017153252,-4.35786965443408));
#30210=CARTESIAN_POINT('Ctrl Pts',(-3.46201643461646,4.46109023849236,-2.52868265552132));
#30211=CARTESIAN_POINT('Ctrl Pts',(-3.32275779053363,5.12728948705797,-0.0804027626875136));
#30212=CARTESIAN_POINT('Ctrl Pts',(-3.18349914645079,4.53818353564321,2.38756199608455));
#30213=CARTESIAN_POINT('Ctrl Pts',(-3.04424050236796,2.83800215050638,4.27098418189009));
#30214=CARTESIAN_POINT('Ctrl Pts',(-2.90498185828511,0.442997727543895,
5.10874887834615));
#30215=CARTESIAN_POINT('Ctrl Pts',(-2.76572321420227,-2.06046504404221,
4.69574763908411));
#30216=CARTESIAN_POINT('Ctrl Pts',(-2.62646457011944,-4.05946780997995,
3.13309482607209));
#30217=CARTESIAN_POINT('Ctrl Pts',(-2.51902035338846,-4.83497050962448,
1.33561036528277));
#30218=CARTESIAN_POINT('Ctrl Pts',(-2.45799568468509,-4.91826851369274,
0.258045492989058));
#30219=CARTESIAN_POINT('Ctrl Pts',(-2.44339056400934,-4.9180447659522,0.000116107698993062));
#30220=CARTESIAN_POINT('Ctrl Pts',(-3.84810943599078,-4.91794199414229,
9.24055450680916E-5));
#30221=CARTESIAN_POINT('Ctrl Pts',(-3.81873408740606,-4.91759410499135,
-0.518713258033689));
#30222=CARTESIAN_POINT('Ctrl Pts',(-3.74293919079372,-4.70672807007167,
-1.85762278311962));
#30223=CARTESIAN_POINT('Ctrl Pts',(-3.62072474615378,-3.51184999623001,
-3.73663908038491));
#30224=CARTESIAN_POINT('Ctrl Pts',(-3.48146610207094,-1.29053252299245,
-4.96287092523671));
#30225=CARTESIAN_POINT('Ctrl Pts',(-3.3422074579881,1.24674374109644,-4.97405187513803));
#30226=CARTESIAN_POINT('Ctrl Pts',(-3.20294881390526,3.47878194424713,-3.76744451832491));
#30227=CARTESIAN_POINT('Ctrl Pts',(-3.06369016982243,4.8591161279818,-1.63846039519689));
#30228=CARTESIAN_POINT('Ctrl Pts',(-2.92443152573959,5.04980152031218,0.891665082289887));
#30229=CARTESIAN_POINT('Ctrl Pts',(-2.78517288165675,4.0041529537823,3.20348577954525));
#30230=CARTESIAN_POINT('Ctrl Pts',(-2.64591423757392,1.9781747155564,4.73100272599303));
#30231=CARTESIAN_POINT('Ctrl Pts',(-2.50665559349108,-0.532116534951586,
5.10023666524732));
#30232=CARTESIAN_POINT('Ctrl Pts',(-2.36739694940823,-2.91213063348896,
4.22078868480285));
#30233=CARTESIAN_POINT('Ctrl Pts',(-2.23121489690814,-4.54234358429553,
2.35023168290226));
#30234=CARTESIAN_POINT('Ctrl Pts',(-2.14145239243567,-4.91818435848776,
0.76512899309031));
#30235=CARTESIAN_POINT('Ctrl Pts',(-2.0981094359908,-4.91862520145862,-5.60121431077924E-5));
#30236=CARTESIAN_POINT('Origin',(-62.8183905640093,0.,0.));
#30237=CARTESIAN_POINT('',(-5.94339056400932,-4.91837823959233,0.000120518161154786));
#30238=CARTESIAN_POINT('',(-5.59810943599078,-4.91833196199783,-0.000125042380879348));
#30239=CARTESIAN_POINT('',(-62.8183905640093,-4.91825,1.40632325245411E-12));
#30240=CARTESIAN_POINT('Ctrl Pts',(-5.94339056400932,-4.91837823959232,
0.000120518161154867));
#30241=CARTESIAN_POINT('Ctrl Pts',(-5.90539817068111,-4.91769263789875,
-0.670702037152937));
#30242=CARTESIAN_POINT('Ctrl Pts',(-5.82098622932529,-4.61046423753281,
-2.16175199008866));
#30243=CARTESIAN_POINT('Ctrl Pts',(-5.69015473994187,-3.150412987362,-4.0460425229334));
#30244=CARTESIAN_POINT('Ctrl Pts',(-5.55089609585902,-0.825006475908536,
-5.06111908603556));
#30245=CARTESIAN_POINT('Ctrl Pts',(-5.41163745177619,1.70238490919671,-4.83709083119842));
#30246=CARTESIAN_POINT('Ctrl Pts',(-5.27237880769335,3.81298441347213,-3.42880619909369));
#30247=CARTESIAN_POINT('Ctrl Pts',(-5.13312016361051,4.99005770009789,-1.18105302083279));
#30248=CARTESIAN_POINT('Ctrl Pts',(-4.99386151952767,4.94542400198837,1.35585527578786));
#30249=CARTESIAN_POINT('Ctrl Pts',(-4.85460287544484,3.69001090836444,3.56081192770356));
#30250=CARTESIAN_POINT('Ctrl Pts',(-4.715344231362,1.53117898244731,4.89398130483108));
#30251=CARTESIAN_POINT('Ctrl Pts',(-4.57608558727916,-1.00252878061676,
5.0289659108369));
#30252=CARTESIAN_POINT('Ctrl Pts',(-4.43682694319632,-3.29078919872254,
3.93271770381442));
#30253=CARTESIAN_POINT('Ctrl Pts',(-4.30926193543972,-4.64887815341735,
2.04653215326229));
#30254=CARTESIAN_POINT('Ctrl Pts',(-4.22811647571071,-4.91757410845133,
0.613083793287724));
#30255=CARTESIAN_POINT('Ctrl Pts',(-4.19339056400932,-4.91819510023076,
-0.000129014012458656));
#30256=CARTESIAN_POINT('Ctrl Pts',(-5.59810943599078,-4.91833196199783,
-0.000125042380879781));
#30257=CARTESIAN_POINT('Ctrl Pts',(-5.58885487843169,-4.9185014666112,-0.163534971373931));
#30258=CARTESIAN_POINT('Ctrl Pts',(-5.53318077284498,-4.87047543051452,
-1.1464867385219));
#30259=CARTESIAN_POINT('Ctrl Pts',(-5.43108711923067,-4.23319416364483,
-2.89406793044928));
#30260=CARTESIAN_POINT('Ctrl Pts',(-5.29182847514784,-2.32751898381641,
-4.56926880289899));
#30261=CARTESIAN_POINT('Ctrl Pts',(-5.15256983106498,0.147998544643936,
-5.12578369071063));
#30262=CARTESIAN_POINT('Ctrl Pts',(-5.01331118698215,2.58728185166053,-4.42736204000073));
#30263=CARTESIAN_POINT('Ctrl Pts',(-4.87405254289932,4.39312552738983,-2.64499718596595));
#30264=CARTESIAN_POINT('Ctrl Pts',(-4.73479389881648,5.12340806451229,-0.215062357612596));
#30265=CARTESIAN_POINT('Ctrl Pts',(-4.59553525473364,4.59933568346607,2.26752580668157));
#30266=CARTESIAN_POINT('Ctrl Pts',(-4.45627661065081,2.94921609668853,4.19495964559934));
#30267=CARTESIAN_POINT('Ctrl Pts',(-4.31701796656797,0.57704515873205,5.09534894761389));
#30268=CARTESIAN_POINT('Ctrl Pts',(-4.17775932248513,-1.93640272295992,
4.74825299533382));
#30269=CARTESIAN_POINT('Ctrl Pts',(-4.03850067840229,-3.97576455713786,
3.2386506757228));
#30270=CARTESIAN_POINT('Ctrl Pts',(-3.92861738290418,-4.81688766647458,
1.42183000652332));
#30271=CARTESIAN_POINT('Ctrl Pts',(-3.86515363543367,-4.91814384679624,
0.301114440283927));
#30272=CARTESIAN_POINT('Ctrl Pts',(-3.84810943599078,-4.91794199414229,
9.24055450680916E-5));
#30273=CARTESIAN_POINT('Origin',(-62.8183905640093,0.,0.));
#30274=CARTESIAN_POINT('',(-7.69339056400932,-4.91791353327688,-8.21695429248617E-5));
#30275=CARTESIAN_POINT('',(-7.34810943599077,-4.91824109546754,0.000129230132873345));
#30276=CARTESIAN_POINT('',(-62.8183905640093,-4.91825,1.40632325245411E-12));
#30277=CARTESIAN_POINT('Ctrl Pts',(-7.69339056400932,-4.91791353327688,
-8.21695429247329E-5));
#30278=CARTESIAN_POINT('Ctrl Pts',(-7.67551896170675,-4.91810032602428,
-0.315722413110651));
#30279=CARTESIAN_POINT('Ctrl Pts',(-7.61122781137655,-4.81048024208871,
-1.45107819583804));
#30280=CARTESIAN_POINT('Ctrl Pts',(-7.50051711301875,-3.94674387586246,
-3.27395401108));
#30281=CARTESIAN_POINT('Ctrl Pts',(-7.36125846893591,-1.89400947691462,
-4.7653216249989));
#30282=CARTESIAN_POINT('Ctrl Pts',(-7.22199982485306,0.622431906234182,
-5.09000398923479));
#30283=CARTESIAN_POINT('Ctrl Pts',(-7.08274118077025,2.98648438867875,-4.16850969586284));
#30284=CARTESIAN_POINT('Ctrl Pts',(-6.94348253668739,4.61936119005255,-2.22644655991574));
#30285=CARTESIAN_POINT('Ctrl Pts',(-6.80422389260458,5.12128797640124,0.260713542211845));
#30286=CARTESIAN_POINT('Ctrl Pts',(-6.66496524852172,4.36937890199675,2.68404360976314));
#30287=CARTESIAN_POINT('Ctrl Pts',(-6.52570660443889,2.54772253320329,4.45024403624483));
#30288=CARTESIAN_POINT('Ctrl Pts',(-6.38644796035604,0.102311770964511,
5.12689910080611));
#30289=CARTESIAN_POINT('Ctrl Pts',(-6.24718931627322,-2.3681478008713,4.54834454296868));
#30290=CARTESIAN_POINT('Ctrl Pts',(-6.10793067219037,-4.25881794278671,
2.85622684997581));
#30291=CARTESIAN_POINT('Ctrl Pts',(-6.00666442143574,-4.87546116306589,
1.11724409472842));
#30292=CARTESIAN_POINT('Ctrl Pts',(-5.95181771870872,-4.91853031402165,
0.14891676273157));
#30293=CARTESIAN_POINT('Ctrl Pts',(-5.94339056400932,-4.91837823959232,
0.000120518161154867));
#30294=CARTESIAN_POINT('Ctrl Pts',(-7.34810943599077,-4.91824109546754,
0.000129230132873172));
#30295=CARTESIAN_POINT('Ctrl Pts',(-7.3125561214297,-4.9175931953426,-0.627677510745102));
#30296=CARTESIAN_POINT('Ctrl Pts',(-7.23058325884101,-4.63937228605784,
-2.07572654968798));
#30297=CARTESIAN_POINT('Ctrl Pts',(-7.10219084822472,-3.25561019578073,
-3.96188897702852));
#30298=CARTESIAN_POINT('Ctrl Pts',(-6.96293220414188,-0.957670908279476,
-5.03770071010642));
#30299=CARTESIAN_POINT('Ctrl Pts',(-6.82367356005904,1.57473325078029,-4.88014110472828));
#30300=CARTESIAN_POINT('Ctrl Pts',(-6.68441491597621,3.72159825835185,-3.52778519989586));
#30301=CARTESIAN_POINT('Ctrl Pts',(-6.54515627189337,4.95731095870299,-1.31172789552367));
#30302=CARTESIAN_POINT('Ctrl Pts',(-6.40589762781053,4.97933400098995,1.22547742523351));
#30303=CARTESIAN_POINT('Ctrl Pts',(-6.26663898372769,3.78227552279275,3.46265127941791));
#30304=CARTESIAN_POINT('Ctrl Pts',(-6.12738033964487,1.65920923023726,4.8520703564012));
#30305=CARTESIAN_POINT('Ctrl Pts',(-5.988121695562,-0.870078318172324,5.05356564550398));
#30306=CARTESIAN_POINT('Ctrl Pts',(-5.84886305147918,-3.18634613365232,
4.01780541212868));
#30307=CARTESIAN_POINT('Ctrl Pts',(-5.71885896495544,-4.62041956406219,
2.13257618342603));
#30308=CARTESIAN_POINT('Ctrl Pts',(-5.6352744264593,-4.91765125551345,0.656106053996394));
#30309=CARTESIAN_POINT('Ctrl Pts',(-5.59810943599078,-4.91833196199783,
-0.000125042380879781));
#30310=CARTESIAN_POINT('Origin',(-62.8183905640093,0.,0.));
#30311=CARTESIAN_POINT('',(-9.44339056400932,-4.91864811437696,4.17001171947731E-5));
#30312=CARTESIAN_POINT('',(-9.09810943599077,-4.91800701852089,-0.000109254779623313));
#30313=CARTESIAN_POINT('',(-62.8183905640093,-4.91825,1.40632325245411E-12));
#30314=CARTESIAN_POINT('Ctrl Pts',(-9.44339056400932,-4.91864811437696,
4.17001171945739E-5));
#30315=CARTESIAN_POINT('Ctrl Pts',(-9.39922020470476,-4.91830005980813,
-0.779739888198681));
#30316=CARTESIAN_POINT('Ctrl Pts',(-9.30863029737259,-4.5312235699483,-2.37934338565543));
#30317=CARTESIAN_POINT('Ctrl Pts',(-9.1716208420128,-2.87439939474084,-4.24657393763936));
#30318=CARTESIAN_POINT('Ctrl Pts',(-9.03236219792996,-0.486642181365819,
-5.1047763394335));
#30319=CARTESIAN_POINT('Ctrl Pts',(-8.89310355384714,2.02025877498237,-4.71318539529599));
#30320=CARTESIAN_POINT('Ctrl Pts',(-8.75384490976428,4.03254335518717,-3.16767362221242));
#30321=CARTESIAN_POINT('Ctrl Pts',(-8.61458626568145,5.05754749108297,-0.846625929064747));
#30322=CARTESIAN_POINT('Ctrl Pts',(-8.47532762159861,4.84432123630313,1.681699690143));
#30323=CARTESIAN_POINT('Ctrl Pts',(-8.33606897751578,3.44506839698563,3.79829775404922));
#30324=CARTESIAN_POINT('Ctrl Pts',(-8.19681033343293,1.20236556641743,4.98496530910879));
#30325=CARTESIAN_POINT('Ctrl Pts',(-8.0575516893501,-1.33471029528195,4.95117264049567));
#30326=CARTESIAN_POINT('Ctrl Pts',(-7.91829304526727,-3.54501140038643,
3.70519314738851));
#30327=CARTESIAN_POINT('Ctrl Pts',(-7.796906003487,-4.7151205220378,1.82839543316926));
#30328=CARTESIAN_POINT('Ctrl Pts',(-7.72193850973436,-4.91761515212871,
0.504118874630245));
#30329=CARTESIAN_POINT('Ctrl Pts',(-7.69339056400932,-4.91791353327688,
-8.21695429247329E-5));
#30330=CARTESIAN_POINT('Ctrl Pts',(-9.09810943599077,-4.91800701852089,
-0.000109254779623522));
#30331=CARTESIAN_POINT('Ctrl Pts',(-9.08267691245533,-4.91822704331746,
-0.272656737973705));
#30332=CARTESIAN_POINT('Ctrl Pts',(-9.02082484089228,-4.82897064533397,
-1.36485826043635));
#30333=CARTESIAN_POINT('Ctrl Pts',(-8.9125532213016,-4.03138450511247,-3.16914830595081));
#30334=CARTESIAN_POINT('Ctrl Pts',(-8.77329457721876,-2.01853479244033,
-4.71392398166109));
#30335=CARTESIAN_POINT('Ctrl Pts',(-8.63403593313593,0.488509216784092,
-5.10459800163426));
#30336=CARTESIAN_POINT('Ctrl Pts',(-8.49477728905309,2.87595238006221,-4.24552233780323));
#30337=CARTESIAN_POINT('Ctrl Pts',(-8.35551864497026,4.5592812180853,-2.34702296273093));
#30338=CARTESIAN_POINT('Ctrl Pts',(-8.21626000088742,5.1263693141631,0.126093885571429));
#30339=CARTESIAN_POINT('Ctrl Pts',(-8.07700135680457,4.43837749456725,2.56833939129752));
#30340=CARTESIAN_POINT('Ctrl Pts',(-7.93774271272176,2.66374557742339,4.38178291474247));
#30341=CARTESIAN_POINT('Ctrl Pts',(-7.7984840686389,0.236953550501235,5.12244229133686));
#30342=CARTESIAN_POINT('Ctrl Pts',(-7.65922542455607,-2.24785139432755,
4.60898319829779));
#30343=CARTESIAN_POINT('Ctrl Pts',(-7.51996678047323,-4.18231886529451,
2.96711491556586));
#30344=CARTESIAN_POINT('Ctrl Pts',(-7.41626145095147,-4.86037762657564,
1.20345049757124));
#30345=CARTESIAN_POINT('Ctrl Pts',(-7.35897566945731,-4.91843911453011,
0.19200710994428));
#30346=CARTESIAN_POINT('Ctrl Pts',(-7.34810943599077,-4.91824109546754,
0.000129230132873172));
#30347=CARTESIAN_POINT('Origin',(-62.8183905640093,0.,0.));
#30348=CARTESIAN_POINT('',(-11.1933905640093,-4.91782725633716,1.39428353682031E-5));
#30349=CARTESIAN_POINT('',(-10.8481094359908,-4.91856570422813,8.11450425239682E-5));
#30350=CARTESIAN_POINT('',(-62.8183905640093,-4.91825,1.40632325245411E-12));
#30351=CARTESIAN_POINT('Ctrl Pts',(-11.1933905640093,-4.91782725633716,
1.3942835367757E-5));
#30352=CARTESIAN_POINT('Ctrl Pts',(-11.1693409957304,-4.91778551848492,
-0.424760092808996));
#30353=CARTESIAN_POINT('Ctrl Pts',(-11.0988718794239,-4.7582004889199,-1.66944734820506));
#30354=CARTESIAN_POINT('Ctrl Pts',(-10.9819832150897,-3.72030772957414,
-3.52914614115021));
#30355=CARTESIAN_POINT('Ctrl Pts',(-10.8427245710069,-1.57294823922665,
-4.88071674296288));
#30356=CARTESIAN_POINT('Ctrl Pts',(-10.703465926924,0.959513381393236,-5.03735011283231));
#30357=CARTESIAN_POINT('Ctrl Pts',(-10.5642072828412,3.25705904102695,-3.96069798035511));
#30358=CARTESIAN_POINT('Ctrl Pts',(-10.4249486387583,4.75718470689197,-1.91435517938488));
#30359=CARTESIAN_POINT('Ctrl Pts',(-10.2856899946755,5.09261727031618,0.60067580807126));
#30360=CARTESIAN_POINT('Ctrl Pts',(-10.1464313505927,4.18123337115581,2.96864440178638));
#30361=CARTESIAN_POINT('Ctrl Pts',(-10.0071727065098,2.24616551454361,4.60980504681049));
#30362=CARTESIAN_POINT('Ctrl Pts',(-9.86791406242699,-0.238827064970182,
5.12235529042668));
#30363=CARTESIAN_POINT('Ctrl Pts',(-9.72865541834415,-2.66534803734968,
4.38080836468806));
#30364=CARTESIAN_POINT('Ctrl Pts',(-9.58939677426131,-4.43931657252653,
2.56671588946183));
#30365=CARTESIAN_POINT('Ctrl Pts',(-9.49430848948303,-4.90847969436099,
0.898935409588413));
#30366=CARTESIAN_POINT('Ctrl Pts',(-9.44563975273237,-4.91866583758374,
0.039748779310035));
#30367=CARTESIAN_POINT('Ctrl Pts',(-9.44339056400932,-4.91864811437696,
4.17001171945739E-5));
#30368=CARTESIAN_POINT('Ctrl Pts',(-10.8481094359908,-4.91856570422813,
8.11450425238988E-5));
#30369=CARTESIAN_POINT('Ctrl Pts',(-10.8063781554533,-4.91799158127243,
-0.736676875350269));
#30370=CARTESIAN_POINT('Ctrl Pts',(-10.7182273268883,-4.5635503776824,-2.29349712765718));
#30371=CARTESIAN_POINT('Ctrl Pts',(-10.5836569502957,-2.98495955491563,
-4.16960171583444));
#30372=CARTESIAN_POINT('Ctrl Pts',(-10.4443983062128,-0.620570198026758,
-5.09023129557908));
#30373=CARTESIAN_POINT('Ctrl Pts',(-10.30513966213,1.89575226084471,-4.76462856670633));
#30374=CARTESIAN_POINT('Ctrl Pts',(-10.1658810180471,3.94794105281364,-3.27251026838425));
#30375=CARTESIAN_POINT('Ctrl Pts',(-10.0266223739643,5.03356243225522,-0.979189079677917));
#30376=CARTESIAN_POINT('Ctrl Pts',(-9.88736372988145,4.88682564047436,1.55386523636191));
#30377=CARTESIAN_POINT('Ctrl Pts',(-9.74810508579864,3.54365598619697,3.7064894799071));
#30378=CARTESIAN_POINT('Ctrl Pts',(-9.6088464417158,1.33289931589153,4.95166047168699));
#30379=CARTESIAN_POINT('Ctrl Pts',(-9.46958779763295,-1.20418873213356,
4.98452520412669));
#30380=CARTESIAN_POINT('Ctrl Pts',(-9.33032915355013,-3.44645738659569,
3.79703746301662));
#30381=CARTESIAN_POINT('Ctrl Pts',(-9.20650303300273,-4.68995778663268,
1.91454404906327));
#30382=CARTESIAN_POINT('Ctrl Pts',(-9.12909646048294,-4.91756522986951,
0.54713990493291));
#30383=CARTESIAN_POINT('Ctrl Pts',(-9.09810943599077,-4.91800701852089,
-0.000109254779623522));
#30384=CARTESIAN_POINT('Origin',(-62.8183905640093,0.,0.));
#30385=CARTESIAN_POINT('',(-12.9433905640093,-4.91859595699376,-6.98021618343542E-5));
#30386=CARTESIAN_POINT('',(-12.5981094359908,-4.9178331468155,-2.64215081000052E-5));
#30387=CARTESIAN_POINT('',(-62.8183905640093,-4.91825,1.40632325245411E-12));
#30388=CARTESIAN_POINT('Ctrl Pts',(-12.9433905640093,-4.91859595699376,
-6.98021618345673E-5));
#30389=CARTESIAN_POINT('Ctrl Pts',(-12.939461786756,-4.91864391970094,-0.0694303996811109));
#30390=CARTESIAN_POINT('Ctrl Pts',(-12.8891134614751,-4.9002331927105,-0.958279418825322));
#30391=CARTESIAN_POINT('Ctrl Pts',(-12.7923455881666,-4.39215783380509,
-2.64660379567266));
#30392=CARTESIAN_POINT('Ctrl Pts',(-12.6530869440837,-2.58566237748044,
-4.42830804687374));
#30393=CARTESIAN_POINT('Ctrl Pts',(-12.5138283000009,-0.146123782862334,
-5.12583748556338));
#30394=CARTESIAN_POINT('Ctrl Pts',(-12.3745696559181,2.3291900385944,-4.56841721523299));
#30395=CARTESIAN_POINT('Ctrl Pts',(-12.2353110118352,4.23425239003886,-2.8925194529639));
#30396=CARTESIAN_POINT('Ctrl Pts',(-12.0960523677524,5.1026502315838,-0.50845127833681));
#30397=CARTESIAN_POINT('Ctrl Pts',(-11.9567937236695,4.72177525841466,2.00010012183084));
#30398=CARTESIAN_POINT('Ctrl Pts',(-11.8175350795867,3.18487641533271,4.01897055318671));
#30399=CARTESIAN_POINT('Ctrl Pts',(-11.6782764355039,0.868229922828961,
5.05388354529751));
#30400=CARTESIAN_POINT('Ctrl Pts',(-11.539017791421,-1.66098376324763,4.85146318408707));
#30401=CARTESIAN_POINT('Ctrl Pts',(-11.3997591473382,-3.78354173769753,
3.461267687918));
#30402=CARTESIAN_POINT('Ctrl Pts',(-11.2845500715343,-4.77319465007402,
1.6100852481797));
#30403=CARTESIAN_POINT('Ctrl Pts',(-11.215760543758,-4.91786607927562,0.395122348313753));
#30404=CARTESIAN_POINT('Ctrl Pts',(-11.1933905640093,-4.91782725633716,
1.3942835367757E-5));
#30405=CARTESIAN_POINT('Ctrl Pts',(-12.5981094359908,-4.9178331468155,-2.64215081003175E-5));
#30406=CARTESIAN_POINT('Ctrl Pts',(-12.576498946479,-4.91790431974439,-0.381719067368811));
#30407=CARTESIAN_POINT('Ctrl Pts',(-12.5084689089396,-4.77978222981794,
-1.58324067107775));
#30408=CARTESIAN_POINT('Ctrl Pts',(-12.3940193233725,-3.81173006932457,
-3.43020056145098));
#30409=CARTESIAN_POINT('Ctrl Pts',(-12.2547606792897,-1.70061563003689,
-4.83771314693687));
#30410=CARTESIAN_POINT('Ctrl Pts',(-12.1155020352069,0.826857520598954,
-5.06081699469566));
#30411=CARTESIAN_POINT('Ctrl Pts',(-11.9762433911241,3.1518926095914,-4.04488998500265));
#30412=CARTESIAN_POINT('Ctrl Pts',(-11.8369847470412,4.70525541587707,-2.03865972750019));
#30413=CARTESIAN_POINT('Ctrl Pts',(-11.6977261029584,5.10663887602661,0.466691978745618));
#30414=CARTESIAN_POINT('Ctrl Pts',(-11.5584674588755,4.25777298871062,2.85778431477567));
#30415=CARTESIAN_POINT('Ctrl Pts',(-11.4192088147927,2.36648408499891,4.54921038078241));
#30416=CARTESIAN_POINT('Ctrl Pts',(-11.2799501707098,-0.104186924024186,
5.12686133009603));
#30417=CARTESIAN_POINT('Ctrl Pts',(-11.140691526627,-2.54935003304931,4.44931190434692));
#30418=CARTESIAN_POINT('Ctrl Pts',(-11.0014328825442,-4.37036029072556,
2.68244532887828));
#30419=CARTESIAN_POINT('Ctrl Pts',(-10.9039055189988,-4.89632593945952,
0.985115881753022));
#30420=CARTESIAN_POINT('Ctrl Pts',(-10.852797703481,-4.91863020361453,0.0828516383189645));
#30421=CARTESIAN_POINT('Ctrl Pts',(-10.8481094359908,-4.91856570422813,
8.11450425238988E-5));
#30422=CARTESIAN_POINT('Origin',(-62.8183905640093,0.,0.));
#30423=CARTESIAN_POINT('',(-14.6933905640093,-4.91797489380483,0.000101859666493039));
#30424=CARTESIAN_POINT('',(-14.3481094359907,-4.9186636817339,-2.79553420690082E-5));
#30425=CARTESIAN_POINT('',(-62.8183905640093,-4.91825,1.40632325245411E-12));
#30426=CARTESIAN_POINT('Ctrl Pts',(-14.6933905640093,-4.91797489380483,
0.000101859666493224));
#30427=CARTESIAN_POINT('Ctrl Pts',(-14.663163029754,-4.91757672879938,-0.533744249622919));
#30428=CARTESIAN_POINT('Ctrl Pts',(-14.5865159474711,-4.69793048423044,
-1.88772206019698));
#30429=CARTESIAN_POINT('Ctrl Pts',(-14.4634493171606,-3.47740377609158,
-3.76871663386205));
#30430=CARTESIAN_POINT('Ctrl Pts',(-14.3241906730778,-1.2449244032235,-4.9745075453338));
#30431=CARTESIAN_POINT('Ctrl Pts',(-14.184932028995,1.29234760538017,-4.96239858890765));
#30432=CARTESIAN_POINT('Ctrl Pts',(-14.0456733849121,3.51321643969437,-3.73535437892922));
#30433=CARTESIAN_POINT('Ctrl Pts',(-13.9064147408293,4.87395071821435,-1.59378997510416));
#30434=CARTESIAN_POINT('Ctrl Pts',(-13.7671560967465,5.04140427864135,0.937979204258423));
#30435=CARTESIAN_POINT('Ctrl Pts',(-13.6278974526636,3.97457976249027,3.24010459706584));
#30436=CARTESIAN_POINT('Ctrl Pts',(-13.4886388085808,1.93466592572345,4.74896092257761));
#30437=CARTESIAN_POINT('Ctrl Pts',(-13.3493801644979,-0.57890874156636,
5.09513756019038));
#30438=CARTESIAN_POINT('Ctrl Pts',(-13.2101215204151,-2.95075020743805,
4.1938806971144));
#30439=CARTESIAN_POINT('Ctrl Pts',(-13.0747916535855,-4.55363129933737,
2.32023741237006));
#30440=CARTESIAN_POINT('Ctrl Pts',(-12.9858813347836,-4.91807722756079,
0.750083505076204));
#30441=CARTESIAN_POINT('Ctrl Pts',(-12.9433905640093,-4.91859595699376,
-6.98021618345673E-5));
#30442=CARTESIAN_POINT('Ctrl Pts',(-14.3481094359907,-4.9186636817339,-2.79553420692337E-5));
#30443=CARTESIAN_POINT('Ctrl Pts',(-14.3466197375046,-4.91867186760678,
-0.0263267848127573));
#30444=CARTESIAN_POINT('Ctrl Pts',(-14.2987104909908,-4.9120309881119,-0.872102582125515));
#30445=CARTESIAN_POINT('Ctrl Pts',(-14.2043816964495,-4.46016506967744,
-2.5303141236615));
#30446=CARTESIAN_POINT('Ctrl Pts',(-14.0651230523666,-2.70109609887331,
-4.35885786391608));
#30447=CARTESIAN_POINT('Ctrl Pts',(-13.9258644082838,-0.280722556306372,
-5.12023015689262));
#30448=CARTESIAN_POINT('Ctrl Pts',(-13.7866057642009,2.20837979230334,-4.62802557319187));
#30449=CARTESIAN_POINT('Ctrl Pts',(-13.6473471201181,4.15680842943421,-3.00274968889455));
#30450=CARTESIAN_POINT('Ctrl Pts',(-13.5080884760352,5.08753302431593,-0.642315918895402));
#30451=CARTESIAN_POINT('Ctrl Pts',(-13.3688298319524,4.7726859235525,1.87537491939491));
#30452=CARTESIAN_POINT('Ctrl Pts',(-13.2295711878696,3.28935058494016,3.93392103918285));
#30453=CARTESIAN_POINT('Ctrl Pts',(-13.0903125437867,1.00068937108082,5.02933224153838));
#30454=CARTESIAN_POINT('Ctrl Pts',(-12.9510538997039,-1.5329688483594,4.89342094276911));
#30455=CARTESIAN_POINT('Ctrl Pts',(-12.8117952556211,-3.69131302095292,
3.55946206532884));
#30456=CARTESIAN_POINT('Ctrl Pts',(-12.69414710105,-4.75122672230175,1.69628807645834));
#30457=CARTESIAN_POINT('Ctrl Pts',(-12.6229184945066,-4.91775143957992,
0.438160560839145));
#30458=CARTESIAN_POINT('Ctrl Pts',(-12.5981094359908,-4.9178331468155,-2.64215081003175E-5));
#30459=CARTESIAN_POINT('Origin',(-62.8183905640093,0.,0.));
#30460=CARTESIAN_POINT('',(-16.4433905640093,-4.91828387020536,-0.000128019577716025));
#30461=CARTESIAN_POINT('',(-16.0981094359907,-4.91789060884963,7.19626684395069E-5));
#30462=CARTESIAN_POINT('',(-62.8183905640093,-4.91825,1.40632325245411E-12));
#30463=CARTESIAN_POINT('Ctrl Pts',(-16.4433905640093,-4.91828387020536,
-0.000128019577716378));
#30464=CARTESIAN_POINT('Ctrl Pts',(-16.4332838207796,-4.91846947797415,
-0.178590220560657));
#30465=CARTESIAN_POINT('Ctrl Pts',(-16.3767575295224,-4.86519987727275,
-1.17660631794529));
#30466=CARTESIAN_POINT('Ctrl Pts',(-16.2738116902375,-4.20645144279858,
-2.93280213238163));
#30467=CARTESIAN_POINT('Ctrl Pts',(-16.1345530461547,-2.28548001951246,
-4.5904404111952));
#30468=CARTESIAN_POINT('Ctrl Pts',(-15.9952944020718,0.195041427264702,
-5.1242092980259));
#30469=CARTESIAN_POINT('Ctrl Pts',(-15.856035757989,2.62781122700226,-4.40342710210641));
#30470=CARTESIAN_POINT('Ctrl Pts',(-15.7167771139062,4.41721866030238,-2.60456165129585));
#30471=CARTESIAN_POINT('Ctrl Pts',(-15.5775184698233,5.12516627595581,-0.16802598647164));
#30472=CARTESIAN_POINT('Ctrl Pts',(-15.4382598257405,4.57832851364817,2.30964718289191));
#30473=CARTESIAN_POINT('Ctrl Pts',(-15.2990011816576,2.91058669377287,4.22185352497654));
#30474=CARTESIAN_POINT('Ctrl Pts',(-15.1597425375748,0.530251090985978,
5.10043094932504));
#30475=CARTESIAN_POINT('Ctrl Pts',(-15.020483893492,-1.97990494684484,4.73027890190248));
#30476=CARTESIAN_POINT('Ctrl Pts',(-14.8812252494091,-4.00532436477151,
3.20202105259979));
#30477=CARTESIAN_POINT('Ctrl Pts',(-14.7721941395816,-4.82334198966169,
1.39170572320378));
#30478=CARTESIAN_POINT('Ctrl Pts',(-14.7095825777816,-4.91818817925502,
0.286067743649002));
#30479=CARTESIAN_POINT('Ctrl Pts',(-14.6933905640093,-4.91797489380483,
0.000101859666493224));
#30480=CARTESIAN_POINT('Ctrl Pts',(-16.0981094359907,-4.91789060884963,
7.19626684395069E-5));
#30481=CARTESIAN_POINT('Ctrl Pts',(-16.0703209805026,-4.9176377461804,-0.490721850450886));
#30482=CARTESIAN_POINT('Ctrl Pts',(-15.9961129769868,-4.72269515954724,
-1.80156433640869));
#30483=CARTESIAN_POINT('Ctrl Pts',(-15.8754854254435,-3.57520314867229,
-3.6760691586116));
#30484=CARTESIAN_POINT('Ctrl Pts',(-15.7362267813606,-1.37516875424451,
-4.94008835047726));
#30485=CARTESIAN_POINT('Ctrl Pts',(-15.5969681372778,1.16154576959681,-4.99463446493368));
#30486=CARTESIAN_POINT('Ctrl Pts',(-15.457709493195,3.41388110083322,-3.82635307342976));
#30487=CARTESIAN_POINT('Ctrl Pts',(-15.3184508491121,4.83040197127458,-1.72127243894698));
#30488=CARTESIAN_POINT('Ctrl Pts',(-15.1791922050293,5.06430408617135,0.805224276807312));
#30489=CARTESIAN_POINT('Ctrl Pts',(-15.0399335609465,4.05832160518909,3.13457935966327));
#30490=CARTESIAN_POINT('Ctrl Pts',(-14.9006749168636,2.05874743662691,4.69650093211465));
#30491=CARTESIAN_POINT('Ctrl Pts',(-14.7614162727808,-0.444866218910259,
5.10858650317719));
#30492=CARTESIAN_POINT('Ctrl Pts',(-14.622157628698,-2.83956406633868,4.26994589267004));
#30493=CARTESIAN_POINT('Ctrl Pts',(-14.4843886831012,-4.52087640940268,
2.40605627265036));
#30494=CARTESIAN_POINT('Ctrl Pts',(-14.3930392855322,-4.9184167928232,0.793154331015322));
#30495=CARTESIAN_POINT('Ctrl Pts',(-14.3481094359907,-4.9186636817339,-2.79553420692337E-5));
#30496=CARTESIAN_POINT('Origin',(-62.8183905640093,0.,0.));
#30497=CARTESIAN_POINT('',(-18.1933905640093,-4.91828910572115,0.00012777880011387));
#30498=CARTESIAN_POINT('',(-17.8481094359907,-4.91841983696433,-0.000114968478700239));
#30499=CARTESIAN_POINT('',(-62.8183905640093,-4.91825,1.40632325245411E-12));
#30500=CARTESIAN_POINT('Ctrl Pts',(-18.1933905640093,-4.91828910572115,
0.000127778800113817));
#30501=CARTESIAN_POINT('Ctrl Pts',(-18.1569850637777,-4.91762032632294,
-0.642708953241472));
#30502=CARTESIAN_POINT('Ctrl Pts',(-18.0741600155184,-4.62942297978745,
-2.10578920461358));
#30503=CARTESIAN_POINT('Ctrl Pts',(-17.9449154192316,-3.21910722095246,
-3.99160503912099));
#30504=CARTESIAN_POINT('Ctrl Pts',(-17.8056567751488,-0.911389954514629,
-5.04627887052769));
#30505=CARTESIAN_POINT('Ctrl Pts',(-17.6663981310659,1.61946129957759,-4.86548118766222));
#30506=CARTESIAN_POINT('Ctrl Pts',(-17.5271394869831,3.75382271324905,-3.49347636686155));
#30507=CARTESIAN_POINT('Ctrl Pts',(-17.3878808429002,4.96914236350674,-1.26616991732043));
#30508=CARTESIAN_POINT('Ctrl Pts',(-17.2486221988174,4.96787569382644,1.27113066952724));
#30509=CARTESIAN_POINT('Ctrl Pts',(-17.1093635547345,3.75033282070164,3.49722258689558));
#30510=CARTESIAN_POINT('Ctrl Pts',(-16.9701049106517,1.61460260837161,4.86709569511061));
#30511=CARTESIAN_POINT('Ctrl Pts',(-16.8308462665689,-0.916427899620469,
5.0453663883926));
#30512=CARTESIAN_POINT('Ctrl Pts',(-16.691587622486,-3.22309098878473,3.98838896878665));
#30513=CARTESIAN_POINT('Ctrl Pts',(-16.5624357216328,-4.63051303268699,
2.1025194946162));
#30514=CARTESIAN_POINT('Ctrl Pts',(-16.4797033688073,-4.9176169947813,0.641073890954786));
#30515=CARTESIAN_POINT('Ctrl Pts',(-16.4433905640093,-4.91828387020536,
-0.000128019577716378));
#30516=CARTESIAN_POINT('Ctrl Pts',(-17.8481094359907,-4.91841983696433,
-0.000114968478700378));
#30517=CARTESIAN_POINT('Ctrl Pts',(-17.8404417715282,-4.91855474342418,
-0.135497772287647));
#30518=CARTESIAN_POINT('Ctrl Pts',(-17.7863545590381,-4.87991970941729,
-1.09040259937276));
#30519=CARTESIAN_POINT('Ctrl Pts',(-17.6858477985204,-4.28204082740422,
-2.82129196745304));
#30520=CARTESIAN_POINT('Ctrl Pts',(-17.5465891544375,-2.40527633894355,
-4.52881968580006));
#30521=CARTESIAN_POINT('Ctrl Pts',(-17.4073305103547,0.0603676936250531,
-5.12756450517573));
#30522=CARTESIAN_POINT('Ctrl Pts',(-17.2680718662719,2.51123201073006,-4.4709367923799));
#30523=CARTESIAN_POINT('Ctrl Pts',(-17.128813222189,4.34727584434856,-2.71969754684507));
#30524=CARTESIAN_POINT('Ctrl Pts',(-16.9895545781062,5.11898383601734,-0.302599570000859));
#30525=CARTESIAN_POINT('Ctrl Pts',(-16.8502959340234,4.63742008554047,2.18858332338469));
#30526=CARTESIAN_POINT('Ctrl Pts',(-16.7110372899405,3.02048499265497,4.14393923969909));
#30527=CARTESIAN_POINT('Ctrl Pts',(-16.5717786458577,0.664049911073469,
5.08474185468397));
#30528=CARTESIAN_POINT('Ctrl Pts',(-16.4325200017749,-1.85496333359322,
4.78065613113894));
#30529=CARTESIAN_POINT('Ctrl Pts',(-16.293261357692,-3.91982919214168,3.30613083794419));
#30530=CARTESIAN_POINT('Ctrl Pts',(-16.1817911690973,-4.80447615881922,
1.47792554344552));
#30531=CARTESIAN_POINT('Ctrl Pts',(-16.1167405285302,-4.91806014356135,
0.329130371615684));
#30532=CARTESIAN_POINT('Ctrl Pts',(-16.0981094359907,-4.91789060884963,
7.19626684395069E-5));
#30533=CARTESIAN_POINT('Origin',(-62.8183905640093,0.,0.));
#30534=CARTESIAN_POINT('',(-19.9433905640093,-4.91797114886923,-0.000100888655958004));
#30535=CARTESIAN_POINT('',(-19.5981094359907,-4.91815380942886,0.000127431703268871));
#30536=CARTESIAN_POINT('',(-62.8183905640093,-4.91825,1.40632325245411E-12));
#30537=CARTESIAN_POINT('Ctrl Pts',(-19.9433905640093,-4.91797114886923,
-0.000100888655957566));
#30538=CARTESIAN_POINT('Ctrl Pts',(-19.9271058548033,-4.91818339028267,
-0.287704486859558));
#30539=CARTESIAN_POINT('Ctrl Pts',(-19.8644015975697,-4.8226470466571,-1.39498245192419));
#30540=CARTESIAN_POINT('Ctrl Pts',(-19.7552777923085,-4.00212534708821,
-3.20601852685208));
#30541=CARTESIAN_POINT('Ctrl Pts',(-19.6160191482256,-1.97518106715403,
-4.7322533575751));
#30542=CARTESIAN_POINT('Ctrl Pts',(-19.4767605041428,0.535343293589886,
-5.09989898393416));
#30543=CARTESIAN_POINT('Ctrl Pts',(-19.3375018600599,2.91480050434934,-4.21894537866626));
#30544=CARTESIAN_POINT('Ctrl Pts',(-19.1982432159771,4.5806322724203,-2.30507485197035));
#30545=CARTESIAN_POINT('Ctrl Pts',(-19.0589845718943,5.12499595774547,0.17314306632675));
#30546=CARTESIAN_POINT('Ctrl Pts',(-18.9197259278114,4.41461596381525,2.60897067449063));
#30547=CARTESIAN_POINT('Ctrl Pts',(-18.7804672837286,2.6234133658075,4.40604861530454));
#30548=CARTESIAN_POINT('Ctrl Pts',(-18.6412086396458,0.189925121925963,
5.12440148079616));
#30549=CARTESIAN_POINT('Ctrl Pts',(-18.5019499955629,-2.29006215302471,
4.58815621177052));
#30550=CARTESIAN_POINT('Ctrl Pts',(-18.3626913514801,-4.20937756885579,
2.92860078725975));
#30551=CARTESIAN_POINT('Ctrl Pts',(-18.2598382076289,-4.86578064424309,
1.17333004967791));
#30552=CARTESIAN_POINT('Ctrl Pts',(-18.2034046118053,-4.9184730666286,0.176952646436098));
#30553=CARTESIAN_POINT('Ctrl Pts',(-18.1933905640093,-4.91828910572115,
0.000127778800113817));
#30554=CARTESIAN_POINT('Ctrl Pts',(-19.5981094359907,-4.91815380942886,
0.00012743170326894));
#30555=CARTESIAN_POINT('Ctrl Pts',(-19.5641430145262,-4.91756248201972,
-0.599688267675223));
#30556=CARTESIAN_POINT('Ctrl Pts',(-19.4837570450341,-4.65747068326959,
-2.01972912110533));
#30557=CARTESIAN_POINT('Ctrl Pts',(-19.3569515275144,-3.32285072098886,
-3.90566576900731));
#30558=CARTESIAN_POINT('Ctrl Pts',(-19.2176928834316,-1.04363474385184,
-5.02059643215792));
#30559=CARTESIAN_POINT('Ctrl Pts',(-19.0784342393487,1.49109247838584,-4.90634336691521));
#30560=CARTESIAN_POINT('Ctrl Pts',(-18.9391755952659,3.66075817123595,-3.59087894879527));
#30561=CARTESIAN_POINT('Ctrl Pts',(-18.7999169511831,4.93416692759049,-1.39626600038956));
#30562=CARTESIAN_POINT('Ctrl Pts',(-18.6606583071003,4.99955233800879,1.14019227882075));
#30563=CARTESIAN_POINT('Ctrl Pts',(-18.5213996630174,3.84090620831584,3.39749930273613));
#30564=CARTESIAN_POINT('Ctrl Pts',(-18.3821410189346,1.74189781741689,4.82300259245731));
#30565=CARTESIAN_POINT('Ctrl Pts',(-18.2428823748517,-0.783576329617824,
5.0676987034387));
#30566=CARTESIAN_POINT('Ctrl Pts',(-18.1036237307689,-3.11720887230625,
4.0716791204105));
#30567=CARTESIAN_POINT('Ctrl Pts',(-17.9720327511486,-4.60119067126923,
2.18852680733519));
#30568=CARTESIAN_POINT('Ctrl Pts',(-17.8868613195558,-4.91773802838363,
0.68410102396266));
#30569=CARTESIAN_POINT('Ctrl Pts',(-17.8481094359907,-4.91841983696433,
-0.000114968478700378));
#30570=CARTESIAN_POINT('Origin',(-62.8183905640093,0.,0.));
#30571=CARTESIAN_POINT('',(-21.6933905640093,-4.91859939228904,6.83533682649098E-5));
#30572=CARTESIAN_POINT('',(-21.3481094359907,-4.9180816331187,-0.00012121564703732));
#30573=CARTESIAN_POINT('',(-62.8183905640093,-4.91825,1.40632325245411E-12));
#30574=CARTESIAN_POINT('Ctrl Pts',(-21.6933905640093,-4.91859939228904,
6.83533682647487E-5));
#30575=CARTESIAN_POINT('Ctrl Pts',(-21.6508070978013,-4.9180883067121,-0.751719922183042));
#30576=CARTESIAN_POINT('Ctrl Pts',(-21.5618040835657,-4.55241160406376,
-2.32350050460025));
#30577=CARTESIAN_POINT('Ctrl Pts',(-21.4263815213025,-2.94656140448722,
-4.19682474948749));
#30578=CARTESIAN_POINT('Ctrl Pts',(-21.2871228772196,-0.573821271236779,
-5.09571302537738));
#30579=CARTESIAN_POINT('Ctrl Pts',(-21.1478642331369,1.93940650708562,-4.74702691045655));
#30580=CARTESIAN_POINT('Ctrl Pts',(-21.008605589054,3.97781282675011,-3.23613460839731));
#30581=CARTESIAN_POINT('Ctrl Pts',(-20.8693469449712,5.04233828040476,-0.932945204333682));
#30582=CARTESIAN_POINT('Ctrl Pts',(-20.7300883008883,4.87235698748461,1.59865552100332));
#30583=CARTESIAN_POINT('Ctrl Pts',(-20.5908296568055,3.50948516674211,3.73886024782176));
#30584=CARTESIAN_POINT('Ctrl Pts',(-20.4515710127226,1.28739231115071,4.96368644512469));
#30585=CARTESIAN_POINT('Ctrl Pts',(-20.3123123686398,-1.24989052282436,
4.97326208531968));
#30586=CARTESIAN_POINT('Ctrl Pts',(-20.173053724557,-3.48116487480147,3.76524278138513));
#30587=CARTESIAN_POINT('Ctrl Pts',(-20.0500797896801,-4.69889501505713,
1.8844482318336));
#30588=CARTESIAN_POINT('Ctrl Pts',(-19.9735254028309,-4.91757839633652,
0.532109294943383));
#30589=CARTESIAN_POINT('Ctrl Pts',(-19.9433905640093,-4.91797114886923,
-0.000100888655957566));
#30590=CARTESIAN_POINT('Ctrl Pts',(-21.3481094359907,-4.9180816331187,-0.000121215647037425));
#30591=CARTESIAN_POINT('Ctrl Pts',(-21.3342638055519,-4.91830558366444,
-0.244632590468481));
#30592=CARTESIAN_POINT('Ctrl Pts',(-21.2739986270854,-4.84035702823606,
-1.30876342941487));
#30593=CARTESIAN_POINT('Ctrl Pts',(-21.1673139005913,-4.08496228675852,
-3.0997814647056));
#30594=CARTESIAN_POINT('Ctrl Pts',(-21.0280552565085,-2.09880971056153,
-4.67873485164786));
#30595=CARTESIAN_POINT('Ctrl Pts',(-20.8887966124256,0.401190728150701,
-5.11220187520187));
#30596=CARTESIAN_POINT('Ctrl Pts',(-20.7495379683428,2.80296835176735,-4.29405757205957));
#30597=CARTESIAN_POINT('Ctrl Pts',(-20.61027932426,4.51850020045465,-2.4246067622736));
#30598=CARTESIAN_POINT('Ctrl Pts',(-20.4710206801771,5.12777565148253,0.0384562249122501));
#30599=CARTESIAN_POINT('Ctrl Pts',(-20.3317620360943,4.48162687576275,2.49210404269421));
#30600=CARTESIAN_POINT('Ctrl Pts',(-20.1925033920114,2.7382493331312,4.33561444351065));
#30601=CARTESIAN_POINT('Ctrl Pts',(-20.0532447479286,0.324471058226111,
5.11764404248138));
#30602=CARTESIAN_POINT('Ctrl Pts',(-19.9139861038458,-2.16874689092793,
4.64672991858383));
#30603=CARTESIAN_POINT('Ctrl Pts',(-19.774727459763,-4.13099438162065,3.03816514234996));
#30604=CARTESIAN_POINT('Ctrl Pts',(-19.6694352371446,-4.84993378643301,
1.25954143487284));
#30605=CARTESIAN_POINT('Ctrl Pts',(-19.6105625625539,-4.91837060810086,
0.220038169922159));
#30606=CARTESIAN_POINT('Ctrl Pts',(-19.5981094359907,-4.91815380942886,
0.00012743170326894));
#30607=CARTESIAN_POINT('Origin',(-62.8183905640093,0.,0.));
#30608=CARTESIAN_POINT('',(-23.4433905640093,-4.91782678713688,-1.24087024978041E-5));
#30609=CARTESIAN_POINT('',(-23.0981094359907,-4.91849236054295,0.000101443248962593));
#30610=CARTESIAN_POINT('',(-62.8183905640093,-4.91825,1.40632325245411E-12));
#30611=CARTESIAN_POINT('Ctrl Pts',(-23.4433905640093,-4.91782678713688,
-1.24087024978153E-5));
#30612=CARTESIAN_POINT('Ctrl Pts',(-23.4209278888269,-4.91786147762014,
-0.396758149880408));
#30613=CARTESIAN_POINT('Ctrl Pts',(-23.352045665617,-4.77238244581433,-1.61336155032251));
#30614=CARTESIAN_POINT('Ctrl Pts',(-23.2367438943794,-3.78008398872379,
-3.46504359662597));
#30615=CARTESIAN_POINT('Ctrl Pts',(-23.0974852502966,-1.65613904746037,
-4.85311915615117));
#30616=CARTESIAN_POINT('Ctrl Pts',(-22.9582266062137,0.873275482247959,
-5.05301415201156));
#30617=CARTESIAN_POINT('Ctrl Pts',(-22.8189679621309,3.18888752301124,-4.01578864656841));
#30618=CARTESIAN_POINT('Ctrl Pts',(-22.679709318048,4.72376988196712,-1.99538472243945));
#30619=CARTESIAN_POINT('Ctrl Pts',(-22.5404506739652,5.10214003086018,0.513545707623582));
#30620=CARTESIAN_POINT('Ctrl Pts',(-22.4011920298823,4.23136227657829,2.89674565205072));
#30621=CARTESIAN_POINT('Ctrl Pts',(-22.2619333857996,2.32462759375435,4.57074049128587));
#30622=CARTESIAN_POINT('Ctrl Pts',(-22.1226747417167,-0.151241543795875,
5.12568903502298));
#30623=CARTESIAN_POINT('Ctrl Pts',(-21.9834160976339,-2.59008248216644,
4.42572421462287));
#30624=CARTESIAN_POINT('Ctrl Pts',(-21.844157453551,-4.39479811584537,2.64221717678288));
#30625=CARTESIAN_POINT('Ctrl Pts',(-21.7474822756762,-4.90070245514728,
0.955004116442912));
#30626=CARTESIAN_POINT('Ctrl Pts',(-21.6972266458289,-4.91864543283634,
0.0677923221493221));
#30627=CARTESIAN_POINT('Ctrl Pts',(-21.6933905640093,-4.91859939228904,
6.83533682647487E-5));
#30628=CARTESIAN_POINT('Ctrl Pts',(-23.0981094359907,-4.91849236054295,
0.00010144324896242));
#30629=CARTESIAN_POINT('Ctrl Pts',(-23.0579650485499,-4.91784091118313,
-0.708670863612696));
#30630=CARTESIAN_POINT('Ctrl Pts',(-22.9714011130814,-4.58384955508688,
-2.23760099730615));
#30631=CARTESIAN_POINT('Ctrl Pts',(-22.8384176295854,-3.05578981514007,
-4.11797409157195));
#30632=CARTESIAN_POINT('Ctrl Pts',(-22.6991589855025,-0.707481122127949,
-5.0788810258761));
#30633=CARTESIAN_POINT('Ctrl Pts',(-22.5599003414197,1.81403892041534,-4.79633451798247));
#30634=CARTESIAN_POINT('Ctrl Pts',(-22.4206416973369,3.89143102840395,-3.33950992876898));
#30635=CARTESIAN_POINT('Ctrl Pts',(-22.281383053254,5.01609097301024,-1.06507904103722));
#30636=CARTESIAN_POINT('Ctrl Pts',(-22.1421244091712,4.91267025280302,1.47011326107748));
#30637=CARTESIAN_POINT('Ctrl Pts',(-22.0028657650884,3.60648917945748,3.64538033840472));
#30638=CARTESIAN_POINT('Ctrl Pts',(-21.8636071210055,1.41733775071325,4.92815540680027));
#30639=CARTESIAN_POINT('Ctrl Pts',(-21.7243484769227,-1.11881796813,5.00437891924276));
#30640=CARTESIAN_POINT('Ctrl Pts',(-21.5850898328398,-3.38105546629115,
3.85538920824271));
#30641=CARTESIAN_POINT('Ctrl Pts',(-21.4596768191959,-4.67289564265827,
1.97057534616266));
#30642=CARTESIAN_POINT('Ctrl Pts',(-21.3806833535795,-4.91755475594594,
0.575128384443069));
#30643=CARTESIAN_POINT('Ctrl Pts',(-21.3481094359907,-4.9180816331187,-0.000121215647037425));
#30644=CARTESIAN_POINT('Origin',(-62.8183905640093,0.,0.));
#30645=CARTESIAN_POINT('',(-25.1933905640093,-4.9186458426816,-4.33410623697303E-5));
#30646=CARTESIAN_POINT('',(-24.8481094359907,-4.91785710431715,-5.1574967852297E-5));
#30647=CARTESIAN_POINT('',(-62.8183905640093,-4.91825,1.40632325245411E-12));
#30648=CARTESIAN_POINT('Ctrl Pts',(-25.1933905640093,-4.9186458426816,-4.33410623697228E-5));
#30649=CARTESIAN_POINT('Ctrl Pts',(-25.1910486798525,-4.91866493426688,
-0.0413869169074745));
#30650=CARTESIAN_POINT('Ctrl Pts',(-25.1422872476682,-4.90803869591004,
-0.902210422761663));
#30651=CARTESIAN_POINT('Ctrl Pts',(-25.0471062674563,-4.43675165169258,
-2.57114699492807));
#30652=CARTESIAN_POINT('Ctrl Pts',(-24.9078476233734,-2.6609727408645,-4.38346736735891));
#30653=CARTESIAN_POINT('Ctrl Pts',(-24.7685889792906,-0.233712588919614,
-5.12259119138986));
#30654=CARTESIAN_POINT('Ctrl Pts',(-24.6293303352077,2.25076700205062,-4.60756009085119));
#30655=CARTESIAN_POINT('Ctrl Pts',(-24.490071691125,4.18419529608634,-2.96446821749421));
#30656=CARTESIAN_POINT('Ctrl Pts',(-24.3508130470421,5.09321446983781,-0.595590843246681));
#30657=CARTESIAN_POINT('Ctrl Pts',(-24.2115544029592,4.75527096970404,1.91910398181406));
#30658=CARTESIAN_POINT('Ctrl Pts',(-24.0722957588764,3.25310290401414,3.96394797950469));
#30659=CARTESIAN_POINT('Ctrl Pts',(-23.9330371147936,0.954483418570409,
5.03830561716918));
#30660=CARTESIAN_POINT('Ctrl Pts',(-23.7937784707108,-1.57782055097424,
4.8791438180533));
#30661=CARTESIAN_POINT('Ctrl Pts',(-23.6545198266279,-3.72382951079462,
3.52542988341273));
#30662=CARTESIAN_POINT('Ctrl Pts',(-23.5377238577274,-4.75904335759611,
1.66617135078586));
#30663=CARTESIAN_POINT('Ctrl Pts',(-23.4673474368545,-4.91778978907276,
0.423124514933955));
#30664=CARTESIAN_POINT('Ctrl Pts',(-23.4433905640093,-4.91782678713688,
-1.24087024978153E-5));
#30665=CARTESIAN_POINT('Ctrl Pts',(-24.8481094359907,-4.91785710431715,
-5.15749678527133E-5));
#30666=CARTESIAN_POINT('Ctrl Pts',(-24.8280858395755,-4.91798659206747,
-0.353710986347212));
#30667=CARTESIAN_POINT('Ctrl Pts',(-24.7616426951327,-4.79316176184979,
-1.527148550185));
#30668=CARTESIAN_POINT('Ctrl Pts',(-24.6487800026622,-3.86980180875062,
-3.36454989176295));
#30669=CARTESIAN_POINT('Ctrl Pts',(-24.5095213585794,-1.7830527771394,-4.80793976741671));
#30670=CARTESIAN_POINT('Ctrl Pts',(-24.3702627144966,0.740237906473115,
-5.07421026909526));
#30671=CARTESIAN_POINT('Ctrl Pts',(-24.2310040704137,3.08229745508568,-4.09817086168255));
#30672=CARTESIAN_POINT('Ctrl Pts',(-24.0917454263309,4.66972357935212,-2.11878354383227));
#30673=CARTESIAN_POINT('Ctrl Pts',(-23.9524867822481,5.11386955405928,0.379341794741001));
#30674=CARTESIAN_POINT('Ctrl Pts',(-23.8132281381652,4.30599590721036,2.78459355387089));
#30675=CARTESIAN_POINT('Ctrl Pts',(-23.6739694940824,2.44389291227653,4.50809820728166));
#30676=CARTESIAN_POINT('Ctrl Pts',(-23.5347108499995,-0.0165440539888569,
5.12789316459004));
#30677=CARTESIAN_POINT('Ctrl Pts',(-23.3954522059167,-2.47293056883089,
4.49223512462487));
#30678=CARTESIAN_POINT('Ctrl Pts',(-23.2561935618339,-4.32387387433953,
2.75675111897605));
#30679=CARTESIAN_POINT('Ctrl Pts',(-23.1570793051919,-4.88780213881696,
1.04119196874099));
#30680=CARTESIAN_POINT('Ctrl Pts',(-23.1043845965775,-4.91859419169813,
0.110893021562895));
#30681=CARTESIAN_POINT('Ctrl Pts',(-23.0981094359907,-4.91849236054295,
0.00010144324896242));
#30682=CARTESIAN_POINT('Origin',(-62.8183905640093,0.,0.));
#30683=CARTESIAN_POINT('',(-26.9433905640093,-4.91791654477181,8.33642798827967E-5));
#30684=CARTESIAN_POINT('',(-26.5981094359907,-4.91867656610995,1.84189480952973E-6));
#30685=CARTESIAN_POINT('',(-62.8183905640093,-4.91825,1.40632325245411E-12));
#30686=CARTESIAN_POINT('Ctrl Pts',(-26.9433905640093,-4.91791654477181,
8.33642798828485E-5));
#30687=CARTESIAN_POINT('Ctrl Pts',(-26.9147499228506,-4.91761260288967,
-0.5057539384102));
#30688=CARTESIAN_POINT('Ctrl Pts',(-26.8396897336642,-4.71418759851164,
-1.83166998375507));
#30689=CARTESIAN_POINT('Ctrl Pts',(-26.7182099964503,-3.54131022572266,
-3.7087307766292));
#30690=CARTESIAN_POINT('Ctrl Pts',(-26.5789513523675,-1.32976618835693,
-4.95250279885102));
#30691=CARTESIAN_POINT('Ctrl Pts',(-26.4396927082847,1.20734214866586,-4.9837623362656));
#30692=CARTESIAN_POINT('Ctrl Pts',(-26.3004340642018,3.44885904674366,-3.79485617171704));
#30693=CARTESIAN_POINT('Ctrl Pts',(-26.161175420119,4.84599789550719,-1.67686209482602));
#30694=CARTESIAN_POINT('Ctrl Pts',(-26.0219167760362,5.05669966623105,0.851675157476819));
#30695=CARTESIAN_POINT('Ctrl Pts',(-25.8826581319533,4.02937861773551,3.1716982900743));
#30696=CARTESIAN_POINT('Ctrl Pts',(-25.7433994878705,2.01555194199366,4.71520015030647));
#30697=CARTESIAN_POINT('Ctrl Pts',(-25.6041408437876,-0.491738744311117,
5.1042879126934));
#30698=CARTESIAN_POINT('Ctrl Pts',(-25.4648821997048,-2.87863790516758,
4.24370190980198));
#30699=CARTESIAN_POINT('Ctrl Pts',(-25.3279654397787,-4.53247725666741,
2.37608246776745));
#30700=CARTESIAN_POINT('Ctrl Pts',(-25.2374682278802,-4.91828651129618,
0.77810285122316));
#30701=CARTESIAN_POINT('Ctrl Pts',(-25.1933905640093,-4.9186458426816,-4.33410623697228E-5));
#30702=CARTESIAN_POINT('Ctrl Pts',(-26.5981094359907,-4.9186765389473,1.84177752225913E-6));
#30703=CARTESIAN_POINT('Ctrl Pts',(-26.5517870825735,-4.91865835826029,
-0.81775719113905));
#30704=CARTESIAN_POINT('Ctrl Pts',(-26.4590451811287,-4.50155560752193,
-2.45500895652049));
#30705=CARTESIAN_POINT('Ctrl Pts',(-26.3198837316563,-2.77520256653693,
-4.31205435121805));
#30706=CARTESIAN_POINT('Ctrl Pts',(-26.1806250875735,-0.36819586088392,
-5.11468413699221));
#30707=CARTESIAN_POINT('Ctrl Pts',(-26.0413664434906,2.12895558497593,-4.6650948683142));
#30708=CARTESIAN_POINT('Ctrl Pts',(-25.9021077994078,4.10487860730363,-3.07335868919861));
#30709=CARTESIAN_POINT('Ctrl Pts',(-25.762849155325,5.07581147371895,-0.729177547950212));
#30710=CARTESIAN_POINT('Ctrl Pts',(-25.6235905112421,4.80404241095214,1.79352684031905));
#30711=CARTESIAN_POINT('Ctrl Pts',(-25.4843318671593,3.35610815708752,3.87712523025787));
#30712=CARTESIAN_POINT('Ctrl Pts',(-25.3450732230764,1.08650388987611,5.01149392002581));
#30713=CARTESIAN_POINT('Ctrl Pts',(-25.2058145789936,-1.44910719949644,
4.91890743331681));
#30714=CARTESIAN_POINT('Ctrl Pts',(-25.0665559349108,-3.62993594091732,
3.62203355561599));
#30715=CARTESIAN_POINT('Ctrl Pts',(-24.9473208872432,-4.7362640055411,1.75236430941362));
#30716=CARTESIAN_POINT('Ctrl Pts',(-24.8745053876031,-4.91768640808852,
0.466157217721872));
#30717=CARTESIAN_POINT('Ctrl Pts',(-24.8481094359907,-4.91785710431715,
-5.15749678527133E-5));
#30718=CARTESIAN_POINT('Origin',(-62.8183905640093,0.,0.));
#30719=CARTESIAN_POINT('',(-28.6933905640092,-4.91837309484402,-0.000121104502655431));
#30720=CARTESIAN_POINT('',(-28.3481094359907,-4.9178533390618,4.85856934917539E-5));
#30721=CARTESIAN_POINT('',(-62.8183905640093,-4.91825,1.40632325245411E-12));
#30722=CARTESIAN_POINT('Ctrl Pts',(-28.6933905640092,-4.91837309484402,
-0.000121104502655602));
#30723=CARTESIAN_POINT('Ctrl Pts',(-28.6848707138762,-4.91852719604813,
-0.150554503830029));
#30724=CARTESIAN_POINT('Ctrl Pts',(-28.6299313157155,-4.87490927511793,
-1.12052014919942));
#30725=CARTESIAN_POINT('Ctrl Pts',(-28.5285723695273,-4.25596405301566,
-2.86047759434731));
#30726=CARTESIAN_POINT('Ctrl Pts',(-28.3893137254443,-2.36360537794301,
-4.55070672595844));
#30727=CARTESIAN_POINT('Ctrl Pts',(-28.2500550813616,0.107430613693398,
-5.12679439333839));
#30728=CARTESIAN_POINT('Ctrl Pts',(-28.1107964372787,2.55216455853763,-4.44769807366338));
#30729=CARTESIAN_POINT('Ctrl Pts',(-27.9715377931959,4.37205657674479,-2.67967971557556));
#30730=CARTESIAN_POINT('Ctrl Pts',(-27.832279149113,5.12154573019909,-0.255600120899675));
#30731=CARTESIAN_POINT('Ctrl Pts',(-27.6930205050302,4.61713591749465,2.23105759847328));
#30732=CARTESIAN_POINT('Ctrl Pts',(-27.5537618609474,2.98232089930236,4.17148943926614));
#30733=CARTESIAN_POINT('Ctrl Pts',(-27.4145032168645,0.617349539765915,
5.09062291218622));
#30734=CARTESIAN_POINT('Ctrl Pts',(-27.2752445727817,-1.89876641369781,
4.76342819768889));
#30735=CARTESIAN_POINT('Ctrl Pts',(-27.1359859286988,-3.9500107505568,3.27001179796192));
#30736=CARTESIAN_POINT('Ctrl Pts',(-27.0253679257747,-4.81120499508792,
1.44780147547091));
#30737=CARTESIAN_POINT('Ctrl Pts',(-26.9611694708782,-4.91810521912398,
0.314085912111188));
#30738=CARTESIAN_POINT('Ctrl Pts',(-26.9433905640093,-4.91791654477181,
8.33642798828485E-5));
#30739=CARTESIAN_POINT('Ctrl Pts',(-28.3481094359907,-4.91785333906181,
4.85856934917886E-5));
#30740=CARTESIAN_POINT('Ctrl Pts',(-28.3219078735991,-4.91769386938119,
-0.462727892406216));
#30741=CARTESIAN_POINT('Ctrl Pts',(-28.24928676318,-4.73812545833518,-1.74549558120992));
#30742=CARTESIAN_POINT('Ctrl Pts',(-28.1302461047332,-3.63751179343058,
-3.61442526078837));
#30743=CARTESIAN_POINT('Ctrl Pts',(-27.9909874606504,-1.45940322528745,
-4.91586251223447));
#30744=CARTESIAN_POINT('Ctrl Pts',(-27.8517288165675,1.07600844855802,-5.01375785532204));
#30745=CARTESIAN_POINT('Ctrl Pts',(-27.7124701724847,3.34798288054322,-3.88414374666556));
#30746=CARTESIAN_POINT('Ctrl Pts',(-27.5732115284018,4.80027659624061,-1.80358160690233));
#30747=CARTESIAN_POINT('Ctrl Pts',(-27.433952884319,5.07732709858328,0.718548221877666));
#30748=CARTESIAN_POINT('Ctrl Pts',(-27.2946942402362,4.11130460399385,3.06475716270483));
#30749=CARTESIAN_POINT('Ctrl Pts',(-27.1554355961534,2.13871868810873,4.66062703788945));
#30750=CARTESIAN_POINT('Ctrl Pts',(-27.0161769520704,-0.357485934549103,
5.11544385364273));
#30751=CARTESIAN_POINT('Ctrl Pts',(-26.8769183079877,-2.76616790928751,
4.3178556148625));
#30752=CARTESIAN_POINT('Ctrl Pts',(-26.7376596639048,-4.49761389622142,
2.46313443678733));
#30753=CARTESIAN_POINT('Ctrl Pts',(-26.6447233732392,-4.9182559093769,0.822908377436444));
#30754=CARTESIAN_POINT('Ctrl Pts',(-26.5982066306011,-4.91867657709443,
0.00171768228997997));
#30755=CARTESIAN_POINT('Ctrl Pts',(-26.5981094359907,-4.9186765389473,1.84177752225913E-6));
#30756=CARTESIAN_POINT('Origin',(-62.8183905640093,0.,0.));
#30757=CARTESIAN_POINT('',(-30.4433905640093,-4.91820020867345,0.000129117068208339));
#30758=CARTESIAN_POINT('',(-30.0981094359907,-4.91850196224555,-9.92246832554056E-5));
#30759=CARTESIAN_POINT('',(-62.8183905640093,-4.91825,1.40632325245411E-12));
#30760=CARTESIAN_POINT('Ctrl Pts',(-30.4433905640093,-4.91820020867345,
0.000129117068208267));
#30761=CARTESIAN_POINT('Ctrl Pts',(-30.4085719568742,-4.91757590647288,
-0.614718730968464));
#30762=CARTESIAN_POINT('Ctrl Pts',(-30.3273338017115,-4.64782072635045,
-2.04980313689827));
#30763=CARTESIAN_POINT('Ctrl Pts',(-30.1996760985213,-3.28686098148408,
-3.93600139440042));
#30764=CARTESIAN_POINT('Ctrl Pts',(-30.0604174544384,-0.997507167463827,
-5.02996436758579));
#30765=CARTESIAN_POINT('Ctrl Pts',(-29.9211588103556,1.53606455886436,-4.89245007734626));
#30766=CARTESIAN_POINT('Ctrl Pts',(-29.7819001662728,3.69356432102827,-3.55712590369689));
#30767=CARTESIAN_POINT('Ctrl Pts',(-29.6426415221899,4.94677527517285,-1.35091689798559));
#30768=CARTESIAN_POINT('Ctrl Pts',(-29.5033828781071,4.98887600398362,1.18603469814376));
#30769=CARTESIAN_POINT('Ctrl Pts',(-29.3641242340243,3.80955906062489,3.43261152068441));
#30770=CARTESIAN_POINT('Ctrl Pts',(-29.2248655899414,1.6975545226847,4.83878814692659));
#30771=CARTESIAN_POINT('Ctrl Pts',(-29.0856069458586,-0.83005928111469,
5.06029284509897));
#30772=CARTESIAN_POINT('Ctrl Pts',(-28.9463483017757,-3.15445114191686,
4.0428950124365));
#30773=CARTESIAN_POINT('Ctrl Pts',(-28.815609507826,-4.6115871884147,2.15848371842179));
#30774=CARTESIAN_POINT('Ctrl Pts',(-28.7312902619038,-4.91768759110979,
0.669066768371859));
#30775=CARTESIAN_POINT('Ctrl Pts',(-28.6933905640092,-4.91837309484402,
-0.000121104502655602));
#30776=CARTESIAN_POINT('Ctrl Pts',(-30.0981094359907,-4.91850196224555,
-9.92246832555964E-5));
#30777=CARTESIAN_POINT('Ctrl Pts',(-30.0920286646248,-4.91859912603189,
-0.107458143160632));
#30778=CARTESIAN_POINT('Ctrl Pts',(-30.0395283452312,-4.8888725063671,-1.03432258519129));
#30779=CARTESIAN_POINT('Ctrl Pts',(-29.9406084778101,-4.32963647845777,
-2.74769175446946));
#30780=CARTESIAN_POINT('Ctrl Pts',(-29.8013498337272,-2.48233098445573,
-4.48704745871744));
#30781=CARTESIAN_POINT('Ctrl Pts',(-29.6620911896444,-0.0272807940196574,
-5.12784728433378));
#30782=CARTESIAN_POINT('Ctrl Pts',(-29.5228325455616,2.43444850487691,-4.5132053454584));
#30783=CARTESIAN_POINT('Ctrl Pts',(-29.3835739014787,4.30015608997081,-2.79360333889022));
#30784=CARTESIAN_POINT('Ctrl Pts',(-29.2443152573959,5.11306407908685,-0.390048376901321));
#30785=CARTESIAN_POINT('Ctrl Pts',(-29.105056613313,4.67414964965714,2.10900143807006));
#30786=CARTESIAN_POINT('Ctrl Pts',(-28.9657979692302,3.09087144371802,4.09170816793918));
#30787=CARTESIAN_POINT('Ctrl Pts',(-28.8265393251474,0.750860658988233,
5.07264923722855));
#30788=CARTESIAN_POINT('Ctrl Pts',(-28.6872806810645,-1.77298201041712,
4.81166258209249));
#30789=CARTESIAN_POINT('Ctrl Pts',(-28.5480220369817,-3.86274863579312,
3.37264510286066));
#30790=CARTESIAN_POINT('Ctrl Pts',(-28.4349649552904,-4.79155068651975,
1.53401980474453));
#30791=CARTESIAN_POINT('Ctrl Pts',(-28.3683274216268,-4.91797639110214,
0.357142107335489));
#30792=CARTESIAN_POINT('Ctrl Pts',(-28.3481094359907,-4.91785333906181,
4.85856934917886E-5));
#30793=CARTESIAN_POINT('Origin',(-62.8183905640093,0.,0.));
#30794=CARTESIAN_POINT('',(-32.1933905640093,-4.9180404057301,-0.000115405238602364));
#30795=CARTESIAN_POINT('',(-31.8481094359907,-4.91807200796895,0.000120019908876473));
#30796=CARTESIAN_POINT('',(-62.8183905640093,-4.91825,1.40632325245411E-12));
#30797=CARTESIAN_POINT('Ctrl Pts',(-32.1933905640093,-4.9180404057301,-0.000115405238602581));
#30798=CARTESIAN_POINT('Ctrl Pts',(-32.1786927478998,-4.91826392058507,
-0.259682470608151));
#30799=CARTESIAN_POINT('Ctrl Pts',(-32.1175753837628,-4.83430517290801,
-1.33888704426319));
#30800=CARTESIAN_POINT('Ctrl Pts',(-32.0100384715981,-4.0563375838621,-3.13714639347168));
#30801=CARTESIAN_POINT('Ctrl Pts',(-31.8707798275153,-2.05577560156633,
-4.69780254633261));
#30802=CARTESIAN_POINT('Ctrl Pts',(-31.7315211834325,0.448098278592388,
-5.10830402590205));
#30803=CARTESIAN_POINT('Ctrl Pts',(-31.5922625393496,2.84226505119731,-4.26814848231254));
#30804=CARTESIAN_POINT('Ctrl Pts',(-31.4530038952668,4.54056510758199,-2.38302970861326));
#30805=CARTESIAN_POINT('Ctrl Pts',(-31.313745251184,5.12720665419247,0.0855220061093843));
#30806=CARTESIAN_POINT('Ctrl Pts',(-31.1744866071012,4.45856328065359,2.5331355196144));
#30807=CARTESIAN_POINT('Ctrl Pts',(-31.0352279630183,2.69833775932673,4.360565952364));
#30808=CARTESIAN_POINT('Ctrl Pts',(-30.8959693189355,0.277482985620765,
5.12040674956741));
#30809=CARTESIAN_POINT('Ctrl Pts',(-30.7567106748526,-2.21130745577726,
4.62662743522194));
#30810=CARTESIAN_POINT('Ctrl Pts',(-30.6174520307698,-4.15870741103577,
3.00011912392169));
#30811=CARTESIAN_POINT('Ctrl Pts',(-30.513011993822,-4.85560432133482,1.22941940689503));
#30812=CARTESIAN_POINT('Ctrl Pts',(-30.4549915049018,-4.91840821506784,
0.204985489275344));
#30813=CARTESIAN_POINT('Ctrl Pts',(-30.4433905640093,-4.91820020867345,
0.000129117068208267));
#30814=CARTESIAN_POINT('Ctrl Pts',(-31.8481094359907,-4.91807200796895,
0.000120019908876265));
#30815=CARTESIAN_POINT('Ctrl Pts',(-31.8157299076228,-4.91755498663457,
-0.57169991192379));
#30816=CARTESIAN_POINT('Ctrl Pts',(-31.7369308312273,-4.67501516669824,
-1.96371255691315));
#30817=CARTESIAN_POINT('Ctrl Pts',(-31.6117122068041,-3.38912046412381,
-3.84830150752625));
#30818=CARTESIAN_POINT('Ctrl Pts',(-31.4724535627214,-1.12929367800508,
-5.00202536998659));
#30819=CARTESIAN_POINT('Ctrl Pts',(-31.3331949186384,1.40701607828237,-4.93111222429854));
#30820=CARTESIAN_POINT('Ctrl Pts',(-31.1939362745556,3.59884858124293,-3.65292361026856));
#30821=CARTESIAN_POINT('Ctrl Pts',(-31.0546776304728,4.90958136292712,-1.48039618142248));
#30822=CARTESIAN_POINT('Ctrl Pts',(-30.9154189863899,5.01831003890801,1.05457402137864));
#30823=CARTESIAN_POINT('Ctrl Pts',(-30.7761603423071,3.89841476010363,3.33135473514573));
#30824=CARTESIAN_POINT('Ctrl Pts',(-30.6369016982242,1.82407750325954,4.79252577199894));
#30825=CARTESIAN_POINT('Ctrl Pts',(-30.4976430541415,-0.696845416589377,
5.08035121606272));
#30826=CARTESIAN_POINT('Ctrl Pts',(-30.3583844100586,-3.04716090784859,
4.12436327387041));
#30827=CARTESIAN_POINT('Ctrl Pts',(-30.2252065373417,-4.5813938197129,2.24444978973811));
#30828=CARTESIAN_POINT('Ctrl Pts',(-30.1384482126524,-4.91785739463383,
0.712101115451537));
#30829=CARTESIAN_POINT('Ctrl Pts',(-30.0981094359907,-4.91850196224555,
-9.92246832555964E-5));
#30830=CARTESIAN_POINT('Origin',(-62.8183905640093,0.,0.));
#30831=CARTESIAN_POINT('',(-33.9433905640093,-4.91853326571986,9.11492385194351E-5));
#30832=CARTESIAN_POINT('',(-33.5981094359907,-4.91816426918661,-0.000127960998163867));
#30833=CARTESIAN_POINT('',(-62.8183905640093,-4.91825,1.40632325245411E-12));
#30834=CARTESIAN_POINT('Ctrl Pts',(-33.9433905640093,-4.91853326571986,
9.11492385192135E-5));
#30835=CARTESIAN_POINT('Ctrl Pts',(-33.9023939908979,-4.91791720891167,
-0.723709576353512));
#30836=CARTESIAN_POINT('Ctrl Pts',(-33.8149778697589,-4.57302002945823,
-2.26762205719794));
#30837=CARTESIAN_POINT('Ctrl Pts',(-33.6811422005921,-3.01786256635649,
-4.1458494447952));
#30838=CARTESIAN_POINT('Ctrl Pts',(-33.5418835565094,-0.660832717283021,
-5.08516098153175));
#30839=CARTESIAN_POINT('Ctrl Pts',(-33.4026249124265,1.85798763502059,-4.7794815656549));
#30840=CARTESIAN_POINT('Ctrl Pts',(-33.2633662683437,3.92192016684631,-3.30365014691457));
#30841=CARTESIAN_POINT('Ctrl Pts',(-33.1241076242608,5.02565593354922,-1.01899191650671));
#30842=CARTESIAN_POINT('Ctrl Pts',(-32.9848489801781,4.89896926309818,1.51514429924805));
#30843=CARTESIAN_POINT('Ctrl Pts',(-32.8455903360952,3.57287662854112,3.67833042093137));
#30844=CARTESIAN_POINT('Ctrl Pts',(-32.7063316920124,1.37204293986752,4.94095742336282));
#30845=CARTESIAN_POINT('Ctrl Pts',(-32.5670730479295,-1.16470559062442,
4.99389857481034));
#30846=CARTESIAN_POINT('Ctrl Pts',(-32.4278144038467,-3.41630131512815,
3.82419238697246));
#30847=CARTESIAN_POINT('Ctrl Pts',(-32.3032535758732,-4.68212636122256,
1.94048764453586));
#30848=CARTESIAN_POINT('Ctrl Pts',(-32.2251122959274,-4.91755800220454,
0.560098221135963));
#30849=CARTESIAN_POINT('Ctrl Pts',(-32.1933905640093,-4.9180404057301,-0.000115405238602581));
#30850=CARTESIAN_POINT('Ctrl Pts',(-33.5981094359907,-4.91816426918661,
-0.00012796099816411));
#30851=CARTESIAN_POINT('Ctrl Pts',(-33.5858506986484,-4.91837934192607,
-0.21660464215519));
#30852=CARTESIAN_POINT('Ctrl Pts',(-33.5271724132785,-4.85123996273957,
-1.25267033401488));
#30853=CARTESIAN_POINT('Ctrl Pts',(-33.422074579881,-4.13734663286075,-3.02950901182476));
#30854=CARTESIAN_POINT('Ctrl Pts',(-33.2828159357982,-2.17847145432949,
-4.64217881342837));
#30855=CARTESIAN_POINT('Ctrl Pts',(-33.1435572917154,0.313755030289582,
-5.11831220170669));
#30856=CARTESIAN_POINT('Ctrl Pts',(-33.0042986476325,2.72916542679145,-4.34133828287751));
#30857=CARTESIAN_POINT('Ctrl Pts',(-32.8650400035497,4.47639908771296,-2.50148220475266));
#30858=CARTESIAN_POINT('Ctrl Pts',(-32.7257813594668,5.12768389180779,-0.0491926708628662));
#30859=CARTESIAN_POINT('Ctrl Pts',(-32.586522715384,4.52356693451351,2.41514061746884));
#30860=CARTESIAN_POINT('Ctrl Pts',(-32.4472640713011,2.81195310003798,4.28817930785997));
#30861=CARTESIAN_POINT('Ctrl Pts',(-32.3080054272183,0.411893770634228,
5.11135065661556));
#30862=CARTESIAN_POINT('Ctrl Pts',(-32.1687467831355,-2.08900878079138,
4.68311908101302));
#30863=CARTESIAN_POINT('Ctrl Pts',(-32.0294881390527,-4.07846301397088,
3.10832775891526));
#30864=CARTESIAN_POINT('Ctrl Pts',(-31.9226090233377,-4.83898935836676,
1.31563478630209));
#30865=CARTESIAN_POINT('Ctrl Pts',(-31.8621494556504,-4.91829619250977,
0.24806566610592));
#30866=CARTESIAN_POINT('Ctrl Pts',(-31.8481094359907,-4.91807200796895,
0.000120019908876265));
#30867=CARTESIAN_POINT('Origin',(-62.8183905640093,0.,0.));
#30868=CARTESIAN_POINT('',(-35.6933905640092,-4.91784231204611,-3.82622793895393E-5));
#30869=CARTESIAN_POINT('',(-35.3481094359907,-4.91840929431599,0.000116514561900802));
#30870=CARTESIAN_POINT('',(-62.8183905640093,-4.91825,1.40632325245411E-12));
#30871=CARTESIAN_POINT('Ctrl Pts',(-35.6933905640093,-4.91784231204611,
-3.82622793893006E-5));
#30872=CARTESIAN_POINT('Ctrl Pts',(-35.6725147819235,-4.91794209965865,
-0.368752264205334));
#30873=CARTESIAN_POINT('Ctrl Pts',(-35.6052194518101,-4.78604129458979,
-1.55727124936419));
#30874=CARTESIAN_POINT('Ctrl Pts',(-35.4915045736691,-3.8387558835552,-3.39992872789929));
#30875=CARTESIAN_POINT('Ctrl Pts',(-35.3522459295862,-1.73884600907171,
-4.82410371416908));
#30876=CARTESIAN_POINT('Ctrl Pts',(-35.2129872855035,0.786782452717923,
-5.06720193602146));
#30877=CARTESIAN_POINT('Ctrl Pts',(-35.0737286414205,3.11978436072366,-4.06970608655078));
#30878=CARTESIAN_POINT('Ctrl Pts',(-34.9344699973378,4.68897499169966,-2.07583130710078));
#30879=CARTESIAN_POINT('Ctrl Pts',(-34.7952113532549,5.11017218394326,0.426265573061127));
#30880=CARTESIAN_POINT('Ctrl Pts',(-34.6559527091721,4.28025497520489,2.82400060827867));
#30881=CARTESIAN_POINT('Ctrl Pts',(-34.5166940650892,2.40241052515365,4.53034057847261));
#30882=CARTESIAN_POINT('Ctrl Pts',(-34.3774354210064,-0.0636118368933031,
5.12752529223713));
#30883=CARTESIAN_POINT('Ctrl Pts',(-34.2381767769235,-2.51406022562872,
4.46934707426445));
#30884=CARTESIAN_POINT('Ctrl Pts',(-34.0989181328408,-4.34899570403538,
2.71694653142206));
#30885=CARTESIAN_POINT('Ctrl Pts',(-34.0006560618693,-4.89244018058238,
1.01107768639465));
#30886=CARTESIAN_POINT('Ctrl Pts',(-33.9488135389255,-4.91861475693642,
0.0958345951248656));
#30887=CARTESIAN_POINT('Ctrl Pts',(-33.9433905640093,-4.91853326571986,
9.11492385192135E-5));
#30888=CARTESIAN_POINT('Ctrl Pts',(-35.3481094359907,-4.91840929431599,
0.000116514561900646));
#30889=CARTESIAN_POINT('Ctrl Pts',(-35.3095519416465,-4.91772571242185,
-0.68067148944363));
#30890=CARTESIAN_POINT('Ctrl Pts',(-35.2245748992746,-4.60357657753055,
-2.18167446257958));
#30891=CARTESIAN_POINT('Ctrl Pts',(-35.0931783088751,-3.125727316038,-4.06514338725531));
#30892=CARTESIAN_POINT('Ctrl Pts',(-34.9539196647922,-0.794185353227152,
-5.06604694390913));
#30893=CARTESIAN_POINT('Ctrl Pts',(-34.8146610207094,1.73179560238191,-4.82663920391221));
#30894=CARTESIAN_POINT('Ctrl Pts',(-34.6754023766266,3.83378410926193,-3.40553394003679));
#30895=CARTESIAN_POINT('Ctrl Pts',(-34.5361437325437,4.99715404582752,-1.15065783595354));
#30896=CARTESIAN_POINT('Ctrl Pts',(-34.3968850884609,4.93707961190701,1.38593178723334));
#30897=CARTESIAN_POINT('Ctrl Pts',(-34.257626444378,3.6682687247101,3.58320618671119));
#30898=CARTESIAN_POINT('Ctrl Pts',(-34.1183678002952,1.5013621055187,4.90321056464884));
#30899=CARTESIAN_POINT('Ctrl Pts',(-33.9791091562124,-1.03312033767432,
5.02277058813713));
#30900=CARTESIAN_POINT('Ctrl Pts',(-33.8398505121295,-3.31466575920044,
3.91261458847608));
#30901=CARTESIAN_POINT('Ctrl Pts',(-33.712850605389,-4.6552835507772,2.02658970348332));
#30902=CARTESIAN_POINT('Ctrl Pts',(-33.632270246676,-4.91756493673245,0.603116787323793));
#30903=CARTESIAN_POINT('Ctrl Pts',(-33.5981094359907,-4.91816426918661,
-0.00012796099816411));
#30904=CARTESIAN_POINT('Origin',(-62.8183905640093,0.,0.));
#30905=CARTESIAN_POINT('',(-37.4433905640093,-4.91867318169596,-1.4270610707154E-5));
#30906=CARTESIAN_POINT('',(-37.0981094359907,-4.91789617187166,-7.46432797521512E-5));
#30907=CARTESIAN_POINT('',(-62.8183905640093,-4.91825,1.40632325245411E-12));
#30908=CARTESIAN_POINT('Ctrl Pts',(-37.4433905640093,-4.91867318169596,
-1.42706107073378E-5));
#30909=CARTESIAN_POINT('Ctrl Pts',(-37.4426355729491,-4.91867538847336,
-0.0133426519680256));
#30910=CARTESIAN_POINT('Ctrl Pts',(-37.3954610338614,-4.91536146633527,
-0.846146440759592));
#30911=CARTESIAN_POINT('Ctrl Pts',(-37.3018669467459,-4.48004925758386,
-2.49493902489554));
#30912=CARTESIAN_POINT('Ctrl Pts',(-37.1626083026632,-2.7355056920653,-4.33734604303171));
#30913=CARTESIAN_POINT('Ctrl Pts',(-37.0233496585803,-0.321233115053798,
-5.11784831487974));
#30914=CARTESIAN_POINT('Ctrl Pts',(-36.8840910144975,2.17168639631715,-4.64535685221012));
#30915=CARTESIAN_POINT('Ctrl Pts',(-36.7448323704146,4.13291577533089,-3.03555090261152));
#30916=CARTESIAN_POINT('Ctrl Pts',(-36.6055737263318,5.08229070826373,-0.68255640427784));
#30917=CARTESIAN_POINT('Ctrl Pts',(-36.4663150822489,4.78737741250149,1.8375471690803));
#30918=CARTESIAN_POINT('Ctrl Pts',(-36.3270564381661,3.3203789876831,3.90776732501783));
#30919=CARTESIAN_POINT('Ctrl Pts',(-36.1877977940833,1.04045805875398,5.02125573101972));
#30920=CARTESIAN_POINT('Ctrl Pts',(-36.0485391500004,-1.49419637309213,
4.90539899365616));
#30921=CARTESIAN_POINT('Ctrl Pts',(-35.9092805059176,-3.66302935450954,
3.58856211264706));
#30922=CARTESIAN_POINT('Ctrl Pts',(-35.7908976439206,-4.74436522801712,
1.72225148136041));
#30923=CARTESIAN_POINT('Ctrl Pts',(-35.7189343299511,-4.91772021116346,
0.451122998456921));
#30924=CARTESIAN_POINT('Ctrl Pts',(-35.6933905640093,-4.91784231204611,
-3.82622793893006E-5));
#30925=CARTESIAN_POINT('Ctrl Pts',(-37.0981094359907,-4.91789617187166,
-7.46432797522553E-5));
#30926=CARTESIAN_POINT('Ctrl Pts',(-37.0796727326721,-4.91807043539616,
-0.325698736799547));
#30927=CARTESIAN_POINT('Ctrl Pts',(-37.0148164813258,-4.80602407783864,
-1.47105406828722));
#30928=CARTESIAN_POINT('Ctrl Pts',(-36.903540681952,-3.92674297249402,-3.29791625744811));
#30929=CARTESIAN_POINT('Ctrl Pts',(-36.7642820378691,-1.86496899934438,
-4.7767617320373));
#30930=CARTESIAN_POINT('Ctrl Pts',(-36.6250233937863,0.653402029340091,
-5.08612109580827));
#30931=CARTESIAN_POINT('Ctrl Pts',(-36.4857647497035,3.01180179695694,-4.15025444388879));
#30932=CARTESIAN_POINT('Ctrl Pts',(-36.3465061056206,4.63282746729464,-2.19828835038808));
#30933=CARTESIAN_POINT('Ctrl Pts',(-36.2072474615378,5.11960619781114,0.291880784748528));
#30934=CARTESIAN_POINT('Ctrl Pts',(-36.0679888174549,4.35296081444672,2.71058926454433));
#30935=CARTESIAN_POINT('Ctrl Pts',(-35.9287301733721,2.52058774797673,4.46566897764727));
#30936=CARTESIAN_POINT('Ctrl Pts',(-35.7894715292892,0.0711036494477585,
5.12742686775803));
#30937=CARTESIAN_POINT('Ctrl Pts',(-35.6502128852065,-2.39578862958558,
4.53384592322236));
#30938=CARTESIAN_POINT('Ctrl Pts',(-35.5109542411235,-4.27612422358166,
2.83025151491343));
#30939=CARTESIAN_POINT('Ctrl Pts',(-35.410253091385,-4.87878928807346,1.09727250995654));
#30940=CARTESIAN_POINT('Ctrl Pts',(-35.3559714896741,-4.9185486798658,0.138932377093802));
#30941=CARTESIAN_POINT('Ctrl Pts',(-35.3481094359907,-4.91840929431599,
0.000116514561900646));
#30942=CARTESIAN_POINT('Origin',(-62.8183905640093,0.,0.));
#30943=CARTESIAN_POINT('',(-39.1933905640093,-4.91787152802865,6.14470143739343E-5));
#30944=CARTESIAN_POINT('',(-38.8481094359907,-4.91866022846763,3.15193572706859E-5));
#30945=CARTESIAN_POINT('',(-62.8183905640093,-4.91825,1.40632325245411E-12));
#30946=CARTESIAN_POINT('Ctrl Pts',(-39.1933905640093,-4.91787152802865,
6.14470143736612E-5));
#30947=CARTESIAN_POINT('Ctrl Pts',(-39.1663368159471,-4.91766233869729,
-0.477761426883304));
#30948=CARTESIAN_POINT('Ctrl Pts',(-39.0928635198574,-4.72990563556455,
-1.7756065190772));
#30949=CARTESIAN_POINT('Ctrl Pts',(-38.9729706757401,-3.60418206959766,
-3.64766140116037));
#30950=CARTESIAN_POINT('Ctrl Pts',(-38.8337120316572,-1.41421947780232,
-4.92905116193056));
#30951=CARTESIAN_POINT('Ctrl Pts',(-38.6944533875743,1.12198396286053,-5.00367006060634));
#30952=CARTESIAN_POINT('Ctrl Pts',(-38.5551947434916,3.38349405796131,-3.85324928444358));
#30953=CARTESIAN_POINT('Ctrl Pts',(-38.4159360994086,4.81662929812997,-1.75944431361739));
#30954=CARTESIAN_POINT('Ctrl Pts',(-38.2766774553259,5.07051772191601,0.765122290918382));
#30955=CARTESIAN_POINT('Ctrl Pts',(-38.137418811243,4.08300027639372,3.10236536070355));
#30956=CARTESIAN_POINT('Ctrl Pts',(-37.9981601671602,2.09584910794909,4.68006181636883));
#30957=CARTESIAN_POINT('Ctrl Pts',(-37.8589015230773,-0.404425083919172,
5.11194703022454));
#30958=CARTESIAN_POINT('Ctrl Pts',(-37.7196428789945,-2.80568459910014,
4.29228331062813));
#30959=CARTESIAN_POINT('Ctrl Pts',(-37.5811392259718,-4.51073897975614,
2.43188858802557));
#30960=CARTESIAN_POINT('Ctrl Pts',(-37.4890551209767,-4.91853970791323,
0.806133857362442));
#30961=CARTESIAN_POINT('Ctrl Pts',(-37.4433905640093,-4.91867318169596,
-1.42706107073378E-5));
#30962=CARTESIAN_POINT('Ctrl Pts',(-38.8481094359907,-4.91866022846763,
3.15193572706382E-5));
#30963=CARTESIAN_POINT('Ctrl Pts',(-38.8033739756701,-4.91838593018476,
-0.789720674032932));
#30964=CARTESIAN_POINT('Ctrl Pts',(-38.7122189673219,-4.52353751094886,
-2.39922006544932));
#30965=CARTESIAN_POINT('Ctrl Pts',(-38.574644410946,-2.84849824938738,-4.26399105726181));
#30966=CARTESIAN_POINT('Ctrl Pts',(-38.4353857668631,-0.455561595795777,
-5.10764384482783));
#30967=CARTESIAN_POINT('Ctrl Pts',(-38.2961271227804,2.04890939607611,-4.70080124019754));
#30968=CARTESIAN_POINT('Ctrl Pts',(-38.1568684786975,4.05174953100885,-3.14306979737026));
#30969=CARTESIAN_POINT('Ctrl Pts',(-38.0176098346146,5.06260700763802,-0.815826145318977));
#30970=CARTESIAN_POINT('Ctrl Pts',(-37.8783511905319,4.83399538111841,1.71115477631265));
#30971=CARTESIAN_POINT('Ctrl Pts',(-37.7390925464489,3.42188523088942,3.81919670608788));
#30972=CARTESIAN_POINT('Ctrl Pts',(-37.5998339023662,1.17200098288635,4.99219147362009));
#30973=CARTESIAN_POINT('Ctrl Pts',(-37.4605752582833,-1.36482218906556,
4.94295684842645));
#30974=CARTESIAN_POINT('Ctrl Pts',(-37.3213166142005,-3.56749836282337,
3.68354685655336));
#30975=CARTESIAN_POINT('Ctrl Pts',(-37.2004946734363,-4.72076817860514,
1.80843190677617));
#30976=CARTESIAN_POINT('Ctrl Pts',(-37.1260922806997,-4.91763167831984,
0.494150831035411));
#30977=CARTESIAN_POINT('Ctrl Pts',(-37.0981094359907,-4.91789617187166,
-7.46432797522553E-5));
#30978=CARTESIAN_POINT('Origin',(-62.8183905640093,0.,0.));
#30979=CARTESIAN_POINT('',(-40.9433905640093,-4.91845884819695,-0.000108359509173095));
#30980=CARTESIAN_POINT('',(-40.5981094359907,-4.91783128990945,2.3246260680565E-5));
#30981=CARTESIAN_POINT('',(-62.8183905640093,-4.91825,1.40632325245411E-12));
#30982=CARTESIAN_POINT('Ctrl Pts',(-40.9433905640093,-4.91845884819695,
-0.000108359509173109));
#30983=CARTESIAN_POINT('Ctrl Pts',(-40.9364576069728,-4.9185764495009,-0.12251612456806));
#30984=CARTESIAN_POINT('Ctrl Pts',(-40.8831051019086,-4.88412565353057,
-1.06443786785133));
#30985=CARTESIAN_POINT('Ctrl Pts',(-40.7833330488169,-4.30423326894481,
-2.78731735811214));
#30986=CARTESIAN_POINT('Ctrl Pts',(-40.6440744047341,-2.4410402010708,-4.50964353636523));
#30987=CARTESIAN_POINT('Ctrl Pts',(-40.5048157606512,0.0197884139050482,
-5.12788167833459));
#30988=CARTESIAN_POINT('Ctrl Pts',(-40.3655571165684,2.47577226656799,-4.49066963518998));
#30989=CARTESIAN_POINT('Ctrl Pts',(-40.2262984724856,4.32561718207586,-2.75401490236612));
#30990=CARTESIAN_POINT('Ctrl Pts',(-40.0870398284027,5.11642890754077,-0.343099580888201));
#30991=CARTESIAN_POINT('Ctrl Pts',(-39.94778118432,4.65459440947177,2.15181620303378));
#30992=CARTESIAN_POINT('Ctrl Pts',(-39.808522540237,3.0531838096976,4.11990663881172));
#30993=CARTESIAN_POINT('Ctrl Pts',(-39.6692638961543,0.704267627790603,
5.07932763235163));
#30994=CARTESIAN_POINT('Ctrl Pts',(-39.5300052520714,-1.81707314952296,
4.79518584182169));
#30995=CARTESIAN_POINT('Ctrl Pts',(-39.3907466079886,-3.89354312734584,
3.33704719832106));
#30996=CARTESIAN_POINT('Ctrl Pts',(-39.2785417119678,-4.79855598410901,
1.50389656853719));
#30997=CARTESIAN_POINT('Ctrl Pts',(-39.2127563639747,-4.91802127137425,
0.342099902225225));
#30998=CARTESIAN_POINT('Ctrl Pts',(-39.1933905640093,-4.91787152802865,
6.14470143736612E-5));
#30999=CARTESIAN_POINT('Ctrl Pts',(-40.5981094359907,-4.91783128990945,
2.32462606805997E-5));
#31000=CARTESIAN_POINT('Ctrl Pts',(-40.5734947666957,-4.91775999740035,
-0.434730829549026));
#31001=CARTESIAN_POINT('Ctrl Pts',(-40.5024605493732,-4.75302315511206,
-1.68941841504038));
#31002=CARTESIAN_POINT('Ctrl Pts',(-40.3850067840229,-3.69875772681961,
-3.5517253964044));
#31003=CARTESIAN_POINT('Ctrl Pts',(-40.2457481399401,-1.54321132674375,
-4.89020048813763));
#31004=CARTESIAN_POINT('Ctrl Pts',(-40.1064894958572,0.990156768012798,
-5.03141645940088));
#31005=CARTESIAN_POINT('Ctrl Pts',(-39.9672308517744,3.28110653573467,-3.9407996541731));
#31006=CARTESIAN_POINT('Ctrl Pts',(-39.8279722076915,4.76874880416872,-1.88536385239323));
#31007=CARTESIAN_POINT('Ctrl Pts',(-39.6887135636088,5.08886675271635,0.631662240655434));
#31008=CARTESIAN_POINT('Ctrl Pts',(-39.5494549195259,4.16308647125779,2.99403958657897));
#31009=CARTESIAN_POINT('Ctrl Pts',(-39.410196275443,2.21806510569457,4.62339152571701));
#31010=CARTESIAN_POINT('Ctrl Pts',(-39.2709376313602,-0.270001209463393,
5.12080670989053));
#31011=CARTESIAN_POINT('Ctrl Pts',(-39.1316789872773,-2.69196360692879,
4.36450386093798));
#31012=CARTESIAN_POINT('Ctrl Pts',(-38.9924203431946,-4.45485732445219,
2.53964726526075));
#31013=CARTESIAN_POINT('Ctrl Pts',(-38.8978971594323,-4.91113255473073,
0.878970252247324));
#31014=CARTESIAN_POINT('Ctrl Pts',(-38.8497935236977,-4.91867055455711,
0.0297621167608296));
#31015=CARTESIAN_POINT('Ctrl Pts',(-38.8481094359907,-4.91866022846763,
3.15193572706382E-5));
#31016=CARTESIAN_POINT('Origin',(-62.8183905640093,0.,0.));
#31017=CARTESIAN_POINT('',(-42.6933905640093,-4.91811507793926,0.00012467419432587));
#31018=CARTESIAN_POINT('',(-42.3481094359907,-4.91857378612503,-7.83346265964546E-5));
#31019=CARTESIAN_POINT('',(-62.8183905640093,-4.91825,1.40632325245411E-12));
#31020=CARTESIAN_POINT('Ctrl Pts',(-42.6933905640093,-4.91811507793926,
0.000124674194325845));
#31021=CARTESIAN_POINT('Ctrl Pts',(-42.6601588499708,-4.91755631155856,
-0.586730043688538));
#31022=CARTESIAN_POINT('Ctrl Pts',(-42.5805075879047,-4.66566210384887,
-1.99379652867801));
#31023=CARTESIAN_POINT('Ctrl Pts',(-42.454436777811,-3.35365447446679,-3.87924783356431));
#31024=CARTESIAN_POINT('Ctrl Pts',(-42.3151781337281,-1.08333295532153,
-5.01218034354698));
#31025=CARTESIAN_POINT('Ctrl Pts',(-42.1759194896453,1.45221905169649,-4.91798962119831));
#31026=CARTESIAN_POINT('Ctrl Pts',(-42.0366608455625,3.63222684150266,-3.61973621417252));
#31027=CARTESIAN_POINT('Ctrl Pts',(-41.8974022014796,4.9229629697167,-1.43526920371147));
#31028=CARTESIAN_POINT('Ctrl Pts',(-41.7581435573968,5.00841879714827,1.10059222271303));
#31029=CARTESIAN_POINT('Ctrl Pts',(-41.618884913314,3.8676723249881,3.36699760541134));
#31030=CARTESIAN_POINT('Ctrl Pts',(-41.4796262692311,1.78001049070443,4.80906693042493));
#31031=CARTESIAN_POINT('Ctrl Pts',(-41.3403676251483,-0.743448157983408,
5.07374092014123));
#31032=CARTESIAN_POINT('Ctrl Pts',(-41.2011089810654,-3.08488971148233,
4.09621991063895));
#31033=CARTESIAN_POINT('Ctrl Pts',(-41.0687832940191,-4.59209593044371,
2.21442192660095));
#31034=CARTESIAN_POINT('Ctrl Pts',(-40.9828771550004,-4.91778905108657,
0.697063904442349));
#31035=CARTESIAN_POINT('Ctrl Pts',(-40.9433905640093,-4.91845884819695,
-0.000108359509173109));
#31036=CARTESIAN_POINT('Ctrl Pts',(-42.3481094359907,-4.91857378612503,
-7.83346265965153E-5));
#31037=CARTESIAN_POINT('Ctrl Pts',(-42.3436155577213,-4.91863393370315,
-0.0794165444578229));
#31038=CARTESIAN_POINT('Ctrl Pts',(-42.2927021314243,-4.89733658468067,
-0.978247065527181));
#31039=CARTESIAN_POINT('Ctrl Pts',(-42.1953691570999,-4.37596721157521,
-2.67328879404945));
#31040=CARTESIAN_POINT('Ctrl Pts',(-42.0561105130169,-2.5586604085778,-4.44396432554854));
#31041=CARTESIAN_POINT('Ctrl Pts',(-41.9168518689342,-0.114921311488126,
-5.12663194556987));
#31042=CARTESIAN_POINT('Ctrl Pts',(-41.7775932248512,2.35695376666187,-4.55415535033556));
#31043=CARTESIAN_POINT('Ctrl Pts',(-41.6383345807685,4.25178003045199,-2.86669297027451));
#31044=CARTESIAN_POINT('Ctrl Pts',(-41.4990759366856,5.10565052319778,-0.477383229849849));
#31045=CARTESIAN_POINT('Ctrl Pts',(-41.3598172926028,4.70951364514992,2.02880340085441));
#31046=CARTESIAN_POINT('Ctrl Pts',(-41.2205586485199,3.16035488623825,4.03828168980343));
#31047=CARTESIAN_POINT('Ctrl Pts',(-41.0813000044371,0.837452040422802,
5.05907462814725));
#31048=CARTESIAN_POINT('Ctrl Pts',(-40.9420413603542,-1.6904827045519,4.84126328955393));
#31049=CARTESIAN_POINT('Ctrl Pts',(-40.8027827162714,-3.80453956437015,
3.43817403810713));
#31050=CARTESIAN_POINT('Ctrl Pts',(-40.6881387414835,-4.77810753769317,
1.59011154568654));
#31051=CARTESIAN_POINT('Ctrl Pts',(-40.6199143147233,-4.91789444430315,
0.385149683993097));
#31052=CARTESIAN_POINT('Ctrl Pts',(-40.5981094359907,-4.91783128990945,
2.32462606805997E-5));
#31053=CARTESIAN_POINT('Origin',(-62.8183905640093,0.,0.));
#31054=CARTESIAN_POINT('',(-44.4433905640093,-4.91811906887483,-0.000125018227360122));
#31055=CARTESIAN_POINT('',(-44.0981094359908,-4.9179985551391,0.000107459425146145));
#31056=CARTESIAN_POINT('',(-62.8183905640093,-4.91825,1.40632325245411E-12));
#31057=CARTESIAN_POINT('Ctrl Pts',(-44.4433905640092,-4.91811906887483,
-0.000125018227360024));
#31058=CARTESIAN_POINT('Ctrl Pts',(-44.4302796409964,-4.91834041492064,
-0.231656533346569));
#31059=CARTESIAN_POINT('Ctrl Pts',(-44.3707491699559,-4.84545805489063,
-1.2827929143631));
#31060=CARTESIAN_POINT('Ctrl Pts',(-44.2647991508879,-4.10936474789597,
-3.06735773216533));
#31061=CARTESIAN_POINT('Ctrl Pts',(-44.125540506805,-2.13576953418586,-4.66197925619238));
#31062=CARTESIAN_POINT('Ctrl Pts',(-43.9862818627222,0.360722350167653,
-5.11521665957699));
#31063=CARTESIAN_POINT('Ctrl Pts',(-43.8470232186393,2.7688992207005,-4.31610463194866));
#31064=CARTESIAN_POINT('Ctrl Pts',(-43.7077645745566,4.49917140129531,-2.46028835506957));
#31065=CARTESIAN_POINT('Ctrl Pts',(-43.5685059304736,5.12791941987977,-0.00212403965129634));
#31066=CARTESIAN_POINT('Ctrl Pts',(-43.4292472863909,4.50120801315461,2.4565603006312));
#31067=CARTESIAN_POINT('Ctrl Pts',(-43.289988642308,2.77247382434629,4.31380933533684));
#31068=CARTESIAN_POINT('Ctrl Pts',(-43.1507299982252,0.364959781723236,
5.11491607419408));
#31069=CARTESIAN_POINT('Ctrl Pts',(-43.0114713541423,-2.13190671757982,
4.66374697382507));
#31070=CARTESIAN_POINT('Ctrl Pts',(-42.8722127100594,-4.10682227278453,
3.0707609656379));
#31071=CARTESIAN_POINT('Ctrl Pts',(-42.7661857800152,-4.84492911504421,
1.28551155191592));
#31072=CARTESIAN_POINT('Ctrl Pts',(-42.7065783979984,-4.91833682148999,
0.233014936376255));
#31073=CARTESIAN_POINT('Ctrl Pts',(-42.6933905640093,-4.91811507793926,
0.000124674194325845));
#31074=CARTESIAN_POINT('Ctrl Pts',(-44.0981094359908,-4.9179985551391,0.000107459425145867));
#31075=CARTESIAN_POINT('Ctrl Pts',(-44.0673168007194,-4.91756779448751,
-0.543711354100132));
#31076=CARTESIAN_POINT('Ctrl Pts',(-43.9901046174204,-4.69201025116029,
-1.90767934972549));
#31077=CARTESIAN_POINT('Ctrl Pts',(-43.8664728860938,-3.45440006425625,
-3.78981295174814));
#31078=CARTESIAN_POINT('Ctrl Pts',(-43.7272142420111,-1.21462268519213,
-4.98199294919094));
#31079=CARTESIAN_POINT('Ctrl Pts',(-43.5879555979281,1.32252861367418,-4.95444044057296));
#31080=CARTESIAN_POINT('Ctrl Pts',(-43.4486969538454,3.53588757546868,-3.71390105775826));
#31081=CARTESIAN_POINT('Ctrl Pts',(-43.3094383097624,4.88356144746871,-1.56409385970568));
#31082=CARTESIAN_POINT('Ctrl Pts',(-43.1701796656797,5.03560162356189,0.968647666570477));
#31083=CARTESIAN_POINT('Ctrl Pts',(-43.0309210215968,3.95478437683829,3.26423690100571));
#31084=CARTESIAN_POINT('Ctrl Pts',(-42.891662377514,1.90572427869227,4.76064879893219));
#31085=CARTESIAN_POINT('Ctrl Pts',(-42.7524037334311,-0.60991091781632,
5.09151948690174));
#31086=CARTESIAN_POINT('Ctrl Pts',(-42.6131450893483,-2.97622270502889,
4.17584248065492));
#31087=CARTESIAN_POINT('Ctrl Pts',(-42.4783803235348,-4.56102422386236,
2.30034197151273));
#31088=CARTESIAN_POINT('Ctrl Pts',(-42.3900351057489,-4.91801263886073,
0.740108066787903));
#31089=CARTESIAN_POINT('Ctrl Pts',(-42.3481094359907,-4.91857378612503,
-7.83346265965153E-5));
#31090=CARTESIAN_POINT('Origin',(-62.8183905640093,0.,0.));
#31091=CARTESIAN_POINT('',(-46.1933905640093,-4.91845483554336,0.000109107315461253));
#31092=CARTESIAN_POINT('',(-45.8481094359907,-4.91825200889249,-0.000129049404935799));
#31093=CARTESIAN_POINT('',(-62.8183905640093,-4.91825,1.40632325245411E-12));
#31094=CARTESIAN_POINT('Ctrl Pts',(-46.1933905640093,-4.91845483554336,
0.000109107315461165));
#31095=CARTESIAN_POINT('Ctrl Pts',(-46.1539808839944,-4.91778337373426,
-0.695706862165678));
#31096=CARTESIAN_POINT('Ctrl Pts',(-46.068151655952,-4.59305371007858,-2.21171144892918));
#31097=CARTESIAN_POINT('Ctrl Pts',(-45.9359028798819,-3.0882820494734,-4.09366291616992));
#31098=CARTESIAN_POINT('Ctrl Pts',(-45.7966442357991,-0.747651098816729,
-5.07312329071181));
#31099=CARTESIAN_POINT('Ctrl Pts',(-45.6573855917162,1.77602594558582,-4.81053987915395));
#31100=CARTESIAN_POINT('Ctrl Pts',(-45.5181269476334,3.86488170470528,-3.37020051287143));
#31101=CARTESIAN_POINT('Ctrl Pts',(-45.3788683035506,5.00750532432036,-1.10474092674605));
#31102=CARTESIAN_POINT('Ctrl Pts',(-45.2396096594678,4.92415028827758,1.43119042296277));
#31103=CARTESIAN_POINT('Ctrl Pts',(-45.1003510153849,3.63522426235287,3.61672595737161));
#31104=CARTESIAN_POINT('Ctrl Pts',(-44.9610923713021,1.45629272160045,4.91678488418377));
#31105=CARTESIAN_POINT('Ctrl Pts',(-44.8218337272192,-1.07918038574816,
5.01307607994741));
#31106=CARTESIAN_POINT('Ctrl Pts',(-44.6825750831364,-3.35043967147466,
3.88202474182395));
#31107=CARTESIAN_POINT('Ctrl Pts',(-44.5564273620664,-4.66481015725751,
1.99651140099669));
#31108=CARTESIAN_POINT('Ctrl Pts',(-44.476699189024,-4.91755673375692,0.588086537026348));
#31109=CARTESIAN_POINT('Ctrl Pts',(-44.4433905640092,-4.91811906887483,
-0.000125018227360024));
#31110=CARTESIAN_POINT('Ctrl Pts',(-45.8481094359907,-4.91825200889249,
-0.000129049404935973));
#31111=CARTESIAN_POINT('Ctrl Pts',(-45.837437591745,-4.91844704284713,-0.18857316690703));
#31112=CARTESIAN_POINT('Ctrl Pts',(-45.7803461994717,-4.86162270123637,
-1.19657974072127));
#31113=CARTESIAN_POINT('Ctrl Pts',(-45.6768352591708,-4.1885222391554,-2.95835147764295));
#31114=CARTESIAN_POINT('Ctrl Pts',(-45.5375766150878,-2.25749675029642,
-4.60426654697279));
#31115=CARTESIAN_POINT('Ctrl Pts',(-45.3983179710051,0.226227667835505,
-5.12292719599619));
#31116=CARTESIAN_POINT('Ctrl Pts',(-45.2590593269221,2.65456516690845,-4.38735065703757));
#31117=CARTESIAN_POINT('Ctrl Pts',(-45.1198006828394,4.43299017984253,-2.57762683074788));
#31118=CARTESIAN_POINT('Ctrl Pts',(-44.9805420387565,5.12609406194675,-0.136827194832999));
#31119=CARTESIAN_POINT('Ctrl Pts',(-44.8412833946737,4.56418541788972,2.33747160074608));
#31120=CARTESIAN_POINT('Ctrl Pts',(-44.7020247505909,2.88483534533912,4.23949136612563));
#31121=CARTESIAN_POINT('Ctrl Pts',(-44.562766106508,0.499196146884659,5.10356397237334));
#31122=CARTESIAN_POINT('Ctrl Pts',(-44.4235074624252,-2.00866035967626,
4.71814005436855));
#31123=CARTESIAN_POINT('Ctrl Pts',(-44.2842488183423,-4.02474010956177,
3.17758226701629));
#31124=CARTESIAN_POINT('Ctrl Pts',(-44.1757828095309,-4.82754107525667,
1.37172977179825));
#31125=CARTESIAN_POINT('Ctrl Pts',(-44.113736348747,-4.91821716127859,0.276089332340098));
#31126=CARTESIAN_POINT('Ctrl Pts',(-44.0981094359908,-4.9179985551391,0.000107459425145867));
#31127=CARTESIAN_POINT('Origin',(-62.8183905640093,0.,0.));
#31128=CARTESIAN_POINT('',(-47.9433905640093,-4.91787338031339,-6.25745746822065E-5));
#31129=CARTESIAN_POINT('',(-47.5981094359907,-4.91832100844767,0.000125872292329049));
#31130=CARTESIAN_POINT('',(-62.8183905640093,-4.91825,1.40632325245411E-12));
#31131=CARTESIAN_POINT('Ctrl Pts',(-47.9433905640093,-4.91787338031339,
-6.25745746826376E-5));
#31132=CARTESIAN_POINT('Ctrl Pts',(-47.9241016750201,-4.918025336644,-0.34074226218686));
#31133=CARTESIAN_POINT('Ctrl Pts',(-47.8583932380032,-4.79918089678194,
-1.50117787435966));
#31134=CARTESIAN_POINT('Ctrl Pts',(-47.7462652529588,-3.89630627287599,
-3.33382055849918));
#31135=CARTESIAN_POINT('Ctrl Pts',(-47.607006608876,-1.82104496094234,-4.79367889397601));
#31136=CARTESIAN_POINT('Ctrl Pts',(-47.4677479647931,0.700059562034036,
-5.07990931985298));
#31137=CARTESIAN_POINT('Ctrl Pts',(-47.3284893207103,3.04976974288669,-4.12243454813989));
#31138=CARTESIAN_POINT('Ctrl Pts',(-47.1892306766275,4.65281020153438,-2.15567143062717));
#31139=CARTESIAN_POINT('Ctrl Pts',(-47.0499720325446,5.11671138294472,0.33886090357014));
#31140=CARTESIAN_POINT('Ctrl Pts',(-46.9107133884618,4.32789718286852,2.75043052318056));
#31141=CARTESIAN_POINT('Ctrl Pts',(-46.771454744379,2.47949158419529,4.48861711134167));
#31142=CARTESIAN_POINT('Ctrl Pts',(-46.6321961002961,0.0240364544226033,
5.12786352560043));
#31143=CARTESIAN_POINT('Ctrl Pts',(-46.4929374562133,-2.43730347789571,
4.51166419904695));
#31144=CARTESIAN_POINT('Ctrl Pts',(-46.3536788121304,-4.30192271842598,
2.79088212094582));
#31145=CARTESIAN_POINT('Ctrl Pts',(-46.2538298480624,-4.88369029434119,
1.06715587713395));
#31146=CARTESIAN_POINT('Ctrl Pts',(-46.2004004320221,-4.91857426961782,
0.123875098447742));
#31147=CARTESIAN_POINT('Ctrl Pts',(-46.1933905640093,-4.91845483554336,
0.000109107315461165));
#31148=CARTESIAN_POINT('Ctrl Pts',(-47.5981094359907,-4.91832100844767,
0.000125872292329066));
#31149=CARTESIAN_POINT('Ctrl Pts',(-47.561138834743,-4.91764271032085,-0.652677035677827));
#31150=CARTESIAN_POINT('Ctrl Pts',(-47.4777486854677,-4.62273622332759,
-2.1257206615366));
#31151=CARTESIAN_POINT('Ctrl Pts',(-47.3479389881648,-3.1947516251322,-4.01112503755328));
#31152=CARTESIAN_POINT('Ctrl Pts',(-47.2086803440819,-0.880657560390307,
-5.05173279919862));
#31153=CARTESIAN_POINT('Ctrl Pts',(-47.0694216999991,1.6490463344078,-4.85553377087915));
#31154=CARTESIAN_POINT('Ctrl Pts',(-46.9301630559163,3.7750171371299,-3.47056301304949));
#31155=CARTESIAN_POINT('Ctrl Pts',(-46.7909044118334,4.97675718319434,-1.23590046229263));
#31156=CARTESIAN_POINT('Ctrl Pts',(-46.6516457677506,4.96004658650958,1.30134540873142));
#31157=CARTESIAN_POINT('Ctrl Pts',(-46.5123871236678,3.72897657285209,3.51998518921485));
#31158=CARTESIAN_POINT('Ctrl Pts',(-46.3731284795849,1.58494783230892,4.87683323295259));
#31159=CARTESIAN_POINT('Ctrl Pts',(-46.2338698355021,-0.947120877618752,
5.03969483762166));
#31160=CARTESIAN_POINT('Ctrl Pts',(-46.0946111914193,-3.24730766130082,
3.9686968851285));
#31161=CARTESIAN_POINT('Ctrl Pts',(-45.9660243915821,-4.63711698689941,
2.08258460884));
#31162=CARTESIAN_POINT('Ctrl Pts',(-45.8838571397726,-4.91759869950401,
0.631106221350268));
#31163=CARTESIAN_POINT('Ctrl Pts',(-45.8481094359907,-4.91825200889249,
-0.000129049404935973));
#31164=CARTESIAN_POINT('Origin',(-62.8183905640093,0.,0.));
#31165=CARTESIAN_POINT('',(-49.6933905640093,-4.91867246230615,1.57158398012151E-5));
#31166=CARTESIAN_POINT('',(-49.3481094359907,-4.91794918791349,-9.46638502663522E-5));
#31167=CARTESIAN_POINT('',(-62.8183905640093,-4.91825,1.40632325245411E-12));
#31168=CARTESIAN_POINT('Ctrl Pts',(-49.6933905640093,-4.91867246230615,
1.57158398011309E-5));
#31169=CARTESIAN_POINT('Ctrl Pts',(-49.6478029180181,-4.91852637123773,
-0.804774992398663));
#31170=CARTESIAN_POINT('Ctrl Pts',(-49.5557957239992,-4.51180610137747,
-2.4291848203257));
#31171=CARTESIAN_POINT('Ctrl Pts',(-49.4173689819529,-2.80923945602917,
-4.28995754839293));
#31172=CARTESIAN_POINT('Ctrl Pts',(-49.27811033787,-0.408659791847362,-5.11161024168038));
#31173=CARTESIAN_POINT('Ctrl Pts',(-49.1388516937872,2.09197132506023,-4.68179645685823));
#31174=CARTESIAN_POINT('Ctrl Pts',(-48.9995930497043,4.08042880925776,-3.10574674126912));
#31175=CARTESIAN_POINT('Ctrl Pts',(-48.8603344056215,5.06988213827541,-0.769322554147787));
#31176=CARTESIAN_POINT('Ctrl Pts',(-48.7210757615387,4.81808520680125,1.75545351072806));
#31177=CARTESIAN_POINT('Ctrl Pts',(-48.5818171174558,3.38668501140426,3.85044500309434));
#31178=CARTESIAN_POINT('Ctrl Pts',(-48.442558473373,1.12612872559781,5.00273886803099));
#31179=CARTESIAN_POINT('Ctrl Pts',(-48.3032998292901,-1.4101356606875,4.93022104035731));
#31180=CARTESIAN_POINT('Ctrl Pts',(-48.1640411852073,-3.60115903181333,
3.65064593132692));
#31181=CARTESIAN_POINT('Ctrl Pts',(-48.0440714301137,-4.72915620559369,
1.77832394507212));
#31182=CARTESIAN_POINT('Ctrl Pts',(-47.9705212230477,-4.91765964714312,
0.479118183377995));
#31183=CARTESIAN_POINT('Ctrl Pts',(-47.9433905640093,-4.91787338031339,
-6.25745746826376E-5));
#31184=CARTESIAN_POINT('Ctrl Pts',(-49.3481094359907,-4.91794918791349,
-9.46638502663175E-5));
#31185=CARTESIAN_POINT('Ctrl Pts',(-49.3312596257687,-4.918154011868,-0.297682293376429));
#31186=CARTESIAN_POINT('Ctrl Pts',(-49.267990267519,-4.81837287639424,-1.41495845453493));
#31187=CARTESIAN_POINT('Ctrl Pts',(-49.1583013612416,-3.98253692500126,
-3.23031912574798));
#31188=CARTESIAN_POINT('Ctrl Pts',(-49.0190427171589,-1.94634036455058,
-4.74418814956709));
#31189=CARTESIAN_POINT('Ctrl Pts',(-48.879784073076,0.566375258594887,-5.09654599504637));
#31190=CARTESIAN_POINT('Ctrl Pts',(-48.7405254289932,2.94042623074984,-4.20112551522683));
#31191=CARTESIAN_POINT('Ctrl Pts',(-48.6012667849103,4.5945778590284,-2.27715091956982));
#31192=CARTESIAN_POINT('Ctrl Pts',(-48.4620081408275,5.12384713130236,0.20433450079776));
#31193=CARTESIAN_POINT('Ctrl Pts',(-48.3227494967446,4.39865398946333,2.63579306739927));
#31194=CARTESIAN_POINT('Ctrl Pts',(-48.1834908526618,2.59654618544401,4.42193508772209));
#31195=CARTESIAN_POINT('Ctrl Pts',(-48.0442322085789,0.158730579712837,
5.12546257583017));
#31196=CARTESIAN_POINT('Ctrl Pts',(-47.9049735644962,-2.31794675259165,
4.57413214340397));
#31197=CARTESIAN_POINT('Ctrl Pts',(-47.7657149204133,-4.22712528867379,
2.90292504330135));
#31198=CARTESIAN_POINT('Ctrl Pts',(-47.6634268775782,-4.86928460793813,
1.15335712439825));
#31199=CARTESIAN_POINT('Ctrl Pts',(-47.6075583827706,-4.91849436789233,
0.166969248569943));
#31200=CARTESIAN_POINT('Ctrl Pts',(-47.5981094359907,-4.91832100844767,
0.000125872292329066));
#31201=CARTESIAN_POINT('Origin',(-62.8183905640093,0.,0.));
#31202=CARTESIAN_POINT('',(-51.4433905640093,-4.91784119574401,3.70365089225223E-5));
#31203=CARTESIAN_POINT('',(-51.0981094359907,-4.91861900665162,5.92428380992091E-5));
#31204=CARTESIAN_POINT('',(-62.8183905640093,-4.91825,1.40632325245411E-12));
#31205=CARTESIAN_POINT('Ctrl Pts',(-51.4433905640093,-4.91784119574402,
3.70365089222974E-5));
#31206=CARTESIAN_POINT('Ctrl Pts',(-51.4179237090437,-4.91772339455084,
-0.449766092710603));
#31207=CARTESIAN_POINT('Ctrl Pts',(-51.3460373060505,-4.74508883257368,
-1.71953364257664));
#31208=CARTESIAN_POINT('Ctrl Pts',(-51.2277313550298,-3.66600093949493,
-3.58552634907998));
#31209=CARTESIAN_POINT('Ctrl Pts',(-51.0884727109469,-1.49825959824569,
-4.90415948604745));
#31210=CARTESIAN_POINT('Ctrl Pts',(-50.9492140668641,1.03629798564688,-5.02211594582091));
#31211=CARTESIAN_POINT('Ctrl Pts',(-50.8099554227812,3.31714056994997,-3.91051665736339));
#31212=CARTESIAN_POINT('Ctrl Pts',(-50.6706967786984,4.78585350621771,-1.84151250480363));
#31213=CARTESIAN_POINT('Ctrl Pts',(-50.5314381346155,5.08285440870451,0.678345891295609));
#31214=CARTESIAN_POINT('Ctrl Pts',(-50.3921794905327,4.13542907271616,3.03212606480312));
#31215=CARTESIAN_POINT('Ctrl Pts',(-50.2529208464499,2.17553396450143,4.64355618654767));
#31216=CARTESIAN_POINT('Ctrl Pts',(-50.113662202367,-0.316993269371489,
5.11811267514673));
#31217=CARTESIAN_POINT('Ctrl Pts',(-49.9744035582842,-2.73191160279071,
4.33961070637241));
#31218=CARTESIAN_POINT('Ctrl Pts',(-49.8351449142014,-4.47798085922564,
2.49864953779702));
#31219=CARTESIAN_POINT('Ctrl Pts',(-49.7414739161098,-4.91501765406269,
0.848863542292382));
#31220=CARTESIAN_POINT('Ctrl Pts',(-49.6942224660457,-4.91867512823581,
0.0147018663202137));
#31221=CARTESIAN_POINT('Ctrl Pts',(-49.6933905640093,-4.91867246230615,
1.57158398011309E-5));
#31222=CARTESIAN_POINT('Ctrl Pts',(-51.0981094359907,-4.91861900665162,
5.92428380991137E-5));
#31223=CARTESIAN_POINT('Ctrl Pts',(-51.0549608687667,-4.91815886707571,
-0.761696767512525));
#31224=CARTESIAN_POINT('Ctrl Pts',(-50.965392753515,-4.54493313080541,-2.3433907057031));
#31225=CARTESIAN_POINT('Ctrl Pts',(-50.8294050902357,-2.92096173384329,
-4.21468202390108));
#31226=CARTESIAN_POINT('Ctrl Pts',(-50.6901464461529,-0.542794236847172,
-5.09911133724467));
#31227=CARTESIAN_POINT('Ctrl Pts',(-50.55088780207,1.96826461136862,-4.73513425710461));
#31228=CARTESIAN_POINT('Ctrl Pts',(-50.4116291579872,3.99743672238916,-3.21186264707355));
#31229=CARTESIAN_POINT('Ctrl Pts',(-50.2723705139044,5.04792348380256,-0.902236396320984));
#31230=CARTESIAN_POINT('Ctrl Pts',(-50.1331118698215,4.86253608318979,1.62828279265274));
#31231=CARTESIAN_POINT('Ctrl Pts',(-49.9938532257387,3.48666258935134,3.76015239068703));
#31232=CARTESIAN_POINT('Ctrl Pts',(-49.8545945816558,1.25715567184686,4.97143054159615));
#31233=CARTESIAN_POINT('Ctrl Pts',(-49.7153359375731,-1.28013844121747,
4.96556216198015));
#31234=CARTESIAN_POINT('Ctrl Pts',(-49.5760772934901,-3.50401852802057,
3.74398399682213));
#31235=CARTESIAN_POINT('Ctrl Pts',(-49.4536684596294,-4.70473504165732,
1.86448895312075));
#31236=CARTESIAN_POINT('Ctrl Pts',(-49.3776791737963,-4.91758974228464,
0.52214197046708));
#31237=CARTESIAN_POINT('Ctrl Pts',(-49.3481094359907,-4.91794918791349,
-9.46638502663175E-5));
#31238=CARTESIAN_POINT('Origin',(-62.8183905640093,0.,0.));
#31239=CARTESIAN_POINT('',(-53.1933905640093,-4.91853679395484,-9.01493930066358E-5));
#31240=CARTESIAN_POINT('',(-52.8481094359907,-4.91782510432338,-3.02706344698644E-6));
#31241=CARTESIAN_POINT('',(-62.8183905640093,-4.91825,1.40632325245411E-12));
#31242=CARTESIAN_POINT('Ctrl Pts',(-53.1933905640093,-4.91853679395484,
-9.01493930066492E-5));
#31243=CARTESIAN_POINT('Ctrl Pts',(-53.1880445000694,-4.9186164742464,-0.0944755243151697));
#31244=CARTESIAN_POINT('Ctrl Pts',(-53.1362788881018,-4.8928518455894,-1.00835989416069));
#31245=CARTESIAN_POINT('Ctrl Pts',(-53.0380937281066,-4.35124498857135,
-2.71334279768651));
#31246=CARTESIAN_POINT('Ctrl Pts',(-52.8988350840238,-2.51776186605044,
-4.46726283916524));
#31247=CARTESIAN_POINT('Ctrl Pts',(-52.759576439941,-0.0678595671353494,
-5.12747083536052));
#31248=CARTESIAN_POINT('Ctrl Pts',(-52.6203177958581,2.39865666935982,-4.53232923239918));
#31249=CARTESIAN_POINT('Ctrl Pts',(-52.4810591517753,4.27791404372175,-2.82754549439134));
#31250=CARTESIAN_POINT('Ctrl Pts',(-52.3418005076925,5.10981730287787,-0.430498803174167));
#31251=CARTESIAN_POINT('Ctrl Pts',(-52.2025418636096,4.69069304595447,2.07194614721496));
#31252=CARTESIAN_POINT('Ctrl Pts',(-52.0632832195268,3.12315472211971,4.06712019370289));
#31253=CARTESIAN_POINT('Ctrl Pts',(-51.924024575444,0.790979961646617,5.06654840977544));
#31254=CARTESIAN_POINT('Ctrl Pts',(-51.7847659313611,-1.73484902128376,
4.82554255619773));
#31255=CARTESIAN_POINT('Ctrl Pts',(-51.6455072872782,-3.83593799234573,
3.40310766905826));
#31256=CARTESIAN_POINT('Ctrl Pts',(-51.531715498161,-4.78539130338917,1.55998982552279));
#31257=CARTESIAN_POINT('Ctrl Pts',(-51.4643432570714,-4.91793811592698,
0.370109702239623));
#31258=CARTESIAN_POINT('Ctrl Pts',(-51.4433905640093,-4.91784119574402,
3.70365089222974E-5));
#31259=CARTESIAN_POINT('Ctrl Pts',(-52.8481094359907,-4.91782510432338,
-3.02706344702114E-6));
#31260=CARTESIAN_POINT('Ctrl Pts',(-52.8250816597923,-4.91783377634347,
-0.406730229006752));
#31261=CARTESIAN_POINT('Ctrl Pts',(-52.7556343355662,-4.76739234533979,
-1.63333459135314));
#31262=CARTESIAN_POINT('Ctrl Pts',(-52.6397674633126,-3.75892305563278,
-3.48798788343709));
#31263=CARTESIAN_POINT('Ctrl Pts',(-52.5005088192298,-1.62656857379318,
-4.86310977543383));
#31264=CARTESIAN_POINT('Ctrl Pts',(-52.3612501751469,0.904015809819905,
-5.04760511814933));
#31265=CARTESIAN_POINT('Ctrl Pts',(-52.2219915310641,3.21327160455789,-3.99630424373741));
#31266=CARTESIAN_POINT('Ctrl Pts',(-52.0827328869813,4.73582780601003,-1.96659528245999));
#31267=CARTESIAN_POINT('Ctrl Pts',(-51.9434742428983,5.09891967722156,0.544591717173908));
#31268=CARTESIAN_POINT('Ctrl Pts',(-51.8042155988156,4.21365207873328,2.92244729166469));
#31269=CARTESIAN_POINT('Ctrl Pts',(-51.6649569547327,2.29676350806032,4.58480527407807));
#31270=CARTESIAN_POINT('Ctrl Pts',(-51.5256983106499,-0.182437602611408,
5.12467350514402));
#31271=CARTESIAN_POINT('Ctrl Pts',(-51.3864396665671,-2.6169728383005,4.40987700245359));
#31272=CARTESIAN_POINT('Ctrl Pts',(-51.2471810224842,-4.41079925105322,
2.61541812719877));
#31273=CARTESIAN_POINT('Ctrl Pts',(-51.1510709456254,-4.90352744261773,
0.935037184879213));
#31274=CARTESIAN_POINT('Ctrl Pts',(-51.1013804167943,-4.91865388863766,
0.0578059873339447));
#31275=CARTESIAN_POINT('Ctrl Pts',(-51.0981094359907,-4.91861900665162,
5.92428380991137E-5));
#31276=CARTESIAN_POINT('Origin',(-62.8183905640093,0.,0.));
#31277=CARTESIAN_POINT('',(-54.9433905640093,-4.91803681242707,0.00011480967905517));
#31278=CARTESIAN_POINT('',(-54.5981094359907,-4.91863036579189,-5.31391465866116E-5));
#31279=CARTESIAN_POINT('',(-62.8183905640093,-4.91825,1.40632325245411E-12));
#31280=CARTESIAN_POINT('Ctrl Pts',(-54.9433905640093,-4.91803681242707,
0.000114809679055));
#31281=CARTESIAN_POINT('Ctrl Pts',(-54.9117457430674,-4.91755857232653,
-0.558741720734804));
#31282=CARTESIAN_POINT('Ctrl Pts',(-54.8336813740978,-4.68295166729167,
-1.93777195873213));
#31283=CARTESIAN_POINT('Ctrl Pts',(-54.7091974571006,-3.41946818595568,
-3.82136093735749));
#31284=CARTESIAN_POINT('Ctrl Pts',(-54.5699388130178,-1.16884224379346,
-4.99293199407404));
#31285=CARTESIAN_POINT('Ctrl Pts',(-54.430680168935,1.36794927382256,-4.94209235775424));
#31286=CARTESIAN_POINT('Ctrl Pts',(-54.2914215248522,3.56982819462436,-3.68128900647443));
#31287=CARTESIAN_POINT('Ctrl Pts',(-54.1521628807693,4.89771240398387,-1.51920219068664));
#31288=CARTESIAN_POINT('Ctrl Pts',(-54.0129042366865,5.02649836382728,1.01482820554322));
#31289=CARTESIAN_POINT('Ctrl Pts',(-53.8736455926037,3.9246556358045,3.30040001040366));
#31290=CARTESIAN_POINT('Ctrl Pts',(-53.7343869485209,1.86194642264088,4.77794072875955));
#31291=CARTESIAN_POINT('Ctrl Pts',(-53.5951283044379,-0.656619833959052,
5.08570668461877));
#31292=CARTESIAN_POINT('Ctrl Pts',(-53.4558696603552,-3.01442702008815,
4.14834808434477));
#31293=CARTESIAN_POINT('Ctrl Pts',(-53.3219570802122,-4.57203450537693,
2.27033105204216));
#31294=CARTESIAN_POINT('Ctrl Pts',(-53.234464048097,-4.91792461512111,0.725066945346297));
#31295=CARTESIAN_POINT('Ctrl Pts',(-53.1933905640093,-4.91853679395484,
-9.01493930066492E-5));
#31296=CARTESIAN_POINT('Ctrl Pts',(-54.5981094359907,-4.91863036579189,
-5.31391465869498E-5));
#31297=CARTESIAN_POINT('Ctrl Pts',(-54.5952024508179,-4.91865864175323,
-0.0513734660281668));
#31298=CARTESIAN_POINT('Ctrl Pts',(-54.5458759176175,-4.90531457595336,
-0.922176319021297));
#31299=CARTESIAN_POINT('Ctrl Pts',(-54.4501298363895,-4.42101949107612,
-2.59810482326958));
#31300=CARTESIAN_POINT('Ctrl Pts',(-54.3108711923067,-2.6342423114104,-4.39958287317637));
#31301=CARTESIAN_POINT('Ctrl Pts',(-54.1716125482239,-0.202528254306939,
-5.12391884394933));
#31302=CARTESIAN_POINT('Ctrl Pts',(-54.0323539041409,2.27877043643476,-4.59377484332902));
#31303=CARTESIAN_POINT('Ctrl Pts',(-53.8930952600582,4.20216179902152,-2.93894508761492));
#31304=CARTESIAN_POINT('Ctrl Pts',(-53.7538366159752,5.09674533424557,-0.564578613673673));
#31305=CARTESIAN_POINT('Ctrl Pts',(-53.6145779718925,4.74350174030785,1.94801264186554));
#31306=CARTESIAN_POINT('Ctrl Pts',(-53.4753193278096,3.22891502039301,3.98367541401808));
#31307=CARTESIAN_POINT('Ctrl Pts',(-53.3360606837268,0.923798757412272,
5.04402199330804));
#31308=CARTESIAN_POINT('Ctrl Pts',(-53.196802039644,-1.60748951844882,4.86944960557646));
#31309=CARTESIAN_POINT('Ctrl Pts',(-53.0575433955611,-3.74521898384984,
3.50269849918351));
#31310=CARTESIAN_POINT('Ctrl Pts',(-52.9413125276768,-4.76414289396322,
1.64619939207857));
#31311=CARTESIAN_POINT('Ctrl Pts',(-52.8715012078199,-4.91781629522634,
0.413153233558466));
#31312=CARTESIAN_POINT('Ctrl Pts',(-52.8481094359907,-4.91782510432338,
-3.02706344702114E-6));
#31313=CARTESIAN_POINT('Origin',(-62.8183905640093,0.,0.));
#31314=CARTESIAN_POINT('',(-56.6933905640093,-4.9182044571118,-0.000129187542790386));
#31315=CARTESIAN_POINT('',(-56.3481094359908,-4.91793587170447,9.03881743496981E-5));
#31316=CARTESIAN_POINT('',(-62.8183905640093,-4.91825,1.40632325245411E-12));
#31317=CARTESIAN_POINT('Ctrl Pts',(-56.6933905640093,-4.9182044571118,-0.000129187542790513));
#31318=CARTESIAN_POINT('Ctrl Pts',(-56.681866534093,-4.91841151819362,-0.203626914331993));
#31319=CARTESIAN_POINT('Ctrl Pts',(-56.623922956149,-4.85610900923186,-1.22670088899472));
#31320=CARTESIAN_POINT('Ctrl Pts',(-56.5195598301776,-4.1611913471364,-2.99667293168903));
#31321=CARTESIAN_POINT('Ctrl Pts',(-56.3803011860948,-2.21513949450856,
-4.62479395317148));
#31322=CARTESIAN_POINT('Ctrl Pts',(-56.2410425420119,0.273241035485556,
-5.12063486534734));
#31323=CARTESIAN_POINT('Ctrl Pts',(-56.1017838979291,2.69472444693603,-4.36279981705527));
#31324=CARTESIAN_POINT('Ctrl Pts',(-55.9625252538462,4.45646324687071,-2.53682821994801));
#31325=CARTESIAN_POINT('Ctrl Pts',(-55.8232666097634,5.1271340465709,-0.089769464874975));
#31326=CARTESIAN_POINT('Ctrl Pts',(-55.6840079656806,4.54253770251526,2.37926738925458));
#31327=CARTESIAN_POINT('Ctrl Pts',(-55.5447493215977,2.84579990176412,4.26579242432466));
#31328=CARTESIAN_POINT('Ctrl Pts',(-55.4054906775149,0.452329953591429,
5.1079310587967));
#31329=CARTESIAN_POINT('Ctrl Pts',(-55.266232033432,-2.05188313562661,4.69950398298055));
#31330=CARTESIAN_POINT('Ctrl Pts',(-55.1269733893492,-4.0537373125207,3.14050567415567));
#31331=CARTESIAN_POINT('Ctrl Pts',(-55.0193595662083,-4.83375182313205,
1.34160576371217));
#31332=CARTESIAN_POINT('Ctrl Pts',(-54.958165291095,-4.91826009910578,0.261040688579662));
#31333=CARTESIAN_POINT('Ctrl Pts',(-54.9433905640093,-4.91803681242707,
0.000114809679055));
#31334=CARTESIAN_POINT('Ctrl Pts',(-56.3481094359908,-4.91793587170447,
9.03881743493859E-5));
#31335=CARTESIAN_POINT('Ctrl Pts',(-56.318903693816,-4.91759809637477,-0.515721651436775));
#31336=CARTESIAN_POINT('Ctrl Pts',(-56.2432784036135,-4.70846037346048,
-1.85163183427517));
#31337=CARTESIAN_POINT('Ctrl Pts',(-56.1212335653836,-3.51867044972994,
-3.73021718930019));
#31338=CARTESIAN_POINT('Ctrl Pts',(-55.9819749213007,-1.29959683625502,
-4.96050502231166));
#31339=CARTESIAN_POINT('Ctrl Pts',(-55.8427162772179,1.23765476786001,-4.97632120032051));
#31340=CARTESIAN_POINT('Ctrl Pts',(-55.7034576331351,3.471893548184,-3.77379347649709));
#31341=CARTESIAN_POINT('Ctrl Pts',(-55.5641989890522,4.85611478302155,-1.64733458267922));
#31342=CARTESIAN_POINT('Ctrl Pts',(-55.4249403449694,5.0514220401755,0.882438318071356));
#31343=CARTESIAN_POINT('Ctrl Pts',(-55.2856817008865,4.00999858994569,3.19616540901837));
#31344=CARTESIAN_POINT('Ctrl Pts',(-55.1464230568037,1.98681429033347,4.72738098622251));
#31345=CARTESIAN_POINT('Ctrl Pts',(-55.0071644127208,-0.522798231506428,
5.10120025310764));
#31346=CARTESIAN_POINT('Ctrl Pts',(-54.867905768638,-2.90441498868291,4.22610170093973));
#31347=CARTESIAN_POINT('Ctrl Pts',(-54.731554109728,-4.54007704180687,2.35620001996191));
#31348=CARTESIAN_POINT('Ctrl Pts',(-54.6416219988456,-4.9182071233356,0.768123792081326));
#31349=CARTESIAN_POINT('Ctrl Pts',(-54.5981094359907,-4.91863036579189,
-5.31391465869498E-5));
#31350=CARTESIAN_POINT('Origin',(-62.8183905640093,0.,0.));
#31351=CARTESIAN_POINT('',(-58.4433905640093,-4.91836886135133,0.000122455552848294));
#31352=CARTESIAN_POINT('',(-58.0981094359908,-4.91834149996792,-0.000124244451389921));
#31353=CARTESIAN_POINT('',(-62.8183905640093,-4.91825,1.40632325245411E-12));
#31354=CARTESIAN_POINT('Ctrl Pts',(-58.4433905640093,-4.91836886135133,
0.000122455552848399));
#31355=CARTESIAN_POINT('Ctrl Pts',(-58.405567777091,-4.91768352809557,-0.667709083104306));
#31356=CARTESIAN_POINT('Ctrl Pts',(-58.321325442145,-4.61251739126612,-2.1557731884816));
#31357=CARTESIAN_POINT('Ctrl Pts',(-58.1906635591718,-3.15779931679017,
-4.04027968761638));
#31358=CARTESIAN_POINT('Ctrl Pts',(-58.0514049150887,-0.834251032978302,
-5.05960384006236));
#31359=CARTESIAN_POINT('Ctrl Pts',(-57.9121462710061,1.69354537464531,-4.84019258737259));
#31360=CARTESIAN_POINT('Ctrl Pts',(-57.772887626923,3.8067141091864,-3.43576636062821));
#31361=CARTESIAN_POINT('Ctrl Pts',(-57.6336289828404,4.98789175297897,-1.19016713333119));
#31362=CARTESIAN_POINT('Ctrl Pts',(-57.4943703387573,4.94789270758304,1.34681839400263));
#31363=CARTESIAN_POINT('Ctrl Pts',(-57.3551116946747,3.69650985244822,3.55406486819218));
#31364=CARTESIAN_POINT('Ctrl Pts',(-57.2158530505917,1.54011704282762,4.89117588296368));
#31365=CARTESIAN_POINT('Ctrl Pts',(-57.076594406509,-0.993339894845993,
5.03078900139859));
#31366=CARTESIAN_POINT('Ctrl Pts',(-56.937335762426,-3.28359918545446,3.93872294825806));
#31367=CARTESIAN_POINT('Ctrl Pts',(-56.8096011482596,-4.64694192022078,
2.05251707513984));
#31368=CARTESIAN_POINT('Ctrl Pts',(-56.7282860821206,-4.91757746258099,
0.616075270651702));
#31369=CARTESIAN_POINT('Ctrl Pts',(-56.6933905640093,-4.9182044571118,-0.000129187542790513));
#31370=CARTESIAN_POINT('Ctrl Pts',(-58.0981094359908,-4.91834149996792,
-0.000124244451390268));
#31371=CARTESIAN_POINT('Ctrl Pts',(-58.0890244848416,-4.91850756103116,
-0.160538493998118));
#31372=CARTESIAN_POINT('Ctrl Pts',(-58.0335199856648,-4.87150837253063,
-1.14049229247011));
#31373=CARTESIAN_POINT('Ctrl Pts',(-57.9315959384605,-4.23847415605518,
-2.88632966415425));
#31374=CARTESIAN_POINT('Ctrl Pts',(-57.7923372943776,-2.33586251016583,
-4.56500912177253));
#31375=CARTESIAN_POINT('Ctrl Pts',(-57.6530786502948,0.13863421179886,-5.12604551322175));
#31376=CARTESIAN_POINT('Ctrl Pts',(-57.5138200062119,2.57918936704391,-4.43208125010674));
#31377=CARTESIAN_POINT('Ctrl Pts',(-57.3745613621292,4.38828615879628,-2.65301839525271));
#31378=CARTESIAN_POINT('Ctrl Pts',(-57.2353027180462,5.12300662642812,-0.224421743812369));
#31379=CARTESIAN_POINT('Ctrl Pts',(-57.0960440739635,4.60347045903611,2.25911968355451));
#31380=CARTESIAN_POINT('Ctrl Pts',(-56.9567854298806,2.95687477625445,4.18956484277621));
#31381=CARTESIAN_POINT('Ctrl Pts',(-56.8175267857977,0.586352681285569,
5.09428626459846));
#31382=CARTESIAN_POINT('Ctrl Pts',(-56.678268141715,-1.92772510164183,4.75178260718661));
#31383=CARTESIAN_POINT('Ctrl Pts',(-56.539009497632,-3.96984136372351,3.24590843369777));
#31384=CARTESIAN_POINT('Ctrl Pts',(-56.428956595724,-4.81558555136314,1.42782549805425));
#31385=CARTESIAN_POINT('Ctrl Pts',(-56.3653232418436,-4.91813495580623,
0.304108969632793));
#31386=CARTESIAN_POINT('Ctrl Pts',(-56.3481094359908,-4.91793587170447,
9.03881743493859E-5));
#31387=CARTESIAN_POINT('Ctrl Pts',(-60.1597342437858,-2.14786219406457,
4.42446279878225));
#31388=CARTESIAN_POINT('Ctrl Pts',(-60.1133146957582,-2.8852624348776,4.06649073049583));
#31389=CARTESIAN_POINT('Ctrl Pts',(-60.0204755997031,-4.17685949869944,
2.97507394228249));
#31390=CARTESIAN_POINT('Ctrl Pts',(-59.8812169556201,-5.09175167965884,
0.607962263996158));
#31391=CARTESIAN_POINT('Ctrl Pts',(-59.7419583115374,-4.75996762098409,
-1.90732467562513));
#31392=CARTESIAN_POINT('Ctrl Pts',(-59.6026996674545,-3.26284724500757,
-3.95597454038308));
#31393=CARTESIAN_POINT('Ctrl Pts',(-59.4634410233716,-0.966870086247853,
-5.03592242336179));
#31394=CARTESIAN_POINT('Ctrl Pts',(-59.3241823792888,1.56581406446455,-4.88302020893749));
#31395=CARTESIAN_POINT('Ctrl Pts',(-59.184923735206,3.71514791027481,-3.53457280157081));
#31396=CARTESIAN_POINT('Ctrl Pts',(-59.0456650911232,4.95490602150955,-1.32078475768876));
#31397=CARTESIAN_POINT('Ctrl Pts',(-58.9064064470403,4.98156463212109,1.21638024324112));
#31398=CARTESIAN_POINT('Ctrl Pts',(-58.7671478029575,3.78859490309226,3.45573509562084));
#31399=CARTESIAN_POINT('Ctrl Pts',(-58.6278891588746,1.66807055469799,4.84903148731836));
#31400=CARTESIAN_POINT('Ctrl Pts',(-58.4886305147918,-0.860844735280108,
5.05514653385482));
#31401=CARTESIAN_POINT('Ctrl Pts',(-58.349371870709,-3.17900084006467,4.02361981064615));
#31402=CARTESIAN_POINT('Ctrl Pts',(-58.2101132266261,-4.71884785030005,
2.00699696920383));
#31403=CARTESIAN_POINT('Ctrl Pts',(-58.0708545825433,-5.10338767805891,
-0.500995174027796));
#31404=CARTESIAN_POINT('Ctrl Pts',(-57.9315959384605,-4.23847415605518,
-2.88632966415425));
#31405=CARTESIAN_POINT('Ctrl Pts',(-57.7923372943776,-2.33586251016583,
-4.56500912177253));
#31406=CARTESIAN_POINT('Ctrl Pts',(-57.6530786502948,0.13863421179886,-5.12604551322175));
#31407=CARTESIAN_POINT('Ctrl Pts',(-57.5138200062119,2.57918936704391,-4.43208125010674));
#31408=CARTESIAN_POINT('Ctrl Pts',(-57.3745613621292,4.38828615879628,-2.65301839525271));
#31409=CARTESIAN_POINT('Ctrl Pts',(-57.2353027180462,5.12300662642812,-0.224421743812369));
#31410=CARTESIAN_POINT('Ctrl Pts',(-57.0960440739635,4.60347045903611,2.25911968355451));
#31411=CARTESIAN_POINT('Ctrl Pts',(-56.9567854298806,2.95687477625445,4.18956484277621));
#31412=CARTESIAN_POINT('Ctrl Pts',(-56.8175267857977,0.586352681285569,
5.09428626459846));
#31413=CARTESIAN_POINT('Ctrl Pts',(-56.678268141715,-1.92772510164183,4.75178260718661));
#31414=CARTESIAN_POINT('Ctrl Pts',(-56.539009497632,-3.96984136372351,3.24590843369777));
#31415=CARTESIAN_POINT('Ctrl Pts',(-56.3997508535493,-5.04002839895529,
0.945344249943794));
#31416=CARTESIAN_POINT('Ctrl Pts',(-56.2604922094663,-4.87627421179875,
-1.58666689148564));
#31417=CARTESIAN_POINT('Ctrl Pts',(-56.1212335653836,-3.51867044972994,
-3.73021718930019));
#31418=CARTESIAN_POINT('Ctrl Pts',(-55.9819749213007,-1.29959683625502,
-4.96050502231166));
#31419=CARTESIAN_POINT('Ctrl Pts',(-55.8427162772179,1.23765476786001,-4.97632120032051));
#31420=CARTESIAN_POINT('Ctrl Pts',(-55.7034576331351,3.471893548184,-3.77379347649709));
#31421=CARTESIAN_POINT('Ctrl Pts',(-55.5641989890522,4.85611478302155,-1.64733458267922));
#31422=CARTESIAN_POINT('Ctrl Pts',(-55.4249403449694,5.0514220401755,0.882438318071356));
#31423=CARTESIAN_POINT('Ctrl Pts',(-55.2856817008865,4.00999858994569,3.19616540901837));
#31424=CARTESIAN_POINT('Ctrl Pts',(-55.1464230568037,1.98681429033347,4.72738098622251));
#31425=CARTESIAN_POINT('Ctrl Pts',(-55.0071644127208,-0.522798231506428,
5.10120025310764));
#31426=CARTESIAN_POINT('Ctrl Pts',(-54.867905768638,-2.90441498868291,4.22610170093973));
#31427=CARTESIAN_POINT('Ctrl Pts',(-54.7286471245552,-4.57494897056921,
2.31633415764206));
#31428=CARTESIAN_POINT('Ctrl Pts',(-54.5893884804724,-5.12540630243158,
-0.160537373113851));
#31429=CARTESIAN_POINT('Ctrl Pts',(-54.4501298363895,-4.42101949107612,
-2.59810482326958));
#31430=CARTESIAN_POINT('Ctrl Pts',(-54.3108711923067,-2.6342423114104,-4.39958287317637));
#31431=CARTESIAN_POINT('Ctrl Pts',(-54.1716125482239,-0.202528254306939,
-5.12391884394933));
#31432=CARTESIAN_POINT('Ctrl Pts',(-54.0323539041409,2.27877043643476,-4.59377484332902));
#31433=CARTESIAN_POINT('Ctrl Pts',(-53.8930952600582,4.20216179902152,-2.93894508761492));
#31434=CARTESIAN_POINT('Ctrl Pts',(-53.7538366159752,5.09674533424557,-0.564578613673673));
#31435=CARTESIAN_POINT('Ctrl Pts',(-53.6145779718925,4.74350174030785,1.94801264186554));
#31436=CARTESIAN_POINT('Ctrl Pts',(-53.4753193278096,3.22891502039301,3.98367541401808));
#31437=CARTESIAN_POINT('Ctrl Pts',(-53.3360606837268,0.923798757412272,
5.04402199330804));
#31438=CARTESIAN_POINT('Ctrl Pts',(-53.196802039644,-1.60748951844882,4.86944960557646));
#31439=CARTESIAN_POINT('Ctrl Pts',(-53.0575433955611,-3.74521898384984,
3.50269849918351));
#31440=CARTESIAN_POINT('Ctrl Pts',(-52.9182847514784,-4.96601312166083,
1.27838792573463));
#31441=CARTESIAN_POINT('Ctrl Pts',(-52.7790261073954,-4.97098706627025,
-1.25890809837161));
#31442=CARTESIAN_POINT('Ctrl Pts',(-52.6397674633126,-3.75892305563278,
-3.48798788343709));
#31443=CARTESIAN_POINT('Ctrl Pts',(-52.5005088192298,-1.62656857379318,
-4.86310977543383));
#31444=CARTESIAN_POINT('Ctrl Pts',(-52.3612501751469,0.904015809819905,
-5.04760511814933));
#31445=CARTESIAN_POINT('Ctrl Pts',(-52.2219915310641,3.21327160455789,-3.99630424373741));
#31446=CARTESIAN_POINT('Ctrl Pts',(-52.0827328869813,4.73582780601003,-1.96659528245999));
#31447=CARTESIAN_POINT('Ctrl Pts',(-51.9434742428983,5.09891967722156,0.544591717173908));
#31448=CARTESIAN_POINT('Ctrl Pts',(-51.8042155988156,4.21365207873328,2.92244729166469));
#31449=CARTESIAN_POINT('Ctrl Pts',(-51.6649569547327,2.29676350806032,4.58480527407807));
#31450=CARTESIAN_POINT('Ctrl Pts',(-51.5256983106499,-0.182437602611408,
5.12467350514402));
#31451=CARTESIAN_POINT('Ctrl Pts',(-51.3864396665671,-2.6169728383005,4.40987700245359));
#31452=CARTESIAN_POINT('Ctrl Pts',(-51.2471810224842,-4.41079925105322,
2.61541812719877));
#31453=CARTESIAN_POINT('Ctrl Pts',(-51.1079223784014,-5.12473749875106,
0.180631066171815));
#31454=CARTESIAN_POINT('Ctrl Pts',(-50.9686637343185,-4.58399534525111,
-2.29837957872232));
#31455=CARTESIAN_POINT('Ctrl Pts',(-50.8294050902357,-2.92096173384329,
-4.21468202390108));
#31456=CARTESIAN_POINT('Ctrl Pts',(-50.6901464461529,-0.542794236847172,
-5.09911133724467));
#31457=CARTESIAN_POINT('Ctrl Pts',(-50.55088780207,1.96826461136862,-4.73513425710461));
#31458=CARTESIAN_POINT('Ctrl Pts',(-50.4116291579872,3.99743672238916,-3.21186264707355));
#31459=CARTESIAN_POINT('Ctrl Pts',(-50.2723705139044,5.04792348380256,-0.902236396320984));
#31460=CARTESIAN_POINT('Ctrl Pts',(-50.1331118698215,4.86253608318979,1.62828279265274));
#31461=CARTESIAN_POINT('Ctrl Pts',(-49.9938532257387,3.48666258935134,3.76015239068703));
#31462=CARTESIAN_POINT('Ctrl Pts',(-49.8545945816558,1.25715567184686,4.97143054159615));
#31463=CARTESIAN_POINT('Ctrl Pts',(-49.7153359375731,-1.28013844121747,
4.96556216198015));
#31464=CARTESIAN_POINT('Ctrl Pts',(-49.5760772934901,-3.50401852802057,
3.74398399682213));
#31465=CARTESIAN_POINT('Ctrl Pts',(-49.4368186494073,-4.87001596744655,
1.60577286375978));
#31466=CARTESIAN_POINT('Ctrl Pts',(-49.2975600053245,-5.04369602683803,
-0.925576794236894));
#31467=CARTESIAN_POINT('Ctrl Pts',(-49.1583013612416,-3.98253692500126,
-3.23031912574798));
#31468=CARTESIAN_POINT('Ctrl Pts',(-49.0190427171589,-1.94634036455058,
-4.74418814956709));
#31469=CARTESIAN_POINT('Ctrl Pts',(-48.879784073076,0.566375258594887,-5.09654599504637));
#31470=CARTESIAN_POINT('Ctrl Pts',(-48.7405254289932,2.94042623074984,-4.20112551522683));
#31471=CARTESIAN_POINT('Ctrl Pts',(-48.6012667849103,4.5945778590284,-2.27715091956982));
#31472=CARTESIAN_POINT('Ctrl Pts',(-48.4620081408275,5.12384713130236,0.20433450079776));
#31473=CARTESIAN_POINT('Ctrl Pts',(-48.3227494967446,4.39865398946333,2.63579306739927));
#31474=CARTESIAN_POINT('Ctrl Pts',(-48.1834908526618,2.59654618544401,4.42193508772209));
#31475=CARTESIAN_POINT('Ctrl Pts',(-48.0442322085789,0.158730579712837,
5.12546257583017));
#31476=CARTESIAN_POINT('Ctrl Pts',(-47.9049735644962,-2.31794675259165,
4.57413214340397));
#31477=CARTESIAN_POINT('Ctrl Pts',(-47.7657149204133,-4.22712528867379,
2.90292504330135));
#31478=CARTESIAN_POINT('Ctrl Pts',(-47.6264562763305,-5.10138423045494,
0.520999948596248));
#31479=CARTESIAN_POINT('Ctrl Pts',(-47.4871976322476,-4.72668031033514,
-1.98848064035377));
#31480=CARTESIAN_POINT('Ctrl Pts',(-47.3479389881648,-3.1947516251322,-4.01112503755328));
#31481=CARTESIAN_POINT('Ctrl Pts',(-47.2086803440819,-0.880657560390307,
-5.05173279919862));
#31482=CARTESIAN_POINT('Ctrl Pts',(-47.0694216999991,1.6490463344078,-4.85553377087915));
#31483=CARTESIAN_POINT('Ctrl Pts',(-46.9301630559163,3.7750171371299,-3.47056301304949));
#31484=CARTESIAN_POINT('Ctrl Pts',(-46.7909044118334,4.97675718319434,-1.23590046229263));
#31485=CARTESIAN_POINT('Ctrl Pts',(-46.6516457677506,4.96004658650958,1.30134540873142));
#31486=CARTESIAN_POINT('Ctrl Pts',(-46.5123871236678,3.72897657285209,3.51998518921485));
#31487=CARTESIAN_POINT('Ctrl Pts',(-46.3731284795849,1.58494783230892,4.87683323295259));
#31488=CARTESIAN_POINT('Ctrl Pts',(-46.2338698355021,-0.947120877618752,
5.03969483762166));
#31489=CARTESIAN_POINT('Ctrl Pts',(-46.0946111914193,-3.24730766130082,
3.9686968851285));
#31490=CARTESIAN_POINT('Ctrl Pts',(-45.9553525473364,-4.75246186423383,
1.92604990646005));
#31491=CARTESIAN_POINT('Ctrl Pts',(-45.8160939032536,-5.09407924992551,
-0.588148458001959));
#31492=CARTESIAN_POINT('Ctrl Pts',(-45.6768352591708,-4.1885222391554,-2.95835147764295));
#31493=CARTESIAN_POINT('Ctrl Pts',(-45.5375766150878,-2.25749675029642,
-4.60426654697279));
#31494=CARTESIAN_POINT('Ctrl Pts',(-45.3983179710051,0.226227667835505,
-5.12292719599619));
#31495=CARTESIAN_POINT('Ctrl Pts',(-45.2590593269221,2.65456516690845,-4.38735065703757));
#31496=CARTESIAN_POINT('Ctrl Pts',(-45.1198006828394,4.43299017984253,-2.57762683074788));
#31497=CARTESIAN_POINT('Ctrl Pts',(-44.9805420387565,5.12609406194675,-0.136827194832999));
#31498=CARTESIAN_POINT('Ctrl Pts',(-44.8412833946737,4.56418541788972,2.33747160074608));
#31499=CARTESIAN_POINT('Ctrl Pts',(-44.7020247505909,2.88483534533912,4.23949136612563));
#31500=CARTESIAN_POINT('Ctrl Pts',(-44.562766106508,0.499196146884659,5.10356397237334));
#31501=CARTESIAN_POINT('Ctrl Pts',(-44.4235074624252,-2.00866035967626,
4.71814005436855));
#31502=CARTESIAN_POINT('Ctrl Pts',(-44.2842488183423,-4.02474010956177,
3.17758226701629));
#31503=CARTESIAN_POINT('Ctrl Pts',(-44.1449901742595,-5.05544986993808,
0.859062643649847));
#31504=CARTESIAN_POINT('Ctrl Pts',(-44.0057315301767,-4.8484427965068,-1.66977976457168));
#31505=CARTESIAN_POINT('Ctrl Pts',(-43.8664728860938,-3.45440006425625,
-3.78981295174814));
#31506=CARTESIAN_POINT('Ctrl Pts',(-43.7272142420111,-1.21462268519213,
-4.98199294919094));
#31507=CARTESIAN_POINT('Ctrl Pts',(-43.5879555979281,1.32252861367418,-4.95444044057296));
#31508=CARTESIAN_POINT('Ctrl Pts',(-43.4486969538454,3.53588757546868,-3.71390105775826));
#31509=CARTESIAN_POINT('Ctrl Pts',(-43.3094383097624,4.88356144746871,-1.56409385970568));
#31510=CARTESIAN_POINT('Ctrl Pts',(-43.1701796656797,5.03560162356189,0.968647666570477));
#31511=CARTESIAN_POINT('Ctrl Pts',(-43.0309210215968,3.95478437683829,3.26423690100571));
#31512=CARTESIAN_POINT('Ctrl Pts',(-42.891662377514,1.90572427869227,4.76064879893219));
#31513=CARTESIAN_POINT('Ctrl Pts',(-42.7524037334311,-0.60991091781632,
5.09151948690174));
#31514=CARTESIAN_POINT('Ctrl Pts',(-42.6131450893483,-2.97622270502889,
4.17584248065492));
#31515=CARTESIAN_POINT('Ctrl Pts',(-42.4738864452655,-4.61387116099574,
2.23780135912538));
#31516=CARTESIAN_POINT('Ctrl Pts',(-42.3346278011826,-5.12191371602353,
-0.248116703955333));
#31517=CARTESIAN_POINT('Ctrl Pts',(-42.1953691570999,-4.37596721157521,
-2.67328879404945));
#31518=CARTESIAN_POINT('Ctrl Pts',(-42.0561105130169,-2.5586604085778,-4.44396432554854));
#31519=CARTESIAN_POINT('Ctrl Pts',(-41.9168518689342,-0.114921311488126,
-5.12663194556987));
#31520=CARTESIAN_POINT('Ctrl Pts',(-41.7775932248512,2.35695376666187,-4.55415535033556));
#31521=CARTESIAN_POINT('Ctrl Pts',(-41.6383345807685,4.25178003045199,-2.86669297027451));
#31522=CARTESIAN_POINT('Ctrl Pts',(-41.4990759366856,5.10565052319778,-0.477383229849849));
#31523=CARTESIAN_POINT('Ctrl Pts',(-41.3598172926028,4.70951364514992,2.02880340085441));
#31524=CARTESIAN_POINT('Ctrl Pts',(-41.2205586485199,3.16035488623825,4.03828168980343));
#31525=CARTESIAN_POINT('Ctrl Pts',(-41.0813000044371,0.837452040422802,
5.05907462814725));
#31526=CARTESIAN_POINT('Ctrl Pts',(-40.9420413603542,-1.6904827045519,4.84126328955393));
#31527=CARTESIAN_POINT('Ctrl Pts',(-40.8027827162714,-3.80453956437015,
3.43817403810713));
#31528=CARTESIAN_POINT('Ctrl Pts',(-40.6635240721885,-4.98713774398085,
1.1933227290776));
#31529=CARTESIAN_POINT('Ctrl Pts',(-40.5242654281058,-4.9487438265385,-1.34368766924037));
#31530=CARTESIAN_POINT('Ctrl Pts',(-40.3850067840229,-3.69875772681961,
-3.5517253964044));
#31531=CARTESIAN_POINT('Ctrl Pts',(-40.2457481399401,-1.54321132674375,
-4.89020048813763));
#31532=CARTESIAN_POINT('Ctrl Pts',(-40.1064894958572,0.990156768012798,
-5.03141645940088));
#31533=CARTESIAN_POINT('Ctrl Pts',(-39.9672308517744,3.28110653573467,-3.9407996541731));
#31534=CARTESIAN_POINT('Ctrl Pts',(-39.8279722076915,4.76874880416872,-1.88536385239323));
#31535=CARTESIAN_POINT('Ctrl Pts',(-39.6887135636088,5.08886675271635,0.631662240655434));
#31536=CARTESIAN_POINT('Ctrl Pts',(-39.5494549195259,4.16308647125779,2.99403958657897));
#31537=CARTESIAN_POINT('Ctrl Pts',(-39.410196275443,2.21806510569457,4.62339152571701));
#31538=CARTESIAN_POINT('Ctrl Pts',(-39.2709376313602,-0.270001209463393,
5.12080670989053));
#31539=CARTESIAN_POINT('Ctrl Pts',(-39.1316789872773,-2.69196360692879,
4.36450386093798));
#31540=CARTESIAN_POINT('Ctrl Pts',(-38.9924203431946,-4.45485732445219,
2.53964726526075));
#31541=CARTESIAN_POINT('Ctrl Pts',(-38.8531616991117,-5.12707621687776,
0.0930133296797844));
#31542=CARTESIAN_POINT('Ctrl Pts',(-38.7139030550288,-4.5440421238906,-2.37639289459456));
#31543=CARTESIAN_POINT('Ctrl Pts',(-38.574644410946,-2.84849824938738,-4.26399105726181));
#31544=CARTESIAN_POINT('Ctrl Pts',(-38.4353857668631,-0.455561595795777,
-5.10764384482783));
#31545=CARTESIAN_POINT('Ctrl Pts',(-38.2961271227804,2.04890939607611,-4.70080124019754));
#31546=CARTESIAN_POINT('Ctrl Pts',(-38.1568684786975,4.05174953100885,-3.14306979737026));
#31547=CARTESIAN_POINT('Ctrl Pts',(-38.0176098346146,5.06260700763802,-0.815826145318977));
#31548=CARTESIAN_POINT('Ctrl Pts',(-37.8783511905319,4.83399538111841,1.71115477631265));
#31549=CARTESIAN_POINT('Ctrl Pts',(-37.7390925464489,3.42188523088942,3.81919670608788));
#31550=CARTESIAN_POINT('Ctrl Pts',(-37.5998339023662,1.17200098288635,4.99219147362009));
#31551=CARTESIAN_POINT('Ctrl Pts',(-37.4605752582833,-1.36482218906556,
4.94295684842645));
#31552=CARTESIAN_POINT('Ctrl Pts',(-37.3213166142005,-3.56749836282337,
3.68354685655336));
#31553=CARTESIAN_POINT('Ctrl Pts',(-37.1820579701177,-4.89675023373046,
1.52230061473821));
#31554=CARTESIAN_POINT('Ctrl Pts',(-37.0427993260348,-5.02713942155972,
-1.01164778918944));
#31555=CARTESIAN_POINT('Ctrl Pts',(-36.903540681952,-3.92674297249402,-3.29791625744811));
#31556=CARTESIAN_POINT('Ctrl Pts',(-36.7642820378691,-1.86496899934438,
-4.7767617320373));
#31557=CARTESIAN_POINT('Ctrl Pts',(-36.6250233937863,0.653402029340091,
-5.08612109580827));
#31558=CARTESIAN_POINT('Ctrl Pts',(-36.4857647497035,3.01180179695694,-4.15025444388879));
#31559=CARTESIAN_POINT('Ctrl Pts',(-36.3465061056206,4.63282746729464,-2.19828835038808));
#31560=CARTESIAN_POINT('Ctrl Pts',(-36.2072474615378,5.11960619781114,0.291880784748528));
#31561=CARTESIAN_POINT('Ctrl Pts',(-36.0679888174549,4.35296081444672,2.71058926454433));
#31562=CARTESIAN_POINT('Ctrl Pts',(-35.9287301733721,2.52058774797673,4.46566897764727));
#31563=CARTESIAN_POINT('Ctrl Pts',(-35.7894715292892,0.0711036494477585,
5.12742686775803));
#31564=CARTESIAN_POINT('Ctrl Pts',(-35.6502128852065,-2.39578862958558,
4.53384592322236));
#31565=CARTESIAN_POINT('Ctrl Pts',(-35.5109542411235,-4.27612422358166,
2.83025151491343));
#31566=CARTESIAN_POINT('Ctrl Pts',(-35.3716955970408,-5.10954390086544,
0.433731643185599));
#31567=CARTESIAN_POINT('Ctrl Pts',(-35.2324369529579,-4.69200299859993,
-2.0689779782059));
#31568=CARTESIAN_POINT('Ctrl Pts',(-35.0931783088751,-3.125727316038,-4.06514338725531));
#31569=CARTESIAN_POINT('Ctrl Pts',(-34.9539196647922,-0.794185353227152,
-5.06604694390913));
#31570=CARTESIAN_POINT('Ctrl Pts',(-34.8146610207094,1.73179560238191,-4.82663920391221));
#31571=CARTESIAN_POINT('Ctrl Pts',(-34.6754023766266,3.83378410926193,-3.40553394003679));
#31572=CARTESIAN_POINT('Ctrl Pts',(-34.5361437325437,4.99715404582752,-1.15065783595354));
#31573=CARTESIAN_POINT('Ctrl Pts',(-34.3968850884609,4.93707961190701,1.38593178723334));
#31574=CARTESIAN_POINT('Ctrl Pts',(-34.257626444378,3.6682687247101,3.58320618671119));
#31575=CARTESIAN_POINT('Ctrl Pts',(-34.1183678002952,1.5013621055187,4.90321056464884));
#31576=CARTESIAN_POINT('Ctrl Pts',(-33.9791091562124,-1.03312033767432,
5.02277058813713));
#31577=CARTESIAN_POINT('Ctrl Pts',(-33.8398505121295,-3.31466575920044,
3.91261458847608));
#31578=CARTESIAN_POINT('Ctrl Pts',(-33.7005918680467,-4.78468743622185,
1.84454009195584));
#31579=CARTESIAN_POINT('Ctrl Pts',(-33.5613332239638,-5.0832825663132,-0.675129886901675));
#31580=CARTESIAN_POINT('Ctrl Pts',(-33.422074579881,-4.13734663286075,-3.02950901182476));
#31581=CARTESIAN_POINT('Ctrl Pts',(-33.2828159357982,-2.17847145432949,
-4.64217881342837));
#31582=CARTESIAN_POINT('Ctrl Pts',(-33.1435572917154,0.313755030289582,
-5.11831220170669));
#31583=CARTESIAN_POINT('Ctrl Pts',(-33.0042986476325,2.72916542679145,-4.34133828287751));
#31584=CARTESIAN_POINT('Ctrl Pts',(-32.8650400035497,4.47639908771296,-2.50148220475266));
#31585=CARTESIAN_POINT('Ctrl Pts',(-32.7257813594668,5.12768389180779,-0.0491926708628662));
#31586=CARTESIAN_POINT('Ctrl Pts',(-32.586522715384,4.52356693451351,2.41514061746884));
#31587=CARTESIAN_POINT('Ctrl Pts',(-32.4472640713011,2.81195310003798,4.28817930785997));
#31588=CARTESIAN_POINT('Ctrl Pts',(-32.3080054272183,0.411893770634228,
5.11135065661556));
#31589=CARTESIAN_POINT('Ctrl Pts',(-32.1687467831355,-2.08900878079138,
4.68311908101302));
#31590=CARTESIAN_POINT('Ctrl Pts',(-32.0294881390527,-4.07846301397088,
3.10832775891526));
#31591=CARTESIAN_POINT('Ctrl Pts',(-31.8902294949698,-5.06939437414735,
0.772530059308323));
#31592=CARTESIAN_POINT('Ctrl Pts',(-31.750970850887,-4.81919489225918,-1.75240480585811));
#31593=CARTESIAN_POINT('Ctrl Pts',(-31.6117122068041,-3.38912046412381,
-3.84830150752625));
#31594=CARTESIAN_POINT('Ctrl Pts',(-31.4724535627214,-1.12929367800508,
-5.00202536998659));
#31595=CARTESIAN_POINT('Ctrl Pts',(-31.3331949186384,1.40701607828237,-4.93111222429854));
#31596=CARTESIAN_POINT('Ctrl Pts',(-31.1939362745556,3.59884858124293,-3.65292361026856));
#31597=CARTESIAN_POINT('Ctrl Pts',(-31.0546776304728,4.90958136292712,-1.48039618142248));
#31598=CARTESIAN_POINT('Ctrl Pts',(-30.9154189863899,5.01831003890801,1.05457402137864));
#31599=CARTESIAN_POINT('Ctrl Pts',(-30.7761603423071,3.89841476010363,3.33135473514573));
#31600=CARTESIAN_POINT('Ctrl Pts',(-30.6369016982242,1.82407750325954,4.79252577199894));
#31601=CARTESIAN_POINT('Ctrl Pts',(-30.4976430541415,-0.696845416589377,
5.08035121606272));
#31602=CARTESIAN_POINT('Ctrl Pts',(-30.3583844100586,-3.04716090784859,
4.12436327387041));
#31603=CARTESIAN_POINT('Ctrl Pts',(-30.2191257659758,-4.65144539336256,
2.15861477937539));
#31604=CARTESIAN_POINT('Ctrl Pts',(-30.0798671218929,-5.11692474520557,
-0.335623546662854));
#31605=CARTESIAN_POINT('Ctrl Pts',(-29.9406084778101,-4.32963647845777,
-2.74769175446946));
#31606=CARTESIAN_POINT('Ctrl Pts',(-29.8013498337272,-2.48233098445573,
-4.48704745871744));
#31607=CARTESIAN_POINT('Ctrl Pts',(-29.6620911896444,-0.0272807940196574,
-5.12784728433378));
#31608=CARTESIAN_POINT('Ctrl Pts',(-29.5228325455616,2.43444850487691,-4.5132053454584));
#31609=CARTESIAN_POINT('Ctrl Pts',(-29.3835739014787,4.30015608997081,-2.79360333889022));
#31610=CARTESIAN_POINT('Ctrl Pts',(-29.2443152573959,5.11306407908685,-0.390048376901321));
#31611=CARTESIAN_POINT('Ctrl Pts',(-29.105056613313,4.67414964965714,2.10900143807006));
#31612=CARTESIAN_POINT('Ctrl Pts',(-28.9657979692302,3.09087144371802,4.09170816793918));
#31613=CARTESIAN_POINT('Ctrl Pts',(-28.8265393251474,0.750860658988233,
5.07264923722855));
#31614=CARTESIAN_POINT('Ctrl Pts',(-28.6872806810645,-1.77298201041712,
4.81166258209249));
#31615=CARTESIAN_POINT('Ctrl Pts',(-28.5480220369817,-3.86274863579312,
3.37264510286066));
#31616=CARTESIAN_POINT('Ctrl Pts',(-28.4087633928988,-5.00680535714688,
1.10790889915052));
#31617=CARTESIAN_POINT('Ctrl Pts',(-28.269504748816,-4.92505479456558,-1.42807467721344));
#31618=CARTESIAN_POINT('Ctrl Pts',(-28.1302461047332,-3.63751179343058,
-3.61442526078837));
#31619=CARTESIAN_POINT('Ctrl Pts',(-27.9909874606504,-1.45940322528745,
-4.91586251223447));
#31620=CARTESIAN_POINT('Ctrl Pts',(-27.8517288165675,1.07600844855802,-5.01375785532204));
#31621=CARTESIAN_POINT('Ctrl Pts',(-27.7124701724847,3.34798288054322,-3.88414374666556));
#31622=CARTESIAN_POINT('Ctrl Pts',(-27.5732115284018,4.80027659624061,-1.80358160690233));
#31623=CARTESIAN_POINT('Ctrl Pts',(-27.433952884319,5.07732709858328,0.718548221877666));
#31624=CARTESIAN_POINT('Ctrl Pts',(-27.2946942402362,4.11130460399385,3.06475716270483));
#31625=CARTESIAN_POINT('Ctrl Pts',(-27.1554355961534,2.13871868810873,4.66062703788945));
#31626=CARTESIAN_POINT('Ctrl Pts',(-27.0161769520704,-0.357485934549103,
5.11544385364273));
#31627=CARTESIAN_POINT('Ctrl Pts',(-26.8769183079877,-2.76616790928751,
4.3178556148625));
#31628=CARTESIAN_POINT('Ctrl Pts',(-26.7376596639048,-4.49761389622142,
2.46313443678733));
#31629=CARTESIAN_POINT('Ctrl Pts',(-26.598401019822,-5.12791704235244,0.00536841902906056));
#31630=CARTESIAN_POINT('Ctrl Pts',(-26.4591423757392,-4.50276134525971,
-2.45371193924766));
#31631=CARTESIAN_POINT('Ctrl Pts',(-26.3198837316563,-2.77520256653693,
-4.31205435121805));
#31632=CARTESIAN_POINT('Ctrl Pts',(-26.1806250875735,-0.36819586088392,
-5.11468413699221));
#31633=CARTESIAN_POINT('Ctrl Pts',(-26.0413664434906,2.12895558497593,-4.6650948683142));
#31634=CARTESIAN_POINT('Ctrl Pts',(-25.9021077994078,4.10487860730363,-3.07335868919861));
#31635=CARTESIAN_POINT('Ctrl Pts',(-25.762849155325,5.07581147371895,-0.729177547950212));
#31636=CARTESIAN_POINT('Ctrl Pts',(-25.6235905112421,4.80404241095214,1.79352684031905));
#31637=CARTESIAN_POINT('Ctrl Pts',(-25.4843318671593,3.35610815708752,3.87712523025787));
#31638=CARTESIAN_POINT('Ctrl Pts',(-25.3450732230764,1.08650388987611,5.01149392002581));
#31639=CARTESIAN_POINT('Ctrl Pts',(-25.2058145789936,-1.44910719949644,
4.91890743331681));
#31640=CARTESIAN_POINT('Ctrl Pts',(-25.0665559349108,-3.62993594091732,
3.62203355561599));
#31641=CARTESIAN_POINT('Ctrl Pts',(-24.9272972908279,-4.9220538978771,1.43838362044503));
#31642=CARTESIAN_POINT('Ctrl Pts',(-24.7880386467451,-5.00911412050208,
-1.09742322781982));
#31643=CARTESIAN_POINT('Ctrl Pts',(-24.6487800026622,-3.86980180875062,
-3.36454989176295));
#31644=CARTESIAN_POINT('Ctrl Pts',(-24.5095213585794,-1.7830527771394,-4.80793976741671));
#31645=CARTESIAN_POINT('Ctrl Pts',(-24.3702627144966,0.740237906473115,
-5.07421026909526));
#31646=CARTESIAN_POINT('Ctrl Pts',(-24.2310040704137,3.08229745508568,-4.09817086168255));
#31647=CARTESIAN_POINT('Ctrl Pts',(-24.0917454263309,4.66972357935212,-2.11878354383227));
#31648=CARTESIAN_POINT('Ctrl Pts',(-23.9524867822481,5.11386955405928,0.379341794741001));
#31649=CARTESIAN_POINT('Ctrl Pts',(-23.8132281381652,4.30599590721036,2.78459355387089));
#31650=CARTESIAN_POINT('Ctrl Pts',(-23.6739694940824,2.44389291227653,4.50809820728166));
#31651=CARTESIAN_POINT('Ctrl Pts',(-23.5347108499995,-0.0165440539888569,
5.12789316459004));
#31652=CARTESIAN_POINT('Ctrl Pts',(-23.3954522059167,-2.47293056883089,
4.49223512462487));
#31653=CARTESIAN_POINT('Ctrl Pts',(-23.2561935618339,-4.32387387433953,
2.75675111897605));
#31654=CARTESIAN_POINT('Ctrl Pts',(-23.116934917751,-5.11621080074934,0.346336621608935));
#31655=CARTESIAN_POINT('Ctrl Pts',(-22.9776762736682,-4.65595490232451,
-2.14887085714615));
#31656=CARTESIAN_POINT('Ctrl Pts',(-22.8384176295854,-3.05578981514007,
-4.11797409157195));
#31657=CARTESIAN_POINT('Ctrl Pts',(-22.6991589855025,-0.707481122127949,
-5.0788810258761));
#31658=CARTESIAN_POINT('Ctrl Pts',(-22.5599003414197,1.81403892041534,-4.79633451798247));
#31659=CARTESIAN_POINT('Ctrl Pts',(-22.4206416973369,3.89143102840395,-3.33950992876898));
#31660=CARTESIAN_POINT('Ctrl Pts',(-22.281383053254,5.01609097301024,-1.06507904103722));
#31661=CARTESIAN_POINT('Ctrl Pts',(-22.1421244091712,4.91267025280302,1.47011326107748));
#31662=CARTESIAN_POINT('Ctrl Pts',(-22.0028657650884,3.60648917945748,3.64538033840472));
#31663=CARTESIAN_POINT('Ctrl Pts',(-21.8636071210055,1.41733775071325,4.92815540680027));
#31664=CARTESIAN_POINT('Ctrl Pts',(-21.7243484769227,-1.11881796813,5.00437891924276));
#31665=CARTESIAN_POINT('Ctrl Pts',(-21.5850898328398,-3.38105546629115,
3.85538920824271));
#31666=CARTESIAN_POINT('Ctrl Pts',(-21.445831188757,-4.81551514559774,1.7624913888273));
#31667=CARTESIAN_POINT('Ctrl Pts',(-21.3065725446742,-5.07100078451202,
-0.761914074322125));
#31668=CARTESIAN_POINT('Ctrl Pts',(-21.1673139005913,-4.08496228675852,
-3.0997814647056));
#31669=CARTESIAN_POINT('Ctrl Pts',(-21.0280552565085,-2.09880971056153,
-4.67873485164786));
#31670=CARTESIAN_POINT('Ctrl Pts',(-20.8887966124256,0.401190728150701,
-5.11220187520187));
#31671=CARTESIAN_POINT('Ctrl Pts',(-20.7495379683428,2.80296835176735,-4.29405757205957));
#31672=CARTESIAN_POINT('Ctrl Pts',(-20.61027932426,4.51850020045465,-2.4246067622736));
#31673=CARTESIAN_POINT('Ctrl Pts',(-20.4710206801771,5.12777565148253,0.0384562249122501));
#31674=CARTESIAN_POINT('Ctrl Pts',(-20.3317620360943,4.48162687576275,2.49210404269421));
#31675=CARTESIAN_POINT('Ctrl Pts',(-20.1925033920114,2.7382493331312,4.33561444351065));
#31676=CARTESIAN_POINT('Ctrl Pts',(-20.0532447479286,0.324471058226111,
5.11764404248138));
#31677=CARTESIAN_POINT('Ctrl Pts',(-19.9139861038458,-2.16874689092793,
4.64672991858383));
#31678=CARTESIAN_POINT('Ctrl Pts',(-19.774727459763,-4.13099438162065,3.03816514234996));
#31679=CARTESIAN_POINT('Ctrl Pts',(-19.6354688156801,-5.08185783764996,
0.6857717776981));
#31680=CARTESIAN_POINT('Ctrl Pts',(-19.4962101715973,-4.78853904392961,
-1.83451787615531));
#31681=CARTESIAN_POINT('Ctrl Pts',(-19.3569515275144,-3.32285072098886,
-3.90566576900731));
#31682=CARTESIAN_POINT('Ctrl Pts',(-19.2176928834316,-1.04363474385184,
-5.02059643215792));
#31683=CARTESIAN_POINT('Ctrl Pts',(-19.0784342393487,1.49109247838584,-4.90634336691521));
#31684=CARTESIAN_POINT('Ctrl Pts',(-18.9391755952659,3.66075817123595,-3.59087894879527));
#31685=CARTESIAN_POINT('Ctrl Pts',(-18.7999169511831,4.93416692759049,-1.39626600038956));
#31686=CARTESIAN_POINT('Ctrl Pts',(-18.6606583071003,4.99955233800879,1.14019227882075));
#31687=CARTESIAN_POINT('Ctrl Pts',(-18.5213996630174,3.84090620831584,3.39749930273613));
#31688=CARTESIAN_POINT('Ctrl Pts',(-18.3821410189346,1.74189781741689,4.82300259245731));
#31689=CARTESIAN_POINT('Ctrl Pts',(-18.2428823748517,-0.783576329617824,
5.0676987034387));
#31690=CARTESIAN_POINT('Ctrl Pts',(-18.1036237307689,-3.11720887230625,
4.0716791204105));
#31691=CARTESIAN_POINT('Ctrl Pts',(-17.9643650866861,-4.68766069023061,
2.07879755301915));
#31692=CARTESIAN_POINT('Ctrl Pts',(-17.8251064426032,-5.11044084752239,
-0.423032335816314));
#31693=CARTESIAN_POINT('Ctrl Pts',(-17.6858477985204,-4.28204082740422,
-2.82129196745304));
#31694=CARTESIAN_POINT('Ctrl Pts',(-17.5465891544375,-2.40527633894355,
-4.52881968580006));
#31695=CARTESIAN_POINT('Ctrl Pts',(-17.4073305103547,0.0603676936250531,
-5.12756450517573));
#31696=CARTESIAN_POINT('Ctrl Pts',(-17.2680718662719,2.51123201073006,-4.4709367923799));
#31697=CARTESIAN_POINT('Ctrl Pts',(-17.128813222189,4.34727584434856,-2.71969754684507));
#31698=CARTESIAN_POINT('Ctrl Pts',(-16.9895545781062,5.11898383601734,-0.302599570000859));
#31699=CARTESIAN_POINT('Ctrl Pts',(-16.8502959340234,4.63742008554047,2.18858332338469));
#31700=CARTESIAN_POINT('Ctrl Pts',(-16.7110372899405,3.02048499265497,4.14393923969909));
#31701=CARTESIAN_POINT('Ctrl Pts',(-16.5717786458577,0.664049911073469,
5.08474185468397));
#31702=CARTESIAN_POINT('Ctrl Pts',(-16.4325200017749,-1.85496333359322,
4.78065613113894));
#31703=CARTESIAN_POINT('Ctrl Pts',(-16.293261357692,-3.91982919214168,3.30613083794419));
#31704=CARTESIAN_POINT('Ctrl Pts',(-16.1540027136092,-5.02501021519924,
1.02217138989266));
#31705=CARTESIAN_POINT('Ctrl Pts',(-16.0147440695263,-4.89992689118224,
-1.51204446834105));
#31706=CARTESIAN_POINT('Ctrl Pts',(-15.8754854254435,-3.57520314867229,
-3.6760691586116));
#31707=CARTESIAN_POINT('Ctrl Pts',(-15.7362267813606,-1.37516875424451,
-4.94008835047726));
#31708=CARTESIAN_POINT('Ctrl Pts',(-15.5969681372778,1.16154576959681,-4.99463446493368));
#31709=CARTESIAN_POINT('Ctrl Pts',(-15.457709493195,3.41388110083322,-3.82635307342976));
#31710=CARTESIAN_POINT('Ctrl Pts',(-15.3184508491121,4.83040197127458,-1.72127243894698));
#31711=CARTESIAN_POINT('Ctrl Pts',(-15.1791922050293,5.06430408617135,0.805224276807312));
#31712=CARTESIAN_POINT('Ctrl Pts',(-15.0399335609465,4.05832160518909,3.13457935966327));
#31713=CARTESIAN_POINT('Ctrl Pts',(-14.9006749168636,2.05874743662691,4.69650093211465));
#31714=CARTESIAN_POINT('Ctrl Pts',(-14.7614162727808,-0.444866218910259,
5.10858650317719));
#31715=CARTESIAN_POINT('Ctrl Pts',(-14.622157628698,-2.83956406633868,4.26994589267004));
#31716=CARTESIAN_POINT('Ctrl Pts',(-14.4828989846151,-4.53905647488387,
2.38590199526017));
#31717=CARTESIAN_POINT('Ctrl Pts',(-14.3436403405323,-5.12725972952516,
-0.0822780600233842));
#31718=CARTESIAN_POINT('Ctrl Pts',(-14.2043816964495,-4.46016506967744,
-2.5303141236615));
#31719=CARTESIAN_POINT('Ctrl Pts',(-14.0651230523666,-2.70109609887331,
-4.35885786391608));
#31720=CARTESIAN_POINT('Ctrl Pts',(-13.9258644082838,-0.280722556306372,
-5.12023015689262));
#31721=CARTESIAN_POINT('Ctrl Pts',(-13.7866057642009,2.20837979230334,-4.62802557319187));
#31722=CARTESIAN_POINT('Ctrl Pts',(-13.6473471201181,4.15680842943421,-3.00274968889455));
#31723=CARTESIAN_POINT('Ctrl Pts',(-13.5080884760352,5.08753302431593,-0.642315918895402));
#31724=CARTESIAN_POINT('Ctrl Pts',(-13.3688298319524,4.7726859235525,1.87537491939491));
#31725=CARTESIAN_POINT('Ctrl Pts',(-13.2295711878696,3.28935058494016,3.93392103918285));
#31726=CARTESIAN_POINT('Ctrl Pts',(-13.0903125437867,1.00068937108082,5.02933224153838));
#31727=CARTESIAN_POINT('Ctrl Pts',(-12.9510538997039,-1.5329688483594,4.89342094276911));
#31728=CARTESIAN_POINT('Ctrl Pts',(-12.8117952556211,-3.69131302095292,
3.55946206532884));
#31729=CARTESIAN_POINT('Ctrl Pts',(-12.6725366115382,-4.94591956733545,
1.35404639751376));
#31730=CARTESIAN_POINT('Ctrl Pts',(-12.5332779674554,-4.98962538981774,
-1.18287805054368));
#31731=CARTESIAN_POINT('Ctrl Pts',(-12.3940193233725,-3.81173006932457,
-3.43020056145098));
#31732=CARTESIAN_POINT('Ctrl Pts',(-12.2547606792897,-1.70061563003689,
-4.83771314693687));
#31733=CARTESIAN_POINT('Ctrl Pts',(-12.1155020352069,0.826857520598954,
-5.06081699469566));
#31734=CARTESIAN_POINT('Ctrl Pts',(-11.9762433911241,3.1518926095914,-4.04488998500265));
#31735=CARTESIAN_POINT('Ctrl Pts',(-11.8369847470412,4.70525541587707,-2.03865972750019));
#31736=CARTESIAN_POINT('Ctrl Pts',(-11.6977261029584,5.10663887602661,0.466691978745618));
#31737=CARTESIAN_POINT('Ctrl Pts',(-11.5584674588755,4.25777298871062,2.85778431477567));
#31738=CARTESIAN_POINT('Ctrl Pts',(-11.4192088147927,2.36648408499891,4.54921038078241));
#31739=CARTESIAN_POINT('Ctrl Pts',(-11.2799501707098,-0.104186924024186,
5.12686133009603));
#31740=CARTESIAN_POINT('Ctrl Pts',(-11.140691526627,-2.54935003304931,4.44931190434692));
#31741=CARTESIAN_POINT('Ctrl Pts',(-11.0014328825442,-4.37036029072556,
2.68244532887828));
#31742=CARTESIAN_POINT('Ctrl Pts',(-10.8621742384613,-5.1213829823493,0.258840416617134));
#31743=CARTESIAN_POINT('Ctrl Pts',(-10.7229155943785,-4.61854655308201,
-2.22813593619999));
#31744=CARTESIAN_POINT('Ctrl Pts',(-10.5836569502957,-2.98495955491563,
-4.16960171583444));
#31745=CARTESIAN_POINT('Ctrl Pts',(-10.4443983062128,-0.620570198026758,
-5.09023129557908));
#31746=CARTESIAN_POINT('Ctrl Pts',(-10.30513966213,1.89575226084471,-4.76462856670633));
#31747=CARTESIAN_POINT('Ctrl Pts',(-10.1658810180471,3.94794105281364,-3.27251026838425));
#31748=CARTESIAN_POINT('Ctrl Pts',(-10.0266223739643,5.03356243225522,-0.979189079677917));
#31749=CARTESIAN_POINT('Ctrl Pts',(-9.88736372988145,4.88682564047436,1.55386523636191));
#31750=CARTESIAN_POINT('Ctrl Pts',(-9.74810508579864,3.54365598619697,3.7064894799071));
#31751=CARTESIAN_POINT('Ctrl Pts',(-9.6088464417158,1.33289931589153,4.95166047168699));
#31752=CARTESIAN_POINT('Ctrl Pts',(-9.46958779763295,-1.20418873213356,
4.98452520412669));
#31753=CARTESIAN_POINT('Ctrl Pts',(-9.33032915355013,-3.44645738659569,
3.79703746301662));
#31754=CARTESIAN_POINT('Ctrl Pts',(-9.19107050946728,-4.84493598594207,
1.67992776788027));
#31755=CARTESIAN_POINT('Ctrl Pts',(-9.05181186538445,-5.05723749268599,
-0.848475665969715));
#31756=CARTESIAN_POINT('Ctrl Pts',(-8.9125532213016,-4.03138450511247,-3.16914830595081));
#31757=CARTESIAN_POINT('Ctrl Pts',(-8.77329457721876,-2.01853479244033,
-4.71392398166109));
#31758=CARTESIAN_POINT('Ctrl Pts',(-8.63403593313593,0.488509216784092,
-5.10459800163426));
#31759=CARTESIAN_POINT('Ctrl Pts',(-8.49477728905309,2.87595238006221,-4.24552233780323));
#31760=CARTESIAN_POINT('Ctrl Pts',(-8.35551864497026,4.5592812180853,-2.34702296273093));
#31761=CARTESIAN_POINT('Ctrl Pts',(-8.21626000088742,5.1263693141631,0.126093885571429));
#31762=CARTESIAN_POINT('Ctrl Pts',(-8.07700135680457,4.43837749456725,2.56833939129752));
#31763=CARTESIAN_POINT('Ctrl Pts',(-7.93774271272176,2.66374557742339,4.38178291474247));
#31764=CARTESIAN_POINT('Ctrl Pts',(-7.7984840686389,0.236953550501235,5.12244229133686));
#31765=CARTESIAN_POINT('Ctrl Pts',(-7.65922542455607,-2.24785139432755,
4.60898319829779));
#31766=CARTESIAN_POINT('Ctrl Pts',(-7.51996678047323,-4.18231886529451,
2.96711491556586));
#31767=CARTESIAN_POINT('Ctrl Pts',(-7.38070813639039,-5.09283661920301,
0.598813145544185));
#31768=CARTESIAN_POINT('Ctrl Pts',(-7.24144949230755,-4.75648420772767,
-1.91609498585244));
#31769=CARTESIAN_POINT('Ctrl Pts',(-7.10219084822472,-3.25561019578073,
-3.96188897702852));
#31770=CARTESIAN_POINT('Ctrl Pts',(-6.96293220414188,-0.957670908279476,
-5.03770071010642));
#31771=CARTESIAN_POINT('Ctrl Pts',(-6.82367356005904,1.57473325078029,-4.88014110472828));
#31772=CARTESIAN_POINT('Ctrl Pts',(-6.68441491597621,3.72159825835185,-3.52778519989586));
#31773=CARTESIAN_POINT('Ctrl Pts',(-6.54515627189337,4.95731095870299,-1.31172789552367));
#31774=CARTESIAN_POINT('Ctrl Pts',(-6.40589762781053,4.97933400098995,1.22547742523351));
#31775=CARTESIAN_POINT('Ctrl Pts',(-6.26663898372769,3.78227552279275,3.46265127941791));
#31776=CARTESIAN_POINT('Ctrl Pts',(-6.12738033964487,1.65920923023726,4.8520703564012));
#31777=CARTESIAN_POINT('Ctrl Pts',(-5.988121695562,-0.870078318172324,5.05356564550398));
#31778=CARTESIAN_POINT('Ctrl Pts',(-5.84886305147918,-3.18634613365232,
4.01780541212868));
#31779=CARTESIAN_POINT('Ctrl Pts',(-5.70960440739635,-4.7225064711785,1.99837299892905));
#31780=CARTESIAN_POINT('Ctrl Pts',(-5.57034576331351,-5.10246391726663,
-0.510317534642611));
#31781=CARTESIAN_POINT('Ctrl Pts',(-5.43108711923067,-4.23319416364483,
-2.89406793044928));
#31782=CARTESIAN_POINT('Ctrl Pts',(-5.29182847514784,-2.32751898381641,
-4.56926880289899));
#31783=CARTESIAN_POINT('Ctrl Pts',(-5.15256983106498,0.147998544643936,
-5.12578369071063));
#31784=CARTESIAN_POINT('Ctrl Pts',(-5.01331118698215,2.58728185166053,-4.42736204000073));
#31785=CARTESIAN_POINT('Ctrl Pts',(-4.87405254289932,4.39312552738983,-2.64499718596595));
#31786=CARTESIAN_POINT('Ctrl Pts',(-4.73479389881648,5.12340806451229,-0.215062357612596));
#31787=CARTESIAN_POINT('Ctrl Pts',(-4.59553525473364,4.59933568346607,2.26752580668157));
#31788=CARTESIAN_POINT('Ctrl Pts',(-4.45627661065081,2.94921609668853,4.19495964559934));
#31789=CARTESIAN_POINT('Ctrl Pts',(-4.31701796656797,0.57704515873205,5.09534894761389));
#31790=CARTESIAN_POINT('Ctrl Pts',(-4.17775932248513,-1.93640272295992,
4.74825299533382));
#31791=CARTESIAN_POINT('Ctrl Pts',(-4.03850067840229,-3.97576455713786,
3.2386506757228));
#31792=CARTESIAN_POINT('Ctrl Pts',(-3.89924203431946,-5.04174699952815,
0.936135249811344));
#31793=CARTESIAN_POINT('Ctrl Pts',(-3.75998339023661,-4.87336745758836,
-1.59557251057302));
#31794=CARTESIAN_POINT('Ctrl Pts',(-3.62072474615378,-3.51184999623001,
-3.73663908038491));
#31795=CARTESIAN_POINT('Ctrl Pts',(-3.48146610207094,-1.29053252299245,
-4.96287092523671));
#31796=CARTESIAN_POINT('Ctrl Pts',(-3.3422074579881,1.24674374109644,-4.97405187513803));
#31797=CARTESIAN_POINT('Ctrl Pts',(-3.20294881390526,3.47878194424713,-3.76744451832491));
#31798=CARTESIAN_POINT('Ctrl Pts',(-3.06369016982243,4.8591161279818,-1.63846039519689));
#31799=CARTESIAN_POINT('Ctrl Pts',(-2.92443152573959,5.04980152031218,0.891665082289887));
#31800=CARTESIAN_POINT('Ctrl Pts',(-2.78517288165675,4.0041529537823,3.20348577954525));
#31801=CARTESIAN_POINT('Ctrl Pts',(-2.64591423757392,1.9781747155564,4.73100272599303));
#31802=CARTESIAN_POINT('Ctrl Pts',(-2.50665559349108,-0.532116534951586,
5.10023666524732));
#31803=CARTESIAN_POINT('Ctrl Pts',(-2.36739694940823,-2.91213063348896,
4.22078868480285));
#31804=CARTESIAN_POINT('Ctrl Pts',(-2.2281383053254,-4.57917295608466,2.30797251716464));
#31805=CARTESIAN_POINT('Ctrl Pts',(-2.08887966124257,-5.12510446412278,
-0.169900526165591));
#31806=CARTESIAN_POINT('Ctrl Pts',(-1.94962101715972,-4.41626575409672,
-2.60617701967216));
#31807=CARTESIAN_POINT('Ctrl Pts',(-1.8103623730769,-2.62620047284534,-4.40438801630634));
#31808=CARTESIAN_POINT('Ctrl Pts',(-1.67110372899405,-0.193167284512309,
-5.12428009940892));
#31809=CARTESIAN_POINT('Ctrl Pts',(-1.53184508491121,2.28715890535059,-4.58960454528829));
#31810=CARTESIAN_POINT('Ctrl Pts',(-1.39258644082838,4.20752364775137,-2.93126272184108));
#31811=CARTESIAN_POINT('Ctrl Pts',(-1.25332779674554,5.0977685824936,-0.555268006901366));
#31812=CARTESIAN_POINT('Ctrl Pts',(-1.1140691526627,4.73993440187225,1.95667777727522));
#31813=CARTESIAN_POINT('Ctrl Pts',(-0.974810508579856,3.22163334032844,
3.98956232001804));
#31814=CARTESIAN_POINT('Ctrl Pts',(-0.835551864497027,0.914579917925479,
5.04571140862161));
#31815=CARTESIAN_POINT('Ctrl Pts',(-0.696293220414185,-1.61637760332782,
4.86648495952254));
#31816=CARTESIAN_POINT('Ctrl Pts',(-0.55703457633135,-3.75162148741517,
3.49588943240163));
#31817=CARTESIAN_POINT('Ctrl Pts',(-0.417775932248522,-4.96832111478826,
1.26923775212314));
#31818=CARTESIAN_POINT('Ctrl Pts',(-0.278517288165672,-4.96871636595204,
-1.26783711748493));
#31819=CARTESIAN_POINT('Ctrl Pts',(-0.139258644082833,-3.75247085555401,
-3.49516562013044));
#31820=CARTESIAN_POINT('Ctrl Pts',(-0.0464195480276115,-2.32937887075175,
-4.40852359138744));
#31821=CARTESIAN_POINT('Ctrl Pts',(0.,-1.55153804394499,-4.66710967952236));
#31822=CARTESIAN_POINT('Ctrl Pts',(-59.9675728291906,-2.29321473482431,
4.72388001049939));
#31823=CARTESIAN_POINT('Ctrl Pts',(-59.921153281163,-3.08051715225516,4.3416828546863));
#31824=CARTESIAN_POINT('Ctrl Pts',(-59.8283141851078,-4.45952062202937,
3.1764064847768));
#31825=CARTESIAN_POINT('Ctrl Pts',(-59.6890555410249,-5.43632641336422,
0.649104968589505));
#31826=CARTESIAN_POINT('Ctrl Pts',(-59.549796896942,-5.08208949153779,-2.03639929150226));
#31827=CARTESIAN_POINT('Ctrl Pts',(-59.4105382528593,-3.48365430538738,
-4.22368768893344));
#31828=CARTESIAN_POINT('Ctrl Pts',(-59.2712796087763,-1.03230120376032,
-5.37671901698262));
#31829=CARTESIAN_POINT('Ctrl Pts',(-59.1320209646936,1.67177759101493,-5.21346943231462));
#31830=CARTESIAN_POINT('Ctrl Pts',(-58.9927623206106,3.96656356885327,-3.77376837874884));
#31831=CARTESIAN_POINT('Ctrl Pts',(-58.8535036765279,5.29021998226643,-1.41016638601528));
#31832=CARTESIAN_POINT('Ctrl Pts',(-58.714245032445,5.31868266429192,1.29869649210185));
#31833=CARTESIAN_POINT('Ctrl Pts',(-58.5749863883622,4.04498094899183,3.68959547908911));
#31834=CARTESIAN_POINT('Ctrl Pts',(-58.4357277442793,1.78095409720902,5.1771805877835));
#31835=CARTESIAN_POINT('Ctrl Pts',(-58.2964691001966,-0.919100786258854,
5.39724408305449));
#31836=CARTESIAN_POINT('Ctrl Pts',(-58.1572104561136,-3.39413375243565,
4.29591072583816));
#31837=CARTESIAN_POINT('Ctrl Pts',(-58.0179518120309,-5.03818701758687,
2.14281672038556));
#31838=CARTESIAN_POINT('Ctrl Pts',(-57.8786931679479,-5.44874985610609,
-0.534899081668944));
#31839=CARTESIAN_POINT('Ctrl Pts',(-57.7394345238652,-4.52530493562246,
-3.08165660426907));
#31840=CARTESIAN_POINT('Ctrl Pts',(-57.6001758797823,-2.49393761929334,
-4.87393754198233));
#31841=CARTESIAN_POINT('Ctrl Pts',(-57.4609172356995,0.148016021757186,
-5.47294101771703));
#31842=CARTESIAN_POINT('Ctrl Pts',(-57.3216585916167,2.75373116429528,-4.73201402621145));
#31843=CARTESIAN_POINT('Ctrl Pts',(-57.1823999475338,4.68525518433443,-2.83255643335289));
#31844=CARTESIAN_POINT('Ctrl Pts',(-57.043141303451,5.46969647996603,-0.239609063908964));
#31845=CARTESIAN_POINT('Ctrl Pts',(-56.9038826593682,4.91500167802301,2.41200136599783));
#31846=CARTESIAN_POINT('Ctrl Pts',(-56.7646240152853,3.15697572436193,4.47308577640863));
#31847=CARTESIAN_POINT('Ctrl Pts',(-56.6253653712025,0.626032997947133,
5.43903252158022));
#31848=CARTESIAN_POINT('Ctrl Pts',(-56.4861067271197,-2.05818027804203,
5.07335057230125));
#31849=CARTESIAN_POINT('Ctrl Pts',(-56.3468480830367,-4.23849292350452,
3.46556919182964));
#31850=CARTESIAN_POINT('Ctrl Pts',(-56.207589438954,-5.38110285676427,1.00931864690527));
#31851=CARTESIAN_POINT('Ctrl Pts',(-56.0683307948711,-5.20626691248704,
-1.69404159394754));
#31852=CARTESIAN_POINT('Ctrl Pts',(-55.9290721507884,-3.75678986510833,
-3.98265263303982));
#31853=CARTESIAN_POINT('Ctrl Pts',(-55.7898135067054,-1.38754461178488,
-5.2961978849341));
#31854=CARTESIAN_POINT('Ctrl Pts',(-55.6505548626227,1.32141073022532,-5.31308439309028));
#31855=CARTESIAN_POINT('Ctrl Pts',(-55.5112962185397,3.70684742458739,-4.02917786364572));
#31856=CARTESIAN_POINT('Ctrl Pts',(-55.372037574457,5.18474323222248,-1.75881485722158));
#31857=CARTESIAN_POINT('Ctrl Pts',(-55.232778930374,5.39326754125922,0.942155674217395));
#31858=CARTESIAN_POINT('Ctrl Pts',(-55.0935202862913,4.28136771460451,3.41245990136191));
#31859=CARTESIAN_POINT('Ctrl Pts',(-54.9542616422084,2.12126821662139,5.0472976174595));
#31860=CARTESIAN_POINT('Ctrl Pts',(-54.8150029981255,-0.558177620120985,
5.44641440127875));
#31861=CARTESIAN_POINT('Ctrl Pts',(-54.6757443540428,-3.10096581917486,
4.51209519783989));
#31862=CARTESIAN_POINT('Ctrl Pts',(-54.5364857099599,-4.88455005138143,
2.47308772218258));
#31863=CARTESIAN_POINT('Ctrl Pts',(-54.3972270658771,-5.47225854953695,
-0.171401438384739));
#31864=CARTESIAN_POINT('Ctrl Pts',(-54.2579684217942,-4.72020368341004,
-2.77392668850185));
#31865=CARTESIAN_POINT('Ctrl Pts',(-54.1187097777114,-2.812509713294,-4.69731638264738));
#31866=CARTESIAN_POINT('Ctrl Pts',(-53.9794511336286,-0.216233973612521,
-5.47067043009504));
#31867=CARTESIAN_POINT('Ctrl Pts',(-53.8401924895457,2.43298194667935,-4.90464992972923));
#31868=CARTESIAN_POINT('Ctrl Pts',(-53.7009338454629,4.48653520801346,-3.13783267771182));
#31869=CARTESIAN_POINT('Ctrl Pts',(-53.56167520138,5.4416580041481,-0.602785411196621));
#31870=CARTESIAN_POINT('Ctrl Pts',(-53.4224165572971,5.06450931330617,2.07984073945473));
#31871=CARTESIAN_POINT('Ctrl Pts',(-53.2831579132145,3.44742578118945,4.2532631671754));
#31872=CARTESIAN_POINT('Ctrl Pts',(-53.1438992691315,0.986315103624491,
5.38536671011573));
#31873=CARTESIAN_POINT('Ctrl Pts',(-53.0046406250487,-1.71627335309004,
5.19898046385382));
#31874=CARTESIAN_POINT('Ctrl Pts',(-52.8653819809658,-3.99866964586547,
3.73973704280055));
#31875=CARTESIAN_POINT('Ctrl Pts',(-52.726123336883,-5.30207873456371,1.3649004280708));
#31876=CARTESIAN_POINT('Ctrl Pts',(-52.5868646928002,-5.30738928153452,
-1.34410233997011));
#31877=CARTESIAN_POINT('Ctrl Pts',(-52.4476060487173,-4.01330111497288,
-3.72403091375702));
#31878=CARTESIAN_POINT('Ctrl Pts',(-52.3083474046345,-1.73664354767827,
-5.19221159761117));
#31879=CARTESIAN_POINT('Ctrl Pts',(-52.1690887605516,0.965193382202131,
-5.38919231620228));
#31880=CARTESIAN_POINT('Ctrl Pts',(-52.0298301164688,3.43072372656281,-4.26674662923164));
#31881=CARTESIAN_POINT('Ctrl Pts',(-51.890571472386,5.05631605991481,-2.09968092535702));
#31882=CARTESIAN_POINT('Ctrl Pts',(-51.7513128283031,5.44397949170202,0.581445939007525));
#31883=CARTESIAN_POINT('Ctrl Pts',(-51.6120541842203,4.49880307082833,3.12021842440015));
#31884=CARTESIAN_POINT('Ctrl Pts',(-51.4727955401375,2.45219266563987,4.89507336172223));
#31885=CARTESIAN_POINT('Ctrl Pts',(-51.3335368960546,-0.194783724789619,
5.47147616156898));
#31886=CARTESIAN_POINT('Ctrl Pts',(-51.1942782519718,-2.79407156101991,
4.70830714779317));
#31887=CARTESIAN_POINT('Ctrl Pts',(-51.055019607889,-4.7092918078351,2.79241163776362));
#31888=CARTESIAN_POINT('Ctrl Pts',(-50.9157609638061,-5.47154448582322,
0.192854934388569));
#31889=CARTESIAN_POINT('Ctrl Pts',(-50.7765023197233,-4.89420862248269,
-2.45391810084947));
#31890=CARTESIAN_POINT('Ctrl Pts',(-50.6372436756404,-3.11863233424258,
-4.49990271560145));
#31891=CARTESIAN_POINT('Ctrl Pts',(-50.4979850315576,-0.579526817574764,
-5.44418412195733));
#31892=CARTESIAN_POINT('Ctrl Pts',(-50.3587263874748,2.10146322296508,-5.05557557638946));
#31893=CARTESIAN_POINT('Ctrl Pts',(-50.2194677433919,4.26795574624971,-3.42921942052629));
#31894=CARTESIAN_POINT('Ctrl Pts',(-50.0802090993091,5.38953222665332,-0.963293550235825));
#31895=CARTESIAN_POINT('Ctrl Pts',(-49.9409504552262,5.19159908182171,1.73847377308041));
#31896=CARTESIAN_POINT('Ctrl Pts',(-49.8016918111434,3.72261593288249,4.01461364296864));
#31897=CARTESIAN_POINT('Ctrl Pts',(-49.6624331670606,1.34223132127078,5.30786276822039));
#31898=CARTESIAN_POINT('Ctrl Pts',(-49.5231745229777,-1.36676940640204,
5.30159725703339));
#31899=CARTESIAN_POINT('Ctrl Pts',(-49.383915878895,-3.74114640211058,3.99735108340956));
#31900=CARTESIAN_POINT('Ctrl Pts',(-49.244657234812,-5.1995851532,1.71444052701824));
#31901=CARTESIAN_POINT('Ctrl Pts',(-49.1053985907293,-5.38501868447694,
-0.988213465752643));
#31902=CARTESIAN_POINT('Ctrl Pts',(-48.9661399466464,-4.25204763305208,
-3.44892490673787));
#31903=CARTESIAN_POINT('Ctrl Pts',(-48.8268813025636,-2.07805529391247,
-5.06524217402316));
#31904=CARTESIAN_POINT('Ctrl Pts',(-48.6876226584808,0.604703640689364,
-5.44144517504289));
#31905=CARTESIAN_POINT('Ctrl Pts',(-48.5483640143978,3.1394140544273,-4.48542879565877));
#31906=CARTESIAN_POINT('Ctrl Pts',(-48.4091053703151,4.90550728800826,-2.43125283205151));
#31907=CARTESIAN_POINT('Ctrl Pts',(-48.2698467262322,5.47059386442934,0.218162454443064));
#31908=CARTESIAN_POINT('Ctrl Pts',(-48.1305880821494,4.6963246384732,2.8141654137826));
#31909=CARTESIAN_POINT('Ctrl Pts',(-47.9913294380664,2.77226257278806,4.72118124133983));
#31910=CARTESIAN_POINT('Ctrl Pts',(-47.8520707939838,0.169472373632881,
5.47231863113212));
#31911=CARTESIAN_POINT('Ctrl Pts',(-47.7128121499008,-2.47480944646745,
4.88367794697152));
#31912=CARTESIAN_POINT('Ctrl Pts',(-47.5735535058181,-4.51318805495189,
3.09937504453724));
#31913=CARTESIAN_POINT('Ctrl Pts',(-47.4342948617351,-5.44661082894759,
0.55625764179145));
#31914=CARTESIAN_POINT('Ctrl Pts',(-47.2950362176524,-5.04654952464708,
-2.12304733375045));
#31915=CARTESIAN_POINT('Ctrl Pts',(-47.1557775735694,-3.41095044230588,
-4.28257039243885));
#31916=CARTESIAN_POINT('Ctrl Pts',(-47.0165189294868,-0.940254407103962,
-5.39359933031572));
#31917=CARTESIAN_POINT('Ctrl Pts',(-46.8772602854037,1.76064244853427,-5.1841229011743));
#31918=CARTESIAN_POINT('Ctrl Pts',(-46.7380016413211,4.03048433321423,-3.70542684798596));
#31919=CARTESIAN_POINT('Ctrl Pts',(-46.5987429972381,5.31354988028646,-1.31953770532269));
#31920=CARTESIAN_POINT('Ctrl Pts',(-46.4594843531554,5.29570842534992,1.38941151562037));
#31921=CARTESIAN_POINT('Ctrl Pts',(-46.3202257090724,3.98132806020307,3.75819357711923));
#31922=CARTESIAN_POINT('Ctrl Pts',(-46.1809670649897,1.69220620066887,5.20686376434782));
#31923=CARTESIAN_POINT('Ctrl Pts',(-46.0417084209068,-1.01121550452221,
5.38074672229371));
#31924=CARTESIAN_POINT('Ctrl Pts',(-45.902449776824,-3.46706310953342,4.23727099446955));
#31925=CARTESIAN_POINT('Ctrl Pts',(-45.7631911327411,-5.07407579679372,
2.05639171717179));
#31926=CARTESIAN_POINT('Ctrl Pts',(-45.6239324886583,-5.43881149757799,
-0.627950300480917));
#31927=CARTESIAN_POINT('Ctrl Pts',(-45.4846738445755,-4.47197261654545,
-3.15855235874414));
#31928=CARTESIAN_POINT('Ctrl Pts',(-45.3454152004926,-2.41026860377883,
-4.915851639716));
#31929=CARTESIAN_POINT('Ctrl Pts',(-45.2061565564098,0.241537200449422,
-5.46961167422877));
#31930=CARTESIAN_POINT('Ctrl Pts',(-45.066897912327,2.8342078798761,-4.68425637425076));
#31931=CARTESIAN_POINT('Ctrl Pts',(-44.9276392682441,4.73298446606043,-2.75206288628934));
#31932=CARTESIAN_POINT('Ctrl Pts',(-44.7883806241613,5.47299285188585,-0.146086718311155));
#31933=CARTESIAN_POINT('Ctrl Pts',(-44.6491219800784,4.8730580954859,2.49565560205727));
#31934=CARTESIAN_POINT('Ctrl Pts',(-44.5098633359956,3.08006116023398,4.52639098347444));
#31935=CARTESIAN_POINT('Ctrl Pts',(-44.3706046919128,0.532978308741886,
5.44893808080723));
#31936=CARTESIAN_POINT('Ctrl Pts',(-44.2313460478299,-2.14459267768491,
5.03743132289471));
#31937=CARTESIAN_POINT('Ctrl Pts',(-44.0920874037471,-4.29710683887934,
3.39261918011984));
#31938=CARTESIAN_POINT('Ctrl Pts',(-43.9528287596642,-5.39756794683762,
0.917198094923704));
#31939=CARTESIAN_POINT('Ctrl Pts',(-43.8135701155814,-5.17655205842662,
-1.78277897465157));
#31940=CARTESIAN_POINT('Ctrl Pts',(-43.6743114714986,-3.68817010198369,
-4.0462814268034));
#31941=CARTESIAN_POINT('Ctrl Pts',(-43.5350528274157,-1.296819994612,-5.31913996691524));
#31942=CARTESIAN_POINT('Ctrl Pts',(-43.395794183333,1.41202825418013,-5.28972289401417));
#31943=CARTESIAN_POINT('Ctrl Pts',(-43.25653553925,3.77517212750151,-3.96523233793384));
#31944=CARTESIAN_POINT('Ctrl Pts',(-43.1172768951672,5.21404729814717,-1.66994097462899));
#31945=CARTESIAN_POINT('Ctrl Pts',(-42.9780182510844,5.37637650765863,1.03419907849356));
#31946=CARTESIAN_POINT('Ctrl Pts',(-42.8387596070015,4.22241698330551,3.48513800374586));
#31947=CARTESIAN_POINT('Ctrl Pts',(-42.6995009629187,2.03469059071199,5.08281676692449));
#31948=CARTESIAN_POINT('Ctrl Pts',(-42.5602423188359,-0.651185493897992,
5.43607850739827));
#31949=CARTESIAN_POINT('Ctrl Pts',(-42.420983674753,-3.17763298788509,4.45843477919831));
#31950=CARTESIAN_POINT('Ctrl Pts',(-42.2817250306702,-4.92610622795756,
2.389240363994));
#31951=CARTESIAN_POINT('Ctrl Pts',(-42.1424663865873,-5.46852960890205,
-0.264907535985755));
#31952=CARTESIAN_POINT('Ctrl Pts',(-42.0032077425046,-4.6721025754924,-2.85419859332491));
#31953=CARTESIAN_POINT('Ctrl Pts',(-41.8639490984217,-2.73181294711378,
-4.74470126647001));
#31954=CARTESIAN_POINT('Ctrl Pts',(-41.7246904543388,-0.122698395445459,
-5.47356713577313));
#31955=CARTESIAN_POINT('Ctrl Pts',(-41.585431810256,2.51645618696809,-4.86234926194433));
#31956=CARTESIAN_POINT('Ctrl Pts',(-41.4461731661731,4.5395112600836,-3.06069103400435));
#31957=CARTESIAN_POINT('Ctrl Pts',(-41.3069145220904,5.45116583504063,-0.509689243506713));
#31958=CARTESIAN_POINT('Ctrl Pts',(-41.1676558780075,5.02822113763075,2.16609886135048));
#31959=CARTESIAN_POINT('Ctrl Pts',(-41.0283972339246,3.37422596869697,4.31156482013568));
#31960=CARTESIAN_POINT('Ctrl Pts',(-40.8891385898418,0.894125034703335,
5.40143800375207));
#31961=CARTESIAN_POINT('Ctrl Pts',(-40.7498799457589,-1.80488294721927,
5.1688866918223));
#31962=CARTESIAN_POINT('Ctrl Pts',(-40.6106213016762,-4.06200463528118,
3.6708460099839));
#31963=CARTESIAN_POINT('Ctrl Pts',(-40.4713626575933,-5.32463292603174,
1.27407860396417));
#31964=CARTESIAN_POINT('Ctrl Pts',(-40.3321040135104,-5.28364077232195,
-1.4346192090996));
#31965=CARTESIAN_POINT('Ctrl Pts',(-40.1928453694276,-3.94906421050984,
-3.79208174322904));
#31966=CARTESIAN_POINT('Ctrl Pts',(-40.0535867253448,-1.64764525546177,
-5.22113562342665));
#31967=CARTESIAN_POINT('Ctrl Pts',(-39.9143280812619,1.05716376798652,-5.37190812037186));
#31968=CARTESIAN_POINT('Ctrl Pts',(-39.7750694371792,3.50314925932756,-4.20748587079426));
#31969=CARTESIAN_POINT('Ctrl Pts',(-39.6358107930962,5.09146492480532,-2.01295231079566));
#31970=CARTESIAN_POINT('Ctrl Pts',(-39.4965521490135,5.43324625440816,0.674408796665931));
#31971=CARTESIAN_POINT('Ctrl Pts',(-39.3572935049306,4.44481553081827,3.1966555934378));
#31972=CARTESIAN_POINT('Ctrl Pts',(-39.2180348608478,2.36816849667272,4.93627086548413));
#31973=CARTESIAN_POINT('Ctrl Pts',(-39.0787762167649,-0.288273034309676,
5.46734768820773));
#31974=CARTESIAN_POINT('Ctrl Pts',(-38.9395175726821,-2.87413718909858,
4.6598634641265));
#31975=CARTESIAN_POINT('Ctrl Pts',(-38.8002589285993,-4.75633142861974,
2.71151312502534));
#31976=CARTESIAN_POINT('Ctrl Pts',(-38.6610002845164,-5.47404147230753,
0.0993078321067214));
#31977=CARTESIAN_POINT('Ctrl Pts',(-38.5217416404335,-4.85155164189017,
-2.53721082138112));
#31978=CARTESIAN_POINT('Ctrl Pts',(-38.3824829963508,-3.04126501954696,
-4.55254864520309));
#31979=CARTESIAN_POINT('Ctrl Pts',(-38.2432243522678,-0.486390871344371,
-5.45329405096895));
#31980=CARTESIAN_POINT('Ctrl Pts',(-38.1039657081851,2.18756549204408,-5.01891913703325));
#31981=CARTESIAN_POINT('Ctrl Pts',(-37.9647070641022,4.32594407220496,-3.35577114389752));
#31982=CARTESIAN_POINT('Ctrl Pts',(-37.8254484200194,5.40520943039183,-0.871035647757145));
#31983=CARTESIAN_POINT('Ctrl Pts',(-37.6861897759365,5.16112694133097,1.82695396261872));
#31984=CARTESIAN_POINT('Ctrl Pts',(-37.5469311318537,3.65345488832461,4.0776536715417));
#31985=CARTESIAN_POINT('Ctrl Pts',(-37.4076724877709,1.25131394863708,5.33002865733449));
#31986=CARTESIAN_POINT('Ctrl Pts',(-37.268413843688,-1.45718396786787,5.27746217133286));
#31987=CARTESIAN_POINT('Ctrl Pts',(-37.1291551996052,-3.80892211553217,
3.93282397316106));
#31988=CARTESIAN_POINT('Ctrl Pts',(-36.9898965555224,-5.22812861075348,
1.62531945028708));
#31989=CARTESIAN_POINT('Ctrl Pts',(-36.8506379114395,-5.36734164202615,
-1.08010915366577));
#31990=CARTESIAN_POINT('Ctrl Pts',(-36.7113792673567,-4.19247792957796,
-3.52109654739291));
#31991=CARTESIAN_POINT('Ctrl Pts',(-36.5721206232738,-1.99117727436389,
-5.10002011252087));
#31992=CARTESIAN_POINT('Ctrl Pts',(-36.432861979191,0.697619784727175,-5.43031479032456));
#31993=CARTESIAN_POINT('Ctrl Pts',(-36.2936033351082,3.21561982804948,-4.43111512009288));
#31994=CARTESIAN_POINT('Ctrl Pts',(-36.1543446910253,4.94634536668937,-2.34705338658735));
#31995=CARTESIAN_POINT('Ctrl Pts',(-36.0150860469425,5.46606593372767,0.311633268767087));
#31996=CARTESIAN_POINT('Ctrl Pts',(-35.8758274028597,4.6475392636393,2.89402330311827));
#31997=CARTESIAN_POINT('Ctrl Pts',(-35.7365687587768,2.6911637906988,4.76787474014284));
#31998=CARTESIAN_POINT('Ctrl Pts',(-35.597310114694,0.0759154554066592,
5.47441585282768));
#31999=CARTESIAN_POINT('Ctrl Pts',(-35.4580514706111,-2.55791912631663,
4.84066543248798));
#32000=CARTESIAN_POINT('Ctrl Pts',(-35.3187928265284,-4.56550290077017,
3.02178347158093));
#32001=CARTESIAN_POINT('Ctrl Pts',(-35.1795341824454,-5.45532268973101,
0.463083617683259));
#32002=CARTESIAN_POINT('Ctrl Pts',(-35.0402755383627,-5.00952549095672,
-2.208992177785));
#32003=CARTESIAN_POINT('Ctrl Pts',(-34.9010168942798,-3.33725504270655,
-4.34024433252211));
#32004=CARTESIAN_POINT('Ctrl Pts',(-34.761758250197,-0.847930355697263,
-5.40888215789063));
#32005=CARTESIAN_POINT('Ctrl Pts',(-34.6224996061141,1.84899161783318,-5.15327294864565));
#32006=CARTESIAN_POINT('Ctrl Pts',(-34.4832409620313,4.09322824983354,-3.63599705456774));
#32007=CARTESIAN_POINT('Ctrl Pts',(-34.3439823179484,5.33532706229741,-1.22852644431343));
#32008=CARTESIAN_POINT('Ctrl Pts',(-34.2047236738656,5.27118720386816,1.47972211845237));
#32009=CARTESIAN_POINT('Ctrl Pts',(-34.0654650297827,3.91651192243436,3.82569293690568));
#32010=CARTESIAN_POINT('Ctrl Pts',(-33.9262063856999,1.60296396677416,5.23502613243565));
#32011=CARTESIAN_POINT('Ctrl Pts',(-33.7869477416171,-1.10303481654853,
5.36267715600542));
#32012=CARTESIAN_POINT('Ctrl Pts',(-33.6476890975343,-3.53897954022436,
4.17739343370168));
#32013=CARTESIAN_POINT('Ctrl Pts',(-33.5084304534514,-5.10848217385333,
1.96936587902892));
#32014=CARTESIAN_POINT('Ctrl Pts',(-33.3691718093686,-5.42728416867607,
-0.720818034248989));
#32015=CARTESIAN_POINT('Ctrl Pts',(-33.2299131652857,-4.4173337971916,-3.23452534543313));
#32016=CARTESIAN_POINT('Ctrl Pts',(-33.0906545212029,-2.32589541929987,
-4.95632954761288));
#32017=CARTESIAN_POINT('Ctrl Pts',(-32.9513958771201,0.334987812800003,
-5.46468436886669));
#32018=CARTESIAN_POINT('Ctrl Pts',(-32.8121372330372,2.91385657226341,-4.63513019907076));
#32019=CARTESIAN_POINT('Ctrl Pts',(-32.6728785889544,4.77933099025839,-2.67076531571315));
#32020=CARTESIAN_POINT('Ctrl Pts',(-32.5336199448715,5.47469027049736,-0.052521692490149));
#32021=CARTESIAN_POINT('Ctrl Pts',(-32.3943613007888,4.82969083251998,2.57858072364102));
#32022=CARTESIAN_POINT('Ctrl Pts',(-32.2551026567059,3.00224674583928,4.57837379024015));
#32023=CARTESIAN_POINT('Ctrl Pts',(-32.115844012623,0.439767908113807,5.45725171428383));
#32024=CARTESIAN_POINT('Ctrl Pts',(-31.9765853685402,-2.23037852732192,
5.0000403709292));
#32025=CARTESIAN_POINT('Ctrl Pts',(-31.8373267244574,-4.35446533996426,
3.31867800322816));
#32026=CARTESIAN_POINT('Ctrl Pts',(-31.6980680803745,-5.41245611918446,
0.824809580426464));
#32027=CARTESIAN_POINT('Ctrl Pts',(-31.5588094362917,-5.14532485718034,
-1.87099551045498));
#32028=CARTESIAN_POINT('Ctrl Pts',(-31.4195507922088,-3.61847282749334,
-4.10872808576484));
#32029=CARTESIAN_POINT('Ctrl Pts',(-31.280292148126,-1.20571650709311,-5.34052804417164));
#32030=CARTESIAN_POINT('Ctrl Pts',(-31.1410335040432,1.50223324930637,-5.26481598450876));
#32031=CARTESIAN_POINT('Ctrl Pts',(-31.0017748599604,3.8423939011143,-3.90012835618781));
#32032=CARTESIAN_POINT('Ctrl Pts',(-30.8625162158775,5.24182806252442,-1.58057921313423));
#32033=CARTESIAN_POINT('Ctrl Pts',(-30.7232575717947,5.35791474748316,1.12594033801213));
#32034=CARTESIAN_POINT('Ctrl Pts',(-30.5839989277118,4.16223265860835,3.55679791127844));
#32035=CARTESIAN_POINT('Ctrl Pts',(-30.444740283629,1.94751852306694,5.11685095428542));
#32036=CARTESIAN_POINT('Ctrl Pts',(-30.3054816395461,-0.74400312163121,
5.42415444480183));
#32037=CARTESIAN_POINT('Ctrl Pts',(-30.1662229954633,-3.25337180037391,
4.40347181376155));
#32038=CARTESIAN_POINT('Ctrl Pts',(-30.0269643513805,-4.96622322594347,
2.30469498115482));
#32039=CARTESIAN_POINT('Ctrl Pts',(-29.8877057072976,-5.4632030188522,-0.358336239954459));
#32040=CARTESIAN_POINT('Ctrl Pts',(-29.7484470632148,-4.62263649701039,
-2.93363663437857));
#32041=CARTESIAN_POINT('Ctrl Pts',(-29.6091884191319,-2.6503180725445,-4.79069996977524));
#32042=CARTESIAN_POINT('Ctrl Pts',(-29.4699297750492,-0.0291269705273693,
-5.47486472030574));
#32043=CARTESIAN_POINT('Ctrl Pts',(-29.3306711309663,2.59919523607336,-4.81862804238241));
#32044=CARTESIAN_POINT('Ctrl Pts',(-29.1914124868835,4.59116107859052,-2.98265519906275));
#32045=CARTESIAN_POINT('Ctrl Pts',(-29.0521538428006,5.45908108940342,-0.416444168380981));
#32046=CARTESIAN_POINT('Ctrl Pts',(-28.9128951987178,4.99046395014899,2.25172415014003));
#32047=CARTESIAN_POINT('Ctrl Pts',(-28.7736365546349,3.30004036467915,4.36860683485581));
#32048=CARTESIAN_POINT('Ctrl Pts',(-28.6343779105521,0.801673744130189,
5.41593124901275));
#32049=CARTESIAN_POINT('Ctrl Pts',(-28.4951192664693,-1.89296523869295,
5.13728281206716));
#32050=CARTESIAN_POINT('Ctrl Pts',(-28.3558606223864,-4.12415289630857,
3.60088252709389));
#32051=CARTESIAN_POINT('Ctrl Pts',(-28.2166019783036,-5.34563150798721,
1.18288455348559));
#32052=CARTESIAN_POINT('Ctrl Pts',(-28.0773433342207,-5.25834862959317,
-1.52471694937658));
#32053=CARTESIAN_POINT('Ctrl Pts',(-27.9380846901379,-3.8836735735854,-3.85902470319832));
#32054=CARTESIAN_POINT('Ctrl Pts',(-27.7988260460551,-1.55816559811303,
-5.24853427681649));
#32055=CARTESIAN_POINT('Ctrl Pts',(-27.6595674019722,1.14882529980163,-5.35305450342104));
#32056=CARTESIAN_POINT('Ctrl Pts',(-27.5203087578894,3.57455133519163,-4.14699588113375));
#32057=CARTESIAN_POINT('Ctrl Pts',(-27.3810501138065,5.12512630100326,-1.92563560541065));
#32058=CARTESIAN_POINT('Ctrl Pts',(-27.2417914697237,5.42092567585061,0.767174623514176));
#32059=CARTESIAN_POINT('Ctrl Pts',(-27.1025328256409,4.38952942292247,3.27215884873556));
#32060=CARTESIAN_POINT('Ctrl Pts',(-26.963274181558,2.28345245927227,4.97602622102256));
#32061=CARTESIAN_POINT('Ctrl Pts',(-26.8240155374752,-0.381678123888043,
5.46162191073365));
#32062=CARTESIAN_POINT('Ctrl Pts',(-26.6847568933923,-2.95336312827968,
4.61005838559325));
#32063=CARTESIAN_POINT('Ctrl Pts',(-26.5454982493096,-4.8019814710958,2.62982243455963));
#32064=CARTESIAN_POINT('Ctrl Pts',(-26.4062396052267,-5.47493919906733,
0.00573171670601601));
#32065=CARTESIAN_POINT('Ctrl Pts',(-26.2669809611439,-4.80747726408187,
-2.61976228719256));
#32066=CARTESIAN_POINT('Ctrl Pts',(-26.127722317061,-2.96300918899314,-4.60386453232529));
#32067=CARTESIAN_POINT('Ctrl Pts',(-25.9884636729782,-0.393112824376433,
-5.4608107816854));
#32068=CARTESIAN_POINT('Ctrl Pts',(-25.8492050288953,2.27302865646815,-4.98079640348159));
#32069=CARTESIAN_POINT('Ctrl Pts',(-25.7099463848125,4.382668558973,-3.28134246738283));
#32070=CARTESIAN_POINT('Ctrl Pts',(-25.5706877407296,5.41930748391964,-0.778523269268893));
#32071=CARTESIAN_POINT('Ctrl Pts',(-25.4314290966468,5.12914696015394,1.91490040137972));
#32072=CARTESIAN_POINT('Ctrl Pts',(-25.292170452564,3.58322647456839,4.13950239980757));
#32073=CARTESIAN_POINT('Ctrl Pts',(-25.1529118084811,1.16003100040254,5.35063736055488));
#32074=CARTESIAN_POINT('Ctrl Pts',(-25.0136531643983,-1.54717280811051,
5.2517852572153));
#32075=CARTESIAN_POINT('Ctrl Pts',(-24.8743945203155,-3.87558503947927,
3.86714787509153));
#32076=CARTESIAN_POINT('Ctrl Pts',(-24.7351358762327,-5.25514465285639,
1.53572353098318));
#32077=CARTESIAN_POINT('Ctrl Pts',(-24.5958772321498,-5.34809651256708,
-1.17168928403761));
#32078=CARTESIAN_POINT('Ctrl Pts',(-24.456618588067,-4.13168337950149,-3.59223948778637));
#32079=CARTESIAN_POINT('Ctrl Pts',(-24.3173599439841,-1.90371752564225,
-5.13330806289892));
#32080=CARTESIAN_POINT('Ctrl Pts',(-24.1781012999013,0.790332116786058,
-5.41759792077973));
#32081=CARTESIAN_POINT('Ctrl Pts',(-24.0388426558185,3.29088614746639,-4.37550687926259));
#32082=CARTESIAN_POINT('Ctrl Pts',(-23.8995840117356,4.98573835384737,-2.26216824154082));
#32083=CARTESIAN_POINT('Ctrl Pts',(-23.7603253676528,5.45994107338208,0.405013038377822));
#32084=CARTESIAN_POINT('Ctrl Pts',(-23.62106672357,4.59739609449573,2.97303569376085));
#32085=CARTESIAN_POINT('Ctrl Pts',(-23.4818080794871,2.60927877600901,4.81317528821976));
#32086=CARTESIAN_POINT('Ctrl Pts',(-23.3425494354043,-0.0176636417764714,
5.47491370542219));
#32087=CARTESIAN_POINT('Ctrl Pts',(-23.2032907913214,-2.64028150144438,
4.79623870123154));
#32088=CARTESIAN_POINT('Ctrl Pts',(-23.0640321472386,-4.61648391947948,
2.94330907436644));
#32089=CARTESIAN_POINT('Ctrl Pts',(-22.9247735031557,-5.46244075954554,
0.369774302130467));
#32090=CARTESIAN_POINT('Ctrl Pts',(-22.7855148590729,-4.97103790745645,
-2.29429165728589));
#32091=CARTESIAN_POINT('Ctrl Pts',(-22.6462562149901,-3.26258465276295,
-4.39665025554866));
#32092=CARTESIAN_POINT('Ctrl Pts',(-22.5069975709072,-0.755358578570335,
-5.42258476225506));
#32093=CARTESIAN_POINT('Ctrl Pts',(-22.3677389268244,1.93680059797925,-5.12091745000131));
#32094=CARTESIAN_POINT('Ctrl Pts',(-22.2284802827416,4.15477631597997,-3.5655049923163));
#32095=CARTESIAN_POINT('Ctrl Pts',(-22.0892216386588,5.35554551046774,-1.13715626514974));
#32096=CARTESIAN_POINT('Ctrl Pts',(-21.9499629945759,5.24512598722233,1.5696004154642));
#32097=CARTESIAN_POINT('Ctrl Pts',(-21.8107043504931,3.85055156246548,3.89207460756537));
#32098=CARTESIAN_POINT('Ctrl Pts',(-21.6714457064102,1.51325342153693,5.26165906993862));
#32099=CARTESIAN_POINT('Ctrl Pts',(-21.5321870623274,-1.19453187322356,
5.34304086545422));
#32100=CARTESIAN_POINT('Ctrl Pts',(-21.3929284182445,-3.60986204607684,
4.11629543331799));
#32101=CARTESIAN_POINT('Ctrl Pts',(-21.2536697741617,-5.14139609057341,
1.88176468398599));
#32102=CARTESIAN_POINT('Ctrl Pts',(-21.1144111300789,-5.41417124035404,
-0.81347517859106));
#32103=CARTESIAN_POINT('Ctrl Pts',(-20.975152485996,-4.36140443883345,-3.30955335460612));
#32104=CARTESIAN_POINT('Ctrl Pts',(-20.8358938419132,-2.24084271661005,
-4.99535944707448));
#32105=CARTESIAN_POINT('Ctrl Pts',(-20.6966351978304,0.42834055732842,-5.45816053748953));
#32106=CARTESIAN_POINT('Ctrl Pts',(-20.5573765537475,2.99265397160103,-4.58464985493124));
#32107=CARTESIAN_POINT('Ctrl Pts',(-20.4181179096647,4.82428121674802,-2.58868747201988));
#32108=CARTESIAN_POINT('Ctrl Pts',(-20.2788592655819,5.4747882398358,0.0410586777207554));
#32109=CARTESIAN_POINT('Ctrl Pts',(-20.139600621499,4.78491255904768,2.66075250414775));
#32110=CARTESIAN_POINT('Ctrl Pts',(-20.0003419774162,2.92355521490692,4.629019009623));
#32111=CARTESIAN_POINT('Ctrl Pts',(-19.8610833333333,0.346429027804539,
5.46397099322049));
#32112=CARTESIAN_POINT('Ctrl Pts',(-19.7218246892505,-2.31551276433093,
4.96118864026364));
#32113=CARTESIAN_POINT('Ctrl Pts',(-19.5825660451676,-4.4105516692771,3.24376726333712));
#32114=CARTESIAN_POINT('Ctrl Pts',(-19.4433074010849,-5.42576302417591,
0.732180095021679));
#32115=CARTESIAN_POINT('Ctrl Pts',(-19.304048757002,-5.11259443188014,-1.95866542859384));
#32116=CARTESIAN_POINT('Ctrl Pts',(-19.1647901129191,-3.54771840393207,
-4.16997436592388));
#32117=CARTESIAN_POINT('Ctrl Pts',(-19.0255314688363,-1.11426076542012,
-5.36035586810296));
#32118=CARTESIAN_POINT('Ctrl Pts',(-18.8862728247535,1.59199936190943,-5.23837094121259));
#32119=CARTESIAN_POINT('Ctrl Pts',(-18.7470141806706,3.90849310635719,-3.83388493875586));
#32120=CARTESIAN_POINT('Ctrl Pts',(-18.6077555365878,5.26807740910997,-1.49075568007831));
#32121=CARTESIAN_POINT('Ctrl Pts',(-18.468496892505,5.33788765439853,1.21735265025395));
#32122=CARTESIAN_POINT('Ctrl Pts',(-18.3292382484221,4.10083232356702,3.62741868827523));
#32123=CARTESIAN_POINT('Ctrl Pts',(-18.1899796043393,1.85977748130069,5.1493902363394));
#32124=CARTESIAN_POINT('Ctrl Pts',(-18.0507209602565,-0.836603386336836,
5.41064569714468));
#32125=CARTESIAN_POINT('Ctrl Pts',(-17.9114623161736,-3.32816012929122,
4.34722235914576));
#32126=CARTESIAN_POINT('Ctrl Pts',(-17.7722036720908,-5.00488932502251,
2.21947627388452));
#32127=CARTESIAN_POINT('Ctrl Pts',(-17.6329450280079,-5.45628033556868,
-0.451660254778956));
#32128=CARTESIAN_POINT('Ctrl Pts',(-17.4936863839251,-4.5718198996462,-3.01221760357043));
#32129=CARTESIAN_POINT('Ctrl Pts',(-17.3544277398423,-2.56804889858935,
-4.8352990538864));
#32130=CARTESIAN_POINT('Ctrl Pts',(-17.2151690957594,0.064452963933669,
-5.47456280459917));
#32131=CARTESIAN_POINT('Ctrl Pts',(-17.0759104516766,2.68117492150221,-4.77349904434557));
#32132=CARTESIAN_POINT('Ctrl Pts',(-16.9366518075937,4.641469573865,-2.90374797132014));
#32133=CARTESIAN_POINT('Ctrl Pts',(-16.7973931635109,5.46540145476815,-0.323077427683596));
#32134=CARTESIAN_POINT('Ctrl Pts',(-16.6581345194281,4.95124878175094,2.33669159010563));
#32135=CARTESIAN_POINT('Ctrl Pts',(-16.5188758753452,3.22489064271104,4.42437254631835));
#32136=CARTESIAN_POINT('Ctrl Pts',(-16.3796172312624,0.708988241862226,
5.42884221164713));
#32137=CARTESIAN_POINT('Ctrl Pts',(-16.2403585871796,-1.98049449397169,
5.10417805776878));
#32138=CARTESIAN_POINT('Ctrl Pts',(-16.1010999430967,-4.185096272123,3.5298670341987));
#32139=CARTESIAN_POINT('Ctrl Pts',(-15.9618412990139,-5.36506834562346,
1.09134491928533));
#32140=CARTESIAN_POINT('Ctrl Pts',(-15.822582654931,-5.23152024253317,-1.61436923844153));
#32141=CARTESIAN_POINT('Ctrl Pts',(-15.6833240108482,-3.81714830829533,
-3.92484023605274));
#32142=CARTESIAN_POINT('Ctrl Pts',(-15.5440653667653,-1.4682307174165,-5.27439955317143));
#32143=CARTESIAN_POINT('Ctrl Pts',(-15.4048067226826,1.24015119842102,-5.33263697349776));
#32144=CARTESIAN_POINT('Ctrl Pts',(-15.2655480785997,3.64490909379705,-4.08529433260519));
#32145=CARTESIAN_POINT('Ctrl Pts',(-15.1262894345169,5.15729035422367,-1.83775631907285));
#32146=CARTESIAN_POINT('Ctrl Pts',(-14.987030790434,5.40702135552813,0.859716317702179));
#32147=CARTESIAN_POINT('Ctrl Pts',(-14.8477721463512,4.33296089916428,3.34670613176209));
#32148=CARTESIAN_POINT('Ctrl Pts',(-14.7085135022683,2.19806930351525,5.01432781367598));
#32149=CARTESIAN_POINT('Ctrl Pts',(-14.5692548581855,-0.474971704911942,
5.45430050195198));
#32150=CARTESIAN_POINT('Ctrl Pts',(-14.4299962141027,-3.03172623243708,
4.55890646291557));
#32151=CARTESIAN_POINT('Ctrl Pts',(-14.2907375700198,-4.84622859844897,
2.54736343257805));
#32152=CARTESIAN_POINT('Ctrl Pts',(-14.151478925937,-5.47423740382875,-0.0878460732350503));
#32153=CARTESIAN_POINT('Ctrl Pts',(-14.0122202818542,-4.76199836553621,
-2.70154838059416));
#32154=CARTESIAN_POINT('Ctrl Pts',(-13.8729616377713,-2.88388770528642,
-4.65383538485821));
#32155=CARTESIAN_POINT('Ctrl Pts',(-13.7337029936885,-0.299719928167668,
-5.46673211806834));
#32156=CARTESIAN_POINT('Ctrl Pts',(-13.5944443496056,2.35782774788484,-4.94121851342003));
#32157=CARTESIAN_POINT('Ctrl Pts',(-13.4551857055228,4.43811263430321,-3.20595513557172));
#32158=CARTESIAN_POINT('Ctrl Pts',(-13.31592706144,5.43182226844271,-0.685783442575275));
#32159=CARTESIAN_POINT('Ctrl Pts',(-13.1766684173571,5.09566848135027,2.00228739551394));
#32160=CARTESIAN_POINT('Ctrl Pts',(-13.0374097732743,3.51195120908233,4.20014175845122));
#32161=CARTESIAN_POINT('Ctrl Pts',(-12.8981511291914,1.06840914518901,5.36968285697927));
#32162=CARTESIAN_POINT('Ctrl Pts',(-12.7588924851086,-1.63670963658612,
5.22457401627795));
#32163=CARTESIAN_POINT('Ctrl Pts',(-12.6196338410258,-3.94111569815331,
3.80034197669499));
#32164=CARTESIAN_POINT('Ctrl Pts',(-12.4803751969429,-5.28062538668073,
1.44567894485724));
#32165=CARTESIAN_POINT('Ctrl Pts',(-12.3411165528601,-5.32728891862932,
-1.26292710142351));
#32166=CARTESIAN_POINT('Ctrl Pts',(-12.2018579087773,-4.06968174415604,
-3.66233294326767));
#32167=CARTESIAN_POINT('Ctrl Pts',(-12.0625992646944,-1.81570159940882,
-5.16509629997009));
#32168=CARTESIAN_POINT('Ctrl Pts',(-11.9233406206116,0.882813550644842,
-5.40329828168483));
#32169=CARTESIAN_POINT('Ctrl Pts',(-11.7840819765288,3.36519102336852,-4.31862031930342));
#32170=CARTESIAN_POINT('Ctrl Pts',(-11.6448233324459,5.02367474068799,-2.17662219639377));
#32171=CARTESIAN_POINT('Ctrl Pts',(-11.5055646883631,5.45222107279121,0.498274482060072));
#32172=CARTESIAN_POINT('Ctrl Pts',(-11.3663060442802,4.5459097805388,3.05117950197334));
#32173=CARTESIAN_POINT('Ctrl Pts',(-11.2270474001974,2.52663145170252,4.85706965086234));
#32174=CARTESIAN_POINT('Ctrl Pts',(-11.0877887561146,-0.111237578466964,
5.47381204346636));
#32175=CARTESIAN_POINT('Ctrl Pts',(-10.9485301120317,-2.72187250940446,
4.75041073262186));
#32176=CARTESIAN_POINT('Ctrl Pts',(-10.8092714679489,-4.66611621680294,
2.86397477945411));
#32177=CARTESIAN_POINT('Ctrl Pts',(-10.670012823866,-5.46796295882303,0.276356955764919));
#32178=CARTESIAN_POINT('Ctrl Pts',(-10.5307541797832,-4.9310980184238,-2.37892085172191));
#32179=CARTESIAN_POINT('Ctrl Pts',(-10.3914955357004,-3.18696108768182,
-4.45177168233753));
#32180=CARTESIAN_POINT('Ctrl Pts',(-10.2522368916175,-0.66256612088064,
-5.43470314014683));
#32181=CARTESIAN_POINT('Ctrl Pts',(-10.1129782475347,2.02404373528209,-5.08706585800951));
#32182=CARTESIAN_POINT('Ctrl Pts',(-9.97371960345187,4.2151105501779,-3.493971255726));
#32183=CARTESIAN_POINT('Ctrl Pts',(-9.83446095936903,5.37419931790948,-1.04545386193834));
#32184=CARTESIAN_POINT('Ctrl Pts',(-9.69520231528619,5.21753238928496,1.65902014840777));
#32185=CARTESIAN_POINT('Ctrl Pts',(-9.55594367120336,3.78346625083831,3.95731919546909));
#32186=CARTESIAN_POINT('Ctrl Pts',(-9.41668502712053,1.4231007741959,5.28675479595409));
#32187=CARTESIAN_POINT('Ctrl Pts',(-9.27742638303767,-1.28567994337311,
5.32184358744868));
#32188=CARTESIAN_POINT('Ctrl Pts',(-9.13816773895486,-3.67968991852724,
4.05399484330575));
#32189=CARTESIAN_POINT('Ctrl Pts',(-8.998909094872,-5.17280793104202,1.7936137250281));
#32190=CARTESIAN_POINT('Ctrl Pts',(-8.85965045078917,-5.39947654359819,
-0.905894663409331));
#32191=CARTESIAN_POINT('Ctrl Pts',(-8.72039180670633,-4.30420088142205,
-3.38361446657658));
#32192=CARTESIAN_POINT('Ctrl Pts',(-8.58113316262349,-2.15513534414405,
-5.03292993538373));
#32193=CARTESIAN_POINT('Ctrl Pts',(-8.44187451854065,0.52156816071472,-5.45004208605669));
#32194=CARTESIAN_POINT('Ctrl Pts',(-8.30261587445781,3.07057705696241,-4.53283008983534));
#32195=CARTESIAN_POINT('Ctrl Pts',(-8.16335723037499,4.86782201316885,-2.50585333452886));
#32196=CARTESIAN_POINT('Ctrl Pts',(-8.02409858629213,5.47328673127907,0.134627052500355));
#32197=CARTESIAN_POINT('Ctrl Pts',(-7.8848399422093,4.73873635719283,2.74214693681418));
#32198=CARTESIAN_POINT('Ctrl Pts',(-7.74558129812648,2.84400955743362,4.67831184545096));
#32199=CARTESIAN_POINT('Ctrl Pts',(-7.60632265404363,0.252988937083455,
5.46909395455718));
#32200=CARTESIAN_POINT('Ctrl Pts',(-7.46706400996079,-2.39997051645686,
4.92088748156248));
#32201=CARTESIAN_POINT('Ctrl Pts',(-7.32780536587795,-4.46534944100724,
3.16790884587246));
#32202=CARTESIAN_POINT('Ctrl Pts',(-7.18854672179511,-5.43748477415477,
0.639336700726373));
#32203=CARTESIAN_POINT('Ctrl Pts',(-7.04928807771227,-5.07837034483033,
-2.04576311600544));
#32204=CARTESIAN_POINT('Ctrl Pts',(-6.91002943362945,-3.47592750244373,
-4.23000237397282));
#32205=CARTESIAN_POINT('Ctrl Pts',(-6.7707707895466,-1.02247948869701,-5.37861764594346));
#32206=CARTESIAN_POINT('Ctrl Pts',(-6.63151214546376,1.68130036651628,-5.21039549013439));
#32207=CARTESIAN_POINT('Ctrl Pts',(-6.49225350138094,3.97345043212405,-3.76652143887618));
#32208=CARTESIAN_POINT('Ctrl Pts',(-6.35299485729809,5.29278766906849,-1.40049661771002));
#32209=CARTESIAN_POINT('Ctrl Pts',(-6.21373621321525,5.31630107938763,1.30840930880301));
#32210=CARTESIAN_POINT('Ctrl Pts',(-6.07447756913241,4.03823391649698,3.69697970263754));
#32211=CARTESIAN_POINT('Ctrl Pts',(-5.93521892504958,1.77149309925507,5.18042510662517));
#32212=CARTESIAN_POINT('Ctrl Pts',(-5.79596028096673,-0.928959234534617,
5.39555621105307));
#32213=CARTESIAN_POINT('Ctrl Pts',(-5.6567016368839,-3.40197612497396,4.28970284881921));
#32214=CARTESIAN_POINT('Ctrl Pts',(-5.51744299280106,-5.04209322876317,
2.13360913911639));
#32215=CARTESIAN_POINT('Ctrl Pts',(-5.37818434871823,-5.44776358153681,
-0.544852315532973));
#32216=CARTESIAN_POINT('Ctrl Pts',(-5.23892570463539,-4.51966762964043,
-3.08991854320483));
#32217=CARTESIAN_POINT('Ctrl Pts',(-5.09966706055256,-2.48502946046558,
-4.87848548903026));
#32218=CARTESIAN_POINT('Ctrl Pts',(-4.96040841646971,0.158014068243348,
-5.47266147685913));
#32219=CARTESIAN_POINT('Ctrl Pts',(-4.82114977238688,2.76237129261238,-4.72697545242317));
#32220=CARTESIAN_POINT('Ctrl Pts',(-4.68189112830404,4.69042204811024,-2.82399240378975));
#32221=CARTESIAN_POINT('Ctrl Pts',(-4.54263248422121,5.47012508461874,-0.229616298823035));
#32222=CARTESIAN_POINT('Ctrl Pts',(-4.40337384013836,4.91058708928048,2.42097635772262));
#32223=CARTESIAN_POINT('Ctrl Pts',(-4.26411519605553,3.14879875803774,4.47884566238253));
#32224=CARTESIAN_POINT('Ctrl Pts',(-4.12485655197269,0.616095606282331,
5.44016711967324));
#32225=CARTESIAN_POINT('Ctrl Pts',(-3.98559790788985,-2.06744514108811,
5.06958210059417));
#32226=CARTESIAN_POINT('Ctrl Pts',(-3.84633926380702,-4.24481695791071,
3.45782027871221));
#32227=CARTESIAN_POINT('Ctrl Pts',(-3.70708061972418,-5.38293776040373,
0.999486444981389));
#32228=CARTESIAN_POINT('Ctrl Pts',(-3.56782197564132,-5.20316344914374,
-1.70354988408383));
#32229=CARTESIAN_POINT('Ctrl Pts',(-3.4285633315585,-3.74950785022513,-3.98950911354476));
#32230=CARTESIAN_POINT('Ctrl Pts',(-3.28930468747566,-1.37786688814311,
-5.29872389589696));
#32231=CARTESIAN_POINT('Ctrl Pts',(-3.15004604339282,1.3311147826584,-5.31066149558737));
#32232=CARTESIAN_POINT('Ctrl Pts',(-3.01078739930999,3.71420197991916,-4.02239925165122));
#32233=CARTESIAN_POINT('Ctrl Pts',(-2.87152875522716,5.18794768756703,-1.7493401257652));
#32234=CARTESIAN_POINT('Ctrl Pts',(-2.73227011114431,5.39153735575714,0.952006842378526));
#32235=CARTESIAN_POINT('Ctrl Pts',(-2.59301146706148,4.27512648599062,3.42027566421813));
#32236=CARTESIAN_POINT('Ctrl Pts',(-2.45375282297864,2.11204397484455,5.05116445166812));
#32237=CARTESIAN_POINT('Ctrl Pts',(-2.3144941788958,-0.568126522254023,
5.44538560441941));
#32238=CARTESIAN_POINT('Ctrl Pts',(-2.17523553481295,-3.10920360575483,
4.50642263331263));
#32239=CARTESIAN_POINT('Ctrl Pts',(-2.03597689073012,-4.8890598871849,2.46416022338722));
#32240=CARTESIAN_POINT('Ctrl Pts',(-1.89671824664729,-5.47193628488737,
-0.181398225237268));
#32241=CARTESIAN_POINT('Ctrl Pts',(-1.75745960256445,-4.71512824620705,
-2.78254515563813));
#32242=CARTESIAN_POINT('Ctrl Pts',(-1.61820095848162,-2.80392365840489,
-4.70244670481565));
#32243=CARTESIAN_POINT('Ctrl Pts',(-1.47894231439878,-0.206239517764929,
-5.47105613283949));
#32244=CARTESIAN_POINT('Ctrl Pts',(-1.33968367031593,2.44193808947732,-4.90019741459951));
#32245=CARTESIAN_POINT('Ctrl Pts',(-1.2004250262331,4.4922599097877,-3.12963042226007));
#32246=CARTESIAN_POINT('Ctrl Pts',(-1.06116638215027,5.44275049879988,-0.592844726594321));
#32247=CARTESIAN_POINT('Ctrl Pts',(-0.92190773806742,5.06070056194062,2.089092271632));
#32248=CARTESIAN_POINT('Ctrl Pts',(-0.782649093984577,3.43965132709995,
4.25954845848455));
#32249=CARTESIAN_POINT('Ctrl Pts',(-0.643390449901751,0.976472396486427,
5.3871704534383));
#32250=CARTESIAN_POINT('Ctrl Pts',(-0.504131805818906,-1.72576292242332,
5.19581519094514));
#32251=CARTESIAN_POINT('Ctrl Pts',(-0.364873161736073,-4.00550542683706,
3.73246718521018));
#32252=CARTESIAN_POINT('Ctrl Pts',(-0.225614517653244,-5.30454291679212,
1.35513103364222));
#32253=CARTESIAN_POINT('Ctrl Pts',(-0.0863558735703945,-5.30496491583615,
-1.35363561368514));
#32254=CARTESIAN_POINT('Ctrl Pts',(0.0529027705124452,-4.00641227436962,
-3.73169439030285));
#32255=CARTESIAN_POINT('Ctrl Pts',(0.145741866567666,-2.48701521175681,
-4.70686214717463));
#32256=CARTESIAN_POINT('Ctrl Pts',(0.192161414595278,-1.65653546761383,
-4.98294756325496));
#32257=CARTESIAN_POINT('Ctrl Pts',(-59.7754114145953,-2.43856727558405,
5.02329722221654));
#32258=CARTESIAN_POINT('Ctrl Pts',(-59.7289918665677,-3.27577186963271,
4.61687497887677));
#32259=CARTESIAN_POINT('Ctrl Pts',(-59.6361527705125,-4.7421817453593,3.37773902727111));
#32260=CARTESIAN_POINT('Ctrl Pts',(-59.4968941264296,-5.7809011470696,0.690247673182852));
#32261=CARTESIAN_POINT('Ctrl Pts',(-59.3576354823468,-5.40421136209148,
-2.16547390737938));
#32262=CARTESIAN_POINT('Ctrl Pts',(-59.2183768382639,-3.70446136576718,
-4.49140083748381));
#32263=CARTESIAN_POINT('Ctrl Pts',(-59.0791181941811,-1.09773232127279,
-5.71751561060345));
#32264=CARTESIAN_POINT('Ctrl Pts',(-58.9398595500983,1.77774111756532,-5.54391865569175));
#32265=CARTESIAN_POINT('Ctrl Pts',(-58.8006009060154,4.21797922743172,-4.01296395592685));
#32266=CARTESIAN_POINT('Ctrl Pts',(-58.6613422619326,5.62553394302333,-1.49954801434181));
#32267=CARTESIAN_POINT('Ctrl Pts',(-58.5220836178498,5.65580069646275,1.38101274096256));
#32268=CARTESIAN_POINT('Ctrl Pts',(-58.3828249737669,4.3013669948914,3.92345586255738));
#32269=CARTESIAN_POINT('Ctrl Pts',(-58.2435663296841,1.89383763972005,5.50532968824863));
#32270=CARTESIAN_POINT('Ctrl Pts',(-58.1043076856012,-0.977356837237599,
5.73934163225416));
#32271=CARTESIAN_POINT('Ctrl Pts',(-57.9650490415184,-3.60926666480663,
4.56820164103017));
#32272=CARTESIAN_POINT('Ctrl Pts',(-57.8257903974356,-5.35752618487369,
2.2786364715673));
#32273=CARTESIAN_POINT('Ctrl Pts',(-57.6865317533527,-5.79411203415328,
-0.568802989310091));
#32274=CARTESIAN_POINT('Ctrl Pts',(-57.54727310927,-4.81213571518974,-3.2769835443839));
#32275=CARTESIAN_POINT('Ctrl Pts',(-57.408014465187,-2.65201272842086,-5.18286596219213));
#32276=CARTESIAN_POINT('Ctrl Pts',(-57.2687558211043,0.157397831715513,
-5.81983652221233));
#32277=CARTESIAN_POINT('Ctrl Pts',(-57.1294971770213,2.92827296154665,-5.03194680231615));
#32278=CARTESIAN_POINT('Ctrl Pts',(-56.9902385329385,4.98222420987256,-3.01209447145306));
#32279=CARTESIAN_POINT('Ctrl Pts',(-56.8509798888557,5.81638633350395,-0.254796384005554));
#32280=CARTESIAN_POINT('Ctrl Pts',(-56.7117212447728,5.2265328970099,2.56488304844114));
#32281=CARTESIAN_POINT('Ctrl Pts',(-56.5724626006901,3.35707667246942,4.75660671004105));
#32282=CARTESIAN_POINT('Ctrl Pts',(-56.4332039566071,0.665713314608688,
5.78377877856199));
#32283=CARTESIAN_POINT('Ctrl Pts',(-56.2939453125244,-2.18863545444221,
5.3949185374159));
#32284=CARTESIAN_POINT('Ctrl Pts',(-56.1546866684414,-4.50714448328554,
3.68522994996149));
#32285=CARTESIAN_POINT('Ctrl Pts',(-56.0154280243587,-5.72217731457325,
1.07329304386676));
#32286=CARTESIAN_POINT('Ctrl Pts',(-55.8761693802758,-5.53625961317535,
-1.80141629640945));
#32287=CARTESIAN_POINT('Ctrl Pts',(-55.7369107361931,-3.99490928048671,
-4.23508807677945));
#32288=CARTESIAN_POINT('Ctrl Pts',(-55.5976520921101,-1.47549238731475,
-5.63189074755655));
#32289=CARTESIAN_POINT('Ctrl Pts',(-55.4583934480274,1.40516669259064,-5.64984758586005));
#32290=CARTESIAN_POINT('Ctrl Pts',(-55.3191348039445,3.94180130099076,-4.28456225079436));
#32291=CARTESIAN_POINT('Ctrl Pts',(-55.1798761598616,5.51337168142342,-1.87029513176393));
#32292=CARTESIAN_POINT('Ctrl Pts',(-55.0406175157788,5.73511304234294,1.00187303036342));
#32293=CARTESIAN_POINT('Ctrl Pts',(-54.9013588716959,4.55273683926334,3.62875439370546));
#32294=CARTESIAN_POINT('Ctrl Pts',(-54.7621002276132,2.25572214290931,5.36721424869647));
#32295=CARTESIAN_POINT('Ctrl Pts',(-54.6228415835303,-0.593557008735543,
5.79162854944988));
#32296=CARTESIAN_POINT('Ctrl Pts',(-54.4835829394474,-3.2975166496668,4.79808869474004));
#32297=CARTESIAN_POINT('Ctrl Pts',(-54.3443242953646,-5.19415113219364,
2.62984128672311));
#32298=CARTESIAN_POINT('Ctrl Pts',(-54.2050656512818,-5.81911079664231,
-0.182265503655628));
#32299=CARTESIAN_POINT('Ctrl Pts',(-54.065807007199,-5.01938787574395,-2.94974855373413));
#32300=CARTESIAN_POINT('Ctrl Pts',(-53.9265483631161,-2.9907771151776,-4.99504989211838));
#32301=CARTESIAN_POINT('Ctrl Pts',(-53.7872897190333,-0.229939692918102,
-5.81742201624076));
#32302=CARTESIAN_POINT('Ctrl Pts',(-53.6480310749504,2.58719345692394,-5.21552501612943));
#32303=CARTESIAN_POINT('Ctrl Pts',(-53.5087724308677,4.7709086170054,-3.33672026780873));
#32304=CARTESIAN_POINT('Ctrl Pts',(-53.3695137867847,5.78657067405063,-0.640992208719566));
#32305=CARTESIAN_POINT('Ctrl Pts',(-53.230255142702,5.38551688630448,2.21166883704392));
#32306=CARTESIAN_POINT('Ctrl Pts',(-53.0909964986191,3.66593654198589,4.52285092033272));
#32307=CARTESIAN_POINT('Ctrl Pts',(-52.9517378545363,1.04883144983671,5.72671142692343));
#32308=CARTESIAN_POINT('Ctrl Pts',(-52.8124792104535,-1.82505718773126,
5.52851132213115));
#32309=CARTESIAN_POINT('Ctrl Pts',(-52.6732205663706,-4.2521203078811,3.97677558641761));
#32310=CARTESIAN_POINT('Ctrl Pts',(-52.5339619222877,-5.63814434746659,
1.45141293040697));
#32311=CARTESIAN_POINT('Ctrl Pts',(-52.3947032782049,-5.64379149679879,
-1.42929658156861));
#32312=CARTESIAN_POINT('Ctrl Pts',(-52.255444634122,-4.26767917431298,-3.96007394407695));
#32313=CARTESIAN_POINT('Ctrl Pts',(-52.1161859900392,-1.84671852156337,
-5.52131341978852));
#32314=CARTESIAN_POINT('Ctrl Pts',(-51.9769273459564,1.02637095458436,-5.73077951425524));
#32315=CARTESIAN_POINT('Ctrl Pts',(-51.8376687018736,3.64817584856774,-4.53718901472586));
#32316=CARTESIAN_POINT('Ctrl Pts',(-51.6984100577907,5.3768043138196,-2.23276656825405));
#32317=CARTESIAN_POINT('Ctrl Pts',(-51.5591514137078,5.78903930618248,0.618300160841148));
#32318=CARTESIAN_POINT('Ctrl Pts',(-51.4198927696251,4.78395406292337,3.3179895571356));
#32319=CARTESIAN_POINT('Ctrl Pts',(-51.2806341255421,2.60762182321943,5.20534144936639));
#32320=CARTESIAN_POINT('Ctrl Pts',(-51.1413754814594,-0.207129846967831,
5.81827881799394));
#32321=CARTESIAN_POINT('Ctrl Pts',(-51.0021168373764,-2.97117028373933,
5.00673729313276));
#32322=CARTESIAN_POINT('Ctrl Pts',(-50.8628581932937,-5.00778436461698,
2.96940514832847));
#32323=CARTESIAN_POINT('Ctrl Pts',(-50.7235995492108,-5.81835147289538,
0.205078802605319));
#32324=CARTESIAN_POINT('Ctrl Pts',(-50.584340905128,-5.20442189971427,-2.60945662297661));
#32325=CARTESIAN_POINT('Ctrl Pts',(-50.4450822610452,-3.31630293464185,
-4.78512340730182));
#32326=CARTESIAN_POINT('Ctrl Pts',(-50.3058236169624,-0.616259398302359,
-5.78925690666997));
#32327=CARTESIAN_POINT('Ctrl Pts',(-50.1665649728795,2.23466183456155,-5.37601689567433));
#32328=CARTESIAN_POINT('Ctrl Pts',(-50.0273063287967,4.53847477011026,-3.64657619397903));
#32329=CARTESIAN_POINT('Ctrl Pts',(-49.8880476847138,5.73114096950406,-1.02435070415067));
#32330=CARTESIAN_POINT('Ctrl Pts',(-49.748789040631,5.52066208045366,1.84866475350808));
#32331=CARTESIAN_POINT('Ctrl Pts',(-49.6095303965482,3.95856927641364,4.26907489525025));
#32332=CARTESIAN_POINT('Ctrl Pts',(-49.4702717524652,1.42730697069471,5.64429499484464));
#32333=CARTESIAN_POINT('Ctrl Pts',(-49.3310131083825,-1.45340037158661,
5.63763235208663));
#32334=CARTESIAN_POINT('Ctrl Pts',(-49.1917544642997,-3.97827427620059,
4.250718169997));
#32335=CARTESIAN_POINT('Ctrl Pts',(-49.0524958202168,-5.52915433895347,
1.8231081902767));
#32336=CARTESIAN_POINT('Ctrl Pts',(-48.913237176134,-5.72634134211583,-1.05085013726839));
#32337=CARTESIAN_POINT('Ctrl Pts',(-48.7739785320511,-4.5215583411029,-3.66753068772775));
#32338=CARTESIAN_POINT('Ctrl Pts',(-48.6347198879683,-2.20977022327436,
-5.38629619847924));
#32339=CARTESIAN_POINT('Ctrl Pts',(-48.4954612438854,0.643032022783838,
-5.7863443550394));
#32340=CARTESIAN_POINT('Ctrl Pts',(-48.3562025998026,3.33840187810475,-4.76973207609072));
#32341=CARTESIAN_POINT('Ctrl Pts',(-48.2169439557197,5.21643671698811,-2.58535474453319));
#32342=CARTESIAN_POINT('Ctrl Pts',(-48.0776853116369,5.81734059755632,0.231990408088362));
#32343=CARTESIAN_POINT('Ctrl Pts',(-47.9384266675541,4.99399528748307,2.99253776016594));
#32344=CARTESIAN_POINT('Ctrl Pts',(-47.7991680234712,2.9479789601321,5.02042739495756));
#32345=CARTESIAN_POINT('Ctrl Pts',(-47.6599093793884,0.18021416755293,5.81917468643407));
#32346=CARTESIAN_POINT('Ctrl Pts',(-47.5206507353056,-2.63167214034327,
5.19322375053906));
#32347=CARTESIAN_POINT('Ctrl Pts',(-47.3813920912227,-4.79925082122997,
3.29582504577313));
#32348=CARTESIAN_POINT('Ctrl Pts',(-47.2421334471399,-5.79183742744024,
0.591515334986651));
#32349=CARTESIAN_POINT('Ctrl Pts',(-47.1028748030571,-5.36641873895901,
-2.25761402714712));
#32350=CARTESIAN_POINT('Ctrl Pts',(-46.9636161589742,-3.62714925947957,
-4.55401574732442));
#32351=CARTESIAN_POINT('Ctrl Pts',(-46.8243575148914,-0.999851253817615,
-5.73546586143282));
#32352=CARTESIAN_POINT('Ctrl Pts',(-46.6850988708086,1.87223856266074,-5.51271203146944));
#32353=CARTESIAN_POINT('Ctrl Pts',(-46.5458402267257,4.28595152929855,-3.94029068292243));
#32354=CARTESIAN_POINT('Ctrl Pts',(-46.4065815826429,5.65034257737858,-1.40317494835275));
#32355=CARTESIAN_POINT('Ctrl Pts',(-46.26732293856,5.63137026419025,1.47747762250932));
#32356=CARTESIAN_POINT('Ctrl Pts',(-46.1280642944772,4.23367954755404,3.9964019650236));
#32357=CARTESIAN_POINT('Ctrl Pts',(-45.9888056503944,1.79946456902883,5.53689429574304));
#32358=CARTESIAN_POINT('Ctrl Pts',(-45.8495470063115,-1.07531013142566,
5.72179860696575));
#32359=CARTESIAN_POINT('Ctrl Pts',(-45.7102883622287,-3.68681855776603,
4.50584510381061));
#32360=CARTESIAN_POINT('Ctrl Pts',(-45.5710297181458,-5.39568972935361,
2.18673352788352));
#32361=CARTESIAN_POINT('Ctrl Pts',(-45.431771074063,-5.78354374523047,-0.667752142959872));
#32362=CARTESIAN_POINT('Ctrl Pts',(-45.2925124299802,-4.7554229939355,-3.35875323984533));
#32363=CARTESIAN_POINT('Ctrl Pts',(-45.1532537858973,-2.56304045726125,
-5.22743673245922));
#32364=CARTESIAN_POINT('Ctrl Pts',(-45.0139951418145,0.256846733063343,
-5.81629615246135));
#32365=CARTESIAN_POINT('Ctrl Pts',(-44.8747364977317,3.01385059284374,-4.98116209146394));
#32366=CARTESIAN_POINT('Ctrl Pts',(-44.7354778536488,5.03297875227833,-2.92649894183081));
#32367=CARTESIAN_POINT('Ctrl Pts',(-44.596219209566,5.81989164182494,-0.155346241789309));
#32368=CARTESIAN_POINT('Ctrl Pts',(-44.4569605654831,5.18193077308208,2.65383960336846));
#32369=CARTESIAN_POINT('Ctrl Pts',(-44.3177019214003,3.27528697512884,4.81329060082324));
#32370=CARTESIAN_POINT('Ctrl Pts',(-44.1784432773175,0.566760470599109,
5.79431218924112));
#32371=CARTESIAN_POINT('Ctrl Pts',(-44.0391846332346,-2.28052499569356,
5.35672259142087));
#32372=CARTESIAN_POINT('Ctrl Pts',(-43.8999259891518,-4.5694735681969,3.60765609322339));
#32373=CARTESIAN_POINT('Ctrl Pts',(-43.7606673450689,-5.73968602373716,
0.975333546197558));
#32374=CARTESIAN_POINT('Ctrl Pts',(-43.6214087009861,-5.50466132034644,
-1.89577818473146));
#32375=CARTESIAN_POINT('Ctrl Pts',(-43.4821500569033,-3.92194013971112,
-4.30274990185865));
#32376=CARTESIAN_POINT('Ctrl Pts',(-43.3428914128205,-1.37901730403188,
-5.65628698463953));
#32377=CARTESIAN_POINT('Ctrl Pts',(-43.2036327687376,1.50152789468607,-5.62500534745538));
#32378=CARTESIAN_POINT('Ctrl Pts',(-43.0643741246547,4.01445667953435,-4.21656361810942));
#32379=CARTESIAN_POINT('Ctrl Pts',(-42.925115480572,5.54453314882563,-1.7757880895523));
#32380=CARTESIAN_POINT('Ctrl Pts',(-42.785856836489,5.71715139175535,1.09975049041664));
#32381=CARTESIAN_POINT('Ctrl Pts',(-42.6465981924063,4.49004958977272,3.70603910648602));
#32382=CARTESIAN_POINT('Ctrl Pts',(-42.5073395483234,2.1636569027317,5.40498473491679));
#32383=CARTESIAN_POINT('Ctrl Pts',(-42.3680809042406,-0.692460069979665,
5.7806375278948));
#32384=CARTESIAN_POINT('Ctrl Pts',(-42.2288222601578,-3.37904327074129,
4.7410270777417));
#32385=CARTESIAN_POINT('Ctrl Pts',(-42.0895636160749,-5.23834129491938,
2.54067936886263));
#32386=CARTESIAN_POINT('Ctrl Pts',(-41.9503049719921,-5.81514550178058,
-0.281698368016173));
#32387=CARTESIAN_POINT('Ctrl Pts',(-41.8110463279093,-4.96823793940958,
-3.03510839260038));
#32388=CARTESIAN_POINT('Ctrl Pts',(-41.6717876838263,-2.90496548564975,
-5.04543820739147));
#32389=CARTESIAN_POINT('Ctrl Pts',(-41.5325290397437,-0.13047547940279,
-5.8205023259764));
#32390=CARTESIAN_POINT('Ctrl Pts',(-41.3932703956606,2.67595860727431,-5.17054317355309));
#32391=CARTESIAN_POINT('Ctrl Pts',(-41.2540117515779,4.82724248971522,-3.2546890977342));
#32392=CARTESIAN_POINT('Ctrl Pts',(-41.1147531074951,5.79668114688347,-0.541995257163577));
#32393=CARTESIAN_POINT('Ctrl Pts',(-40.9754944634122,5.34692863011159,2.30339432184656));
#32394=CARTESIAN_POINT('Ctrl Pts',(-40.8362358193294,3.58809705115569,4.58484795046792));
#32395=CARTESIAN_POINT('Ctrl Pts',(-40.6969771752465,0.950798028983867,
5.7438013793569));
#32396=CARTESIAN_POINT('Ctrl Pts',(-40.5577185311637,-1.91928318988664,
5.49651009409065));
#32397=CARTESIAN_POINT('Ctrl Pts',(-40.4184598870809,-4.31946970619222,
3.90351798186069));
#32398=CARTESIAN_POINT('Ctrl Pts',(-40.279201242998,-5.66212810808261,1.35483447885073));
#32399=CARTESIAN_POINT('Ctrl Pts',(-40.1399425989152,-5.6185377181054,-1.52555074895882));
#32400=CARTESIAN_POINT('Ctrl Pts',(-40.0006839548323,-4.19937069420006,
-4.03243809005368));
#32401=CARTESIAN_POINT('Ctrl Pts',(-39.8614253107495,-1.75207918417979,
-5.55207075871569));
#32402=CARTESIAN_POINT('Ctrl Pts',(-39.7221666666667,1.12417076796024,-5.71239978134284));
#32403=CARTESIAN_POINT('Ctrl Pts',(-39.5829080225839,3.72519198292045,-4.4741720874154));
#32404=CARTESIAN_POINT('Ctrl Pts',(-39.443649378501,5.41418104544193,-2.14054076919809));
#32405=CARTESIAN_POINT('Ctrl Pts',(-39.3043907344182,5.77762575609995,0.717155352676428));
#32406=CARTESIAN_POINT('Ctrl Pts',(-39.1651320903353,4.72654459037877,3.39927160029664));
#32407=CARTESIAN_POINT('Ctrl Pts',(-39.0258734462525,2.51827188765085,5.24915020525126));
#32408=CARTESIAN_POINT('Ctrl Pts',(-38.8866148021696,-0.306544859155955,
5.81388866652493));
#32409=CARTESIAN_POINT('Ctrl Pts',(-38.7473561580868,-3.05631077126836,
4.95522306731501));
#32410=CARTESIAN_POINT('Ctrl Pts',(-38.608097514004,-5.05780553278731,2.88337898478993));
#32411=CARTESIAN_POINT('Ctrl Pts',(-38.4688388699212,-5.8210067277373,0.105602334533653));
#32412=CARTESIAN_POINT('Ctrl Pts',(-38.3295802258383,-5.15906115988973,
-2.69802874816768));
#32413=CARTESIAN_POINT('Ctrl Pts',(-38.1903215817555,-3.23403178970654,
-4.84110623314438));
#32414=CARTESIAN_POINT('Ctrl Pts',(-38.0510629376726,-0.517220146892966,
-5.79894425711007));
#32415=CARTESIAN_POINT('Ctrl Pts',(-37.9118042935898,2.32622158801205,-5.33703703386896));
#32416=CARTESIAN_POINT('Ctrl Pts',(-37.7725456495069,4.60013861340107,-3.56847249042477));
#32417=CARTESIAN_POINT('Ctrl Pts',(-37.6332870054241,5.74781185314564,-0.926245150195311));
#32418=CARTESIAN_POINT('Ctrl Pts',(-37.4940283613413,5.48825850154353,1.9427531489248));
#32419=CARTESIAN_POINT('Ctrl Pts',(-37.3547697172584,3.88502454575981,4.33611063699552));
#32420=CARTESIAN_POINT('Ctrl Pts',(-37.2155110731756,1.33062691438782,5.66786584104888));
#32421=CARTESIAN_POINT('Ctrl Pts',(-37.0762524290928,-1.54954574667018,
5.61196749423928));
#32422=CARTESIAN_POINT('Ctrl Pts',(-36.9369937850099,-4.05034586824098,
4.18210108976877));
#32423=CARTESIAN_POINT('Ctrl Pts',(-36.7977351409272,-5.55950698777649,
1.72833828583595));
#32424=CARTESIAN_POINT('Ctrl Pts',(-36.6584764968442,-5.70754386249259,
-1.1485705181421));
#32425=CARTESIAN_POINT('Ctrl Pts',(-36.5192178527615,-4.4582128866619,-3.74427683733772));
#32426=CARTESIAN_POINT('Ctrl Pts',(-36.3799592086786,-2.11738554938339,
-5.42327849300442));
#32427=CARTESIAN_POINT('Ctrl Pts',(-36.2407005645957,0.741837540114254,
-5.77450848484087));
#32428=CARTESIAN_POINT('Ctrl Pts',(-36.1014419205129,3.41943785914202,-4.71197579629695));
#32429=CARTESIAN_POINT('Ctrl Pts',(-35.96218327643,5.25986326608409,-2.49581842278662));
#32430=CARTESIAN_POINT('Ctrl Pts',(-35.8229246323472,5.81252566964419,0.331385752785651));
#32431=CARTESIAN_POINT('Ctrl Pts',(-35.6836659882644,4.94211771283189,3.0774573416922));
#32432=CARTESIAN_POINT('Ctrl Pts',(-35.5444073441815,2.86173983342087,5.07008050263841));
#32433=CARTESIAN_POINT('Ctrl Pts',(-35.4051487000987,0.0807272613655634,
5.82140483789733));
#32434=CARTESIAN_POINT('Ctrl Pts',(-35.2658900560158,-2.72004962304768,
5.1474849417536));
#32435=CARTESIAN_POINT('Ctrl Pts',(-35.126631411933,-4.85488157795867,3.21331542824843));
#32436=CARTESIAN_POINT('Ctrl Pts',(-34.9873727678502,-5.80110147859658,
0.492435592180922));
#32437=CARTESIAN_POINT('Ctrl Pts',(-34.8481141237674,-5.32704798331352,
-2.34900637736412));
#32438=CARTESIAN_POINT('Ctrl Pts',(-34.7088554796845,-3.5487827693751,-4.61534527778891));
#32439=CARTESIAN_POINT('Ctrl Pts',(-34.5695968356017,-0.901675358167371,
-5.75171737187212));
#32440=CARTESIAN_POINT('Ctrl Pts',(-34.4303381915188,1.96618763328446,-5.47990669337911));
#32441=CARTESIAN_POINT('Ctrl Pts',(-34.2910795474361,4.35267239040516,-3.86646016909869));
#32442=CARTESIAN_POINT('Ctrl Pts',(-34.1518209033531,5.6735000787673,-1.30639505267333));
#32443=CARTESIAN_POINT('Ctrl Pts',(-34.0125622592703,5.60529479582931,1.57351244967139));
#32444=CARTESIAN_POINT('Ctrl Pts',(-33.8733036151875,4.16475512015862,4.06817968710017));
#32445=CARTESIAN_POINT('Ctrl Pts',(-33.7340449711046,1.70456582802962,5.56684170022245));
#32446=CARTESIAN_POINT('Ctrl Pts',(-33.5947863270218,-1.17294929542274,
5.7025837238737));
#32447=CARTESIAN_POINT('Ctrl Pts',(-33.455527682939,-3.76329332124829,4.44217227892728));
#32448=CARTESIAN_POINT('Ctrl Pts',(-33.3162690388561,-5.43227691148481,
2.09419166610201));
#32449=CARTESIAN_POINT('Ctrl Pts',(-33.1770103947733,-5.77128577103893,
-0.766506181596307));
#32450=CARTESIAN_POINT('Ctrl Pts',(-33.0377517506904,-4.69732096152246,
-3.4395416790415));
#32451=CARTESIAN_POINT('Ctrl Pts',(-32.8984931066076,-2.47331938427025,
-5.27048028179739));
#32452=CARTESIAN_POINT('Ctrl Pts',(-32.7592344625248,0.356220595310421,
-5.8110565360267));
#32453=CARTESIAN_POINT('Ctrl Pts',(-32.619975818442,3.09854771773538,-4.92892211526402));
#32454=CARTESIAN_POINT('Ctrl Pts',(-32.4807171743591,5.08226289280382,-2.84004842667364));
#32455=CARTESIAN_POINT('Ctrl Pts',(-32.3414585302763,5.82169664918694,-0.0558507141174293));
#32456=CARTESIAN_POINT('Ctrl Pts',(-32.2021998861934,5.13581473052646,2.74202082981319));
#32457=CARTESIAN_POINT('Ctrl Pts',(-32.0629412421106,3.19254039164058,4.86856827262033));
#32458=CARTESIAN_POINT('Ctrl Pts',(-31.9236825980277,0.467642045593386,
5.80315277195208));
#32459=CARTESIAN_POINT('Ctrl Pts',(-31.784423953945,-2.37174827385247,5.3169616608454));
#32460=CARTESIAN_POINT('Ctrl Pts',(-31.6451653098621,-4.63046766595764,
3.52902824754106));
#32461=CARTESIAN_POINT('Ctrl Pts',(-31.5059066657793,-5.75551786422157,
0.877089101544608));
#32462=CARTESIAN_POINT('Ctrl Pts',(-31.3666480216964,-5.47145482210148,
-1.98958621505185));
#32463=CARTESIAN_POINT('Ctrl Pts',(-31.2273893776136,-3.84782519086287,
-4.36915466400344));
#32464=CARTESIAN_POINT('Ctrl Pts',(-31.0881307335308,-1.28213933618114,
-5.6790307183567));
#32465=CARTESIAN_POINT('Ctrl Pts',(-30.9488720894479,1.59745042033037,-5.59851974471898));
#32466=CARTESIAN_POINT('Ctrl Pts',(-30.8096134453651,4.08593922098567,-4.14733310210707));
#32467=CARTESIAN_POINT('Ctrl Pts',(-30.6703548012822,5.57407476212171,-1.68076224484598));
#32468=CARTESIAN_POINT('Ctrl Pts',(-30.5310961571994,5.69751945605833,1.19730665464562));
#32469=CARTESIAN_POINT('Ctrl Pts',(-30.3918375131165,4.42605055711307,3.78224108741116));
#32470=CARTESIAN_POINT('Ctrl Pts',(-30.2525788690338,2.07095954287434,5.4411761365719));
#32471=CARTESIAN_POINT('Ctrl Pts',(-30.1133202249508,-0.79116082667304,
5.76795767354096));
#32472=CARTESIAN_POINT('Ctrl Pts',(-29.9740615808681,-3.45958269289924,
4.68258035365267));
#32473=CARTESIAN_POINT('Ctrl Pts',(-29.8348029367852,-5.28100105852438,
2.45077518293425));
#32474=CARTESIAN_POINT('Ctrl Pts',(-29.6955442927024,-5.80948129249884,
-0.381048933246069));
#32475=CARTESIAN_POINT('Ctrl Pts',(-29.5562856486195,-4.91563651556301,
-3.11958151428768));
#32476=CARTESIAN_POINT('Ctrl Pts',(-29.4170270045367,-2.81830516063327,
-5.09435248083305));
#32477=CARTESIAN_POINT('Ctrl Pts',(-29.2777683604539,-0.0309731470350815,
-5.8218821562777));
#32478=CARTESIAN_POINT('Ctrl Pts',(-29.138509716371,2.76394196726982,-5.12405073930642));
#32479=CARTESIAN_POINT('Ctrl Pts',(-28.9992510722882,4.88216606721023,-3.17170705923528));
#32480=CARTESIAN_POINT('Ctrl Pts',(-28.8599924282053,5.80509809971998,-0.442839959860642));
#32481=CARTESIAN_POINT('Ctrl Pts',(-28.7207337841225,5.30677825064084,2.39444686220999));
#32482=CARTESIAN_POINT('Ctrl Pts',(-28.5814751400397,3.50920928564028,4.64550550177244));
#32483=CARTESIAN_POINT('Ctrl Pts',(-28.4422164959568,0.852486829272148,
5.75921326079695));
#32484=CARTESIAN_POINT('Ctrl Pts',(-28.302957851874,-2.01294846696878,5.46290304204184));
#32485=CARTESIAN_POINT('Ctrl Pts',(-28.1636992077911,-4.38555715682404,
3.82911995132712));
#32486=CARTESIAN_POINT('Ctrl Pts',(-28.0244405637083,-5.68445765882755,
1.25786020782067));
#32487=CARTESIAN_POINT('Ctrl Pts',(-27.8851819196254,-5.59164246462076,
-1.62135922153972));
#32488=CARTESIAN_POINT('Ctrl Pts',(-27.7459232755427,-4.12983535374023,
-4.10362414560827));
#32489=CARTESIAN_POINT('Ctrl Pts',(-27.6066646314598,-1.65692797093859,
-5.58120604139851));
#32490=CARTESIAN_POINT('Ctrl Pts',(-27.467405987377,1.22164215104524,-5.69235115152004));
#32491=CARTESIAN_POINT('Ctrl Pts',(-27.3281473432941,3.80111978984003,-4.40984801560195));
#32492=CARTESIAN_POINT('Ctrl Pts',(-27.1888886992113,5.44997600576591,-2.04768960391896));
#32493=CARTESIAN_POINT('Ctrl Pts',(-27.0496300551284,5.76452425311795,0.815801025150685));
#32494=CARTESIAN_POINT('Ctrl Pts',(-26.9103714110456,4.66775424185108,3.4795605347663));
#32495=CARTESIAN_POINT('Ctrl Pts',(-26.7711127669628,2.42818623043581,5.29142540415567));
#32496=CARTESIAN_POINT('Ctrl Pts',(-26.6318541228799,-0.405870313226985,
5.80779996782456));
#32497=CARTESIAN_POINT('Ctrl Pts',(-26.4925954787971,-3.14055834727186,
4.902261156324));
#32498=CARTESIAN_POINT('Ctrl Pts',(-26.3533368347143,-5.10634904597018,
2.79651043233193));
#32499=CARTESIAN_POINT('Ctrl Pts',(-26.2140781906314,-5.82196135578221,
0.00609501438297373));
#32500=CARTESIAN_POINT('Ctrl Pts',(-26.0748195465486,-5.11219318290401,
-2.78581263513747));
#32501=CARTESIAN_POINT('Ctrl Pts',(-25.9355609024658,-3.15081581144937,
-4.89567471343253));
#32502=CARTESIAN_POINT('Ctrl Pts',(-25.7963022583829,-0.418029787868941,
-5.80693742637859));
#32503=CARTESIAN_POINT('Ctrl Pts',(-25.6570436143001,2.41710172796037,-5.29649793864898));
#32504=CARTESIAN_POINT('Ctrl Pts',(-25.5177849702173,4.66045851064236,-3.48932624556705));
#32505=CARTESIAN_POINT('Ctrl Pts',(-25.3785263261344,5.76280349412033,-0.827868990587574));
#32506=CARTESIAN_POINT('Ctrl Pts',(-25.2392676820516,5.45425150935574,2.03627396244039));
#32507=CARTESIAN_POINT('Ctrl Pts',(-25.1000090379688,3.81034479204925,4.40187956935728));
#32508=CARTESIAN_POINT('Ctrl Pts',(-24.9607503938859,1.23355811092897,5.68978080108393));
#32509=CARTESIAN_POINT('Ctrl Pts',(-24.8214917498031,-1.64523841672459,
5.58466308111381));
#32510=CARTESIAN_POINT('Ctrl Pts',(-24.6822331057202,-4.12123413804123,
4.11226219456705));
#32511=CARTESIAN_POINT('Ctrl Pts',(-24.5429744616374,-5.58823540783568,
1.63306344152135));
#32512=CARTESIAN_POINT('Ctrl Pts',(-24.4037158175545,-5.68707890463208,
-1.24595534025541));
#32513=CARTESIAN_POINT('Ctrl Pts',(-24.2644571734717,-4.39356495025238,
-3.81992908380977));
#32514=CARTESIAN_POINT('Ctrl Pts',(-24.1251985293889,-2.02438227414509,
-5.45867635838113));
#32515=CARTESIAN_POINT('Ctrl Pts',(-23.985939885306,0.840426327098998,-5.7609855724642));
#32516=CARTESIAN_POINT('Ctrl Pts',(-23.8466812412232,3.49947483984709,-4.65284289684264));
#32517=CARTESIAN_POINT('Ctrl Pts',(-23.7074225971403,5.30175312834262,-2.40555293924936));
#32518=CARTESIAN_POINT('Ctrl Pts',(-23.5681639530575,5.80601259270488,0.430684282014642));
#32519=CARTESIAN_POINT('Ctrl Pts',(-23.4289053089747,4.88879628178109,3.1614778336508));
#32520=CARTESIAN_POINT('Ctrl Pts',(-23.2896466648918,2.77466463974149,5.11825236915787));
#32521=CARTESIAN_POINT('Ctrl Pts',(-23.150388020809,-0.0187832295640885,
5.82193424625433));
#32522=CARTESIAN_POINT('Ctrl Pts',(-23.0111293767262,-2.80763243405787,
5.10024227783821));
#32523=CARTESIAN_POINT('Ctrl Pts',(-22.8718707326433,-4.90909396461944,
3.12986702975682));
#32524=CARTESIAN_POINT('Ctrl Pts',(-22.7326120885605,-5.80867071834175,
0.393211982651999));
#32525=CARTESIAN_POINT('Ctrl Pts',(-22.5933534444777,-5.28612091258838,
-2.43971245742563));
#32526=CARTESIAN_POINT('Ctrl Pts',(-22.4540948003948,-3.46937949038583,
-4.67532641952538));
#32527=CARTESIAN_POINT('Ctrl Pts',(-22.314836156312,-0.803236035012722,
-5.76628849863402));
#32528=CARTESIAN_POINT('Ctrl Pts',(-22.1755775122291,2.05956227554316,-5.44550038202015));
#32529=CARTESIAN_POINT('Ctrl Pts',(-22.0363188681463,4.41812160355599,-3.79150005586361));
#32530=CARTESIAN_POINT('Ctrl Pts',(-21.8970602240635,5.69500004792524,-1.20923348926227));
#32531=CARTESIAN_POINT('Ctrl Pts',(-21.7578015799806,5.57758172164165,1.66908756985091));
#32532=CARTESIAN_POINT('Ctrl Pts',(-21.6185429358978,4.09461394547347,4.13876887672602));
#32533=CARTESIAN_POINT('Ctrl Pts',(-21.4792842918149,1.60916909236062,5.59516273307697));
#32534=CARTESIAN_POINT('Ctrl Pts',(-21.3400256477321,-1.27024577831713,
5.68170281166567));
#32535=CARTESIAN_POINT('Ctrl Pts',(-21.2007670036493,-3.83866862586252,
4.37720165839326));
#32536=CARTESIAN_POINT('Ctrl Pts',(-21.0615083595664,-5.4672770355491,2.00103797914468));
#32537=CARTESIAN_POINT('Ctrl Pts',(-20.9222497154836,-5.75734169619605,
-0.865036282859993));
#32538=CARTESIAN_POINT('Ctrl Pts',(-20.7829910714007,-4.63784659090838,
-3.51932524450664));
#32539=CARTESIAN_POINT('Ctrl Pts',(-20.6437324273179,-2.38287572265856,
-5.3119840425011));
#32540=CARTESIAN_POINT('Ctrl Pts',(-20.5044737832351,0.455490386506136,
-5.8041191997772));
#32541=CARTESIAN_POINT('Ctrl Pts',(-20.3652151391522,3.18233959143471,-4.8752421378029));
#32542=CARTESIAN_POINT('Ctrl Pts',(-20.2259564950694,5.1300622330414,-2.75276818176615));
#32543=CARTESIAN_POINT('Ctrl Pts',(-20.0866978509866,5.82180082818906,0.0436611305292647));
#32544=CARTESIAN_POINT('Ctrl Pts',(-19.9474392069038,5.08819824233262,2.82940096560128));
#32545=CARTESIAN_POINT('Ctrl Pts',(-19.8081805628209,3.10886109668263,4.92242357573535));
#32546=CARTESIAN_POINT('Ctrl Pts',(-19.6689219187381,0.368386997382966,
5.81029794395959));
#32547=CARTESIAN_POINT('Ctrl Pts',(-19.5296632746552,-2.46227863773393,
5.27564736194346));
#32548=CARTESIAN_POINT('Ctrl Pts',(-19.3904046305724,-4.69010895693356,
3.44936938432428));
#32549=CARTESIAN_POINT('Ctrl Pts',(-19.2511459864896,-5.76966821070186,
0.778588412345258));
#32550=CARTESIAN_POINT('Ctrl Pts',(-19.1118873424067,-5.43664981983068,
-2.08281298103237));
#32551=CARTESIAN_POINT('Ctrl Pts',(-18.9726286983239,-3.77258608687527,
-4.43428296284045));
#32552=CARTESIAN_POINT('Ctrl Pts',(-18.8333700542411,-1.18488678698841,
-5.70011530404799));
#32553=CARTESIAN_POINT('Ctrl Pts',(-18.6941114101582,1.69290624543302,-5.57039851550999));
#32554=CARTESIAN_POINT('Ctrl Pts',(-18.5548527660754,4.15622804147844,-4.07689092871645));
#32555=CARTESIAN_POINT('Ctrl Pts',(-18.4155941219925,5.60198789062944,-1.58524535976706));
#32556=CARTESIAN_POINT('Ctrl Pts',(-18.2763354779097,5.67622297078826,1.29451302168715));
#32557=CARTESIAN_POINT('Ctrl Pts',(-18.1370768338268,4.36075843881821,3.85733807381434));
#32558=CARTESIAN_POINT('Ctrl Pts',(-17.997818189744,1.97765714518448,5.47577788022147));
#32559=CARTESIAN_POINT('Ctrl Pts',(-17.8585595456612,-0.889630443055851,
5.75359269085066));
#32560=CARTESIAN_POINT('Ctrl Pts',(-17.7193009015783,-3.53911138627618,
4.62276559788101));
#32561=CARTESIAN_POINT('Ctrl Pts',(-17.5800422574955,-5.32211795981442,
2.36015499474989));
#32562=CARTESIAN_POINT('Ctrl Pts',(-17.4407836134127,-5.80211982361497,
-0.480288173741599));
#32563=CARTESIAN_POINT('Ctrl Pts',(-17.3015249693298,-4.86159897188818,
-3.20314323968782));
#32564=CARTESIAN_POINT('Ctrl Pts',(-17.162266325247,-2.73082145823515,-5.14177842197275));
#32565=CARTESIAN_POINT('Ctrl Pts',(-17.0230076811641,0.0685382342422849,
-5.82156110402261));
#32566=CARTESIAN_POINT('Ctrl Pts',(-16.8837490370813,2.85111783227435,-5.07606129631125));
#32567=CARTESIAN_POINT('Ctrl Pts',(-16.7444903929985,4.93566330338145,-3.08779839579521));
#32568=CARTESIAN_POINT('Ctrl Pts',(-16.6052317489156,5.81181907351895,-0.343555285366334));
#32569=CARTESIAN_POINT('Ctrl Pts',(-16.4659731048328,5.26507747796142,2.48479985682658));
#32570=CARTESIAN_POINT('Ctrl Pts',(-16.32671446075,3.42929629276711,4.7048058529376));
#32571=CARTESIAN_POINT('Ctrl Pts',(-16.1874558166671,0.753926572650982,
5.77294256861028));
#32572=CARTESIAN_POINT('Ctrl Pts',(-16.0481971725843,-2.10602565435016,
5.42769998439863));
#32573=CARTESIAN_POINT('Ctrl Pts',(-15.9089385285014,-4.45036335210432,
3.7536032304532));
#32574=CARTESIAN_POINT('Ctrl Pts',(-15.7696798844186,-5.70512647604768,
1.16051844867799));
#32575=CARTESIAN_POINT('Ctrl Pts',(-15.6304212403358,-5.56311359388409,
-1.716694008542));
#32576=CARTESIAN_POINT('Ctrl Pts',(-15.4911625962529,-4.05909346791839,
-4.17361131349388));
#32577=CARTESIAN_POINT('Ctrl Pts',(-15.3519039521701,-1.56129268058847,
-5.60871075586562));
#32578=CARTESIAN_POINT('Ctrl Pts',(-15.2126453080873,1.31875662724521,-5.67063948206185));
#32579=CARTESIAN_POINT('Ctrl Pts',(-15.0733866640044,3.87593708676088,-4.34423559178062));
#32580=CARTESIAN_POINT('Ctrl Pts',(-14.9341280199216,5.48417873717277,-1.95424019919872));
#32581=CARTESIAN_POINT('Ctrl Pts',(-14.7948693758387,5.7497386248849,0.914208358597051));
#32582=CARTESIAN_POINT('Ctrl Pts',(-14.6556107317559,4.60760019313947,3.55883290386089));
#32583=CARTESIAN_POINT('Ctrl Pts',(-14.5163520876731,2.33739117040358,5.33215469523732));
#32584=CARTESIAN_POINT('Ctrl Pts',(-14.3770934435902,-0.505077190913626,
5.80001450072677));
#32585=CARTESIAN_POINT('Ctrl Pts',(-14.2378347995074,-3.22388839853548,
4.8478670331611));
#32586=CARTESIAN_POINT('Ctrl Pts',(-14.0985761554245,-5.15340072201409,
2.70882486989593));
#32587=CARTESIAN_POINT('Ctrl Pts',(-13.9593175113417,-5.82121507813234,
-0.0934140864467144));
#32588=CARTESIAN_POINT('Ctrl Pts',(-13.8200588672589,-5.06383166139498,
-2.87278263752683));
#32589=CARTESIAN_POINT('Ctrl Pts',(-13.680800223176,-3.06667931169952,-4.94881290580035));
#32590=CARTESIAN_POINT('Ctrl Pts',(-13.5415415790932,-0.318717300028964,
-5.81323407924405));
#32591=CARTESIAN_POINT('Ctrl Pts',(-13.4022829350104,2.50727570346634,-5.25441145364819));
#32592=CARTESIAN_POINT('Ctrl Pts',(-13.2630242909275,4.71941683917222,-3.40916058224889));
#32593=CARTESIAN_POINT('Ctrl Pts',(-13.1237656468447,5.77611151256949,-0.729250966255149));
#32594=CARTESIAN_POINT('Ctrl Pts',(-12.9845070027619,5.41865103914805,2.12919987163296));
#32595=CARTESIAN_POINT('Ctrl Pts',(-12.845248358679,3.73455183322449,4.46636247771959));
#32596=CARTESIAN_POINT('Ctrl Pts',(-12.7059897145962,1.1361289192972,5.71003347242015));
#32597=CARTESIAN_POINT('Ctrl Pts',(-12.5667310705133,-1.74045042481285,
5.55572708978679));
#32598=CARTESIAN_POINT('Ctrl Pts',(-12.4274724264305,-4.1909183753537,4.04122188806115));
#32599=CARTESIAN_POINT('Ctrl Pts',(-12.2882137823477,-5.61533120602602,
1.5373114922007));
#32600=CARTESIAN_POINT('Ctrl Pts',(-12.1489551382648,-5.6649524474409,-1.34297615230335));
#32601=CARTESIAN_POINT('Ctrl Pts',(-12.009696494182,-4.32763341898751,-3.89446532508437));
#32602=CARTESIAN_POINT('Ctrl Pts',(-11.8704378500991,-1.93078756878074,
-5.49247945300331));
#32603=CARTESIAN_POINT('Ctrl Pts',(-11.7311792060163,0.938769580690719,
-5.745779568674));
#32604=CARTESIAN_POINT('Ctrl Pts',(-11.5919205619335,3.57848943714567,-4.59235065360418));
#32605=CARTESIAN_POINT('Ctrl Pts',(-11.4526619178506,5.34209406549889,-2.31458466528736));
#32606=CARTESIAN_POINT('Ctrl Pts',(-11.3134032737678,5.79780326955581,0.52985698537453));
#32607=CARTESIAN_POINT('Ctrl Pts',(-11.174144629685,4.83404657236697,3.244574689171));
#32608=CARTESIAN_POINT('Ctrl Pts',(-11.0348859856021,2.68677881840614,5.16492892094228));
#32609=CARTESIAN_POINT('Ctrl Pts',(-10.8956273415193,-0.118288232909747,
5.82076275683669));
#32610=CARTESIAN_POINT('Ctrl Pts',(-10.7563686974365,-2.8943949857596,5.05150956089681));
#32611=CARTESIAN_POINT('Ctrl Pts',(-10.6171100533536,-4.96187214288032,
3.04550423002994));
#32612=CARTESIAN_POINT('Ctrl Pts',(-10.4778514092708,-5.81454293529678,
0.2938734949127));
#32613=CARTESIAN_POINT('Ctrl Pts',(-10.3385927651879,-5.24364948376559,
-2.52970576724383));
#32614=CARTESIAN_POINT('Ctrl Pts',(-10.1993341211051,-3.38896262044802,
-4.73394164884063));
#32615=CARTESIAN_POINT('Ctrl Pts',(-10.0600754770223,-0.704562043734518,
-5.77917498471456));
#32616=CARTESIAN_POINT('Ctrl Pts',(-9.92081683293943,2.15233520971946,-5.4095031493127));
#32617=CARTESIAN_POINT('Ctrl Pts',(-9.78155818885659,4.48228004754217,-3.71543224306774));
#32618=CARTESIAN_POINT('Ctrl Pts',(-9.64229954477375,5.71483620356373,-1.11171864419876));
#32619=CARTESIAN_POINT('Ctrl Pts',(-9.50304090069091,5.54823913809556,1.76417506045364));
#32620=CARTESIAN_POINT('Ctrl Pts',(-9.36378225660808,4.02327651547963,4.20814891103108));
#32621=CARTESIAN_POINT('Ctrl Pts',(-9.22452361252525,1.51330223250026,5.62184912022118));
#32622=CARTESIAN_POINT('Ctrl Pts',(-9.08526496844239,-1.36717115461266,
5.65916197077067));
#32623=CARTESIAN_POINT('Ctrl Pts',(-8.94600632435957,-3.91292245045877,
4.31095222359489));
#32624=CARTESIAN_POINT('Ctrl Pts',(-8.80674768027673,-5.50067987614199,
1.90729968217594));
#32625=CARTESIAN_POINT('Ctrl Pts',(-8.66748903619388,-5.74171559451039,
-0.96331366084895));
#32626=CARTESIAN_POINT('Ctrl Pts',(-8.52823039211106,-4.57701725773164,
-3.59808062720235));
#32627=CARTESIAN_POINT('Ctrl Pts',(-8.38897174802821,-2.29173589584776,
-5.35193588910637));
#32628=CARTESIAN_POINT('Ctrl Pts',(-8.24971310394538,0.554627104645345,
-5.79548617047911));
#32629=CARTESIAN_POINT('Ctrl Pts',(-8.11045445986253,3.26520173386261,-4.82013784186744));
#32630=CARTESIAN_POINT('Ctrl Pts',(-7.9711958157797,5.17636280825239,-2.6646837063268));
#32631=CARTESIAN_POINT('Ctrl Pts',(-7.83193717169687,5.82020414839504,0.143160219429282));
#32632=CARTESIAN_POINT('Ctrl Pts',(-7.69267852761401,5.0390952198184,2.91595448233083));
#32633=CARTESIAN_POINT('Ctrl Pts',(-7.5534198835312,3.02427353744386,4.97484077615946));
#32634=CARTESIAN_POINT('Ctrl Pts',(-7.41416123944835,0.269024323665677,
5.81574561777749));
#32635=CARTESIAN_POINT('Ctrl Pts',(-7.27490259536551,-2.55208963858617,
5.23279176482717));
#32636=CARTESIAN_POINT('Ctrl Pts',(-7.13564395128268,-4.74838001671997,
3.36870277617907));
#32637=CARTESIAN_POINT('Ctrl Pts',(-6.99638530719984,-5.78213292910652,
0.679860255908561));
#32638=CARTESIAN_POINT('Ctrl Pts',(-6.85712666311699,-5.400256481933,-2.17543124615844));
#32639=CARTESIAN_POINT('Ctrl Pts',(-6.71786801903417,-3.69624480910674,
-4.49811577091712));
#32640=CARTESIAN_POINT('Ctrl Pts',(-6.57860937495133,-1.08728806911454,
-5.71953458178049));
#32641=CARTESIAN_POINT('Ctrl Pts',(-6.43935073086849,1.78786748225226,-5.5406498755405));
#32642=CARTESIAN_POINT('Ctrl Pts',(-6.30009208678565,4.22530260589625,-4.00525767785651));
#32643=CARTESIAN_POINT('Ctrl Pts',(-6.16083344270281,5.62826437943398,-1.48926533989636));
#32644=CARTESIAN_POINT('Ctrl Pts',(-6.02157479861997,5.65326815778531,1.39134119237251));
#32645=CARTESIAN_POINT('Ctrl Pts',(-5.88231615453714,4.29419231020122,3.93130812585718));
#32646=CARTESIAN_POINT('Ctrl Pts',(-5.74305751045431,1.88377696827288,5.50877985684914));
#32647=CARTESIAN_POINT('Ctrl Pts',(-5.60379886637146,-0.987840150896906,
5.73754677660216));
#32648=CARTESIAN_POINT('Ctrl Pts',(-5.46454022228862,-3.6176061162956,4.56160028550974));
#32649=CARTESIAN_POINT('Ctrl Pts',(-5.32528157820579,-5.36167998634783,
2.26884527930375));
#32650=CARTESIAN_POINT('Ctrl Pts',(-5.18602293412295,-5.793063245807,-0.579387096423341));
#32651=CARTESIAN_POINT('Ctrl Pts',(-5.04676429004011,-4.80614109563603,
-3.28576915596036));
#32652=CARTESIAN_POINT('Ctrl Pts',(-4.90750564595728,-2.64253993711476,
-5.18770217516153));
#32653=CARTESIAN_POINT('Ctrl Pts',(-4.76824700187443,0.16802959184276,-5.81953926300762));
#32654=CARTESIAN_POINT('Ctrl Pts',(-4.6289883577916,2.93746073356423,-5.02658886484561));
#32655=CARTESIAN_POINT('Ctrl Pts',(-4.48972971370876,4.98771856883065,-3.00298762161356));
#32656=CARTESIAN_POINT('Ctrl Pts',(-4.35047106962593,5.81684210472518,-0.244170240033472));
#32657=CARTESIAN_POINT('Ctrl Pts',(-4.21121242554308,5.2218384950949,2.57442690876366));
#32658=CARTESIAN_POINT('Ctrl Pts',(-4.07195378146025,3.34838141938695,4.76273167916573));
#32659=CARTESIAN_POINT('Ctrl Pts',(-3.93269513737742,0.655146053832615,
5.78498529173258));
#32660=CARTESIAN_POINT('Ctrl Pts',(-3.79343649329457,-2.1984875592163,5.39091120585453));
#32661=CARTESIAN_POINT('Ctrl Pts',(-3.65417784921174,-4.51386935868354,
3.67698988170163));
#32662=CARTESIAN_POINT('Ctrl Pts',(-3.5149192051289,-5.72412852127934,1.06283764015143));
#32663=CARTESIAN_POINT('Ctrl Pts',(-3.37566056104605,-5.53295944069909,
-1.81152725759464));
#32664=CARTESIAN_POINT('Ctrl Pts',(-3.23640191696322,-3.98716570422026,
-4.24237914670461));
#32665=CARTESIAN_POINT('Ctrl Pts',(-3.09714327288039,-1.46520125329375,
-5.6345768665572));
#32666=CARTESIAN_POINT('Ctrl Pts',(-2.95788462879754,1.41548582422035,-5.64727111603672));
#32667=CARTESIAN_POINT('Ctrl Pts',(-2.81862598471471,3.94962201559119,-4.27735398497753));
#32668=CARTESIAN_POINT('Ctrl Pts',(-2.67936734063188,5.51677924715227,-1.8602198563335));
#32669=CARTESIAN_POINT('Ctrl Pts',(-2.54010869654903,5.73327319120209,1.01234860246717));
#32670=CARTESIAN_POINT('Ctrl Pts',(-2.4008500524662,4.54610001819894,3.63706554889101));
#32671=CARTESIAN_POINT('Ctrl Pts',(-2.26159140838336,2.24591323413269,5.37132617734322));
#32672=CARTESIAN_POINT('Ctrl Pts',(-2.12233276430053,-0.604136509556456,
5.79053454359149));
#32673=CARTESIAN_POINT('Ctrl Pts',(-1.98307412021767,-3.30627657802072,
4.79205658182243));
#32674=CARTESIAN_POINT('Ctrl Pts',(-1.84381547613485,-5.19894681828512,
2.62034792960979));
#32675=CARTESIAN_POINT('Ctrl Pts',(-1.70455683205201,-5.81876810565199,
-0.192895924308944));
#32676=CARTESIAN_POINT('Ctrl Pts',(-1.56529818796917,-5.01399073831737,
-2.9589132916041));
#32677=CARTESIAN_POINT('Ctrl Pts',(-1.42603954388634,-2.98164684396445,
-5.00050539332495));
#32678=CARTESIAN_POINT('Ctrl Pts',(-1.2867808998035,-0.219311751017547,
-5.81783216627008));
#32679=CARTESIAN_POINT('Ctrl Pts',(-1.14752225572065,2.59671727360405,-5.21079028391074));
#32680=CARTESIAN_POINT('Ctrl Pts',(-1.00826361163782,4.77699617182404,-3.32799812267906));
#32681=CARTESIAN_POINT('Ctrl Pts',(-0.869004967554989,5.78773241510616,
-0.630421446287272));
#32682=CARTESIAN_POINT('Ctrl Pts',(-0.729746323472141,5.381466722009,2.22150676598878));
#32683=CARTESIAN_POINT('Ctrl Pts',(-0.5904876793893,3.65766931387145,4.52953459695107));
#32684=CARTESIAN_POINT('Ctrl Pts',(-0.451229035306472,1.03836487504737,
5.72862949825498));
#32685=CARTESIAN_POINT('Ctrl Pts',(-0.311970391223629,-1.83514824151881,
5.52514542236776));
#32686=CARTESIAN_POINT('Ctrl Pts',(-0.172711747140795,-4.25938936625894,
3.96904493801873));
#32687=CARTESIAN_POINT('Ctrl Pts',(-0.0334531030579666,-5.64076471879598,
1.44102431516129));
#32688=CARTESIAN_POINT('Ctrl Pts',(0.105805541024883,-5.64121346572028,
-1.43943410988536));
#32689=CARTESIAN_POINT('Ctrl Pts',(0.245064185107723,-4.26035369318523,
-3.96822316047526));
#32690=CARTESIAN_POINT('Ctrl Pts',(0.337903281162944,-2.64465155276186,
-5.00520070296182));
#32691=CARTESIAN_POINT('Ctrl Pts',(0.384322829190555,-1.76153289128266,
-5.29878544698756));
#32692=CARTESIAN_POINT('Ctrl Pts',(-59.58325,-2.58391981634379,5.32271443393368));
#32693=CARTESIAN_POINT('Ctrl Pts',(-59.5368304519724,-3.47102658701026,
4.89206710306723));
#32694=CARTESIAN_POINT('Ctrl Pts',(-59.4439913559172,-5.02484286868922,
3.57907156976542));
#32695=CARTESIAN_POINT('Ctrl Pts',(-59.3047327118343,-6.125475880775,0.731390377776202));
#32696=CARTESIAN_POINT('Ctrl Pts',(-59.1654740677516,-5.72633323264516,
-2.29454852325651));
#32697=CARTESIAN_POINT('Ctrl Pts',(-59.0262154236686,-3.925268426147,-4.75911398603417));
#32698=CARTESIAN_POINT('Ctrl Pts',(-58.8869567795858,-1.16316343878524,
-6.05831220422429));
#32699=CARTESIAN_POINT('Ctrl Pts',(-58.747698135503,1.88370464411569,-5.87436787906887));
#32700=CARTESIAN_POINT('Ctrl Pts',(-58.6084394914201,4.46939488601017,-4.25215953310488));
#32701=CARTESIAN_POINT('Ctrl Pts',(-58.4691808473373,5.96084790378021,-1.58892964266834));
#32702=CARTESIAN_POINT('Ctrl Pts',(-58.3299222032545,5.99291872863358,1.46332898982328));
#32703=CARTESIAN_POINT('Ctrl Pts',(-58.1906635591716,4.55775304079097,4.15731624602566));
#32704=CARTESIAN_POINT('Ctrl Pts',(-58.0514049150888,2.00672118223107,5.83347878871376));
#32705=CARTESIAN_POINT('Ctrl Pts',(-57.912146271006,-1.03561288821634,6.08143918145384));
#32706=CARTESIAN_POINT('Ctrl Pts',(-57.7728876269232,-3.82439957717761,
4.84049255622217));
#32707=CARTESIAN_POINT('Ctrl Pts',(-57.6336289828403,-5.6768653521605,2.41445622274904));
#32708=CARTESIAN_POINT('Ctrl Pts',(-57.4943703387574,-6.13947421220047,
-0.602706896951242));
#32709=CARTESIAN_POINT('Ctrl Pts',(-57.3551116946747,-5.09896649475701,
-3.47231048449872));
#32710=CARTESIAN_POINT('Ctrl Pts',(-57.2158530505918,-2.81008783754839,
-5.49179438240193));
#32711=CARTESIAN_POINT('Ctrl Pts',(-57.0765944065089,0.166779641673839,
-6.16673202670761));
#32712=CARTESIAN_POINT('Ctrl Pts',(-56.9373357624261,3.10281475879802,-5.33187957842086));
#32713=CARTESIAN_POINT('Ctrl Pts',(-56.7980771183432,5.2791932354107,-3.19163250955323));
#32714=CARTESIAN_POINT('Ctrl Pts',(-56.6588184742605,6.16307618704186,-0.269983704102151));
#32715=CARTESIAN_POINT('Ctrl Pts',(-56.5195598301775,5.5380641159968,2.71776473088446));
#32716=CARTESIAN_POINT('Ctrl Pts',(-56.3803011860948,3.5571776205769,5.04012764367346));
#32717=CARTESIAN_POINT('Ctrl Pts',(-56.2410425420118,0.705393631270256,
6.12852503554376));
#32718=CARTESIAN_POINT('Ctrl Pts',(-56.1017838979292,-2.31909063084241,
5.71648650253054));
#32719=CARTESIAN_POINT('Ctrl Pts',(-55.9625252538461,-4.77579604306655,
3.90489070809336));
#32720=CARTESIAN_POINT('Ctrl Pts',(-55.8232666097635,-6.06325177238225,
1.13726744082824));
#32721=CARTESIAN_POINT('Ctrl Pts',(-55.6840079656805,-5.86625231386363,
-1.90879099887135));
#32722=CARTESIAN_POINT('Ctrl Pts',(-55.5447493215978,-4.23302869586511,
-4.48752352051908));
#32723=CARTESIAN_POINT('Ctrl Pts',(-55.4054906775148,-1.56344016284461,
-5.967583610179));
#32724=CARTESIAN_POINT('Ctrl Pts',(-55.2662320334321,1.48892265495596,-5.98661077862981));
#32725=CARTESIAN_POINT('Ctrl Pts',(-55.1269733893491,4.17675517739415,-4.539946637943));
#32726=CARTESIAN_POINT('Ctrl Pts',(-54.9877147452664,5.84200013062435,-1.98177540630629));
#32727=CARTESIAN_POINT('Ctrl Pts',(-54.8484561011835,6.07695854342666,1.06159038650946));
#32728=CARTESIAN_POINT('Ctrl Pts',(-54.7091974571007,4.82410596392218,3.84504888604902));
#32729=CARTESIAN_POINT('Ctrl Pts',(-54.5699388130179,2.39017606919722,5.68713087993344));
#32730=CARTESIAN_POINT('Ctrl Pts',(-54.430680168935,-0.628936397350093,
6.13684269762101));
#32731=CARTESIAN_POINT('Ctrl Pts',(-54.2914215248522,-3.49406748015876,
5.08408219164018));
#32732=CARTESIAN_POINT('Ctrl Pts',(-54.1521628807693,-5.50375221300585,
2.78659485126364));
#32733=CARTESIAN_POINT('Ctrl Pts',(-54.0129042366865,-6.16596304374769,
-0.193129568926519));
#32734=CARTESIAN_POINT('Ctrl Pts',(-53.8736455926037,-5.31857206807786,
-3.12557041896641));
#32735=CARTESIAN_POINT('Ctrl Pts',(-53.7343869485208,-3.1690445170612,-5.29278340158939));
#32736=CARTESIAN_POINT('Ctrl Pts',(-53.595128304438,-0.243645412223681,
-6.16417360238647));
#32737=CARTESIAN_POINT('Ctrl Pts',(-53.4558696603552,2.74140496716854,-5.52640010252963));
#32738=CARTESIAN_POINT('Ctrl Pts',(-53.3166110162723,5.05528202599734,-3.53560785790563));
#32739=CARTESIAN_POINT('Ctrl Pts',(-53.1773523721895,6.13148334395316,-0.679199006242515));
#32740=CARTESIAN_POINT('Ctrl Pts',(-53.0380937281066,5.70652445930279,2.34349693463311));
#32741=CARTESIAN_POINT('Ctrl Pts',(-52.8988350840238,3.88444730278233,4.79243867349005));
#32742=CARTESIAN_POINT('Ctrl Pts',(-52.759576439941,1.11134779604893,6.06805614373112));
#32743=CARTESIAN_POINT('Ctrl Pts',(-52.6203177958581,-1.93384102237248,
5.85804218040851));
#32744=CARTESIAN_POINT('Ctrl Pts',(-52.4810591517753,-4.50557096989672,
4.21381413003465));
#32745=CARTESIAN_POINT('Ctrl Pts',(-52.3418005076924,-5.97420996036946,
1.53792543274314));
#32746=CARTESIAN_POINT('Ctrl Pts',(-52.2025418636096,-5.98019371206306,
-1.51449082316711));
#32747=CARTESIAN_POINT('Ctrl Pts',(-52.0632832195268,-4.52205723365308,
-4.19611697439688));
#32748=CARTESIAN_POINT('Ctrl Pts',(-51.9240245754439,-1.95679349544846,
-5.85041524196586));
#32749=CARTESIAN_POINT('Ctrl Pts',(-51.7847659313611,1.08754852696658,-6.0723667123082));
#32750=CARTESIAN_POINT('Ctrl Pts',(-51.6455072872782,3.86562797057267,-4.80763140022008));
#32751=CARTESIAN_POINT('Ctrl Pts',(-51.5062486431954,5.69729256772438,-2.36585221115108));
#32752=CARTESIAN_POINT('Ctrl Pts',(-51.3669899991126,6.13409912066294,0.655154382674766));
#32753=CARTESIAN_POINT('Ctrl Pts',(-51.2277313550298,5.06910505501842,3.51576068987105));
#32754=CARTESIAN_POINT('Ctrl Pts',(-51.0884727109469,2.76305098079898,5.51560953701054));
#32755=CARTESIAN_POINT('Ctrl Pts',(-50.9492140668641,-0.21947596914604,
6.16508147441892));
#32756=CARTESIAN_POINT('Ctrl Pts',(-50.8099554227812,-3.14826900645875,
5.30516743847233));
#32757=CARTESIAN_POINT('Ctrl Pts',(-50.6706967786984,-5.30627692139886,
3.14639865889332));
#32758=CARTESIAN_POINT('Ctrl Pts',(-50.5314381346156,-6.16515845996755,
0.217302670822068));
#32759=CARTESIAN_POINT('Ctrl Pts',(-50.3921794905327,-5.51463517694584,
-2.76499514510376));
#32760=CARTESIAN_POINT('Ctrl Pts',(-50.2529208464499,-3.51397353504114,
-5.07034409900219));
#32761=CARTESIAN_POINT('Ctrl Pts',(-50.113662202367,-0.652991979029951,
-6.13432969138262));
#32762=CARTESIAN_POINT('Ctrl Pts',(-49.9744035582842,2.36786044615801,-5.6964582149592));
#32763=CARTESIAN_POINT('Ctrl Pts',(-49.8351449142013,4.80899379397081,-3.86393296743177));
#32764=CARTESIAN_POINT('Ctrl Pts',(-49.6958862701186,6.07274971235482,-1.08540785806552));
#32765=CARTESIAN_POINT('Ctrl Pts',(-49.5566276260357,5.84972507908559,1.95885573393575));
#32766=CARTESIAN_POINT('Ctrl Pts',(-49.4173689819528,4.19452261994479,4.52353614753185));
#32767=CARTESIAN_POINT('Ctrl Pts',(-49.2781103378701,1.51238262011864,5.98072722146889));
#32768=CARTESIAN_POINT('Ctrl Pts',(-49.1388516937871,-1.54003133677118,
5.97366744713988));
#32769=CARTESIAN_POINT('Ctrl Pts',(-48.9995930497044,-4.2154021502906,4.50408525658442));
#32770=CARTESIAN_POINT('Ctrl Pts',(-48.8603344056215,-5.85872352470692,
1.93177585353516));
#32771=CARTESIAN_POINT('Ctrl Pts',(-48.7210757615387,-6.06766399975473,
-1.11348680878414));
#32772=CARTESIAN_POINT('Ctrl Pts',(-48.5818171174559,-4.79106904915372,
-3.88613646871764));
#32773=CARTESIAN_POINT('Ctrl Pts',(-48.4425584733729,-2.34148515263626,
-5.70735022293531));
#32774=CARTESIAN_POINT('Ctrl Pts',(-48.3032998292902,0.681360404878315,
-6.13124353503593));
#32775=CARTESIAN_POINT('Ctrl Pts',(-48.1640411852073,3.5373897017822,-5.05403535652265));
#32776=CARTESIAN_POINT('Ctrl Pts',(-48.0247825411245,5.52736614596797,-2.73945665701488));
#32777=CARTESIAN_POINT('Ctrl Pts',(-47.8855238970416,6.1640873306833,0.245818361733667));
#32778=CARTESIAN_POINT('Ctrl Pts',(-47.7462652529589,5.29166593649294,3.17091010654926));
#32779=CARTESIAN_POINT('Ctrl Pts',(-47.6070066088759,3.12369534747615,5.31967354857529));
#32780=CARTESIAN_POINT('Ctrl Pts',(-47.4677479647933,0.190955961472976,
6.16603074173603));
#32781=CARTESIAN_POINT('Ctrl Pts',(-47.3284893207102,-2.78853483421908,
5.50276955410661));
#32782=CARTESIAN_POINT('Ctrl Pts',(-47.1892306766276,-5.08531358750806,
3.49227504700901));
#32783=CARTESIAN_POINT('Ctrl Pts',(-47.0499720325445,-6.13706402593289,
0.626773028181855));
#32784=CARTESIAN_POINT('Ctrl Pts',(-46.9107133884618,-5.68628795327095,
-2.3921807205438));
#32785=CARTESIAN_POINT('Ctrl Pts',(-46.7714547443789,-3.84334807665325,
-4.82546110220999));
#32786=CARTESIAN_POINT('Ctrl Pts',(-46.6321961002961,-1.05944810053127,
-6.07733239254992));
#32787=CARTESIAN_POINT('Ctrl Pts',(-46.4929374562133,1.98383467678721,-5.84130116176459));
#32788=CARTESIAN_POINT('Ctrl Pts',(-46.3536788121304,4.54141872538288,-4.1751545178589));
#32789=CARTESIAN_POINT('Ctrl Pts',(-46.2144201680476,5.98713527447069,-1.48681219138281));
#32790=CARTESIAN_POINT('Ctrl Pts',(-46.0751615239648,5.96703210303059,1.56554372939827));
#32791=CARTESIAN_POINT('Ctrl Pts',(-45.9359028798819,4.48603103490502,4.23461035292798));
#32792=CARTESIAN_POINT('Ctrl Pts',(-45.7966442357991,1.90672293738878,5.86692482713825));
#32793=CARTESIAN_POINT('Ctrl Pts',(-45.6573855917162,-1.13940475832912,
6.06285049163781));
#32794=CARTESIAN_POINT('Ctrl Pts',(-45.5181269476334,-3.90657400599862,
4.77441921315165));
#32795=CARTESIAN_POINT('Ctrl Pts',(-45.3788683035505,-5.71730366191351,
2.31707533859527));
#32796=CARTESIAN_POINT('Ctrl Pts',(-45.2396096594678,-6.12827599288294,
-0.707553985438834));
#32797=CARTESIAN_POINT('Ctrl Pts',(-45.1003510153848,-5.03887337132555,
-3.55895412094651));
#32798=CARTESIAN_POINT('Ctrl Pts',(-44.9610923713022,-2.71581231074366,
-5.53902182520244));
#32799=CARTESIAN_POINT('Ctrl Pts',(-44.8218337272191,0.272156265677259,
-6.16298063069392));
#32800=CARTESIAN_POINT('Ctrl Pts',(-44.6825750831364,3.19349330581138,-5.27806780867713));
#32801=CARTESIAN_POINT('Ctrl Pts',(-44.5433164390535,5.33297303849622,-3.10093499737228));
#32802=CARTESIAN_POINT('Ctrl Pts',(-44.4040577949708,6.16679043176404,-0.16460576526746));
#32803=CARTESIAN_POINT('Ctrl Pts',(-44.2647991508878,5.49080345067826,2.81202360467965));
#32804=CARTESIAN_POINT('Ctrl Pts',(-44.1255405068051,3.4705127900237,5.10019021817205));
#32805=CARTESIAN_POINT('Ctrl Pts',(-43.9862818627222,0.60054263245633,6.13968629767501));
#32806=CARTESIAN_POINT('Ctrl Pts',(-43.8470232186394,-2.4164573137022,5.67601385994704));
#32807=CARTESIAN_POINT('Ctrl Pts',(-43.7077645745565,-4.84184029751447,
3.82269300632694));
#32808=CARTESIAN_POINT('Ctrl Pts',(-43.5685059304737,-6.08180410063669,
1.03346899747141));
#32809=CARTESIAN_POINT('Ctrl Pts',(-43.4292472863909,-5.83277058226627,
-2.00877739481134));
#32810=CARTESIAN_POINT('Ctrl Pts',(-43.289988642308,-4.15571017743855,-4.55921837691391));
#32811=CARTESIAN_POINT('Ctrl Pts',(-43.1507299982251,-1.46121461345175,
-5.99343400236382));
#32812=CARTESIAN_POINT('Ctrl Pts',(-43.0114713541424,1.59102753519202,-5.9602878008966));
#32813=CARTESIAN_POINT('Ctrl Pts',(-42.8722127100595,4.25374123156719,-4.46789489828499));
#32814=CARTESIAN_POINT('Ctrl Pts',(-42.7329540659767,5.87501899950408,-1.88163520447562));
#32815=CARTESIAN_POINT('Ctrl Pts',(-42.5936954218938,6.05792627585209,1.16530190233972));
#32816=CARTESIAN_POINT('Ctrl Pts',(-42.454436777811,4.75768219623993,3.92694020922617));
#32817=CARTESIAN_POINT('Ctrl Pts',(-42.3151781337282,2.29262321475141,5.72715270290909));
#32818=CARTESIAN_POINT('Ctrl Pts',(-42.1759194896453,-0.733734646061337,
6.12519654839133));
#32819=CARTESIAN_POINT('Ctrl Pts',(-42.0366608455625,-3.58045355359749,
5.0236193762851));
#32820=CARTESIAN_POINT('Ctrl Pts',(-41.8974022014796,-5.5505763618812,2.69211837373126));
#32821=CARTESIAN_POINT('Ctrl Pts',(-41.7581435573968,-6.1617613946591,-0.298489200046597));
#32822=CARTESIAN_POINT('Ctrl Pts',(-41.6188849133139,-5.26437330332677,
-3.21601819187584));
#32823=CARTESIAN_POINT('Ctrl Pts',(-41.4796262692311,-3.07811802418573,
-5.34617514831293));
#32824=CARTESIAN_POINT('Ctrl Pts',(-41.3403676251482,-0.13825256336012,
-6.16743751617966));
#32825=CARTESIAN_POINT('Ctrl Pts',(-41.2011089810655,2.83546102758053,-5.47873708516185));
#32826=CARTESIAN_POINT('Ctrl Pts',(-41.0618503369825,5.11497371934684,-3.44868716146404));
#32827=CARTESIAN_POINT('Ctrl Pts',(-40.9225916928999,6.14219645872631,-0.57430127082044));
#32828=CARTESIAN_POINT('Ctrl Pts',(-40.7833330488169,5.66563612259242,2.44068978234263));
#32829=CARTESIAN_POINT('Ctrl Pts',(-40.6440744047341,3.8019681336144,4.85813108080016));
#32830=CARTESIAN_POINT('Ctrl Pts',(-40.5048157606512,1.0074710232644,6.08616475496173));
#32831=CARTESIAN_POINT('Ctrl Pts',(-40.3655571165684,-2.03368343255402,
5.82413349635901));
#32832=CARTESIAN_POINT('Ctrl Pts',(-40.2262984724856,-4.57693477710325,
4.13618995373747));
#32833=CARTESIAN_POINT('Ctrl Pts',(-40.0870398284027,-5.99962329013349,
1.4355903537373));
#32834=CARTESIAN_POINT('Ctrl Pts',(-39.9477811843199,-5.95343466388885,
-1.61648228881805));
#32835=CARTESIAN_POINT('Ctrl Pts',(-39.8085225402371,-4.44967717789028,
-4.27279443687832));
#32836=CARTESIAN_POINT('Ctrl Pts',(-39.6692638961542,-1.85651311289782,
-5.88300589400472));
#32837=CARTESIAN_POINT('Ctrl Pts',(-39.5300052520714,1.19117776793395,-6.05289144231381));
#32838=CARTESIAN_POINT('Ctrl Pts',(-39.3907466079885,3.94723470651334,-4.74085830403655));
#32839=CARTESIAN_POINT('Ctrl Pts',(-39.2514879639057,5.73689716607855,-2.26812922760052));
#32840=CARTESIAN_POINT('Ctrl Pts',(-39.1122293198229,6.12200525779175,0.75990190868693));
#32841=CARTESIAN_POINT('Ctrl Pts',(-38.97297067574,5.00827364993925,3.60188760715546));
#32842=CARTESIAN_POINT('Ctrl Pts',(-38.8337120316572,2.66837527862899,5.56202954501839));
#32843=CARTESIAN_POINT('Ctrl Pts',(-38.6944533875744,-0.324816684002235,
6.16042964484212));
#32844=CARTESIAN_POINT('Ctrl Pts',(-38.5551947434915,-3.23848435343815,
5.25058267050353));
#32845=CARTESIAN_POINT('Ctrl Pts',(-38.4159360994087,-5.35927963695485,
3.05524484455452));
#32846=CARTESIAN_POINT('Ctrl Pts',(-38.2766774553258,-6.16797198316708,
0.111896836960587));
#32847=CARTESIAN_POINT('Ctrl Pts',(-38.137418811243,-5.46657067788929,-2.85884667495424));
#32848=CARTESIAN_POINT('Ctrl Pts',(-37.9981601671602,-3.42679855986613,
-5.12966382108567));
#32849=CARTESIAN_POINT('Ctrl Pts',(-37.8589015230773,-0.548049422441559,
-6.14459446325119));
#32850=CARTESIAN_POINT('Ctrl Pts',(-37.7196428789945,2.46487768398001,-5.65515493070466));
#32851=CARTESIAN_POINT('Ctrl Pts',(-37.5803842349116,4.87433315459717,-3.78117383695203));
#32852=CARTESIAN_POINT('Ctrl Pts',(-37.4411255908288,6.09041427589945,-0.98145465263348));
#32853=CARTESIAN_POINT('Ctrl Pts',(-37.301866946746,5.81539006175608,2.05855233523087));
#32854=CARTESIAN_POINT('Ctrl Pts',(-37.1626083026632,4.11659420319502,4.59456760244934));
#32855=CARTESIAN_POINT('Ctrl Pts',(-37.0233496585803,1.40993988013854,6.00570302476329));
#32856=CARTESIAN_POINT('Ctrl Pts',(-36.8840910144975,-1.64190752547249,
5.94647281714569));
#32857=CARTESIAN_POINT('Ctrl Pts',(-36.7448323704146,-4.29176962094978,
4.43137820637648));
#32858=CARTESIAN_POINT('Ctrl Pts',(-36.6055737263319,-5.89088536479951,
1.83135712138482));
#32859=CARTESIAN_POINT('Ctrl Pts',(-36.4663150822489,-6.04774608295902,
-1.21703188261843));
#32860=CARTESIAN_POINT('Ctrl Pts',(-36.3270564381662,-4.72394784374585,
-3.96745712728251));
#32861=CARTESIAN_POINT('Ctrl Pts',(-36.1877977940833,-2.24359382440289,
-5.74653687348798));
#32862=CARTESIAN_POINT('Ctrl Pts',(-36.0485391500005,0.786055295501336,
-6.11870217935716));
#32863=CARTESIAN_POINT('Ctrl Pts',(-35.9092805059176,3.62325589023456,-4.99283647250103));
#32864=CARTESIAN_POINT('Ctrl Pts',(-35.7700218618348,5.57338116547882,-2.64458345898589));
#32865=CARTESIAN_POINT('Ctrl Pts',(-35.6307632177519,6.15898540556072,0.351138236804208));
#32866=CARTESIAN_POINT('Ctrl Pts',(-35.4915045736691,5.23669616202447,3.26089138026614));
#32867=CARTESIAN_POINT('Ctrl Pts',(-35.3522459295863,3.03231587614294,5.37228626513397));
#32868=CARTESIAN_POINT('Ctrl Pts',(-35.2129872855034,0.0855390673244696,
6.16839382296698));
#32869=CARTESIAN_POINT('Ctrl Pts',(-35.0737286414206,-2.88218011977874,
5.45430445101921));
#32870=CARTESIAN_POINT('Ctrl Pts',(-34.9344699973377,-5.14426025514717,
3.40484738491593));
#32871=CARTESIAN_POINT('Ctrl Pts',(-34.7952113532549,-6.14688026746215,
0.521787566678581));
#32872=CARTESIAN_POINT('Ctrl Pts',(-34.6559527091721,-5.64457047567031,
-2.48902057694323));
#32873=CARTESIAN_POINT('Ctrl Pts',(-34.5166940650892,-3.76031049604365,
-4.89044622305572));
#32874=CARTESIAN_POINT('Ctrl Pts',(-34.3774354210064,-0.955420360637483,
-6.09455258585363));
#32875=CARTESIAN_POINT('Ctrl Pts',(-34.2381767769235,2.08338364873574,-5.80654043811255));
#32876=CARTESIAN_POINT('Ctrl Pts',(-34.0989181328408,4.61211653097676,-4.09692328362966));
#32877=CARTESIAN_POINT('Ctrl Pts',(-33.9596594887579,6.0116730952372,-1.38426366103323));
#32878=CARTESIAN_POINT('Ctrl Pts',(-33.820400844675,5.93940238779045,1.66730278089042));
#32879=CARTESIAN_POINT('Ctrl Pts',(-33.6811422005922,4.41299831788288,4.31066643729467));
#32880=CARTESIAN_POINT('Ctrl Pts',(-33.5418835565093,1.80616768928508,5.89865726800925));
#32881=CARTESIAN_POINT('Ctrl Pts',(-33.4026249124266,-1.24286377429694,
6.04249029174199));
#32882=CARTESIAN_POINT('Ctrl Pts',(-33.2633662683437,-3.98760710227222,
4.70695112415288));
#32883=CARTESIAN_POINT('Ctrl Pts',(-33.1241076242609,-5.75607164911629,
2.21901745317509));
#32884=CARTESIAN_POINT('Ctrl Pts',(-32.984848980178,-6.11528737340181,-0.812194328943618));
#32885=CARTESIAN_POINT('Ctrl Pts',(-32.8455903360952,-4.9773081258533,-3.64455801264989));
#32886=CARTESIAN_POINT('Ctrl Pts',(-32.7063316920124,-2.62074334924062,
-5.58463101598189));
#32887=CARTESIAN_POINT('Ctrl Pts',(-32.5670730479295,0.37745337782084,-6.1574287031867));
#32888=CARTESIAN_POINT('Ctrl Pts',(-32.4278144038467,3.28323886320735,-5.22271403145727));
#32889=CARTESIAN_POINT('Ctrl Pts',(-32.2885557597638,5.38519479534925,-3.00933153763413));
#32890=CARTESIAN_POINT('Ctrl Pts',(-32.149297115681,6.16870302787652,-0.0591797357447051));
#32891=CARTESIAN_POINT('Ctrl Pts',(-32.0100384715982,5.44193862853294,2.90546093598537));
#32892=CARTESIAN_POINT('Ctrl Pts',(-31.8707798275153,3.38283403744187,5.15876275500052));
#32893=CARTESIAN_POINT('Ctrl Pts',(-31.7315211834324,0.495516183072966,
6.14905382962034));
#32894=CARTESIAN_POINT('Ctrl Pts',(-31.5922625393497,-2.51311802038301,
5.63388295076159));
#32895=CARTESIAN_POINT('Ctrl Pts',(-31.4530038952668,-4.90646999195102,
3.73937849185396));
#32896=CARTESIAN_POINT('Ctrl Pts',(-31.313745251184,-6.09857960925869,0.929368622662752));
#32897=CARTESIAN_POINT('Ctrl Pts',(-31.1744866071011,-5.79758478702263,
-2.10817691964873));
#32898=CARTESIAN_POINT('Ctrl Pts',(-31.0352279630183,-4.07717755423239,
-4.62958124224203));
#32899=CARTESIAN_POINT('Ctrl Pts',(-30.8959693189355,-1.35856216526917,
-6.01753339254177));
#32900=CARTESIAN_POINT('Ctrl Pts',(-30.7567106748526,1.69266759135437,-5.93222350492919));
#32901=CARTESIAN_POINT('Ctrl Pts',(-30.6174520307698,4.32948454085704,-4.39453784802633));
#32902=CARTESIAN_POINT('Ctrl Pts',(-30.478193386687,5.90632146171901,-1.78094527655773));
#32903=CARTESIAN_POINT('Ctrl Pts',(-30.3389347426041,6.03712416463348,1.26867297127911));
#32904=CARTESIAN_POINT('Ctrl Pts',(-30.1996760985213,4.6898684556178,4.00768426354387));
#32905=CARTESIAN_POINT('Ctrl Pts',(-30.0604174544385,2.19440056268174,5.76550131885839));
#32906=CARTESIAN_POINT('Ctrl Pts',(-29.9211588103556,-0.838318531714867,
6.11176090228006));
#32907=CARTESIAN_POINT('Ctrl Pts',(-29.7819001662728,-3.66579358542456,
4.96168889354382));
#32908=CARTESIAN_POINT('Ctrl Pts',(-29.6426415221899,-5.59577889110529,
2.59685538471367));
#32909=CARTESIAN_POINT('Ctrl Pts',(-29.5033828781071,-6.15575956614548,
-0.403761626537673));
#32910=CARTESIAN_POINT('Ctrl Pts',(-29.3641242340242,-5.20863653411563,
-3.3055263941968));
#32911=CARTESIAN_POINT('Ctrl Pts',(-29.2248655899414,-2.98629224872204,
-5.39800499189085));
#32912=CARTESIAN_POINT('Ctrl Pts',(-29.0856069458586,-0.0328193235427931,
-6.16889959224967));
#32913=CARTESIAN_POINT('Ctrl Pts',(-28.9463483017757,2.92868869846627,-5.42947343623043));
#32914=CARTESIAN_POINT('Ctrl Pts',(-28.8070896576929,5.17317105582995,-3.36075891940781));
#32915=CARTESIAN_POINT('Ctrl Pts',(-28.6678310136101,6.15111511003654,-0.469235751340301));
#32916=CARTESIAN_POINT('Ctrl Pts',(-28.5285723695272,5.62309255113269,2.53716957427995));
#32917=CARTESIAN_POINT('Ctrl Pts',(-28.3893137254444,3.71837820660141,4.92240416868907));
#32918=CARTESIAN_POINT('Ctrl Pts',(-28.2500550813615,0.903299914414111,
6.10249527258116));
#32919=CARTESIAN_POINT('Ctrl Pts',(-28.1107964372787,-2.13293169524463,
5.78852327201652));
#32920=CARTESIAN_POINT('Ctrl Pts',(-27.9715377931959,-4.64696141733948,
4.05735737556035));
#32921=CARTESIAN_POINT('Ctrl Pts',(-27.832279149113,-6.0232838096679,1.33283586215573));
#32922=CARTESIAN_POINT('Ctrl Pts',(-27.6930205050302,-5.92493629964835,
-1.71800149370285));
#32923=CARTESIAN_POINT('Ctrl Pts',(-27.5537618609473,-4.37599713389506,
-4.34822358801822));
#32924=CARTESIAN_POINT('Ctrl Pts',(-27.4145032168645,-1.75569034376417,
-5.91387780598052));
#32925=CARTESIAN_POINT('Ctrl Pts',(-27.2752445727817,1.29445900228884,-6.03164779961905));
#32926=CARTESIAN_POINT('Ctrl Pts',(-27.1359859286988,4.02768824448843,-4.67270015007014));
#32927=CARTESIAN_POINT('Ctrl Pts',(-26.996727284616,5.77482571052857,-2.16974360242729));
#32928=CARTESIAN_POINT('Ctrl Pts',(-26.8574686405332,6.10812283038528,0.864427426787198));
#32929=CARTESIAN_POINT('Ctrl Pts',(-26.7182099964503,4.9459790607797,3.68696222079703));
#32930=CARTESIAN_POINT('Ctrl Pts',(-26.5789513523675,2.57292000159934,5.60682458728878));
#32931=CARTESIAN_POINT('Ctrl Pts',(-26.4396927082847,-0.430062502565925,
6.15397802491548));
#32932=CARTESIAN_POINT('Ctrl Pts',(-26.3004340642018,-3.32775356626403,
5.19446392705473));
#32933=CARTESIAN_POINT('Ctrl Pts',(-26.161175420119,-5.41071662084457,2.96319843010423));
#32934=CARTESIAN_POINT('Ctrl Pts',(-26.0219167760361,-6.16898351249709,
0.00645831205992788));
#32935=CARTESIAN_POINT('Ctrl Pts',(-25.8826581319533,-5.41690910172617,
-2.95186298308237));
#32936=CARTESIAN_POINT('Ctrl Pts',(-25.7433994878705,-3.33862243390558,
-5.18748489453977));
#32937=CARTESIAN_POINT('Ctrl Pts',(-25.6041408437877,-0.442946751361456,
-6.15306407107178));
#32938=CARTESIAN_POINT('Ctrl Pts',(-25.4648821997048,2.56117479945259,-5.61219947381638));
#32939=CARTESIAN_POINT('Ctrl Pts',(-25.325623555622,4.93824846231173,-3.69731002375127));
#32940=CARTESIAN_POINT('Ctrl Pts',(-25.1863649115391,6.10629950432101,-0.877214711906259));
#32941=CARTESIAN_POINT('Ctrl Pts',(-25.0471062674563,5.77935605855753,2.15764752350107));
#32942=CARTESIAN_POINT('Ctrl Pts',(-24.9078476233735,4.03746310953012,4.66425673890698));
#32943=CARTESIAN_POINT('Ctrl Pts',(-24.7685889792906,1.30708522145541,6.02892424161299));
#32944=CARTESIAN_POINT('Ctrl Pts',(-24.6293303352078,-1.74330402533868,
5.91754090501231));
#32945=CARTESIAN_POINT('Ctrl Pts',(-24.490071691125,-4.36688323660318,4.35737651404258));
#32946=CARTESIAN_POINT('Ctrl Pts',(-24.3508130470421,-5.92132616281497,
1.73040335205951));
#32947=CARTESIAN_POINT('Ctrl Pts',(-24.2115544029593,-6.02606129669707,
-1.32022139647321));
#32948=CARTESIAN_POINT('Ctrl Pts',(-24.0722957588764,-4.65544652100326,
-4.04761867983319));
#32949=CARTESIAN_POINT('Ctrl Pts',(-23.9330371147936,-2.14504702264793,
-5.78404465386333));
#32950=CARTESIAN_POINT('Ctrl Pts',(-23.7937784707107,0.890520537411933,
-6.10437322414867));
#32951=CARTESIAN_POINT('Ctrl Pts',(-23.654519826628,3.70806353222781,-4.93017891442268));
#32952=CARTESIAN_POINT('Ctrl Pts',(-23.515261182545,5.61776790283785,-2.54893763695791));
#32953=CARTESIAN_POINT('Ctrl Pts',(-23.3760025384623,6.15208411202769,0.456355525651462));
#32954=CARTESIAN_POINT('Ctrl Pts',(-23.2367438943793,5.18019646906645,3.34991997354075));
#32955=CARTESIAN_POINT('Ctrl Pts',(-23.0974852502966,2.94005050347398,5.42332945009597));
#32956=CARTESIAN_POINT('Ctrl Pts',(-22.9582266062137,-0.0199028173517082,
6.16895478708649));
#32957=CARTESIAN_POINT('Ctrl Pts',(-22.8189679621309,-2.97498336667136,
5.40424585444488));
#32958=CARTESIAN_POINT('Ctrl Pts',(-22.679709318048,-5.2017040097594,3.31642498514721));
#32959=CARTESIAN_POINT('Ctrl Pts',(-22.5404506739652,-6.15490067713796,
0.416649663173528));
#32960=CARTESIAN_POINT('Ctrl Pts',(-22.4011920298824,-5.60120391772031,
-2.58513325756536));
#32961=CARTESIAN_POINT('Ctrl Pts',(-22.2619333857995,-3.67617432800871,
-4.9540025835021));
#32962=CARTESIAN_POINT('Ctrl Pts',(-22.1226747417167,-0.851113491455105,
-6.10999223501298));
#32963=CARTESIAN_POINT('Ctrl Pts',(-21.9834160976338,2.18232395310707,-5.770083314039));
#32964=CARTESIAN_POINT('Ctrl Pts',(-21.8441574535511,4.68146689113202,-4.01749511941093));
#32965=CARTESIAN_POINT('Ctrl Pts',(-21.7048988094681,6.03445458538273,-1.28131071337479));
#32966=CARTESIAN_POINT('Ctrl Pts',(-21.5656401653854,5.91003745606096,1.76857472423761));
#32967=CARTESIAN_POINT('Ctrl Pts',(-21.4263815213025,4.33867632848147,4.38546314588668));
#32968=CARTESIAN_POINT('Ctrl Pts',(-21.2871228772197,1.70508476318431,5.92866639621531));
#32969=CARTESIAN_POINT('Ctrl Pts',(-21.1478642331368,-1.34595968341069,
6.02036475787713));
#32970=CARTESIAN_POINT('Ctrl Pts',(-21.008605589054,-4.06747520564821,4.63810788346854));
#32971=CARTESIAN_POINT('Ctrl Pts',(-20.8693469449712,-5.79315798052477,
2.12031127430337));
#32972=CARTESIAN_POINT('Ctrl Pts',(-20.7300883008883,-6.10051215203808,
-0.91659738712893));
#32973=CARTESIAN_POINT('Ctrl Pts',(-20.5908296568055,-4.9142887429833,-3.72909713440716));
#32974=CARTESIAN_POINT('Ctrl Pts',(-20.4515710127226,-2.52490872870708,
-5.62860863792773));
#32975=CARTESIAN_POINT('Ctrl Pts',(-20.3123123686398,0.482640215683851,
-6.15007786206487));
#32976=CARTESIAN_POINT('Ctrl Pts',(-20.173053724557,3.37202521126839,-5.16583442067456));
#32977=CARTESIAN_POINT('Ctrl Pts',(-20.0337950804741,5.43584324933477,-2.91684889151244));
#32978=CARTESIAN_POINT('Ctrl Pts',(-19.8945364363913,6.16881341654233,0.0462635833377749));
#32979=CARTESIAN_POINT('Ctrl Pts',(-19.7552777923085,5.39148392561755,2.99804942705481));
#32980=CARTESIAN_POINT('Ctrl Pts',(-19.6160191482256,3.29416697845835,5.2158281418477));
#32981=CARTESIAN_POINT('Ctrl Pts',(-19.4767605041428,0.390344966961397,
6.15662489469869));
#32982=CARTESIAN_POINT('Ctrl Pts',(-19.33750186006,-2.60904451113693,5.59010608362329));
#32983=CARTESIAN_POINT('Ctrl Pts',(-19.1982432159771,-4.96966624459001,
3.65497150531144));
#32984=CARTESIAN_POINT('Ctrl Pts',(-19.0589845718943,-6.11357339722781,
0.824996729668839));
#32985=CARTESIAN_POINT('Ctrl Pts',(-18.9197259278114,-5.76070520778121,
-2.20696053347091));
#32986=CARTESIAN_POINT('Ctrl Pts',(-18.7804672837286,-3.99745376981848,
-4.69859155975702));
#32987=CARTESIAN_POINT('Ctrl Pts',(-18.6412086396458,-1.25551280855669,
-6.03987473999303));
#32988=CARTESIAN_POINT('Ctrl Pts',(-18.5019499955629,1.7938131289566,-5.90242608980737));
#32989=CARTESIAN_POINT('Ctrl Pts',(-18.3626913514801,4.40396297659968,-4.31989691867704));
#32990=CARTESIAN_POINT('Ctrl Pts',(-18.2234327073972,5.93589837214893,-1.67973503945581));
#32991=CARTESIAN_POINT('Ctrl Pts',(-18.0841740633144,6.01455828717799,1.37167339312034));
#32992=CARTESIAN_POINT('Ctrl Pts',(-17.9449154192316,4.6206845540694,4.08725745935344));
#32993=CARTESIAN_POINT('Ctrl Pts',(-17.8056567751487,2.09553680906827,5.80216552410355));
#32994=CARTESIAN_POINT('Ctrl Pts',(-17.6663981310659,-0.94265749977486,
6.09653968455664));
#32995=CARTESIAN_POINT('Ctrl Pts',(-17.527139486983,-3.75006264326115,4.89830883661627));
#32996=CARTESIAN_POINT('Ctrl Pts',(-17.3878808429002,-5.63934659460633,
2.50083371561525));
#32997=CARTESIAN_POINT('Ctrl Pts',(-17.2486221988174,-6.14795931166126,
-0.508916092704237));
#32998=CARTESIAN_POINT('Ctrl Pts',(-17.1093635547345,-5.15137804413015,
-3.39406887580522));
#32999=CARTESIAN_POINT('Ctrl Pts',(-16.9701049106517,-2.89359401788095,
-5.44825779005909));
#33000=CARTESIAN_POINT('Ctrl Pts',(-16.8308462665689,0.0726235045509067,
-6.16855940344605));
#33001=CARTESIAN_POINT('Ctrl Pts',(-16.691587622486,3.02106074304649,-5.37862354827693));
#33002=CARTESIAN_POINT('Ctrl Pts',(-16.5523289784032,5.2298570328979,-3.27184882027028));
#33003=CARTESIAN_POINT('Ctrl Pts',(-16.4130703343204,6.15823669226976,-0.364033143049074));
#33004=CARTESIAN_POINT('Ctrl Pts',(-16.2738116902375,5.57890617417189,2.63290812354753));
#33005=CARTESIAN_POINT('Ctrl Pts',(-16.1345530461547,3.63370194282318,4.98523915955686));
#33006=CARTESIAN_POINT('Ctrl Pts',(-15.9952944020718,0.798864903439737,
6.11704292557344));
#33007=CARTESIAN_POINT('Ctrl Pts',(-15.856035757989,-2.23155681472863,5.75122191102848));
#33008=CARTESIAN_POINT('Ctrl Pts',(-15.7167771139061,-4.71563043208565,
3.9773394267077));
#33009=CARTESIAN_POINT('Ctrl Pts',(-15.5775184698233,-6.0451846064719,1.22969197807065));
#33010=CARTESIAN_POINT('Ctrl Pts',(-15.4382598257405,-5.89470694523501,
-1.81901877864247));
#33011=CARTESIAN_POINT('Ctrl Pts',(-15.2990011816577,-4.30103862754144,
-4.42238239093502));
#33012=CARTESIAN_POINT('Ctrl Pts',(-15.1597425375748,-1.65435464376045,
-5.9430219585598));
#33013=CARTESIAN_POINT('Ctrl Pts',(-15.020483893492,1.39736205606941,-6.00864199062594));
#33014=CARTESIAN_POINT('Ctrl Pts',(-14.8812252494091,4.10696507972471,-4.60317685095605));
#33015=CARTESIAN_POINT('Ctrl Pts',(-14.7419666053263,5.81106712012186,-2.07072407932459));
#33016=CARTESIAN_POINT('Ctrl Pts',(-14.6027079612435,6.09245589424167,0.968700399491914));
#33017=CARTESIAN_POINT('Ctrl Pts',(-14.4634493171606,4.88223948711466,3.77095967595971));
#33018=CARTESIAN_POINT('Ctrl Pts',(-14.3241906730778,2.47671303729191,5.64998157679864));
#33019=CARTESIAN_POINT('Ctrl Pts',(-14.1849320289949,-0.53518267691531,
6.14572849950156));
#33020=CARTESIAN_POINT('Ctrl Pts',(-14.0456733849121,-3.41605056463389,
5.13682760340662));
#33021=CARTESIAN_POINT('Ctrl Pts',(-13.9064147408293,-5.46057284557919,
2.87028630721381));
#33022=CARTESIAN_POINT('Ctrl Pts',(-13.7671560967464,-6.16819275243593,
-0.0989820996583846));
#33023=CARTESIAN_POINT('Ctrl Pts',(-13.6278974526636,-5.36566495725375,
-3.04401689445949));
#33024=CARTESIAN_POINT('Ctrl Pts',(-13.4886388085808,-3.24947091811263,
-5.24379042674249));
#33025=CARTESIAN_POINT('Ctrl Pts',(-13.3493801644979,-0.337714671890257,
-6.15973604041975));
#33026=CARTESIAN_POINT('Ctrl Pts',(-13.2101215204151,2.65672365904785,-5.56760439387636));
#33027=CARTESIAN_POINT('Ctrl Pts',(-13.0708628763323,5.00072104404122,-3.61236602892606));
#33028=CARTESIAN_POINT('Ctrl Pts',(-12.9316042322494,6.12040075669628,-0.772718489935025));
#33029=CARTESIAN_POINT('Ctrl Pts',(-12.7923455881666,5.74163359694582,2.25611234775199));
#33030=CARTESIAN_POINT('Ctrl Pts',(-12.6530869440838,3.95715245736665,4.73258319698796));
#33031=CARTESIAN_POINT('Ctrl Pts',(-12.5138283000009,1.20384869340539,6.05038408786103));
#33032=CARTESIAN_POINT('Ctrl Pts',(-12.3745696559181,-1.84419121303957,
5.88688016329563));
#33033=CARTESIAN_POINT('Ctrl Pts',(-12.2353110118352,-4.4407210525541,4.28210179942731));
#33034=CARTESIAN_POINT('Ctrl Pts',(-12.0960523677524,-5.95003702537131,
1.62894403954418));
#33035=CARTESIAN_POINT('Ctrl Pts',(-11.9567937236695,-6.00261597625248,
-1.42302520318319));
#33036=CARTESIAN_POINT('Ctrl Pts',(-11.8175350795867,-4.58558509381898,
-4.12659770690106));
#33037=CARTESIAN_POINT('Ctrl Pts',(-11.6782764355039,-2.04587353815267,
-5.81986260603654));
#33038=CARTESIAN_POINT('Ctrl Pts',(-11.539017791421,0.994725610736604,-6.08826085566316));
#33039=CARTESIAN_POINT('Ctrl Pts',(-11.3997591473382,3.7917878509228,-4.86608098790496));
#33040=CARTESIAN_POINT('Ctrl Pts',(-11.2605005032553,5.66051339030982,-2.45254713418094));
#33041=CARTESIAN_POINT('Ctrl Pts',(-11.1212418591725,6.1433854663204,0.561439488688986));
#33042=CARTESIAN_POINT('Ctrl Pts',(-10.9819832150897,5.12218336419516,3.43796987636866));
#33043=CARTESIAN_POINT('Ctrl Pts',(-10.8427245710069,2.84692618510974,5.47278819102222));
#33044=CARTESIAN_POINT('Ctrl Pts',(-10.703465926924,-0.125338887352521,
6.16771347020701));
#33045=CARTESIAN_POINT('Ctrl Pts',(-10.5642072828412,-3.06691746211474,
5.35260838917175));
#33046=CARTESIAN_POINT('Ctrl Pts',(-10.4249486387583,-5.2576280689577,3.22703368060576));
#33047=CARTESIAN_POINT('Ctrl Pts',(-10.2856899946755,-6.16112291177051,
0.311390034060484));
#33048=CARTESIAN_POINT('Ctrl Pts',(-10.1464313505927,-5.55620094910737,
-2.68049068276575));
#33049=CARTESIAN_POINT('Ctrl Pts',(-10.0071727065098,-3.59096415321422,
-5.01611161534373));
#33050=CARTESIAN_POINT('Ctrl Pts',(-9.86791406242698,-0.746557966588395,
-6.12364682928231));
#33051=CARTESIAN_POINT('Ctrl Pts',(-9.72865541834415,2.28062668415683,-5.73194044061589));
#33052=CARTESIAN_POINT('Ctrl Pts',(-9.58939677426131,4.74944954490643,-3.93689323040948));
#33053=CARTESIAN_POINT('Ctrl Pts',(-9.45013813017848,6.05547308921799,-1.17798342645918));
#33054=CARTESIAN_POINT('Ctrl Pts',(-9.31087948609562,5.87894588690616,1.86932997249951));
#33055=CARTESIAN_POINT('Ctrl Pts',(-9.17162084201281,4.26308678012096,4.45897862659307));
#33056=CARTESIAN_POINT('Ctrl Pts',(-9.03236219792997,1.60350369080462,5.95694344448826));
#33057=CARTESIAN_POINT('Ctrl Pts',(-8.89310355384712,-1.44866236585221,
5.99648035409267));
#33058=CARTESIAN_POINT('Ctrl Pts',(-8.7538449097643,-4.14615498239031,4.56790960388402));
#33059=CARTESIAN_POINT('Ctrl Pts',(-8.61458626568144,-5.82855182124194,
2.02098563932378));
#33060=CARTESIAN_POINT('Ctrl Pts',(-8.47532762159861,-6.08395464542259,
-1.02073265828857));
#33061=CARTESIAN_POINT('Ctrl Pts',(-8.33606897751578,-4.84983363404122,
-3.81254678782812));
#33062=CARTESIAN_POINT('Ctrl Pts',(-8.19681033343293,-2.42833644755147,
-5.67094184282902));
#33063=CARTESIAN_POINT('Ctrl Pts',(-8.05755168935011,0.587686048575971,
-6.14093025490153));
#33064=CARTESIAN_POINT('Ctrl Pts',(-7.91829304526725,3.45982641076282,-5.10744559389954));
#33065=CARTESIAN_POINT('Ctrl Pts',(-7.77903440118443,5.48490360333593,-2.82351407812473));
#33066=CARTESIAN_POINT('Ctrl Pts',(-7.63977575710159,6.16712156551101,0.151693386358204));
#33067=CARTESIAN_POINT('Ctrl Pts',(-7.50051711301874,5.33945408244398,3.08976202784748));
#33068=CARTESIAN_POINT('Ctrl Pts',(-7.36125846893593,3.20453751745409,5.27136970686795));
#33069=CARTESIAN_POINT('Ctrl Pts',(-7.22199982485307,0.2850597102479,6.1623972809978));
#33070=CARTESIAN_POINT('Ctrl Pts',(-7.08274118077024,-2.70420876071548,
5.54469604809187));
#33071=CARTESIAN_POINT('Ctrl Pts',(-6.94348253668739,-5.0314105924327,3.56949670648567));
#33072=CARTESIAN_POINT('Ctrl Pts',(-6.80422389260456,-6.12678108405827,
0.720383811090751));
#33073=CARTESIAN_POINT('Ctrl Pts',(-6.66496524852172,-5.72214261903566,
-2.30509937631144));
#33074=CARTESIAN_POINT('Ctrl Pts',(-6.52570660443889,-3.91656211576974,
-4.76622916786142));
#33075=CARTESIAN_POINT('Ctrl Pts',(-6.38644796035605,-1.15209664953208,
-6.06045151761753));
#33076=CARTESIAN_POINT('Ctrl Pts',(-6.24718931627322,1.89443459798825,-5.87090426094661));
#33077=CARTESIAN_POINT('Ctrl Pts',(-6.10793067219037,4.47715477966845,-4.24399391683683));
#33078=CARTESIAN_POINT('Ctrl Pts',(-5.96867202810754,5.96374108979948,-1.57803406208271));
#33079=CARTESIAN_POINT('Ctrl Pts',(-5.82941338402469,5.99023523618298,1.47427307594201));
#33080=CARTESIAN_POINT('Ctrl Pts',(-5.69015473994186,4.55015070390546,4.16563654907681));
#33081=CARTESIAN_POINT('Ctrl Pts',(-5.55089609585903,1.99606083729069,5.8371346070731));
#33082=CARTESIAN_POINT('Ctrl Pts',(-5.41163745177617,-1.0467210672592,6.07953734215126));
#33083=CARTESIAN_POINT('Ctrl Pts',(-5.27237880769334,-3.83323610761724,
4.83349772220027));
#33084=CARTESIAN_POINT('Ctrl Pts',(-5.13312016361051,-5.6812667439325,2.4040814194911));
#33085=CARTESIAN_POINT('Ctrl Pts',(-4.99386151952768,-6.1383629100772,-0.613921877313705));
#33086=CARTESIAN_POINT('Ctrl Pts',(-4.85460287544483,-5.09261456163162,
-3.4816197687159));
#33087=CARTESIAN_POINT('Ctrl Pts',(-4.71534423136201,-2.80005041376394,
-5.49691886129279));
#33088=CARTESIAN_POINT('Ctrl Pts',(-4.57608558727915,0.178045115442175,
-6.16641704915611));
#33089=CARTESIAN_POINT('Ctrl Pts',(-4.43682694319632,3.11255017451608,-5.32620227726806));
#33090=CARTESIAN_POINT('Ctrl Pts',(-4.29756829911348,5.28501508955106,-3.18198283943735));
#33091=CARTESIAN_POINT('Ctrl Pts',(-4.15830965503065,6.16355912483164,-0.258724181243916));
#33092=CARTESIAN_POINT('Ctrl Pts',(-4.01905101094781,5.53308990090931,2.72787745980472));
#33093=CARTESIAN_POINT('Ctrl Pts',(-3.87979236686497,3.54796408073617,5.04661769594891));
#33094=CARTESIAN_POINT('Ctrl Pts',(-3.74053372278214,0.694196501382891,
6.12980346379193));
#33095=CARTESIAN_POINT('Ctrl Pts',(-3.60127507869929,-2.32952997734448,
5.71224031111489));
#33096=CARTESIAN_POINT('Ctrl Pts',(-3.46201643461646,-4.78292175945639,
3.89615948469104));
#33097=CARTESIAN_POINT('Ctrl Pts',(-3.32275779053362,-6.06531928215492,
1.12618883532147));
#33098=CARTESIAN_POINT('Ctrl Pts',(-3.18349914645078,-5.86275543225447,
-1.91950463110544));
#33099=CARTESIAN_POINT('Ctrl Pts',(-3.04424050236794,-4.22482355821538,
-4.49524917986447));
#33100=CARTESIAN_POINT('Ctrl Pts',(-2.90498185828511,-1.55253561844441,
-5.97042983721744));
#33101=CARTESIAN_POINT('Ctrl Pts',(-2.76572321420226,1.4998568657823,-5.98388073648606));
#33102=CARTESIAN_POINT('Ctrl Pts',(-2.62646457011943,4.18504205126321,-4.53230871830385));
#33103=CARTESIAN_POINT('Ctrl Pts',(-2.4872059260366,5.84561080673752,-1.97109958690181));
#33104=CARTESIAN_POINT('Ctrl Pts',(-2.34794728195376,6.07500902664705,1.07269036255581));
#33105=CARTESIAN_POINT('Ctrl Pts',(-2.20868863787092,4.81707355040727,3.85385543356388));
#33106=CARTESIAN_POINT('Ctrl Pts',(-2.06942999378809,2.37978249342083,5.69148790301832));
#33107=CARTESIAN_POINT('Ctrl Pts',(-1.93017134970525,-0.640146496858891,
6.13568348276358));
#33108=CARTESIAN_POINT('Ctrl Pts',(-1.7909127056224,-3.50334955028659,5.07769053033222));
#33109=CARTESIAN_POINT('Ctrl Pts',(-1.65165406153957,-5.50883374938536,
2.77653563583237));
#33110=CARTESIAN_POINT('Ctrl Pts',(-1.51239541745673,-6.16559992641659,
-0.204393623380619));
#33111=CARTESIAN_POINT('Ctrl Pts',(-1.37313677337389,-5.3128532304277,-3.13528142757007));
#33112=CARTESIAN_POINT('Ctrl Pts',(-1.23387812929106,-3.159370029524,-5.29856408183426));
#33113=CARTESIAN_POINT('Ctrl Pts',(-1.09461948520822,-0.232383984270165,
-6.16460819970066));
#33114=CARTESIAN_POINT('Ctrl Pts',(-0.955360841125374,2.75149645773078,
-5.52138315322195));
#33115=CARTESIAN_POINT('Ctrl Pts',(-0.816102197042544,5.06173243386037,
-3.52636582309806));
#33116=CARTESIAN_POINT('Ctrl Pts',(-0.676843552959711,6.13271433141243,
-0.66799816598022));
#33117=CARTESIAN_POINT('Ctrl Pts',(-0.537584908876864,5.70223288207738,
2.35392126034556));
#33118=CARTESIAN_POINT('Ctrl Pts',(-0.398326264794022,3.87568730064295,
4.7995207354176));
#33119=CARTESIAN_POINT('Ctrl Pts',(-0.259067620711194,1.10025735360832,
6.07008854307166));
#33120=CARTESIAN_POINT('Ctrl Pts',(-0.119808976628351,-1.9445335606143,
5.85447565379037));
#33121=CARTESIAN_POINT('Ctrl Pts',(0.0194496674544829,-4.51327330568083,
4.20562269082728));
#33122=CARTESIAN_POINT('Ctrl Pts',(0.158708311537311,-5.97698652079983,
1.52691759668036));
#33123=CARTESIAN_POINT('Ctrl Pts',(0.297966955620161,-5.97746201560441,
-1.52523260608557));
#33124=CARTESIAN_POINT('Ctrl Pts',(0.437225599703,-4.51429511200085,-4.20475193064767));
#33125=CARTESIAN_POINT('Ctrl Pts',(0.530064695758222,-2.80228789376692,
-5.30353925874901));
#33126=CARTESIAN_POINT('Ctrl Pts',(0.576484243785833,-1.8665303149515,-5.61462333072015));
#33127=CARTESIAN_POINT('',(-8.88178419700125E-15,-4.03672702691112,4.32582540941094));
#33128=CARTESIAN_POINT('Ctrl Pts',(-1.02140518265514E-14,-4.03701234814588,
4.32595897371309));
#33129=CARTESIAN_POINT('Ctrl Pts',(-9.9843844026724E-15,-4.1299458592561,
4.22407952174816));
#33130=CARTESIAN_POINT('Ctrl Pts',(-5.92110397111577E-15,-4.21916354543406,
4.11905201329014));
#33131=CARTESIAN_POINT('Ctrl Pts',(-3.33066907387547E-15,-4.30445389140253,
4.01101265725413));
#33132=CARTESIAN_POINT('Ctrl Pts',(-9.4273941981131E-17,-4.40735712598554,
3.88066262675386));
#33133=CARTESIAN_POINT('Ctrl Pts',(-1.51545993841484E-15,-4.50454492550802,
3.74592848472362));
#33134=CARTESIAN_POINT('Ctrl Pts',(3.33066907387547E-16,-4.59581941741086,
3.60722779298289));
#33135=CARTESIAN_POINT('Ctrl Pts',(2.17437774338676E-15,-4.68673760524928,
3.46906854079636));
#33136=CARTESIAN_POINT('Ctrl Pts',(8.54816426306082E-15,-4.77178878425916,
3.3269729018291));
#33137=CARTESIAN_POINT('Ctrl Pts',(6.10622663543836E-15,-4.85072810092883,
3.18133880832367));
#33138=CARTESIAN_POINT('Ctrl Pts',(5.53956788225534E-15,-4.86904619974314,
3.14754399189869));
#33139=CARTESIAN_POINT('Ctrl Pts',(1.2664160508966E-15,-4.88703496548394,
3.11355859884732));
#33140=CARTESIAN_POINT('Ctrl Pts',(2.22044604925031E-16,-4.90469093726253,
3.07938755292361));
#33141=CARTESIAN_POINT('Ctrl Pts',(-4.42079666650615E-16,-4.91591851289345,
3.05765790771874));
#33142=CARTESIAN_POINT('Ctrl Pts',(1.71356643288325E-14,-4.92701076494171,
3.03585452116636));
#33143=CARTESIAN_POINT('Ctrl Pts',(1.69864122767649E-14,-4.9379615767523,
3.01398949575384));
#33144=CARTESIAN_POINT('Ctrl Pts',(1.5989203206649E-14,-5.01112806733903,
2.86790104097132));
#33145=CARTESIAN_POINT('Ctrl Pts',(9.31012957414554E-15,-5.07805250460248,
2.71893170034809));
#33146=CARTESIAN_POINT('Ctrl Pts',(4.55191440096314E-15,-5.13854422193342,
2.56748287243489));
#33147=CARTESIAN_POINT('Ctrl Pts',(-1.71363691774166E-16,-5.19859178028505,
2.41714605389738));
#33148=CARTESIAN_POINT('Ctrl Pts',(-4.82591573396116E-15,-5.25230089977517,
2.26436530798515));
#33149=CARTESIAN_POINT('Ctrl Pts',(-4.05231403988182E-15,-5.29943494362445,
2.10952414416537));
#33150=CARTESIAN_POINT('Ctrl Pts',(-3.46892256503307E-15,-5.33497984944261,
1.99275473218054));
#33151=CARTESIAN_POINT('Ctrl Pts',(7.69623986356005E-15,-5.36678449339774,
1.87481330294842));
#33152=CARTESIAN_POINT('Ctrl Pts',(9.6034291630076E-15,-5.39472742260068,
1.75586454471506));
#33153=CARTESIAN_POINT('Ctrl Pts',(1.01947903236083E-14,-5.40339167163397,
1.71898216720734));
#33154=CARTESIAN_POINT('Ctrl Pts',(6.937645723431E-15,-5.41168451537563,
1.68200295496824));
#33155=CARTESIAN_POINT('Ctrl Pts',(7.04991620636974E-15,-5.41960198349953,
1.64493186461997));
#33156=CARTESIAN_POINT('Ctrl Pts',(7.11459518622115E-15,-5.42416323368618,
1.62357522445113));
#33157=CARTESIAN_POINT('Ctrl Pts',(-1.68019455085037E-14,-5.42859776171347,
1.60219807679196));
#33158=CARTESIAN_POINT('Ctrl Pts',(-1.63757896132211E-14,-5.43290502002547,
1.58080206259592));
#33159=CARTESIAN_POINT('Ctrl Pts',(-1.51559929927354E-14,-5.44523379264295,
1.51955971889707));
#33160=CARTESIAN_POINT('Ctrl Pts',(4.59923465264813E-15,-5.45652033974346,
1.45816097348265));
#33161=CARTESIAN_POINT('Ctrl Pts',(4.38538094726937E-15,-5.46675441513566,
1.39662819681779));
#33162=CARTESIAN_POINT('Ctrl Pts',(3.83850247844808E-15,-5.49288327644095,
1.23952740113381));
#33163=CARTESIAN_POINT('Ctrl Pts',(2.01620486307756E-14,-5.51215540965326,
1.08155306540347));
#33164=CARTESIAN_POINT('Ctrl Pts',(1.94844140821715E-14,-5.52463713258762,
0.923142281064311));
#33165=CARTESIAN_POINT('Ctrl Pts',(1.88042532098635E-14,-5.53716538926583,
0.764140917451617));
#33166=CARTESIAN_POINT('Ctrl Pts',(4.56756685228552E-15,-5.54285239098084,
0.604699060344447));
#33167=CARTESIAN_POINT('Ctrl Pts',(2.66453525910038E-15,-5.54171302337198,
0.445262773869298));
#33168=CARTESIAN_POINT('Ctrl Pts',(7.86960708762468E-16,-5.54058889719691,
0.287959282451643));
#33169=CARTESIAN_POINT('Ctrl Pts',(4.79544066007618E-15,-5.53281957145188,
0.130660511512922));
#33170=CARTESIAN_POINT('Ctrl Pts',(4.71844785465692E-15,-5.51837155975906,
-0.0261901709885422));
#33171=CARTESIAN_POINT('Ctrl Pts',(4.66374349800356E-15,-5.50810606572656,
-0.137634553748184));
#33172=CARTESIAN_POINT('Ctrl Pts',(-4.94803098190201E-15,-5.4944679918248,
-0.248852439276699));
#33173=CARTESIAN_POINT('Ctrl Pts',(-6.82787160144471E-15,-5.47743131033041,
-0.359677207278218));
#33174=CARTESIAN_POINT('Ctrl Pts',(-7.48657969095659E-15,-5.47146154895696,
-0.398510909689988));
#33175=CARTESIAN_POINT('Ctrl Pts',(1.73538460866958E-14,-5.46507438832126,
-0.437296275458263));
#33176=CARTESIAN_POINT('Ctrl Pts',(1.80966353013901E-14,-5.45826837936944,
-0.476025900372521));
#33177=CARTESIAN_POINT('Ctrl Pts',(1.85346830350253E-14,-5.45425464742845,
-0.498866060249126));
#33178=CARTESIAN_POINT('Ctrl Pts',(-7.23173250167379E-15,-5.45009491258204,
-0.521688207844201));
#33179=CARTESIAN_POINT('Ctrl Pts',(-6.77236045021345E-15,-5.44579287453235,
-0.544470609171142));
#33180=CARTESIAN_POINT('Ctrl Pts',(-3.69376219740839E-15,-5.41696167598384,
-0.697152646959159));
#33181=CARTESIAN_POINT('Ctrl Pts',(-6.13749631345723E-15,-5.38170771746027,
-0.848259769607838));
#33182=CARTESIAN_POINT('Ctrl Pts',(-3.83026943495679E-15,-5.34006209286253,
-0.997382404033546));
#33183=CARTESIAN_POINT('Ctrl Pts',(-2.06755517157137E-15,-5.30824496331619,
-1.11131163966496));
#33184=CARTESIAN_POINT('Ctrl Pts',(-6.3369974246489E-15,-5.27269602122346,
-1.22408245652815));
#33185=CARTESIAN_POINT('Ctrl Pts',(-4.27435864480685E-15,-5.23340997239925,
-1.33550483482684));
#33186=CARTESIAN_POINT('Ctrl Pts',(-1.56325154693959E-15,-5.18177287197461,
-1.48195704139786));
#33187=CARTESIAN_POINT('Ctrl Pts',(1.51022923062233E-14,-5.12368063549572,
-1.62608107617323));
#33188=CARTESIAN_POINT('Ctrl Pts',(1.29340982368831E-14,-5.05935921644069,
-1.76748797034581));
#33189=CARTESIAN_POINT('Ctrl Pts',(1.07809790568834E-14,-4.9954850074801,
-1.90791169916812));
#33190=CARTESIAN_POINT('Ctrl Pts',(4.29962680979437E-15,-4.92546739796093,
-2.04565651048916));
#33191=CARTESIAN_POINT('Ctrl Pts',(6.41153796721028E-15,-4.84949146114621,
-2.18030540628267));
#33192=CARTESIAN_POINT('Ctrl Pts',(7.393084765491E-15,-4.81418034625153,
-2.24288578145331));
#33193=CARTESIAN_POINT('Ctrl Pts',(1.40120518047632E-14,-4.77758171885201,
-2.30479684864787));
#33194=CARTESIAN_POINT('Ctrl Pts',(1.40998324127395E-14,-4.73971195737352,
-2.36599353753954));
#33195=CARTESIAN_POINT('Ctrl Pts',(1.41270155954857E-14,-4.72798475850173,
-2.38494442904003));
#33196=CARTESIAN_POINT('Ctrl Pts',(1.3925834722576E-14,-4.71613565303999,
-2.40382679808695));
#33197=CARTESIAN_POINT('Ctrl Pts',(1.42663658664333E-14,-4.70416510366087,
-2.42263926232305));
#33198=CARTESIAN_POINT('Ctrl Pts',(1.45308547402812E-14,-4.69486763650776,
-2.43725081128081));
#33199=CARTESIAN_POINT('Ctrl Pts',(-1.62837640444609E-16,-4.68549762532919,
-2.45181900290397));
#33200=CARTESIAN_POINT('Ctrl Pts',(2.77555756156289E-17,-4.67606063554748,
-2.46633519301188));
#33201=CARTESIAN_POINT('Ctrl Pts',(1.69856282096252E-15,-4.59333266008503,
-2.59358922706657));
#33202=CARTESIAN_POINT('Ctrl Pts',(-4.00822838861647E-15,-4.50535159703235,
-2.71702212155416));
#33203=CARTESIAN_POINT('Ctrl Pts',(-2.08166817117217E-15,-4.41235800541746,
-2.83629106116441));
#33204=CARTESIAN_POINT('Ctrl Pts',(-9.83010432275142E-17,-4.31662238757981,
-2.95907678676274));
#33205=CARTESIAN_POINT('Ctrl Pts',(5.58857198077528E-15,-4.21557390510044,
-3.07745022281706));
#33206=CARTESIAN_POINT('Ctrl Pts',(3.91353616180368E-15,-4.10943425467638,
-3.19099631382378));
#33207=CARTESIAN_POINT('Ctrl Pts',(2.23850034283208E-15,-4.00329460425232,
-3.3045424048305));
#33208=CARTESIAN_POINT('Ctrl Pts',(3.87429654806338E-15,-3.89206320923292,
-3.41326181578148));
#33209=CARTESIAN_POINT('Ctrl Pts',(3.13638004456607E-15,-3.77592911856888,
-3.51668791312134));
#33210=CARTESIAN_POINT('Ctrl Pts',(2.66650929863803E-15,-3.69724273478636,
-3.58676402550038));
#33211=CARTESIAN_POINT('Ctrl Pts',(8.72292990203801E-15,-3.61630486923059,
-3.65440893269852));
#33212=CARTESIAN_POINT('Ctrl Pts',(8.90953977261688E-15,-3.5332392463504,
-3.71953115971285));
#33213=CARTESIAN_POINT('Ctrl Pts',(9.00727170106557E-15,-3.48973584812881,
-3.75363718428294));
#33214=CARTESIAN_POINT('Ctrl Pts',(1.35643768055353E-14,-3.44564878417463,
-3.78705107374077));
#33215=CARTESIAN_POINT('Ctrl Pts',(1.31838984174237E-14,-3.40099558655679,
-3.81975833303289));
#33216=CARTESIAN_POINT('Ctrl Pts',(1.29459073673587E-14,-3.37306479804978,
-3.84021688002767));
#33217=CARTESIAN_POINT('Ctrl Pts',(-1.02962754854352E-14,-3.34491250359703,
-3.86039893481383));
#33218=CARTESIAN_POINT('Ctrl Pts',(-1.092181900475E-14,-3.31654297785117,
-3.88030075778515));
#33219=CARTESIAN_POINT('Ctrl Pts',(-1.12805760383569E-14,-3.30027269994537,
-3.89171470222243));
#33220=CARTESIAN_POINT('Ctrl Pts',(-1.25188543466211E-14,-3.28393878107512,
-3.90303097900495));
#33221=CARTESIAN_POINT('Ctrl Pts',(-1.23095977855314E-14,-3.26754449164669,
-3.9142476194029));
#33222=CARTESIAN_POINT('Ctrl Pts',(-1.07581489276142E-14,-3.14599560697777,
-3.99740890163195));
#33223=CARTESIAN_POINT('Ctrl Pts',(-1.38744807549176E-15,-3.02108905880586,
-4.07512598255334));
#33224=CARTESIAN_POINT('Ctrl Pts',(-2.26207941267376E-15,-2.89320350651368,
-4.1472297958351));
#33225=CARTESIAN_POINT('Ctrl Pts',(-3.13634849819265E-15,-2.76537092139982,
-4.21930374541867));
#33226=CARTESIAN_POINT('Ctrl Pts',(2.21681871676629E-15,-2.63456105055413,
-4.2857693370254));
#33227=CARTESIAN_POINT('Ctrl Pts',(1.25593979660721E-15,-2.50113319349224,
-4.34640974797566));
#33228=CARTESIAN_POINT('Ctrl Pts',(3.04280062723563E-16,-2.3689855146534,
-4.40646834239041));
#33229=CARTESIAN_POINT('Ctrl Pts',(6.54382616372687E-15,-2.23426913139978,
-4.46081317271807));
#33230=CARTESIAN_POINT('Ctrl Pts',(4.03843625207401E-15,-2.09732548174527,
-4.50918342436963));
#33231=CARTESIAN_POINT('Ctrl Pts',(1.58747746198249E-15,-1.96335701627535,
-4.55650280284757));
#33232=CARTESIAN_POINT('Ctrl Pts',(4.96478138896302E-15,-1.82725639023716,
-4.59810443322033));
#33233=CARTESIAN_POINT('Ctrl Pts',(5.59968738045313E-15,-1.68934572884667,
-4.63369442980763));
#33234=CARTESIAN_POINT('Ctrl Pts',(5.81026669552682E-15,-1.64360489003554,
-4.64549856649129));
#33235=CARTESIAN_POINT('Ctrl Pts',(-8.97215586048935E-17,-1.59766499830972,
-4.65664097727771));
#33236=CARTESIAN_POINT('Ctrl Pts',(-2.77555756156289E-17,-1.55153804394499,
-4.66710967952236));
#33237=CARTESIAN_POINT('Ctrl Pts',(-1.52162519220488,-5.91720137462112,
-6.73836950611244E-5));
#33238=CARTESIAN_POINT('Ctrl Pts',(-1.51854860062216,-5.9172390196691,-0.0654090771404739));
#33239=CARTESIAN_POINT('Ctrl Pts',(-1.51547200903945,-5.91617931145235,
-0.13074954736745));
#33240=CARTESIAN_POINT('Ctrl Pts',(-1.51239541745673,-5.9140144475799,-0.196053380876696));
#33241=CARTESIAN_POINT('Ctrl Pts',(-1.46597586942912,-5.88135102775363,
-1.1813562247771));
#33242=CARTESIAN_POINT('Ctrl Pts',(-1.41955632140151,-5.59710212909066,
-2.15831882617359));
#33243=CARTESIAN_POINT('Ctrl Pts',(-1.3731367733739,-5.0960638129419,-3.00734723591585));
#33244=CARTESIAN_POINT('Ctrl Pts',(-1.32671722534628,-4.59502549679315,
-3.85637564565811));
#33245=CARTESIAN_POINT('Ctrl Pts',(-1.28029767731867,-3.87719776315859,
-4.57746986374617));
#33246=CARTESIAN_POINT('Ctrl Pts',(-1.23387812929106,-3.03045288879903,
-5.08235765910126));
#33247=CARTESIAN_POINT('Ctrl Pts',(-1.18745858126345,-2.18370801443943,
-5.58724545445638));
#33248=CARTESIAN_POINT('Ctrl Pts',(-1.14103903323584,-1.20804599935479,
-5.87592682707852));
#33249=CARTESIAN_POINT('Ctrl Pts',(-1.09461948520822,-0.222901584812313,
-5.91306333897647));
#33250=CARTESIAN_POINT('Ctrl Pts',(-1.04819993718061,0.762242829730162,
-5.95019985087442));
#33251=CARTESIAN_POINT('Ctrl Pts',(-1.00178038915299,1.75686964373051,-5.73579150204818));
#33252=CARTESIAN_POINT('Ctrl Pts',(-0.955360841125374,2.63922238008561,
-5.29608443928106));
#33253=CARTESIAN_POINT('Ctrl Pts',(-0.90894129309776,3.52157511644072,-4.85637737651394));
#33254=CARTESIAN_POINT('Ctrl Pts',(-0.862521745070147,4.29165377515062,
-4.19137159980593));
#33255=CARTESIAN_POINT('Ctrl Pts',(-0.816102197042535,4.85519008743088,
-3.38247410193227));
#33256=CARTESIAN_POINT('Ctrl Pts',(-0.769682649014926,5.41872639971112,
-2.57357660405865));
#33257=CARTESIAN_POINT('Ctrl Pts',(-0.723263100987323,5.77572036556173,
-1.62078738501953));
#33258=CARTESIAN_POINT('Ctrl Pts',(-0.676843552959712,5.88247044026457,
-0.640739537778962));
#33259=CARTESIAN_POINT('Ctrl Pts',(-0.630424004932098,5.98922051496742,
0.339308309461658));
#33260=CARTESIAN_POINT('Ctrl Pts',(-0.58400445690448,5.84572669852239,1.34661478490362));
#33261=CARTESIAN_POINT('Ctrl Pts',(-0.537584908876865,5.46955552672748,
2.2578679351366));
#33262=CARTESIAN_POINT('Ctrl Pts',(-0.49116536084925,5.09338435493256,3.16912108536958));
#33263=CARTESIAN_POINT('Ctrl Pts',(-0.444745812821634,4.48453582778773,
3.98432091039362));
#33264=CARTESIAN_POINT('Ctrl Pts',(-0.398326264794021,3.7175399063762,4.60368212418131));
#33265=CARTESIAN_POINT('Ctrl Pts',(-0.351906716766411,2.95054398496471,
5.22304333796897));
#33266=CARTESIAN_POINT('Ctrl Pts',(-0.305487168738803,2.02540066928651,
5.64656594052032));
#33267=CARTESIAN_POINT('Ctrl Pts',(-0.259067620711191,1.05536385907698,
5.82239176024911));
#33268=CARTESIAN_POINT('Ctrl Pts',(-0.21264807268358,0.085327048867453,
5.9982175799779));
#33269=CARTESIAN_POINT('Ctrl Pts',(-0.166228524655965,-0.929603255873433,
5.92634661688413));
#33270=CARTESIAN_POINT('Ctrl Pts',(-0.119808976628353,-1.86519169908829,
5.61560230817674));
#33271=CARTESIAN_POINT('Ctrl Pts',(-0.0798726510855764,-2.67011045056044,
5.34825834641043));
#33272=CARTESIAN_POINT('Ctrl Pts',(-0.0399363255428003,-3.41630234235058,
4.90410631410206));
#33273=CARTESIAN_POINT('Ctrl Pts',(-2.60208521396521E-14,-4.03701234814564,
4.32595897371332));
#33274=CARTESIAN_POINT('',(-59.58325,-2.85728527160914,-4.0034352877952));
#33275=CARTESIAN_POINT('Ctrl Pts',(-59.58325,-2.85728527160908,-4.00343528779524));
#33276=CARTESIAN_POINT('Ctrl Pts',(-59.58325,-2.95747118827891,-3.9459219613317));
#33277=CARTESIAN_POINT('Ctrl Pts',(-59.58325,-3.0554882232272,-3.88491300663017));
#33278=CARTESIAN_POINT('Ctrl Pts',(-59.58325,-3.15114152320849,-3.82051500336858));
#33279=CARTESIAN_POINT('Ctrl Pts',(-59.58325,-3.27116313425674,-3.7397111826822));
#33280=CARTESIAN_POINT('Ctrl Pts',(-59.58325,-3.38746433751411,-3.65357321571129));
#33281=CARTESIAN_POINT('Ctrl Pts',(-59.58325,-3.49982428652864,-3.56247863507039));
#33282=CARTESIAN_POINT('Ctrl Pts',(-59.58325,-3.57206065704153,-3.50391380003259));
#33283=CARTESIAN_POINT('Ctrl Pts',(-59.58325,-3.64266772742874,-3.443299223485));
#33284=CARTESIAN_POINT('Ctrl Pts',(-59.58325,-3.71158231514896,-3.38072490033225));
#33285=CARTESIAN_POINT('Ctrl Pts',(-59.58325,-3.74837014811767,-3.34732161338785));
#33286=CARTESIAN_POINT('Ctrl Pts',(-59.58325,-3.78467562111936,-3.31335974384355));
#33287=CARTESIAN_POINT('Ctrl Pts',(-59.58325,-3.82048860435084,-3.27885213139493));
#33288=CARTESIAN_POINT('Ctrl Pts',(-59.58325,-3.84234667310303,-3.25779078164642));
#33289=CARTESIAN_POINT('Ctrl Pts',(-59.58325,-3.86402127513146,-3.23652612382414));
#33290=CARTESIAN_POINT('Ctrl Pts',(-59.58325,-3.8855100329079,-3.21506097592997));
#33291=CARTESIAN_POINT('Ctrl Pts',(-59.58325,-3.90210456603726,-3.19848467535634));
#33292=CARTESIAN_POINT('Ctrl Pts',(-59.58325,-3.91858452173466,-3.18179249883958));
#33293=CARTESIAN_POINT('Ctrl Pts',(-59.58325,-3.93494336450657,-3.16499175093224));
#33294=CARTESIAN_POINT('Ctrl Pts',(-59.58325,-4.03888838843746,-3.05823883646053));
#33295=CARTESIAN_POINT('Ctrl Pts',(-59.58325,-4.1380152907603,-2.94703675275575));
#33296=CARTESIAN_POINT('Ctrl Pts',(-59.58325,-4.23209117418264,-2.83177988663891));
#33297=CARTESIAN_POINT('Ctrl Pts',(-59.58325,-4.32673851465113,-2.71582290115179));
#33298=CARTESIAN_POINT('Ctrl Pts',(-59.58325,-4.41627390021231,-2.59576123435737));
#33299=CARTESIAN_POINT('Ctrl Pts',(-59.58325,-4.50043285477973,-2.47195122881639));
#33300=CARTESIAN_POINT('Ctrl Pts',(-59.58325,-4.55927868770607,-2.38538048969394));
#33301=CARTESIAN_POINT('Ctrl Pts',(-59.58325,-4.61549536035516,-2.29697618702752));
#33302=CARTESIAN_POINT('Ctrl Pts',(-59.58325,-4.66898213393302,-2.20684909182908));
#33303=CARTESIAN_POINT('Ctrl Pts',(-59.58325,-4.68018502488076,-2.18797182645289));
#33304=CARTESIAN_POINT('Ctrl Pts',(-59.58325,-4.6912681217303,-2.16901895381225));
#33305=CARTESIAN_POINT('Ctrl Pts',(-59.58325,-4.70223044399627,-2.14999144802621));
#33306=CARTESIAN_POINT('Ctrl Pts',(-59.58325,-4.71373786468606,-2.13001780481038));
#33307=CARTESIAN_POINT('Ctrl Pts',(-59.58325,-4.72510830074832,-2.10996863045952));
#33308=CARTESIAN_POINT('Ctrl Pts',(-59.58325,-4.73633763714775,-2.08985117085674));
#33309=CARTESIAN_POINT('Ctrl Pts',(-59.58325,-4.76548431241845,-2.03763463361387));
#33310=CARTESIAN_POINT('Ctrl Pts',(-59.58325,-4.79368754177112,-1.98494582209745));
#33311=CARTESIAN_POINT('Ctrl Pts',(-59.58325,-4.82093354346874,-1.93180915190821));
#33312=CARTESIAN_POINT('Ctrl Pts',(-59.58325,-4.88897898047618,-1.79910315033508));
#33313=CARTESIAN_POINT('Ctrl Pts',(-59.58325,-4.95105661819981,-1.66360652146873));
#33314=CARTESIAN_POINT('Ctrl Pts',(-59.58325,-5.00718259483252,-1.52577115922053));
#33315=CARTESIAN_POINT('Ctrl Pts',(-59.58325,-5.06418821702403,-1.38577554477676));
#33316=CARTESIAN_POINT('Ctrl Pts',(-59.58325,-5.11505449397166,-1.24336673915174));
#33317=CARTESIAN_POINT('Ctrl Pts',(-59.58325,-5.15975833801014,-1.09898206153507));
#33318=CARTESIAN_POINT('Ctrl Pts',(-59.58325,-5.20488323012226,-0.953237480946295));
#33319=CARTESIAN_POINT('Ctrl Pts',(-59.58325,-5.24372938483295,-0.805478959672225));
#33320=CARTESIAN_POINT('Ctrl Pts',(-59.58325,-5.27622766283853,-0.656129274418985));
#33321=CARTESIAN_POINT('Ctrl Pts',(-59.58325,-5.29940736442347,-0.549604210679269));
#33322=CARTESIAN_POINT('Ctrl Pts',(-59.58325,-5.3193567154633,-0.442269066215297));
#33323=CARTESIAN_POINT('Ctrl Pts',(-59.58325,-5.33603533027086,-0.334271925679514));
#33324=CARTESIAN_POINT('Ctrl Pts',(-59.58325,-5.34099072117784,-0.302184845645285));
#33325=CARTESIAN_POINT('Ctrl Pts',(-59.58325,-5.34565730024493,-0.27003930767804));
#33326=CARTESIAN_POINT('Ctrl Pts',(-59.58325,-5.35003377981377,-0.237839152221993));
#33327=CARTESIAN_POINT('Ctrl Pts',(-59.58325,-5.352660372538,-0.218513872003155));
#33328=CARTESIAN_POINT('Ctrl Pts',(-59.58325,-5.35518231401894,-0.199169720534567));
#33329=CARTESIAN_POINT('Ctrl Pts',(-59.58325,-5.35759784303445,-0.17982062955677));
#33330=CARTESIAN_POINT('Ctrl Pts',(-59.58325,-5.37701026531633,-0.024321472883059));
#33331=CARTESIAN_POINT('Ctrl Pts',(-59.58325,-5.38958429037093,0.13171511776847));
#33332=CARTESIAN_POINT('Ctrl Pts',(-59.58325,-5.3953137326205,0.287821200437283));
#33333=CARTESIAN_POINT('Ctrl Pts',(-59.58325,-5.39967792196466,0.40672919756276));
#33334=CARTESIAN_POINT('Ctrl Pts',(-59.58325,-5.40006999862904,0.525678303322171));
#33335=CARTESIAN_POINT('Ctrl Pts',(-59.58325,-5.39646930124031,0.644471130262479));
#33336=CARTESIAN_POINT('Ctrl Pts',(-59.58325,-5.39177018485815,0.799502575255909));
#33337=CARTESIAN_POINT('Ctrl Pts',(-59.58325,-5.38027275281682,0.954267914689577));
#33338=CARTESIAN_POINT('Ctrl Pts',(-59.58325,-5.36216621021034,1.10837045744723));
#33339=CARTESIAN_POINT('Ctrl Pts',(-59.58325,-5.34390859252952,1.26375878146143));
#33340=CARTESIAN_POINT('Ctrl Pts',(-59.58325,-5.31893107268399,1.41847392843383));
#33341=CARTESIAN_POINT('Ctrl Pts',(-59.58325,-5.28737476637574,1.57211259015712));
#33342=CARTESIAN_POINT('Ctrl Pts',(-59.58325,-5.27183516770569,1.64777046722494));
#33343=CARTESIAN_POINT('Ctrl Pts',(-59.58325,-5.2546994281243,1.7231672826984));
#33344=CARTESIAN_POINT('Ctrl Pts',(-59.58325,-5.23597979923346,1.79825433423466));
#33345=CARTESIAN_POINT('Ctrl Pts',(-59.58325,-5.22958197362955,1.82391690819068));
#33346=CARTESIAN_POINT('Ctrl Pts',(-59.58325,-5.222999112305,1.8495432939777));
#33347=CARTESIAN_POINT('Ctrl Pts',(-59.58325,-5.21623162451923,1.87513152788836));
#33348=CARTESIAN_POINT('Ctrl Pts',(-59.58325,-5.21116093774669,1.89430406625579));
#33349=CARTESIAN_POINT('Ctrl Pts',(-59.58325,-5.20598907532358,1.91344580701779));
#33350=CARTESIAN_POINT('Ctrl Pts',(-59.58325,-5.20071683417188,1.93255481558272));
#33351=CARTESIAN_POINT('Ctrl Pts',(-59.58325,-5.15824206256221,2.08650277644576));
#33352=CARTESIAN_POINT('Ctrl Pts',(-59.58325,-5.10925020939434,2.23834978988568));
#33353=CARTESIAN_POINT('Ctrl Pts',(-59.58325,-5.05397150557403,2.3876831941389));
#33354=CARTESIAN_POINT('Ctrl Pts',(-59.58325,-4.99583927336141,2.5447253013737));
#33355=CARTESIAN_POINT('Ctrl Pts',(-59.58325,-4.93075469787697,2.69898843399027));
#33356=CARTESIAN_POINT('Ctrl Pts',(-59.58325,-4.85892433062117,2.84999610861345));
#33357=CARTESIAN_POINT('Ctrl Pts',(-59.58325,-4.78709396336536,3.00100378323664));
#33358=CARTESIAN_POINT('Ctrl Pts',(-59.58325,-4.70851762016637,3.14875695019248));
#33359=CARTESIAN_POINT('Ctrl Pts',(-59.58325,-4.62334187522332,3.2927687170727));
#33360=CARTESIAN_POINT('Ctrl Pts',(-59.58325,-4.56177409370411,3.39686507696254));
#33361=CARTESIAN_POINT('Ctrl Pts',(-59.58325,-4.49675694033257,3.49900642576255));
#33362=CARTESIAN_POINT('Ctrl Pts',(-59.58325,-4.42842615286909,3.59907504329026));
#33363=CARTESIAN_POINT('Ctrl Pts',(-59.58325,-4.39835351315343,3.64311562285131));
#33364=CARTESIAN_POINT('Ctrl Pts',(-59.58325,-4.36763885459402,3.68675462947469));
#33365=CARTESIAN_POINT('Ctrl Pts',(-59.58325,-4.33629285797398,3.72998149499838));
#33366=CARTESIAN_POINT('Ctrl Pts',(-59.58325,-4.3166147172816,3.75711811316934));
#33367=CARTESIAN_POINT('Ctrl Pts',(-59.58325,-4.2966877571498,3.78409230058656));
#33368=CARTESIAN_POINT('Ctrl Pts',(-59.58325,-4.27651451736783,3.81090136797568));
#33369=CARTESIAN_POINT('Ctrl Pts',(-59.58325,-4.26373058384259,3.82789047528221));
#33370=CARTESIAN_POINT('Ctrl Pts',(-59.58325,-4.25084725050488,3.84481382990744));
#33371=CARTESIAN_POINT('Ctrl Pts',(-59.58325,-4.23787521996861,3.86165791344566));
#33372=CARTESIAN_POINT('Ctrl Pts',(-59.58325,-4.13930729891155,3.98964761342608));
#33373=CARTESIAN_POINT('Ctrl Pts',(-59.58325,-4.03548977851738,4.11323945679425));
#33374=CARTESIAN_POINT('Ctrl Pts',(-59.58325,-3.92682461937095,4.23220103909675));
#33375=CARTESIAN_POINT('Ctrl Pts',(-59.58325,-3.81589473640299,4.35364193612537));
#33376=CARTESIAN_POINT('Ctrl Pts',(-59.58325,-3.69991275233022,4.47025816964232));
#33377=CARTESIAN_POINT('Ctrl Pts',(-59.58325,-3.57925525293198,4.58178425450939));
#33378=CARTESIAN_POINT('Ctrl Pts',(-59.58325,-3.45813211677665,4.69374073653162));
#33379=CARTESIAN_POINT('Ctrl Pts',(-59.58325,-3.33229684896289,4.80056830700697));
#33380=CARTESIAN_POINT('Ctrl Pts',(-59.58325,-3.20208544403337,4.9019710938485));
#33381=CARTESIAN_POINT('Ctrl Pts',(-59.58325,-3.07288444991452,5.00258701818661));
#33382=CARTESIAN_POINT('Ctrl Pts',(-59.58325,-2.9393744417493,5.09786256374746));
#33383=CARTESIAN_POINT('Ctrl Pts',(-59.58325,-2.80184697473418,5.18747342871888));
#33384=CARTESIAN_POINT('Ctrl Pts',(-59.58325,-2.730280444168,5.2341051223451));
#33385=CARTESIAN_POINT('Ctrl Pts',(-59.58325,-2.65762544766573,5.27920221586187));
#33386=CARTESIAN_POINT('Ctrl Pts',(-59.58325,-2.58391981634397,5.32271443393359));
#33387=CARTESIAN_POINT('Ctrl Pts',(-59.58325,-2.85728527160914,-4.0034352877952));
#33388=CARTESIAN_POINT('Ctrl Pts',(-59.5433136744572,-2.28297233951893,
-4.4125035738704));
#33389=CARTESIAN_POINT('Ctrl Pts',(-59.4569578008868,-0.848960315252899,
-5.02880402090236));
#33390=CARTESIAN_POINT('Ctrl Pts',(-59.3241823792888,1.56581406446455,-4.88302020893749));
#33391=CARTESIAN_POINT('Ctrl Pts',(-59.184923735206,3.71514791027481,-3.53457280157081));
#33392=CARTESIAN_POINT('Ctrl Pts',(-59.0456650911232,4.95490602150955,-1.32078475768876));
#33393=CARTESIAN_POINT('Ctrl Pts',(-58.9064064470403,4.98156463212109,1.21638024324112));
#33394=CARTESIAN_POINT('Ctrl Pts',(-58.7671478029575,3.78859490309226,3.45573509562084));
#33395=CARTESIAN_POINT('Ctrl Pts',(-58.6278891588746,1.66807055469799,4.84903148731836));
#33396=CARTESIAN_POINT('Ctrl Pts',(-58.4886305147918,-0.860844735280108,
5.05514653385482));
#33397=CARTESIAN_POINT('Ctrl Pts',(-58.349371870709,-3.17900084006467,4.02361981064615));
#33398=CARTESIAN_POINT('Ctrl Pts',(-58.2191981777753,-4.61839135830064,
2.13855734824838));
#33399=CARTESIAN_POINT('Ctrl Pts',(-58.1354440328692,-4.91765907220889,
0.659097939802908));
#33400=CARTESIAN_POINT('Ctrl Pts',(-58.0981094359908,-4.91834149996792,
-0.000124244451390268));
#33401=CARTESIAN_POINT('Origin',(-59.58325,-7.01450167938425E-16,0.));
#33402=CARTESIAN_POINT('',(-59.58325,-5.91675,-7.2459289488551E-16));
#33403=CARTESIAN_POINT('Origin',(-59.58325,0.,0.));
#33404=CARTESIAN_POINT('Origin',(-59.58325,0.,0.));
#33405=CARTESIAN_POINT('',(-59.58325,2.8570646345847,-4.0032942355397));
#33406=CARTESIAN_POINT('Ctrl Pts',(-59.58325,2.58415317085794,5.32292607787884));
#33407=CARTESIAN_POINT('Ctrl Pts',(-59.58325,2.70296646487954,5.25292992541471));
#33408=CARTESIAN_POINT('Ctrl Pts',(-59.58325,2.81915569555313,5.17883110287497));
#33409=CARTESIAN_POINT('Ctrl Pts',(-59.58325,2.93247861654453,5.10069749527868));
#33410=CARTESIAN_POINT('Ctrl Pts',(-59.58325,3.06920329489612,5.00642890183267));
#33411=CARTESIAN_POINT('Ctrl Pts',(-59.58325,3.20175694045079,4.90628756576197));
#33412=CARTESIAN_POINT('Ctrl Pts',(-59.58325,3.32982749537687,4.80061426652425));
#33413=CARTESIAN_POINT('Ctrl Pts',(-59.58325,3.45739810776431,4.69535347879252));
#33414=CARTESIAN_POINT('Ctrl Pts',(-59.58325,3.58052099337265,4.58460318693842));
#33415=CARTESIAN_POINT('Ctrl Pts',(-59.58325,3.69884497680949,4.46867157675984));
#33416=CARTESIAN_POINT('Ctrl Pts',(-59.58325,3.72630240576341,4.44176930506873));
#33417=CARTESIAN_POINT('Ctrl Pts',(-59.58325,3.75350122285113,4.41458792820906));
#33418=CARTESIAN_POINT('Ctrl Pts',(-59.58325,3.78043667074496,4.38713113248787));
#33419=CARTESIAN_POINT('Ctrl Pts',(-59.58325,3.79756513892093,4.36967113503105));
#33420=CARTESIAN_POINT('Ctrl Pts',(-59.58325,3.81458599818276,4.35210081720947));
#33421=CARTESIAN_POINT('Ctrl Pts',(-59.58325,3.83148983927773,4.33442994372371));
#33422=CARTESIAN_POINT('Ctrl Pts',(-59.58325,3.94443075290801,4.2163641984937));
#33423=CARTESIAN_POINT('Ctrl Pts',(-59.58325,4.05225471233772,4.09370721020746));
#33424=CARTESIAN_POINT('Ctrl Pts',(-59.58325,4.15466130575339,3.96678643366706));
#33425=CARTESIAN_POINT('Ctrl Pts',(-59.58325,4.2563159827758,3.84079756794747));
#33426=CARTESIAN_POINT('Ctrl Pts',(-59.58325,4.35263292305005,3.7106066599572));
#33427=CARTESIAN_POINT('Ctrl Pts',(-59.58325,4.44327305063394,3.57651053181448));
#33428=CARTESIAN_POINT('Ctrl Pts',(-59.58325,4.5116269274949,3.47538545095982));
#33429=CARTESIAN_POINT('Ctrl Pts',(-59.58325,4.57675150588568,3.37203892619259));
#33430=CARTESIAN_POINT('Ctrl Pts',(-59.58325,4.63848222257101,3.26659257919084));
#33431=CARTESIAN_POINT('Ctrl Pts',(-59.58325,4.65762303654452,3.23389688050918));
#33432=CARTESIAN_POINT('Ctrl Pts',(-59.58325,4.67643742778736,3.20099927304137));
#33433=CARTESIAN_POINT('Ctrl Pts',(-59.58325,4.6949201424431,3.16790332449171));
#33434=CARTESIAN_POINT('Ctrl Pts',(-59.58325,4.7055680211765,3.14883677213252));
#33435=CARTESIAN_POINT('Ctrl Pts',(-59.58325,4.71610083541303,3.12971330580686));
#33436=CARTESIAN_POINT('Ctrl Pts',(-59.58325,4.72651757868068,3.1105343324428));
#33437=CARTESIAN_POINT('Ctrl Pts',(-59.58325,4.75633369194143,3.05563786169807));
#33438=CARTESIAN_POINT('Ctrl Pts',(-59.58325,4.7851998467299,3.00028502027509));
#33439=CARTESIAN_POINT('Ctrl Pts',(-59.58325,4.81309966376949,2.94449416952489));
#33440=CARTESIAN_POINT('Ctrl Pts',(-59.58325,4.88433135386074,2.80205321426967));
#33441=CARTESIAN_POINT('Ctrl Pts',(-59.58325,4.94926756855005,2.65675835282064));
#33442=CARTESIAN_POINT('Ctrl Pts',(-59.58325,5.00784297450621,2.5090468261143));
#33443=CARTESIAN_POINT('Ctrl Pts',(-59.58325,5.0666367561758,2.36078461419289));
#33444=CARTESIAN_POINT('Ctrl Pts',(-59.58325,5.1190223304161,2.21008689945141));
#33445=CARTESIAN_POINT('Ctrl Pts',(-59.58325,5.16488256999809,2.05738435244192));
#33446=CARTESIAN_POINT('Ctrl Pts',(-59.58325,5.21012932720205,1.90672454054514));
#33447=CARTESIAN_POINT('Ctrl Pts',(-59.58325,5.24902413845654,1.75411243330923));
#33448=CARTESIAN_POINT('Ctrl Pts',(-59.58325,5.28140444330562,1.59996188041636));
#33449=CARTESIAN_POINT('Ctrl Pts',(-59.58325,5.30441106192448,1.49043595109536));
#33450=CARTESIAN_POINT('Ctrl Pts',(-59.58325,5.32412794044939,1.38013335563645));
#33451=CARTESIAN_POINT('Ctrl Pts',(-59.58325,5.34048114038691,1.26920566262887));
#33452=CARTESIAN_POINT('Ctrl Pts',(-59.58325,5.34621139891097,1.23033593922064));
#33453=CARTESIAN_POINT('Ctrl Pts',(-59.58325,5.35152853242856,1.19138949828347));
#33454=CARTESIAN_POINT('Ctrl Pts',(-59.58325,5.35642897582421,1.152372989026));
#33455=CARTESIAN_POINT('Ctrl Pts',(-59.58325,5.359318940468,1.12936357473948));
#33456=CARTESIAN_POINT('Ctrl Pts',(-59.58325,5.36206407119635,1.106328380616));
#33457=CARTESIAN_POINT('Ctrl Pts',(-59.58325,5.36466150365874,1.08328926655645));
#33458=CARTESIAN_POINT('Ctrl Pts',(-59.58325,5.3820688210545,0.928887111058601));
#33459=CARTESIAN_POINT('Ctrl Pts',(-59.58325,5.39287439304195,0.774098737382789));
#33460=CARTESIAN_POINT('Ctrl Pts',(-59.58325,5.39698732754428,0.619324715726741));
#33461=CARTESIAN_POINT('Ctrl Pts',(-59.58325,5.40012959795112,0.501077797931173));
#33462=CARTESIAN_POINT('Ctrl Pts',(-59.58325,5.39936439889502,0.382839033567496));
#33463=CARTESIAN_POINT('Ctrl Pts',(-59.58325,5.39463071560031,0.264788458795355));
#33464=CARTESIAN_POINT('Ctrl Pts',(-59.58325,5.38840882171842,0.109624265671113));
#33465=CARTESIAN_POINT('Ctrl Pts',(-59.58325,5.3753324281636,-0.0452158194266503));
#33466=CARTESIAN_POINT('Ctrl Pts',(-59.58325,5.35550293155849,-0.199293539444912));
#33467=CARTESIAN_POINT('Ctrl Pts',(-59.58325,5.33581130130685,-0.352300020296972));
#33468=CARTESIAN_POINT('Ctrl Pts',(-59.58325,5.30945980007245,-0.504555404036452));
#33469=CARTESIAN_POINT('Ctrl Pts',(-59.58325,5.27650250311296,-0.655606684917678));
#33470=CARTESIAN_POINT('Ctrl Pts',(-59.58325,5.26118504007137,-0.725810331021533));
#33471=CARTESIAN_POINT('Ctrl Pts',(-59.58325,5.24444006104799,-0.795753478288869));
#33472=CARTESIAN_POINT('Ctrl Pts',(-59.58325,5.22626994654444,-0.865388232001238));
#33473=CARTESIAN_POINT('Ctrl Pts',(-59.58325,5.22064316880509,-0.886952173273992));
#33474=CARTESIAN_POINT('Ctrl Pts',(-59.58325,5.21487971172168,-0.908486528003936));
#33475=CARTESIAN_POINT('Ctrl Pts',(-59.58325,5.20897961039385,-0.929989838884862));
#33476=CARTESIAN_POINT('Ctrl Pts',(-59.58325,5.20439703260389,-0.946691347787532));
#33477=CARTESIAN_POINT('Ctrl Pts',(-59.58325,5.19973235987882,-0.963372783691243));
#33478=CARTESIAN_POINT('Ctrl Pts',(-59.58325,5.1949883654161,-0.980024246908933));
#33479=CARTESIAN_POINT('Ctrl Pts',(-59.58325,5.15340085215999,-1.12599679235358));
#33480=CARTESIAN_POINT('Ctrl Pts',(-59.58325,5.10566795980971,-1.26986449671757));
#33481=CARTESIAN_POINT('Ctrl Pts',(-59.58325,5.05191863367101,-1.41122890907032));
#33482=CARTESIAN_POINT('Ctrl Pts',(-59.58325,4.99658445894275,-1.55676158185768));
#33483=CARTESIAN_POINT('Ctrl Pts',(-59.58325,4.93487370729753,-1.69964208005801));
#33484=CARTESIAN_POINT('Ctrl Pts',(-59.58325,4.86687602556661,-1.83940847048739));
#33485=CARTESIAN_POINT('Ctrl Pts',(-59.58325,4.79887834383569,-1.97917486091677));
#33486=CARTESIAN_POINT('Ctrl Pts',(-59.58325,4.72459337675515,-2.11582794888444));
#33487=CARTESIAN_POINT('Ctrl Pts',(-59.58325,4.64406438290419,-2.24886612391969));
#33488=CARTESIAN_POINT('Ctrl Pts',(-59.58325,4.589502138863,-2.33900584907884));
#33489=CARTESIAN_POINT('Ctrl Pts',(-59.58325,4.5320723280881,-2.42748516111421));
#33490=CARTESIAN_POINT('Ctrl Pts',(-59.58325,4.47186625223104,-2.51418020727366));
#33491=CARTESIAN_POINT('Ctrl Pts',(-59.58325,4.44033492565804,-2.55958442559882));
#33492=CARTESIAN_POINT('Ctrl Pts',(-59.58325,4.40804200014479,-2.6044990694282));
#33493=CARTESIAN_POINT('Ctrl Pts',(-59.58325,4.37499996200529,-2.64890512365198));
#33494=CARTESIAN_POINT('Ctrl Pts',(-59.58325,4.35433201309379,-2.67668131760779));
#33495=CARTESIAN_POINT('Ctrl Pts',(-59.58325,4.33337096128033,-2.70425850563629));
#33496=CARTESIAN_POINT('Ctrl Pts',(-59.58325,4.31211979047038,-2.73163185516577));
#33497=CARTESIAN_POINT('Ctrl Pts',(-59.58325,4.29993198098909,-2.74733080991578));
#33498=CARTESIAN_POINT('Ctrl Pts',(-59.58325,4.28765459229105,-2.76295516788741));
#33499=CARTESIAN_POINT('Ctrl Pts',(-59.58325,4.27529017002798,-2.77850208462221));
#33500=CARTESIAN_POINT('Ctrl Pts',(-59.58325,4.18361908532631,-2.89376850714675));
#33501=CARTESIAN_POINT('Ctrl Pts',(-59.58325,4.08713606344259,-3.00482084934681));
#33502=CARTESIAN_POINT('Ctrl Pts',(-59.58325,3.9861531884936,-3.11138603574584));
#33503=CARTESIAN_POINT('Ctrl Pts',(-59.58325,3.88521216477139,-3.21790705739133));
#33504=CARTESIAN_POINT('Ctrl Pts',(-59.58325,3.77977437828728,-3.31994511155099));
#33505=CARTESIAN_POINT('Ctrl Pts',(-59.58325,3.67011934868638,-3.41718718499577));
#33506=CARTESIAN_POINT('Ctrl Pts',(-59.58325,3.56151642211555,-3.51349625353879));
#33507=CARTESIAN_POINT('Ctrl Pts',(-59.58325,3.44877615893273,-3.60510130706221));
#33508=CARTESIAN_POINT('Ctrl Pts',(-59.58325,3.33214805491118,-3.69165255083082));
#33509=CARTESIAN_POINT('Ctrl Pts',(-59.58325,3.21805378133788,-3.77632340583177));
#33510=CARTESIAN_POINT('Ctrl Pts',(-59.58325,3.10023818545153,-3.85615788944432));
#33511=CARTESIAN_POINT('Ctrl Pts',(-59.58325,2.97892256809559,-3.93078028943487));
#33512=CARTESIAN_POINT('Ctrl Pts',(-59.58325,2.9386857006511,-3.95553037258368));
#33513=CARTESIAN_POINT('Ctrl Pts',(-59.58325,2.89806374610355,-3.97970668204472));
#33514=CARTESIAN_POINT('Ctrl Pts',(-59.58325,2.85706463458446,-4.00329423553987));
#33515=CARTESIAN_POINT('Origin',(-59.58325,0.,0.));
#33516=CARTESIAN_POINT('Origin',(-62.8183905640093,0.,0.));
#33517=CARTESIAN_POINT('Ctrl Pts',(-59.58325,2.85706463458446,-4.00329423553987));
#33518=CARTESIAN_POINT('Ctrl Pts',(-59.5368304519724,3.52427108824591,-3.52712339958193));
#33519=CARTESIAN_POINT('Ctrl Pts',(-59.4439913559172,4.61530848209962,-2.23520568907806));
#33520=CARTESIAN_POINT('Ctrl Pts',(-59.3047327118343,5.12174738739822,0.251511598513074));
#33521=CARTESIAN_POINT('Ctrl Pts',(-59.1654740677515,4.3742789497841,2.67597888304926));
#33522=CARTESIAN_POINT('Ctrl Pts',(-59.0262154236687,2.55584624568566,4.44562215581043));
#33523=CARTESIAN_POINT('Ctrl Pts',(-58.8869567795858,0.111678748687467,
5.12668320818063));
#33524=CARTESIAN_POINT('Ctrl Pts',(-58.747698135503,-2.35983518894881,4.55267369514457));
#33525=CARTESIAN_POINT('Ctrl Pts',(-58.60843949142,-4.25359264236838,2.86399697899764));
#33526=CARTESIAN_POINT('Ctrl Pts',(-58.5070036342556,-4.87445011480876,
1.12323890322437));
#33527=CARTESIAN_POINT('Ctrl Pts',(-58.4519873251187,-4.91852463110708,
0.151914236828057));
#33528=CARTESIAN_POINT('Ctrl Pts',(-58.4433905640093,-4.91836886135133,
0.000122455552848399));
#33529=CARTESIAN_POINT('Ctrl Pts',(-60.1597342437858,3.43710408716083,-4.81604049573115));
#33530=CARTESIAN_POINT('Ctrl Pts',(-60.1133146957582,4.23976637246581,-4.24319775824234));
#33531=CARTESIAN_POINT('Ctrl Pts',(-60.020475599703,5.55230548700525,-2.68899573239491));
#33532=CARTESIAN_POINT('Ctrl Pts',(-59.8812169556201,6.16156129810163,0.302573323947274));
#33533=CARTESIAN_POINT('Ctrl Pts',(-59.7419583115374,5.2623422916961,3.21925442104062));
#33534=CARTESIAN_POINT('Ctrl Pts',(-59.6026996674544,3.07473253172559,5.34816955022458));
#33535=CARTESIAN_POINT('Ctrl Pts',(-59.4634410233717,0.134351697513361,
6.16749918609318));
#33536=CARTESIAN_POINT('Ctrl Pts',(-59.3241823792887,-2.83892743439519,
5.47695462527239));
#33537=CARTESIAN_POINT('Ctrl Pts',(-59.184923735206,-5.11715432658648,3.44544383174565));
#33538=CARTESIAN_POINT('Ctrl Pts',(-59.0456650911231,-6.14255875840504,
0.570418363169113));
#33539=CARTESIAN_POINT('Ctrl Pts',(-58.9064064470402,-5.66409071331427,
-2.44427558051098));
#33540=CARTESIAN_POINT('Ctrl Pts',(-58.7671478029575,-3.79889373407555,
-4.86053471086364));
#33541=CARTESIAN_POINT('Ctrl Pts',(-58.6278891588746,-1.0036201493159,-6.08680140714466));
#33542=CARTESIAN_POINT('Ctrl Pts',(-58.4886305147919,2.03736788399004,-5.82284542089895));
#33543=CARTESIAN_POINT('Ctrl Pts',(-58.3493718707089,4.57955079663083,-4.13329347110169));
#33544=CARTESIAN_POINT('Ctrl Pts',(-58.2101132266262,6.00053037756086,-1.43179411094106));
#33545=CARTESIAN_POINT('Ctrl Pts',(-58.0708545825432,5.95241075130211,1.62024861133869));
#33546=CARTESIAN_POINT('Ctrl Pts',(-57.9315959384605,4.44697294148773,4.27560886674674));
#33547=CARTESIAN_POINT('Ctrl Pts',(-57.7923372943776,1.85279062942082,5.88417931287061));
#33548=CARTESIAN_POINT('Ctrl Pts',(-57.6530786502948,-1.19500713116077,
6.05213659818529));
#33549=CARTESIAN_POINT('Ctrl Pts',(-57.5138200062119,-3.95023341240051,
4.73835998660194));
#33550=CARTESIAN_POINT('Ctrl Pts',(-57.3745613621291,-5.73833104722617,
2.26449910444055));
#33551=CARTESIAN_POINT('Ctrl Pts',(-57.2353027180462,-6.12152325938902,
-0.763775085538537));
#33552=CARTESIAN_POINT('Ctrl Pts',(-57.0960440739634,-5.00599377891902,
-3.60505557232192));
#33553=CARTESIAN_POINT('Ctrl Pts',(-56.9567854298806,-2.66485571171295,
-5.56371669240644));
#33554=CARTESIAN_POINT('Ctrl Pts',(-56.8175267857977,0.328714257451459,
-6.1602229125286));
#33555=CARTESIAN_POINT('Ctrl Pts',(-56.6782681417149,3.24180569743506,-5.24853267271102));
#33556=CARTESIAN_POINT('Ctrl Pts',(-56.5390094976321,5.36121159272567,-3.05185347844784));
#33557=CARTESIAN_POINT('Ctrl Pts',(-56.3997508535491,6.16804155340788,-0.10799440477762));
#33558=CARTESIAN_POINT('Ctrl Pts',(-56.2604922094665,5.46476082983919,2.86230474769956));
#33559=CARTESIAN_POINT('Ctrl Pts',(-56.1212335653834,3.42355239541739,5.13183090054873));
#33560=CARTESIAN_POINT('Ctrl Pts',(-55.9819749213008,0.544161694283669,
6.14493998721812));
#33561=CARTESIAN_POINT('Ctrl Pts',(-55.8427162772178,-2.46845515025061,
5.6535943051491));
#33562=CARTESIAN_POINT('Ctrl Pts',(-55.7034576331351,-4.87672449425258,
3.77808914706642));
#33563=CARTESIAN_POINT('Ctrl Pts',(-55.5641989890521,-6.091034021489,0.977601117575148));
#33564=CARTESIAN_POINT('Ctrl Pts',(-55.4249403449694,-5.81408648206527,
-2.06223126130096));
#33565=CARTESIAN_POINT('Ctrl Pts',(-55.2856817008865,-4.11368645132967,
-4.59717121458057));
#33566=CARTESIAN_POINT('Ctrl Pts',(-55.1464230568037,-1.40613985583562,
-6.00659388521078));
#33567=CARTESIAN_POINT('Ctrl Pts',(-55.0071644127209,1.6456694689963,-5.94543281812475));
#33568=CARTESIAN_POINT('Ctrl Pts',(-54.867905768638,4.29457245372739,-4.42866196900453));
#33569=CARTESIAN_POINT('Ctrl Pts',(-54.7286471245552,5.89204287424835,-1.82762965724471));
#33570=CARTESIAN_POINT('Ctrl Pts',(-54.5893884804723,6.04697487809177,1.22085798508602));
#33571=CARTESIAN_POINT('Ctrl Pts',(-54.4501298363896,4.72143673728365,3.97044513019));
#33572=CARTESIAN_POINT('Ctrl Pts',(-54.3108711923066,2.23995760609141,5.74795522937805));
#33573=CARTESIAN_POINT('Ctrl Pts',(-54.1716125482238,-0.789926376776022,
6.11820363467045));
#33574=CARTESIAN_POINT('Ctrl Pts',(-54.032353904141,-3.62641408450318,4.99054308504978));
#33575=CARTESIAN_POINT('Ctrl Pts',(-53.8930952600581,-5.57505325763465,
2.64105671475614));
#33576=CARTESIAN_POINT('Ctrl Pts',(-53.7538366159754,-6.15876202024408,
-0.355034891271801));
#33577=CARTESIAN_POINT('Ctrl Pts',(-53.6145779718924,-5.23463199026661,
-3.26420393396288));
#33578=CARTESIAN_POINT('Ctrl Pts',(-53.4753193278097,-3.02891628545778,
-5.37420371140784));
#33579=CARTESIAN_POINT('Ctrl Pts',(-53.3360606837268,-0.0816363734756486,
-6.16844671684429));
#33580=CARTESIAN_POINT('Ctrl Pts',(-53.1968020396439,2.88563042717145,-5.4524798425857));
#33581=CARTESIAN_POINT('Ctrl Pts',(-53.0575433955611,5.14641344343852,-3.40159198982133));
#33582=CARTESIAN_POINT('Ctrl Pts',(-52.9182847514783,6.14720917537799,-0.517898397535566));
#33583=CARTESIAN_POINT('Ctrl Pts',(-52.7790261073954,5.64299457726843,2.49259134174462));
#33584=CARTESIAN_POINT('Ctrl Pts',(-52.6397674633126,3.75721561573744,4.89282435949625));
#33585=CARTESIAN_POINT('Ctrl Pts',(-52.5005088192298,0.951564212488417,
6.09515585900251));
#33586=CARTESIAN_POINT('Ctrl Pts',(-52.361250175147,-2.08705697080914,5.80522114967365));
#33587=CARTESIAN_POINT('Ctrl Pts',(-52.2219915310641,-4.61470769404007,
4.09400443265376));
#33588=CARTESIAN_POINT('Ctrl Pts',(-52.0827328869813,-6.01254770942893,
1.38045986463286));
#33589=CARTESIAN_POINT('Ctrl Pts',(-51.9434742428984,-5.93834632286783,
-1.67106024598258));
#33590=CARTESIAN_POINT('Ctrl Pts',(-51.8042155988156,-4.41027012834964,
-4.31345763755807));
#33591=CARTESIAN_POINT('Ctrl Pts',(-51.6649569547327,-1.8024353129505,-5.8997988388292));
#33592=CARTESIAN_POINT('Ctrl Pts',(-51.5256983106499,1.24668654634832,-6.04170274435736));
#33593=CARTESIAN_POINT('Ctrl Pts',(-51.3864396665671,3.99058434753268,-4.70442727239442));
#33594=CARTESIAN_POINT('Ctrl Pts',(-51.2471810224842,5.75747445390417,-2.21537520719677));
#33595=CARTESIAN_POINT('Ctrl Pts',(-51.1079223784014,6.11477229150658,0.81606324451273));
#33596=CARTESIAN_POINT('Ctrl Pts',(-50.9686637343185,4.97500126386264,3.6477063780664));
#33597=CARTESIAN_POINT('Ctrl Pts',(-50.8294050902357,2.61720949208814,5.58628802251951));
#33598=CARTESIAN_POINT('Ctrl Pts',(-50.6901464461529,-0.381349042150201,
6.15718866887091));
#33599=CARTESIAN_POINT('Ctrl Pts',(-50.55088780207,-3.28654256611867,5.22063572346428));
#33600=CARTESIAN_POINT('Ctrl Pts',(-50.4116291579872,-5.3870976971126,3.00592378442723));
#33601=CARTESIAN_POINT('Ctrl Pts',(-50.2723705139044,-6.168739244425,0.0552768515033475));
#33602=CARTESIAN_POINT('Ctrl Pts',(-50.1331118698215,-5.44009929303315,
-2.90890341502798));
#33603=CARTESIAN_POINT('Ctrl Pts',(-49.9938532257387,-3.37956947114509,
-5.16090201280022));
#33604=CARTESIAN_POINT('Ctrl Pts',(-49.8545945816558,-0.491625643961048,
-6.14936611548061));
#33605=CARTESIAN_POINT('Ctrl Pts',(-49.715335937573,2.51668201851298,-5.63229180828859));
#33606=CARTESIAN_POINT('Ctrl Pts',(-49.5760772934902,4.90883488175199,-3.73627347764));
#33607=CARTESIAN_POINT('Ctrl Pts',(-49.4368186494074,6.0991663989511,-0.925509931836011));
#33608=CARTESIAN_POINT('Ctrl Pts',(-49.2975600053245,5.79624981392584,2.11184457065046));
#33609=CARTESIAN_POINT('Ctrl Pts',(-49.1583013612417,4.07424765744423,4.63215990892277));
#33610=CARTESIAN_POINT('Ctrl Pts',(-49.0190427171588,1.35475466622873,6.01839174450722));
#33611=CARTESIAN_POINT('Ctrl Pts',(-48.879784073076,-1.69642050940358,5.93115139338866));
#33612=CARTESIAN_POINT('Ctrl Pts',(-48.7405254289932,-4.33226405763891,
4.39179775614853));
#33613=CARTESIAN_POINT('Ctrl Pts',(-48.6012667849103,-5.90744707306491,
1.77720805618193));
#33614=CARTESIAN_POINT('Ctrl Pts',(-48.4620081408274,-6.03632028911212,
-1.27249234311039));
#33615=CARTESIAN_POINT('Ctrl Pts',(-48.3227494967447,-4.68733190464862,
-4.01065069679278));
#33616=CARTESIAN_POINT('Ctrl Pts',(-48.1834908526618,-2.19075235554399,
-5.7668885469289));
#33617=CARTESIAN_POINT('Ctrl Pts',(-48.044232208579,0.842185210932005,-6.1112292925817));
#33618=CARTESIAN_POINT('Ctrl Pts',(-47.9049735644961,3.66893206449977,-4.95936859913705));
#33619=CARTESIAN_POINT('Ctrl Pts',(-47.7657149204133,5.59742078176774,-2.59331447916677));
#33620=CARTESIAN_POINT('Ctrl Pts',(-47.6264562763304,6.15550288721356,0.407656229593879));
#33621=CARTESIAN_POINT('Ctrl Pts',(-47.4871976322476,5.20654412783746,3.30882118599701));
#33622=CARTESIAN_POINT('Ctrl Pts',(-47.3479389881648,2.98287639521906,5.39989331439669));
#33623=CARTESIAN_POINT('Ctrl Pts',(-47.2086803440819,0.0289163201755667,
6.16891913080799));
#33624=CARTESIAN_POINT('Ctrl Pts',(-47.0694216999991,-2.93212328629913,
5.42761940725061));
#33625=CARTESIAN_POINT('Ctrl Pts',(-46.9301630559163,-5.17529634407517,
3.35748524151984));
#33626=CARTESIAN_POINT('Ctrl Pts',(-46.7909044118334,-6.1514107681389,0.465343913300744));
#33627=CARTESIAN_POINT('Ctrl Pts',(-46.6516457677506,-5.62148619364284,
-2.54072674065987));
#33628=CARTESIAN_POINT('Ctrl Pts',(-46.5123871236677,-3.71526311517727,
-4.92475576866757));
#33629=CARTESIAN_POINT('Ctrl Pts',(-46.3731284795849,-0.899438751369376,
-6.10306556810234));
#33630=CARTESIAN_POINT('Ctrl Pts',(-46.2338698355021,2.13659360820338,-5.78717263863846));
#33631=CARTESIAN_POINT('Ctrl Pts',(-46.0946111914193,4.6495275405512,-4.05441648645981));
#33632=CARTESIAN_POINT('Ctrl Pts',(-45.9553525473364,6.02412588373361,-1.32902473000016));
#33633=CARTESIAN_POINT('Ctrl Pts',(-45.8160939032536,5.92384816106664,1.72174979618084));
#33634=CARTESIAN_POINT('Ctrl Pts',(-45.6768352591706,4.37324518970676,4.35099137056464));
#33635=CARTESIAN_POINT('Ctrl Pts',(-45.537576615088,1.75194834758869,5.91498743729879));
#33636=CARTESIAN_POINT('Ctrl Pts',(-45.398317971005,-1.29827490415837,6.03082761063967));
#33637=CARTESIAN_POINT('Ctrl Pts',(-45.2590593269223,-4.03064381155875,
4.67015094620768));
#33638=CARTESIAN_POINT('Ctrl Pts',(-45.1198006828393,-5.77619733655087,
2.1660895007464));
#33639=CARTESIAN_POINT('Ctrl Pts',(-44.9805420387566,-6.10757470259099,
-0.868291799046749));
#33640=CARTESIAN_POINT('Ctrl Pts',(-44.8412833946737,-4.94364537632544,
-3.69009075622231));
#33641=CARTESIAN_POINT('Ctrl Pts',(-44.7020247505909,-2.56937211231493,
-5.60845133209513));
#33642=CARTESIAN_POINT('Ctrl Pts',(-44.562766106508,0.433955973233554,-6.15370470605441));
#33643=CARTESIAN_POINT('Ctrl Pts',(-44.4235074624252,3.33103938679021,-5.19235746069871));
#33644=CARTESIAN_POINT('Ctrl Pts',(-44.2842488183423,5.41259032961209,-2.95977453867871));
#33645=CARTESIAN_POINT('Ctrl Pts',(-44.1449901742595,6.16898637270852,-0.00255526083573153));
#33646=CARTESIAN_POINT('Ctrl Pts',(-44.0057315301767,5.41504041312089,2.95528961698998));
#33647=CARTESIAN_POINT('Ctrl Pts',(-43.8664728860938,3.33533970420366,5.18959617442281));
#33648=CARTESIAN_POINT('Ctrl Pts',(-43.727214242011,0.439053685459154,6.15334309601748));
#33649=CARTESIAN_POINT('Ctrl Pts',(-43.5879555979281,-2.56472506912859,
5.61057793064176));
#33650=CARTESIAN_POINT('Ctrl Pts',(-43.4486969538453,-4.94058672952753,
3.69418491199856));
#33651=CARTESIAN_POINT('Ctrl Pts',(-43.3094383097625,-6.10685329525738,
0.873351147148346));
#33652=CARTESIAN_POINT('Ctrl Pts',(-43.1701796656797,-5.77798978956076,
-2.16130363155039));
#33653=CARTESIAN_POINT('Ctrl Pts',(-43.0309210215968,-4.03451128181777,
-4.66681027179233));
#33654=CARTESIAN_POINT('Ctrl Pts',(-42.891662377514,-1.30327052577588,-6.02975002240266));
#33655=CARTESIAN_POINT('Ctrl Pts',(-42.7524037334311,1.74704764380147,-5.91643675925883));
#33656=CARTESIAN_POINT('Ctrl Pts',(-42.6131450893483,4.36963923437441,-4.35461276779428));
#33657=CARTESIAN_POINT('Ctrl Pts',(-42.4738864452654,5.92241979384368,-1.72665664841325));
#33658=CARTESIAN_POINT('Ctrl Pts',(-42.3346278011826,6.02522480923636,1.32403375870253));
#33659=CARTESIAN_POINT('Ctrl Pts',(-42.1953691570998,4.65288471079598,4.0505633267562));
#33660=CARTESIAN_POINT('Ctrl Pts',(-42.0561105130169,2.14138709314778,5.78540065279159));
#33661=CARTESIAN_POINT('Ctrl Pts',(-41.9168518689341,-0.89438253215062,
6.10380858826726));
#33662=CARTESIAN_POINT('Ctrl Pts',(-41.7775932248513,-3.71118206687627,
4.92783188253386));
#33663=CARTESIAN_POINT('Ctrl Pts',(-41.6383345807684,-5.61937947208383,
2.54538282872028));
#33664=CARTESIAN_POINT('Ctrl Pts',(-41.4990759366856,-6.15179415822822,
-0.460247792835837));
#33665=CARTESIAN_POINT('Ctrl Pts',(-41.3598172926027,-5.17807598109662,
-3.35319676279393));
#33666=CARTESIAN_POINT('Ctrl Pts',(-41.22055864852,-2.93661863664603,-5.42518851091134));
#33667=CARTESIAN_POINT('Ctrl Pts',(-41.081300004437,0.023805845163246,-6.16894096889873));
#33668=CARTESIAN_POINT('Ctrl Pts',(-40.9420413603543,2.97840198408325,-5.40236254033643));
#33669=CARTESIAN_POINT('Ctrl Pts',(-40.8027827162714,5.20380124272823,-3.31313326357414));
#33670=CARTESIAN_POINT('Ctrl Pts',(-40.6635240721886,6.15516306383205,-0.41275544049587));
#33671=CARTESIAN_POINT('Ctrl Pts',(-40.5242654281057,5.59956721847028,2.58867656570964));
#33672=CARTESIAN_POINT('Ctrl Pts',(-40.3850067840229,3.67303925299184,4.9563274752585));
#33673=CARTESIAN_POINT('Ctrl Pts',(-40.2457481399401,0.847247595532676,
6.11052951125231));
#33674=CARTESIAN_POINT('Ctrl Pts',(-40.1064894958572,-2.18597418948637,
5.76870143437157));
#33675=CARTESIAN_POINT('Ctrl Pts',(-39.9672308517744,-4.68400778706338,
4.01453240698724));
#33676=CARTESIAN_POINT('Ctrl Pts',(-39.8279722076915,-6.03526405781763,
1.27749252382781));
#33677=CARTESIAN_POINT('Ctrl Pts',(-39.6887135636088,-5.90891732329743,
-1.77231359032672));
#33678=CARTESIAN_POINT('Ctrl Pts',(-39.5494549195258,-4.33590083063914,
-4.38820730855825));
#33679=CARTESIAN_POINT('Ctrl Pts',(-39.4101962754431,-1.70133342048197,
-5.92974400698482));
#33680=CARTESIAN_POINT('Ctrl Pts',(-39.2709376313602,1.3497684363862,-6.01951198720932));
#33681=CARTESIAN_POINT('Ctrl Pts',(-39.1316789872773,4.07040887865475,-4.63553351369504));
#33682=CARTESIAN_POINT('Ctrl Pts',(-38.9924203431945,5.79449832759843,-2.11664558381422));
#33683=CARTESIAN_POINT('Ctrl Pts',(-38.8531616991117,6.09993101837978,0.92045693382662));
#33684=CARTESIAN_POINT('Ctrl Pts',(-38.7139030550289,4.91192840651688,3.73220561133409));
#33685=CARTESIAN_POINT('Ctrl Pts',(-38.574644410946,2.52134706642738,5.63020500218591));
#33686=CARTESIAN_POINT('Ctrl Pts',(-38.4353857668632,-0.486531208311943,
6.14977127862165));
#33687=CARTESIAN_POINT('Ctrl Pts',(-38.2961271227804,-3.37529290941433,
5.16369994981105));
#33688=CARTESIAN_POINT('Ctrl Pts',(-38.1568684786975,-5.43768762825154,
2.91340911194795));
#33689=CARTESIAN_POINT('Ctrl Pts',(-38.0176098346146,-6.16878292020774,
-0.0501665164674183));
#33690=CARTESIAN_POINT('Ctrl Pts',(-37.8783511905318,-5.38958602039518,
-3.00145996554709));
#33691=CARTESIAN_POINT('Ctrl Pts',(-37.739092546449,-3.29086632512096,-5.2179112896068));
#33692=CARTESIAN_POINT('Ctrl Pts',(-37.5998339023661,-0.386449658617007,
-6.15687063834997));
#33693=CARTESIAN_POINT('Ctrl Pts',(-37.4605752582833,2.61258079304851,-5.58845425818403));
#33694=CARTESIAN_POINT('Ctrl Pts',(-37.3213166142004,4.97197771843438,-3.65182652427703));
#33695=CARTESIAN_POINT('Ctrl Pts',(-37.1820579701176,6.11409414895942,-0.821128573173274));
#33696=CARTESIAN_POINT('Ctrl Pts',(-37.0427993260348,5.7593077426763,2.21060483152691));
#33697=CARTESIAN_POINT('Ctrl Pts',(-36.903540681952,3.99448022678247,4.70111977233776));
#33698=CARTESIAN_POINT('Ctrl Pts',(-36.7642820378691,1.25169119486223,6.04066788929217));
#33699=CARTESIAN_POINT('Ctrl Pts',(-36.6250233937863,-1.7975471744003,5.9012899904874));
#33700=CARTESIAN_POINT('Ctrl Pts',(-36.4857647497034,-4.40669525406299,
4.31710971992141));
#33701=CARTESIAN_POINT('Ctrl Pts',(-36.3465061056206,-5.93695994298196,
1.67597912619723));
#33702=CARTESIAN_POINT('Ctrl Pts',(-36.2072474615378,-6.01368924887476,
-1.37547846729399));
#33703=CARTESIAN_POINT('Ctrl Pts',(-36.0679888174549,-4.61809767173776,
-4.09018010487455));
#33704=CARTESIAN_POINT('Ctrl Pts',(-35.9287301733721,-2.09186542452573,
-5.80349019484784));
#33705=CARTESIAN_POINT('Ctrl Pts',(-35.7894715292893,0.946514527956128,
-6.09594206373299));
#33706=CARTESIAN_POINT('Ctrl Pts',(-35.6502128852064,3.75316100570587,-4.89593523867198));
#33707=CARTESIAN_POINT('Ctrl Pts',(-35.5109542411236,5.6409277247272,-2.49726526432922));
#33708=CARTESIAN_POINT('Ctrl Pts',(-35.3716955970407,6.14763610417245,0.512805739726707));
#33709=CARTESIAN_POINT('Ctrl Pts',(-35.2324369529579,5.14922962934839,3.39732742317573));
#33710=CARTESIAN_POINT('Ctrl Pts',(-35.093178308875,2.89014638839049,5.45008745339877));
#33711=CARTESIAN_POINT('Ctrl Pts',(-34.9539196647922,-0.0765262717307818,
6.16851222952148));
#33712=CARTESIAN_POINT('Ctrl Pts',(-34.8146610207094,-3.0244631403426,5.37671108659656));
#33713=CARTESIAN_POINT('Ctrl Pts',(-34.6754023766266,-5.23192605740906,
3.26853929543846));
#33714=CARTESIAN_POINT('Ctrl Pts',(-34.5361437325437,-6.15846578839096,
0.360136820166138));
#33715=CARTESIAN_POINT('Ctrl Pts',(-34.3968850884609,-5.57723925270567,
-2.63643731465406));
#33716=CARTESIAN_POINT('Ctrl Pts',(-34.2576264443781,-3.63054711319852,
-4.98753717328173));
#33717=CARTESIAN_POINT('Ctrl Pts',(-34.1183678002952,-0.794994557003578,
-6.1175471432884));
#33718=CARTESIAN_POINT('Ctrl Pts',(-33.9791091562124,2.23519510791631,-5.74980888600379));
#33719=CARTESIAN_POINT('Ctrl Pts',(-33.8398505121295,4.71814591515049,-3.97435510735641));
#33720=CARTESIAN_POINT('Ctrl Pts',(-33.7005918680467,6.04596141815232,-1.22586701001161));
#33721=CARTESIAN_POINT('Ctrl Pts',(-33.5613332239639,5.89355490010385,1.82274793525691));
#33722=CARTESIAN_POINT('Ctrl Pts',(-33.422074579881,4.29823977876676,4.42510273329878));
#33723=CARTESIAN_POINT('Ctrl Pts',(-33.2828159357982,1.6505942285284,5.94406747007215));
#33724=CARTESIAN_POINT('Ctrl Pts',(-33.1435572917153,-1.40116338196076,
6.00775670055583));
#33725=CARTESIAN_POINT('Ctrl Pts',(-33.0042986476325,-4.10987664439294,
4.60057750330268));
#33726=CARTESIAN_POINT('Ctrl Pts',(-32.8650400035497,-5.81237609034828,
2.06704706776813));
#33727=CARTESIAN_POINT('Ctrl Pts',(-32.7257813594668,-6.09184179716521,
-0.972554838727414));
#33728=CARTESIAN_POINT('Ctrl Pts',(-32.586522715384,-4.87985267103444,-3.77404786734606));
#33729=CARTESIAN_POINT('Ctrl Pts',(-32.4472640713012,-2.47313786215956,
-5.65154744391074));
#33730=CARTESIAN_POINT('Ctrl Pts',(-32.3080054272183,0.539070907307067,
-6.14538867386893));
#33731=CARTESIAN_POINT('Ctrl Pts',(-32.1687467831355,3.41929990172783,-5.13466528393674));
#33732=CARTESIAN_POINT('Ctrl Pts',(-32.0294881390526,5.46238775993218,-2.86683089075102));
#33733=CARTESIAN_POINT('Ctrl Pts',(-31.8902294949698,6.16812890178281,0.102884629624194));
#33734=CARTESIAN_POINT('Ctrl Pts',(-31.750970850887,5.36373797403678,3.04741108843181));
#33735=CARTESIAN_POINT('Ctrl Pts',(-31.6117122068041,3.24615258221831,5.24584529022528));
#33736=CARTESIAN_POINT('Ctrl Pts',(-31.4724535627213,0.333817405615856,
6.15994848482754));
#33737=CARTESIAN_POINT('Ctrl Pts',(-31.3331949186384,-2.66024569490599,
5.56592240682129));
#33738=CARTESIAN_POINT('Ctrl Pts',(-31.1939362745556,-5.00300555568481,
3.6092014083185));
#33739=CARTESIAN_POINT('Ctrl Pts',(-31.0546776304728,-6.12088843118756,
0.768846024230809));
#33740=CARTESIAN_POINT('Ctrl Pts',(-30.9154189863899,-5.74020503780319,
-2.25974456963618));
#33741=CARTESIAN_POINT('Ctrl Pts',(-30.7761603423071,-3.95415741619372,
-4.7350859046042));
#33742=CARTESIAN_POINT('Ctrl Pts',(-30.6369016982242,-1.20002044082553,
-6.05114454773822));
#33743=CARTESIAN_POINT('Ctrl Pts',(-30.4976430541415,1.84791541273056,-5.88571219338953));
#33744=CARTESIAN_POINT('Ctrl Pts',(-30.3583844100586,4.44342941014487,-4.27929135174046));
#33745=CARTESIAN_POINT('Ctrl Pts',(-30.2191257659758,5.95106645847189,-1.62517919100388));
#33746=CARTESIAN_POINT('Ctrl Pts',(-30.0798671218929,6.00171445058094,1.42682271137977));
#33747=CARTESIAN_POINT('Ctrl Pts',(-29.9406084778101,4.58297332830811,4.12949813755107));
#33748=CARTESIAN_POINT('Ctrl Pts',(-29.8013498337272,2.04219096672461,5.82115585184332));
#33749=CARTESIAN_POINT('Ctrl Pts',(-29.6620911896444,-0.998577390644394,
6.08763029354732));
#33750=CARTESIAN_POINT('Ctrl Pts',(-29.5228325455615,-3.79486581486051,
4.86368099727195));
#33751=CARTESIAN_POINT('Ctrl Pts',(-29.3835739014788,-5.66206396582044,
2.44896530048487));
#33752=CARTESIAN_POINT('Ctrl Pts',(-29.2443152573959,-6.14302902874915,
-0.56532623145096));
#33753=CARTESIAN_POINT('Ctrl Pts',(-29.105056613313,-5.12000717952109,-3.44120994385313));
#33754=CARTESIAN_POINT('Ctrl Pts',(-28.9657979692302,-2.8434630447706,-5.47458832324816));
#33755=CARTESIAN_POINT('Ctrl Pts',(-28.8265393251474,0.129241108843973,
-6.16763294399124));
#33756=CARTESIAN_POINT('Ctrl Pts',(-28.6872806810645,3.07030339078509,-5.35066691960496));
#33757=CARTESIAN_POINT('Ctrl Pts',(-28.5480220369817,5.2596687338902,-3.22370659424195));
#33758=CARTESIAN_POINT('Ctrl Pts',(-28.4087633928988,6.16131870058569,-0.307491895558727));
#33759=CARTESIAN_POINT('Ctrl Pts',(-28.2695047488161,5.5545039271765,2.68400549906331));
#33760=CARTESIAN_POINT('Ctrl Pts',(-28.1302461047331,3.58778979940956,5.01838258319093));
#33761=CARTESIAN_POINT('Ctrl Pts',(-27.9909874606504,0.742683452327253,
6.124117951645));
#33762=CARTESIAN_POINT('Ctrl Pts',(-27.8517288165675,-2.28425276841313,
5.73049637344079));
#33763=CARTESIAN_POINT('Ctrl Pts',(-27.7124701724847,-4.75193943137455,
3.93388752210442));
#33764=CARTESIAN_POINT('Ctrl Pts',(-27.5732115284019,-6.05621718340592,
1.17415195926256));
#33765=CARTESIAN_POINT('Ctrl Pts',(-27.433952884319,-5.87776201355233,-1.873049147263));
#33766=CARTESIAN_POINT('Ctrl Pts',(-27.2946942402362,-4.26026478484084,
-4.46167494995614));
#33767=CARTESIAN_POINT('Ctrl Pts',(-27.1554355961533,-1.59973447770233,
-5.95795678037964));
#33768=CARTESIAN_POINT('Ctrl Pts',(-27.0161769520705,1.45245598701167,-5.99556260928159));
#33769=CARTESIAN_POINT('Ctrl Pts',(-26.8769183079876,4.14904422606042,-4.56528546820633));
#33770=CARTESIAN_POINT('Ctrl Pts',(-26.7376596639048,5.82982931901441,-2.01729757526773));
#33771=CARTESIAN_POINT('Ctrl Pts',(-26.598401019822,6.0833076297814,1.02458170853503));
#33772=CARTESIAN_POINT('Ctrl Pts',(-26.4591423757391,4.84742051267944,3.81561446811331));
#33773=CARTESIAN_POINT('Ctrl Pts',(-26.3198837316563,2.42474802069631,5.67247709842451));
#33774=CARTESIAN_POINT('Ctrl Pts',(-26.1806250875734,-0.591571232736088,
6.14055721190029));
#33775=CARTESIAN_POINT('Ctrl Pts',(-26.0413664434907,-3.4630571494742,5.10525558375845));
#33776=CARTESIAN_POINT('Ctrl Pts',(-25.9021077994078,-5.48668892056439,
2.82004327714613));
#33777=CARTESIAN_POINT('Ctrl Pts',(-25.762849155325,-6.167024365203,-0.155595228120675));
#33778=CARTESIAN_POINT('Ctrl Pts',(-25.6235905112421,-5.33749816197862,
-3.09313962938889));
#33779=CARTESIAN_POINT('Ctrl Pts',(-25.4843318671593,-3.20120174137321,
-5.27339613598772));
#33780=CARTESIAN_POINT('Ctrl Pts',(-25.3450732230764,-0.281160770698653,
-6.16257641064526));
#33781=CARTESIAN_POINT('Ctrl Pts',(-25.2058145789936,2.70771629327186,-5.54298402227278));
#33782=CARTESIAN_POINT('Ctrl Pts',(-25.0665559349107,5.03366797501545,-3.56631267744781));
#33783=CARTESIAN_POINT('Ctrl Pts',(-24.927297290828,6.12723564568964,-0.716507319021675));
#33784=CARTESIAN_POINT('Ctrl Pts',(-24.7880386467451,5.72068307019689,2.30871925672743));
#33785=CARTESIAN_POINT('Ctrl Pts',(-24.6487800026623,3.91354579521671,4.76870618771622));
#33786=CARTESIAN_POINT('Ctrl Pts',(-24.5095213585794,1.14826203768109,6.06117923252906));
#33787=CARTESIAN_POINT('Ctrl Pts',(-24.3702627144966,-1.89814867991221,
5.8697045057625));
#33788=CARTESIAN_POINT('Ctrl Pts',(-24.2310040704137,-4.47983901956898,
4.24116042549305));
#33789=CARTESIAN_POINT('Ctrl Pts',(-24.0917454263309,-5.96473830997809,
1.57426055324427));
#33790=CARTESIAN_POINT('Ctrl Pts',(-23.9524867822481,-5.98930128899039,
-1.47806274079266));
#33791=CARTESIAN_POINT('Ctrl Pts',(-23.8132281381652,-4.54751424597783,
-4.16851455300926));
#33792=CARTESIAN_POINT('Ctrl Pts',(-23.6739694940824,-1.99236734795095,
-5.83839633348404));
#33793=CARTESIAN_POINT('Ctrl Pts',(-23.5347108499996,1.05056731756053,-6.07887388479931));
#33794=CARTESIAN_POINT('Ctrl Pts',(-23.3954522059167,3.83629344823421,-4.83107151417328));
#33795=CARTESIAN_POINT('Ctrl Pts',(-23.2561935618339,5.68278665157923,-2.40048646500123));
#33796=CARTESIAN_POINT('Ctrl Pts',(-23.1169349177511,6.13797326845765,0.617805431928693));
#33797=CARTESIAN_POINT('Ctrl Pts',(-22.9776762736682,5.09041076601307,3.48484111966091));
#33798=CARTESIAN_POINT('Ctrl Pts',(-22.8384176295854,2.79657201552275,5.49868933092388));
#33799=CARTESIAN_POINT('Ctrl Pts',(-22.6991589855025,-0.181946506227972,
6.16630317653071));
#33800=CARTESIAN_POINT('Ctrl Pts',(-22.5599003414197,-3.1159193872535,5.32423194161931));
#33801=CARTESIAN_POINT('Ctrl Pts',(-22.4206416973369,-5.28702724585551,
3.17863843455068));
#33802=CARTESIAN_POINT('Ctrl Pts',(-22.281383053254,-6.16372159204044,0.254824511841945));
#33803=CARTESIAN_POINT('Ctrl Pts',(-22.1421244091712,-5.53136290246361,
-2.73137764457251));
#33804=CARTESIAN_POINT('Ctrl Pts',(-22.0028657650883,-3.54477043460551,
-5.04886145204716));
#33805=CARTESIAN_POINT('Ctrl Pts',(-21.8636071210055,-0.690318102290196,
-6.13024145639238));
#33806=CARTESIAN_POINT('Ctrl Pts',(-21.7243484769227,2.33314358782091,-5.71076530726238));
#33807=CARTESIAN_POINT('Ctrl Pts',(-21.5850898328398,4.78538586746803,-3.89313260697071));
#33808=CARTESIAN_POINT('Ctrl Pts',(-21.445831188757,6.0660306045006,-1.12235114883137));
#33809=CARTESIAN_POINT('Ctrl Pts',(-21.3065725446741,5.86153981715024,1.92321355236066));
#33810=CARTESIAN_POINT('Ctrl Pts',(-21.1673139005913,4.22197862254263,4.49792128730755));
#33811=CARTESIAN_POINT('Ctrl Pts',(-21.0280552565085,1.54875788278341,5.97141092343657));
#33812=CARTESIAN_POINT('Ctrl Pts',(-20.8887966124256,-1.50364250514358,
5.98293060403901));
#33813=CARTESIAN_POINT('Ctrl Pts',(-20.7495379683428,-4.18790876286945,
4.52965998612505));
#33814=CARTESIAN_POINT('Ctrl Pts',(-20.61027932426,-5.84685673881853,1.96740074000022));
#33815=CARTESIAN_POINT('Ctrl Pts',(-20.4710206801771,-6.07432913956122,
-1.07653374322349));
#33816=CARTESIAN_POINT('Ctrl Pts',(-20.3317620360943,-4.81463430028632,
-3.85690237762481));
#33817=CARTESIAN_POINT('Ctrl Pts',(-20.1925033920115,-2.37618107641586,
-5.69299243703208));
#33818=CARTESIAN_POINT('Ctrl Pts',(-20.0532447479286,0.644028349992261,
-6.13527724560409));
#33819=CARTESIAN_POINT('Ctrl Pts',(-19.9139861038458,3.50656145663806,-5.07547299735125));
#33820=CARTESIAN_POINT('Ctrl Pts',(-19.7747274597629,5.5105893351992,-2.7730496884856));
#33821=CARTESIAN_POINT('Ctrl Pts',(-19.6354688156801,6.16546939114328,0.208294461991614));
#33822=CARTESIAN_POINT('Ctrl Pts',(-19.4962101715973,5.31086850076819,3.13864224842042));
#33823=CARTESIAN_POINT('Ctrl Pts',(-19.3569515275144,3.15601708578056,5.30056181458931));
#33824=CARTESIAN_POINT('Ctrl Pts',(-19.2176928834316,0.228483599888984,
6.16475422386026));
#33825=CARTESIAN_POINT('Ctrl Pts',(-19.0784342393487,-2.75498912090891,
5.5196407799507));
#33826=CARTESIAN_POINT('Ctrl Pts',(-18.9391755952659,-5.06396273685321,
3.52316346424397));
#33827=CARTESIAN_POINT('Ctrl Pts',(-18.7999169511831,-6.13313532886714,
0.664116280347789));
#33828=CARTESIAN_POINT('Ctrl Pts',(-18.6606583071002,-5.70074326573555,
-2.35752531570539));
#33829=CARTESIAN_POINT('Ctrl Pts',(-18.5213996630174,-3.87264833011119,
-4.80197816605908));
#33830=CARTESIAN_POINT('Ctrl Pts',(-18.3821410189346,-1.09641976584618,
-6.0707712107345));
#33831=CARTESIAN_POINT('Ctrl Pts',(-18.2428823748517,1.94824330692361,-5.85326809680273));
#33832=CARTESIAN_POINT('Ctrl Pts',(-18.1036237307689,4.51592142298934,-4.20271972624959));
#33833=CARTESIAN_POINT('Ctrl Pts',(-17.964365086686,5.977974498913,-1.52322693199904));
#33834=CARTESIAN_POINT('Ctrl Pts',(-17.8251064426032,5.97645067075632,1.52919481297753));
#33835=CARTESIAN_POINT('Ctrl Pts',(-17.6858477985204,4.51172301466689,4.20722650150267));
#33836=CARTESIAN_POINT('Ctrl Pts',(-17.5465891544375,1.94239820730572,5.85521038053091));
#33837=CARTESIAN_POINT('Ctrl Pts',(-17.4073305103547,-1.10248051137719,
6.06967347705416));
#33838=CARTESIAN_POINT('Ctrl Pts',(-17.2680718662719,-3.87744087996609,
4.798109171162));
#33839=CARTESIAN_POINT('Ctrl Pts',(-17.128813222189,-5.70309426842532,2.35183229875672));
#33840=CARTESIAN_POINT('Ctrl Pts',(-16.9895545781062,-6.13246919256903,
-0.670239508096043));
#33841=CARTESIAN_POINT('Ctrl Pts',(-16.8502959340233,-5.06044255053681,
-3.52821776379204));
#33842=CARTESIAN_POINT('Ctrl Pts',(-16.7110372899405,-2.74947672555259,
-5.52238871609615));
#33843=CARTESIAN_POINT('Ctrl Pts',(-16.5717786458577,0.234638614297742,
-6.16452302426568));
#33844=CARTESIAN_POINT('Ctrl Pts',(-16.4325200017748,3.16130779797019,-5.29740808344175));
#33845=CARTESIAN_POINT('Ctrl Pts',(-16.293261357692,5.31399959504801,-3.13333810812859));
#33846=CARTESIAN_POINT('Ctrl Pts',(-16.1540027136092,6.16567428724885,-0.202138515824657));
#33847=CARTESIAN_POINT('Ctrl Pts',(-16.0147440695263,5.50781786877998,2.77855029113547));
#33848=CARTESIAN_POINT('Ctrl Pts',(-15.8754854254435,3.50149216090672,5.07897155368388));
#33849=CARTESIAN_POINT('Ctrl Pts',(-15.7362267813607,0.637902331640281,
6.13591721027176));
#33850=CARTESIAN_POINT('Ctrl Pts',(-15.5969681372778,-2.38186399517015,
5.69061712861911));
#33851=CARTESIAN_POINT('Ctrl Pts',(-15.457709493195,-4.81848278051395,3.85209333868117));
#33852=CARTESIAN_POINT('Ctrl Pts',(-15.3184508491121,-6.07540096466732,
1.0704683622325));
#33853=CARTESIAN_POINT('Ctrl Pts',(-15.1791922050293,-5.84488949576155,
-1.97323748655797));
#33854=CARTESIAN_POINT('Ctrl Pts',(-15.0399335609465,-4.18338408828115,
-4.53383909793204));
#33855=CARTESIAN_POINT('Ctrl Pts',(-14.9006749168636,-1.4976681670861,-5.98442891655653));
#33856=CARTESIAN_POINT('Ctrl Pts',(-14.7614162727808,1.55471919770946,-5.96986160746585));
#33857=CARTESIAN_POINT('Ctrl Pts',(-14.6221576286979,4.22646741616687,-4.49370365913252));
#33858=CARTESIAN_POINT('Ctrl Pts',(-14.4828989846151,5.8634571060835,-1.9173602064141));
#33859=CARTESIAN_POINT('Ctrl Pts',(-14.3436403405323,6.06490698229064,1.12840714823311));
#33860=CARTESIAN_POINT('Ctrl Pts',(-14.2043816964494,4.78149642854946,3.89790858022476));
#33861=CARTESIAN_POINT('Ctrl Pts',(-14.0651230523666,2.32744057663251,5.71309196129958));
#33862=CARTESIAN_POINT('Ctrl Pts',(-13.9258644082838,-0.696438427624502,
6.1295491606275));
#33863=CARTESIAN_POINT('Ctrl Pts',(-13.7866057642009,-3.54980964567892,
5.04531970002558));
#33864=CARTESIAN_POINT('Ctrl Pts',(-13.6473471201181,-5.53408725815802,
2.72585355716592));
#33865=CARTESIAN_POINT('Ctrl Pts',(-13.5080884760353,-6.16346409317852,
-0.26097848210198));
#33866=CARTESIAN_POINT('Ctrl Pts',(-13.3688298319524,-5.28385093542735,
-3.18391562202968));
#33867=CARTESIAN_POINT('Ctrl Pts',(-13.2295711878696,-3.11060191571313,
-5.32734034185756));
#33868=CARTESIAN_POINT('Ctrl Pts',(-13.0903125437867,-0.175789740710468,
-6.16648176540581));
#33869=CARTESIAN_POINT('Ctrl Pts',(-12.9510538997039,2.80206072502511,-5.49589438483793));
#33870=CARTESIAN_POINT('Ctrl Pts',(-12.811795255621,5.09388762847827,-3.47975692031169));
#33871=CARTESIAN_POINT('Ctrl Pts',(-12.6725366115382,6.1385870498091,-0.61167673483411));
#33872=CARTESIAN_POINT('Ctrl Pts',(-12.5332779674554,5.68038708081621,2.40615918179108));
#33873=CARTESIAN_POINT('Ctrl Pts',(-12.3940193233725,3.83146800801478,4.83489940945832));
#33874=CARTESIAN_POINT('Ctrl Pts',(-12.2547606792897,1.04449741186333,6.07991978175963));
#33875=CARTESIAN_POINT('Ctrl Pts',(-12.1155020352069,-1.99819563486947,
5.83640416702013));
#33876=CARTESIAN_POINT('Ctrl Pts',(-11.9762433911241,-4.55167398495864,
4.16397206170644));
#33877=CARTESIAN_POINT('Ctrl Pts',(-11.8369847470412,-5.99077405850954,
1.47208205474779));
#33878=CARTESIAN_POINT('Ctrl Pts',(-11.6977261029584,-5.9631635344839,-1.58021519326419));
#33879=CARTESIAN_POINT('Ctrl Pts',(-11.5584674588755,-4.47560224855524,
-4.24563115552312));
#33880=CARTESIAN_POINT('Ctrl Pts',(-11.4192088147927,-1.89228719451897,
-5.87159676489119));
#33881=CARTESIAN_POINT('Ctrl Pts',(-11.2799501707098,1.15431318037104,-6.06002974230678));
#33882=CARTESIAN_POINT('Ctrl Pts',(-11.140691526627,3.91830510466066,-4.76479637579732));
#33883=CARTESIAN_POINT('Ctrl Pts',(-11.0014328825442,5.72298533309686,-2.30300635543621));
#33884=CARTESIAN_POINT('Ctrl Pts',(-10.8621742384613,6.12651720309929,0.72262463018494));
#33885=CARTESIAN_POINT('Ctrl Pts',(-10.7229155943785,5.03010472196112,3.57133670803045));
#33886=CARTESIAN_POINT('Ctrl Pts',(-10.5836569502956,2.70218061468502,5.54568474776935));
#33887=CARTESIAN_POINT('Ctrl Pts',(-10.4443983062128,-0.287313584438326,
6.16229261721792));
#33888=CARTESIAN_POINT('Ctrl Pts',(-10.30513966213,-3.2064653077802,5.27019730427842));
#33889=CARTESIAN_POINT('Ctrl Pts',(-10.1658810180471,-5.34058381141607,
3.08780892369685));
#33890=CARTESIAN_POINT('Ctrl Pts',(-10.0266223739643,-6.16717664358659,
0.149437755674944));
#33891=CARTESIAN_POINT('Ctrl Pts',(-9.88736372988148,-5.48387054584736,
-2.82551999327713));
#33892=CARTESIAN_POINT('Ctrl Pts',(-9.74810508579863,-3.45795813934461,
-5.10871068886872));
#33893=CARTESIAN_POINT('Ctrl Pts',(-9.6088464417158,-0.585439968808977,
-6.14114479872785));
#33894=CARTESIAN_POINT('Ctrl Pts',(-9.46958779763296,2.43041043193784,-5.67005330912764));
#33895=CARTESIAN_POINT('Ctrl Pts',(-9.33032915355013,4.8512277531245,-3.81077271473068));
#33896=CARTESIAN_POINT('Ctrl Pts',(-9.19107050946727,6.08432757949787,-1.01850738896811));
#33897=CARTESIAN_POINT('Ctrl Pts',(-9.05181186538446,5.82781226552048,2.0231172961226));
#33898=CARTESIAN_POINT('Ctrl Pts',(-8.9125532213016,4.14448400098889,4.56942575840426));
#33899=CARTESIAN_POINT('Ctrl Pts',(-8.77329457721878,1.44646906218654,5.99700980890963));
#33900=CARTESIAN_POINT('Ctrl Pts',(-8.63403593313592,-1.60568233408446,
5.9563565741173));
#33901=CARTESIAN_POINT('Ctrl Pts',(-8.49477728905311,-4.26471736964113,
4.45741911346718));
#33902=CARTESIAN_POINT('Ctrl Pts',(-8.35551864497025,-5.8796292083237,1.86717962945399));
#33903=CARTESIAN_POINT('Ctrl Pts',(-8.21626000088743,-6.05504184616107,
-1.18019813474674));
#33904=CARTESIAN_POINT('Ctrl Pts',(-8.07700135680458,-4.74800931784848,
-3.93863008083336));
#33905=CARTESIAN_POINT('Ctrl Pts',(-7.93774271272175,-2.27853008133649,
-5.7327742031643));
#33906=CARTESIAN_POINT('Ctrl Pts',(-7.79848406863889,0.748797637617561,
-6.12337337534789));
#33907=CARTESIAN_POINT('Ctrl Pts',(-7.65922542455608,3.59279855776266,-5.01479789416878));
#33908=CARTESIAN_POINT('Ctrl Pts',(-7.51996678047323,5.55718097315999,-2.67845833037771));
#33909=CARTESIAN_POINT('Ctrl Pts',(-7.3807081363904,6.16100861777501,0.313643440427673));
#33910=CARTESIAN_POINT('Ctrl Pts',(-7.24144949230756,5.25644743931043,3.22895644346409));
#33911=CARTESIAN_POINT('Ctrl Pts',(-7.10219084822472,3.06495954828024,5.3537297618975));
#33912=CARTESIAN_POINT('Ctrl Pts',(-6.96293220414188,0.12308304190572,6.16775890910275));
#33913=CARTESIAN_POINT('Ctrl Pts',(-6.82367356005905,-2.84892766752535,
5.47174657136365));
#33914=CARTESIAN_POINT('Ctrl Pts',(-6.68441491597621,-5.12344046418626,
3.43609621605106));
#33915=CARTESIAN_POINT('Ctrl Pts',(-6.54515627189336,-6.14359041032356,
0.55919251264796));
#33916=CARTESIAN_POINT('Ctrl Pts',(-6.40589762781053,-5.65961600224796,
-2.45461730278265));
#33917=CARTESIAN_POINT('Ctrl Pts',(-6.2666389837277,-3.79000783672504,-4.86746751335681));
#33918=CARTESIAN_POINT('Ctrl Pts',(-6.12738033964486,-0.992498768124922,
-6.08862427739564));
#33919=CARTESIAN_POINT('Ctrl Pts',(-5.98812169556202,2.04800201524751,-5.81911394815082));
#33920=CARTESIAN_POINT('Ctrl Pts',(-5.84886305147919,4.58709409412132,-4.12492026198068));
#33921=CARTESIAN_POINT('Ctrl Pts',(-5.70960440739633,6.00313605389204,-1.42082965709572));
#33922=CARTESIAN_POINT('Ctrl Pts',(-5.5703457633135,5.94944085066117,1.6311201551404));
#33923=CARTESIAN_POINT('Ctrl Pts',(-5.43108711923068,4.4391545858922,4.28372571000683));
#33924=CARTESIAN_POINT('Ctrl Pts',(-5.29182847514783,1.84203796968307,5.88755428970869));
#33925=CARTESIAN_POINT('Ctrl Pts',(-5.15256983106499,-1.20606153870089,
6.04994338493243));
#33926=CARTESIAN_POINT('Ctrl Pts',(-5.01331118698216,-3.95888313760845,
4.7311355612348));
#33927=CARTESIAN_POINT('Ctrl Pts',(-4.87405254289932,-5.74245839275694,
2.25401220127068));
#33928=CARTESIAN_POINT('Ctrl Pts',(-4.73479389881648,-6.12011773477969,
-0.774956972002906));
#33929=CARTESIAN_POINT('Ctrl Pts',(-4.59553525473365,-4.99939949615145,
-3.61419480298191));
#33930=CARTESIAN_POINT('Ctrl Pts',(-4.45627661065081,-2.65468713741269,
-5.56857572440924));
#33931=CARTESIAN_POINT('Ctrl Pts',(-4.31701796656796,0.339967569286781,
-6.15961211829499));
#33932=CARTESIAN_POINT('Ctrl Pts',(-4.17775932248513,3.251388618394,-5.24260159159703));
#33933=CARTESIAN_POINT('Ctrl Pts',(-4.0385006784023,5.36677795325581,-3.04205420669029));
#33934=CARTESIAN_POINT('Ctrl Pts',(-3.89924203431946,6.1682285513242,-0.0967260806445108));
#33935=CARTESIAN_POINT('Ctrl Pts',(-3.75998339023662,5.45952268276649,2.87228332035471));
#33936=CARTESIAN_POINT('Ctrl Pts',(-3.62072474615379,3.41417154963807,5.13807668544686));
#33937=CARTESIAN_POINT('Ctrl Pts',(-3.48146610207094,0.532934845614573,
6.14592383997453));
#33938=CARTESIAN_POINT('Ctrl Pts',(-3.3422074579881,-2.47877935227735,5.64907535069391));
#33939=CARTESIAN_POINT('Ctrl Pts',(-3.20294881390527,-4.88361839367658,
3.76917375329861));
#33940=CARTESIAN_POINT('Ctrl Pts',(-3.06369016982243,-6.09280979687953,
0.966472023989456));
#33941=CARTESIAN_POINT('Ctrl Pts',(-2.92443152573958,-5.81030937396819,
-2.07284933733924));
#33942=CARTESIAN_POINT('Ctrl Pts',(-2.78517288165675,-4.10528120147494,
-4.60467867048159));
#33943=CARTESIAN_POINT('Ctrl Pts',(-2.64591423757392,-1.39516430851072,
-6.00915267964906));
#33944=CARTESIAN_POINT('Ctrl Pts',(-2.50665559349108,1.65652819361447,-5.94241649418644));
#33945=CARTESIAN_POINT('Ctrl Pts',(-2.36739694940825,4.30265582625509,-4.42080899194675));
#33946=CARTESIAN_POINT('Ctrl Pts',(-2.22813830532541,5.89537187071915,-1.81686268871946));
#33947=CARTESIAN_POINT('Ctrl Pts',(-2.08887966124256,6.0447344392611,1.23190294811429));
#33948=CARTESIAN_POINT('Ctrl Pts',(-1.94962101715973,4.71417543837697,3.97906385024911));
#33949=CARTESIAN_POINT('Ctrl Pts',(-1.81036237307689,2.22945311551249,5.75203783218659));
#33950=CARTESIAN_POINT('Ctrl Pts',(-1.67110372899405,-0.801102063147124,
6.11675013179543));
#33951=CARTESIAN_POINT('Ctrl Pts',(-1.53184508491122,-3.63552523351456,
4.98391021694912));
#33952=CARTESIAN_POINT('Ctrl Pts',(-1.39258644082839,-5.57986844123835,
2.6308666740793));
#33953=CARTESIAN_POINT('Ctrl Pts',(-1.25332779674554,-6.15810383146443,
-0.366283937729162));
#33954=CARTESIAN_POINT('Ctrl Pts',(-1.1140691526627,-5.22865867321571,-3.27376445220254));
#33955=CARTESIAN_POINT('Ctrl Pts',(-0.974810508579875,-3.01909593307338,
-5.37972223694837));
#33956=CARTESIAN_POINT('Ctrl Pts',(-0.835551864497024,-0.0703622493363052,
-6.16859709325572));
#33957=CARTESIAN_POINT('Ctrl Pts',(-0.696293220414186,2.89557656689768,
-5.44717660208643));
#33958=CARTESIAN_POINT('Ctrl Pts',(-0.557034576331352,5.15263851981499,
-3.3922284657316));
#33959=CARTESIAN_POINT('Ctrl Pts',(-0.417775932248521,6.14810707551576,
-0.50658149428877));
#33960=CARTESIAN_POINT('Ctrl Pts',(-0.278517288165677,5.63850617107878,
2.50272579507521));
#33961=CARTESIAN_POINT('Ctrl Pts',(-0.139258644082849,3.74811954234602,
4.90004022087069));
#33962=CARTESIAN_POINT('Ctrl Pts',(-0.046419548027623,1.87656122511999,
5.69726812402409));
#33963=CARTESIAN_POINT('Ctrl Pts',(-8.88178419700125E-15,0.901975524283881,
5.84759529345977));
#33964=CARTESIAN_POINT('Ctrl Pts',(-59.9675728291906,3.24375760296871,-4.54512507566739));
#33965=CARTESIAN_POINT('Ctrl Pts',(-59.9211532811629,4.00126794439251,-4.00450630535553));
#33966=CARTESIAN_POINT('Ctrl Pts',(-59.8283141851077,5.2399731520367,-2.53773238462263));
#33967=CARTESIAN_POINT('Ctrl Pts',(-59.6890555410249,5.8149566612005,0.285552748802543));
#33968=CARTESIAN_POINT('Ctrl Pts',(-59.549796896942,4.96632117772543,3.0381625750435));
#33969=CARTESIAN_POINT('Ctrl Pts',(-59.4105382528592,2.90177043637895,5.0473204187532));
#33970=CARTESIAN_POINT('Ctrl Pts',(-59.2712796087763,0.126794047904731,
5.820560526789));
#33971=CARTESIAN_POINT('Ctrl Pts',(-59.1320209646935,-2.67923001924639,
5.16886098189645));
#33972=CARTESIAN_POINT('Ctrl Pts',(-58.9927623206107,-4.82930043184711,
3.25162821416299));
#33973=CARTESIAN_POINT('Ctrl Pts',(-58.8535036765279,-5.79702306621662,
0.538330773663447));
#33974=CARTESIAN_POINT('Ctrl Pts',(-58.714245032445,-5.3454701543225,-2.30677840908288));
#33975=CARTESIAN_POINT('Ctrl Pts',(-58.5749863883622,-3.58519559498042,
-4.58711636978122));
#33976=CARTESIAN_POINT('Ctrl Pts',(-58.4357277442793,-0.947163777203368,
-5.74440221811722));
#33977=CARTESIAN_POINT('Ctrl Pts',(-58.2964691001966,1.92276038087513,-5.49529447639017));
#33978=CARTESIAN_POINT('Ctrl Pts',(-58.1572104561136,4.32193856748268,-3.9007844342772));
#33979=CARTESIAN_POINT('Ctrl Pts',(-58.0179518120309,5.66298416936691,-1.3512517850711));
#33980=CARTESIAN_POINT('Ctrl Pts',(-57.878693167948,5.61757140339575,1.52910520556));
#33981=CARTESIAN_POINT('Ctrl Pts',(-57.7394345238651,4.19681857847456,4.03509420056188));
#33982=CARTESIAN_POINT('Ctrl Pts',(-57.6001758797823,1.74856610055642,5.5531781695683));
#33983=CARTESIAN_POINT('Ctrl Pts',(-57.4609172356995,-1.12778471905584,
5.71168739925639));
#33984=CARTESIAN_POINT('Ctrl Pts',(-57.3216585916167,-3.7280220034185,4.47181430715398));
#33985=CARTESIAN_POINT('Ctrl Pts',(-57.1823999475338,-5.41553426686218,
2.13711485037188));
#33986=CARTESIAN_POINT('Ctrl Pts',(-57.043141303451,-5.77717087142268,-0.720810652760878));
#33987=CARTESIAN_POINT('Ctrl Pts',(-56.9038826593682,-4.72439296832481,
-3.40226135877762));
#33988=CARTESIAN_POINT('Ctrl Pts',(-56.7646240152853,-2.51495030597815,
-5.25074244599479));
#33989=CARTESIAN_POINT('Ctrl Pts',(-56.6253653712025,0.310223183462825,
-5.81369356346818));
#33990=CARTESIAN_POINT('Ctrl Pts',(-56.4861067271197,3.05944528060205,-4.95328838749244));
#33991=CARTESIAN_POINT('Ctrl Pts',(-56.3468480830367,5.05962881077401,-2.88017839228123));
#33992=CARTESIAN_POINT('Ctrl Pts',(-56.207589438954,5.82107238446222,-0.101919424810071));
#33993=CARTESIAN_POINT('Ctrl Pts',(-56.0683307948711,5.15735312073121,2.70129229488456));
#33994=CARTESIAN_POINT('Ctrl Pts',(-55.9290721507883,3.2309682308663,4.84315140847404));
#33995=CARTESIAN_POINT('Ctrl Pts',(-55.7898135067055,0.513551114052919,
5.79927034441098));
#33996=CARTESIAN_POINT('Ctrl Pts',(-55.6505548626226,-2.32959781204261,
5.33556419775959));
#33997=CARTESIAN_POINT('Ctrl Pts',(-55.5112962185398,-4.60239543367529,
3.56556132276284));
#33998=CARTESIAN_POINT('Ctrl Pts',(-55.3720375744569,-5.7483967363546,0.922608386999673));
#33999=CARTESIAN_POINT('Ctrl Pts',(-55.2327789303741,-5.48702825176757,
-1.94622512536426));
#34000=CARTESIAN_POINT('Ctrl Pts',(-55.0935202862912,-3.88228036287168,
-4.33856778883955));
#34001=CARTESIAN_POINT('Ctrl Pts',(-54.9542616422084,-1.32704065182156,
-5.6687065881652));
#34002=CARTESIAN_POINT('Ctrl Pts',(-54.8150029981255,1.55309607060505,-5.61098599800124));
#34003=CARTESIAN_POINT('Ctrl Pts',(-54.6757443540427,4.05299103402638,-4.17953764816116));
#34004=CARTESIAN_POINT('Ctrl Pts',(-54.5364857099599,5.56059938416019,-1.72482050172535));
#34005=CARTESIAN_POINT('Ctrl Pts',(-54.397227065877,5.70681604000361,1.15218139190509));
#34006=CARTESIAN_POINT('Ctrl Pts',(-54.2579684217942,4.45584303679061,3.74709675692789));
#34007=CARTESIAN_POINT('Ctrl Pts',(-54.1187097777113,2.11395387827456,5.42461706250522));
#34008=CARTESIAN_POINT('Ctrl Pts',(-53.9794511336286,-0.745490862503697,
5.77403798465323));
#34009=CARTESIAN_POINT('Ctrl Pts',(-53.8401924895457,-3.42241839636484,
4.70981141814811));
#34010=CARTESIAN_POINT('Ctrl Pts',(-53.7009338454629,-5.26144129849329,
2.4924900675437));
#34011=CARTESIAN_POINT('Ctrl Pts',(-53.56167520138,-5.8123148503612,-0.335063209806113));
#34012=CARTESIAN_POINT('Ctrl Pts',(-53.4224165572972,-4.94016965636819,
-3.08058355520409));
#34013=CARTESIAN_POINT('Ctrl Pts',(-53.2831579132143,-2.85853147898867,
-5.07189008732698));
#34014=CARTESIAN_POINT('Ctrl Pts',(-53.1438992691315,-0.0770441046955488,
-5.82145475634969));
#34015=CARTESIAN_POINT('Ctrl Pts',(-53.0046406250486,2.72330584123424,-5.14576297252353));
#34016=CARTESIAN_POINT('Ctrl Pts',(-52.8653819809659,4.85691364353293,-3.21024315801133));
#34017=CARTESIAN_POINT('Ctrl Pts',(-52.726123336883,5.80141188454461,-0.488765199415102));
#34018=CARTESIAN_POINT('Ctrl Pts',(-52.5868646928002,5.32556073349711,2.3523762769014));
#34019=CARTESIAN_POINT('Ctrl Pts',(-52.4476060487173,3.54586198453153,4.61758963756513));
#34020=CARTESIAN_POINT('Ctrl Pts',(-52.3083474046345,0.898036128874486,
5.75228670926015));
#34021=CARTESIAN_POINT('Ctrl Pts',(-52.1690887605517,-1.96965432096735,
5.47866161851501));
#34022=CARTESIAN_POINT('Ctrl Pts',(-52.0298301164688,-4.35511779347528,
3.86370551145526));
#34023=CARTESIAN_POINT('Ctrl Pts',(-51.890571472386,-5.67432549352408,1.30280523020041));
#34024=CARTESIAN_POINT('Ctrl Pts',(-51.7513128283031,-5.6042981374404,-1.57705854709862));
#34025=CARTESIAN_POINT('Ctrl Pts',(-51.6120541842203,-4.16218039873141,
-4.07081387473205));
#34026=CARTESIAN_POINT('Ctrl Pts',(-51.4727955401375,-1.70104340804889,
-5.56791905456861));
#34027=CARTESIAN_POINT('Ctrl Pts',(-51.3335368960546,1.17655702611451,-5.70184047817855));
#34028=CARTESIAN_POINT('Ctrl Pts',(-51.1942782519718,3.76610308833844,-4.43979040071741));
#34029=CARTESIAN_POINT('Ctrl Pts',(-51.055019607889,5.43360080467535,-2.09075430639906));
#34030=CARTESIAN_POINT('Ctrl Pts',(-50.9157609638061,5.77079966390589,0.770157460107026));
#34031=CARTESIAN_POINT('Ctrl Pts',(-50.7765023197233,4.69514386681382,3.44251294031197));
#34032=CARTESIAN_POINT('Ctrl Pts',(-50.6372436756404,2.46998431622591,5.27204407719557));
#34033=CARTESIAN_POINT('Ctrl Pts',(-50.4979850315576,-0.359897117890633,
5.81083000429618));
#34034=CARTESIAN_POINT('Ctrl Pts',(-50.3587263874747,-3.10166557834268,
4.92696071776699));
#34035=CARTESIAN_POINT('Ctrl Pts',(-50.2194677433919,-5.08405875115028,
2.83683236888383));
#34036=CARTESIAN_POINT('Ctrl Pts',(-50.0802090993091,-5.82173082845574,
0.0521673777649718));
#34037=CARTESIAN_POINT('Ctrl Pts',(-49.9409504552262,-5.13407886266778,
-2.7452696600157));
#34038=CARTESIAN_POINT('Ctrl Pts',(-49.8016918111435,-3.18945946610645,
-4.87058719133112));
#34039=CARTESIAN_POINT('Ctrl Pts',(-49.6624331670605,-0.463970359923155,
-5.80344749088054));
#34040=CARTESIAN_POINT('Ctrl Pts',(-49.5231745229778,2.37511178736206,-5.31546002447846));
#34041=CARTESIAN_POINT('Ctrl Pts',(-49.3839158788949,4.63269952425391,-3.52609789884971));
#34042=CARTESIAN_POINT('Ctrl Pts',(-49.2446572348121,5.75607164539254,-0.8734474726066));
#34043=CARTESIAN_POINT('Ctrl Pts',(-49.1053985907293,5.47019494488432,1.99304755067632));
#34044=CARTESIAN_POINT('Ctrl Pts',(-48.9661399466464,3.84506010876424,4.37158827364663));
#34045=CARTESIAN_POINT('Ctrl Pts',(-48.8268813025635,1.27854601935176,5.67984078568181));
#34046=CARTESIAN_POINT('Ctrl Pts',(-48.6876226584807,-1.60099222649822,
5.5975079423782));
#34047=CARTESIAN_POINT('Ctrl Pts',(-48.5483640143979,-4.08856238236371,
4.14474714787467));
#34048=CARTESIAN_POINT('Ctrl Pts',(-48.4091053703151,-5.57513705475781,
1.67723525331457));
#34049=CARTESIAN_POINT('Ctrl Pts',(-48.2698467262321,-5.69676080072868,
-1.20091117638895));
#34050=CARTESIAN_POINT('Ctrl Pts',(-48.1305880821495,-4.42365669405774,
-3.78504065069492));
#34051=CARTESIAN_POINT('Ctrl Pts',(-47.9913294380665,-2.06751655734344,
-5.44248532927793));
#34052=CARTESIAN_POINT('Ctrl Pts',(-47.8520707939837,0.794809994632685,
-5.76745596833879));
#34053=CARTESIAN_POINT('Ctrl Pts',(-47.7128121499008,3.46254462396208,-4.680390582138));
#34054=CARTESIAN_POINT('Ctrl Pts',(-47.5735535058181,5.28255058835662,-2.4474334629869));
#34055=CARTESIAN_POINT('Ctrl Pts',(-47.4342948617351,5.80923905245728,0.384724454252631));
#34056=CARTESIAN_POINT('Ctrl Pts',(-47.2950362176524,4.91366181284781,3.1226909650582));
#34057=CARTESIAN_POINT('Ctrl Pts',(-47.1557775735695,2.81508145821114,5.09613458004502));
#34058=CARTESIAN_POINT('Ctrl Pts',(-47.0165189294867,0.0272896982579126,
5.8219005957388));
#34059=CARTESIAN_POINT('Ctrl Pts',(-46.8772602854038,-2.76718335016466,
5.12230100451606));
#34060=CARTESIAN_POINT('Ctrl Pts',(-46.738001641321,-4.8841718021921,3.16861753466183));
#34061=CARTESIAN_POINT('Ctrl Pts',(-46.5987429972381,-5.80537712624728,
0.439167048330993));
#34062=CARTESIAN_POINT('Ctrl Pts',(-46.4594843531554,-5.30526225514328,
-2.39780392827412));
#34063=CARTESIAN_POINT('Ctrl Pts',(-46.3202257090724,-3.50626942660932,
-4.64772481783502));
#34064=CARTESIAN_POINT('Ctrl Pts',(-46.1809670649897,-0.848842867185158,
-5.75975147563883));
#34065=CARTESIAN_POINT('Ctrl Pts',(-46.0417084209067,2.01640438733086,-5.46162838547696));
#34066=CARTESIAN_POINT('Ctrl Pts',(-45.902449776824,4.38797892860256,-3.82634449526369));
#34067=CARTESIAN_POINT('Ctrl Pts',(-45.7631911327411,5.68525236392919,-1.25426346224879));
#34068=CARTESIAN_POINT('Ctrl Pts',(-45.6239324886583,5.59061553680362,1.62489667177482));
#34069=CARTESIAN_POINT('Ctrl Pts',(-45.4846738445754,4.12723821392213,4.10623623283363));
#34070=CARTESIAN_POINT('Ctrl Pts',(-45.3454152004926,1.65339647225928,5.58225325292712));
#34071=CARTESIAN_POINT('Ctrl Pts',(-45.2061565564098,-1.22524339802163,
5.69157710040891));
#34072=CARTESIAN_POINT('Ctrl Pts',(-45.0668979123269,-3.80390909819738,
4.40744221141311));
#34073=CARTESIAN_POINT('Ctrl Pts',(-44.9276392682442,-5.45127047408152,
2.04424105542907));
#34074=CARTESIAN_POINT('Ctrl Pts',(-44.7883806241612,-5.76400695900782,
-0.819448015925402));
#34075=CARTESIAN_POINT('Ctrl Pts',(-44.6491219800785,-4.66555183351562,
-3.48251308153665));
#34076=CARTESIAN_POINT('Ctrl Pts',(-44.5098633359956,-2.42483791960524,
-5.29296064012754));
#34077=CARTESIAN_POINT('Ctrl Pts',(-44.3706046919128,0.409544765544918,
-5.80754202389527));
#34078=CARTESIAN_POINT('Ctrl Pts',(-44.2313460478299,3.14365933142698,-4.90027318444869));
#34079=CARTESIAN_POINT('Ctrl Pts',(-44.0920874037471,5.1081173535065,-2.79327914414233));
#34080=CARTESIAN_POINT('Ctrl Pts',(-43.9528287596642,5.82196405509893,-0.00241152044091948));
#34081=CARTESIAN_POINT('Ctrl Pts',(-43.8135701155814,5.11042961313214,2.78904651153705));
#34082=CARTESIAN_POINT('Ctrl Pts',(-43.6743114714985,3.1477177442512,4.89766722806082));
#34083=CARTESIAN_POINT('Ctrl Pts',(-43.5350528274158,0.414355717547182,
5.80720075540968));
#34084=CARTESIAN_POINT('Ctrl Pts',(-43.3957941833329,-2.420452285279,5.29496761170287));
#34085=CARTESIAN_POINT('Ctrl Pts',(-43.25653553925,-4.66266524394653,3.48637692987834));
#34086=CARTESIAN_POINT('Ctrl Pts',(-43.1172768951672,-5.76332613280533,
0.824222761890331));
#34087=CARTESIAN_POINT('Ctrl Pts',(-42.9780182510844,-5.45296209671835,
-2.03972440443504));
#34088=CARTESIAN_POINT('Ctrl Pts',(-42.8387596070015,-3.80755901270078,
-4.40428945904965));
#34089=CARTESIAN_POINT('Ctrl Pts',(-42.6995009629187,-1.2299580022911,-5.69056012945078));
#34090=CARTESIAN_POINT('Ctrl Pts',(-42.5602423188358,1.64877144643314,-5.58362104657198));
#34091=CARTESIAN_POINT('Ctrl Pts',(-42.4209836747531,4.12383510341716,-4.10965391658703));
#34092=CARTESIAN_POINT('Ctrl Pts',(-42.2817250306701,5.58926751913469,-1.62952750017931));
#34093=CARTESIAN_POINT('Ctrl Pts',(-42.1424663865874,5.68628947187366,1.24955324670603));
#34094=CARTESIAN_POINT('Ctrl Pts',(-42.0032077425045,4.39114724886002,3.82270808630791));
#34095=CARTESIAN_POINT('Ctrl Pts',(-41.8639490984217,2.02092822566666,5.45995607866938));
#34096=CARTESIAN_POINT('Ctrl Pts',(-41.7246904543388,-0.844071074094882,
5.76045269889192));
#34097=CARTESIAN_POINT('Ctrl Pts',(-41.585431810256,-3.50241794841162,4.65062789190223));
#34098=CARTESIAN_POINT('Ctrl Pts',(-41.4461731661731,-5.3032740424208,2.40219809867558));
#34099=CARTESIAN_POINT('Ctrl Pts',(-41.3069145220903,-5.80573894959788,
-0.434357598548544));
#34100=CARTESIAN_POINT('Ctrl Pts',(-41.1676558780075,-4.88679507704601,
-3.16457029456666));
#34101=CARTESIAN_POINT('Ctrl Pts',(-41.0283972339247,-2.77142582478762,
-5.1200068527293));
#34102=CARTESIAN_POINT('Ctrl Pts',(-40.8891385898418,0.0224667014105143,
-5.82192120537735));
#34103=CARTESIAN_POINT('Ctrl Pts',(-40.749879945759,2.81085874491149,-5.09846490528761));
#34104=CARTESIAN_POINT('Ctrl Pts',(-40.6106213016761,4.91107322251077,-3.1267604765048));
#34105=CARTESIAN_POINT('Ctrl Pts',(-40.4713626575933,5.80891834506829,-0.389536820626648));
#34106=CARTESIAN_POINT('Ctrl Pts',(-40.3321040135105,5.28457628213744,2.44305644481769));
#34107=CARTESIAN_POINT('Ctrl Pts',(-40.1928453694276,3.46642077189376,4.67752052977624));
#34108=CARTESIAN_POINT('Ctrl Pts',(-40.0535867253448,0.799587606285317,
5.76679555161875));
#34109=CARTESIAN_POINT('Ctrl Pts',(-39.9143280812619,-2.06300717616523,
5.44419623685495));
#34110=CARTESIAN_POINT('Ctrl Pts',(-39.7750694371791,-4.42051956715754,
3.78870400409851));
#34111=CARTESIAN_POINT('Ctrl Pts',(-39.6358107930963,-5.69576398532674,
1.20563008329652));
#34112=CARTESIAN_POINT('Ctrl Pts',(-39.4965521490134,-5.57652459940273,
-1.67261611451975));
#34113=CARTESIAN_POINT('Ctrl Pts',(-39.3572935049306,-4.09199457695864,
-4.14135867275896));
#34114=CARTESIAN_POINT('Ctrl Pts',(-39.2180348608478,-1.60562877292209,
-5.59617972530006));
#34115=CARTESIAN_POINT('Ctrl Pts',(-39.0787762167649,1.27384027854431,-5.68089801167499));
#34116=CARTESIAN_POINT('Ctrl Pts',(-38.9395175726821,3.84143727175693,-4.37477210394456));
#34117=CARTESIAN_POINT('Ctrl Pts',(-38.8002589285993,5.46854198444228,-1.9975784937486));
#34118=CARTESIAN_POINT('Ctrl Pts',(-38.6610002845164,5.75679325289186,0.868678719523871));
#34119=CARTESIAN_POINT('Ctrl Pts',(-38.5217416404336,4.63561902980916,3.52225886112391));
#34120=CARTESIAN_POINT('Ctrl Pts',(-38.3824829963507,2.37951441360128,5.31349060691355));
#34121=CARTESIAN_POINT('Ctrl Pts',(-38.2432243522679,-0.459162500181017,
5.80382986248928));
#34122=CARTESIAN_POINT('Ctrl Pts',(-38.1039657081851,-3.18542347264294,
4.87322773675008));
#34123=CARTESIAN_POINT('Ctrl Pts',(-37.9647070641022,-5.1318028606111,2.74952189918877));
#34124=CARTESIAN_POINT('Ctrl Pts',(-37.8254484200194,-5.82177204735652,
-0.0473445130199082));
#34125=CARTESIAN_POINT('Ctrl Pts',(-37.6861897759365,-5.08640709945809,
-2.83261965199657));
#34126=CARTESIAN_POINT('Ctrl Pts',(-37.5469311318537,-3.1057461141024,-4.92438954074844));
#34127=CARTESIAN_POINT('Ctrl Pts',(-37.4076724877709,-0.364710810762607,
-5.8105298638599));
#34128=CARTESIAN_POINT('Ctrl Pts',(-37.2684138436881,2.46561599413806,-5.27408845619272));
#34129=CARTESIAN_POINT('Ctrl Pts',(-37.1291551996052,4.69229040406655,-3.4464013170552));
#34130=CARTESIAN_POINT('Ctrl Pts',(-36.9898965555224,5.77015966872752,-0.774937850208125));
#34131=CARTESIAN_POINT('Ctrl Pts',(-36.8506379114395,5.43533096595136,2.08625227737804));
#34132=CARTESIAN_POINT('Ctrl Pts',(-36.7113792673567,3.76977981374935,4.43666895656445));
#34133=CARTESIAN_POINT('Ctrl Pts',(-36.5721206232738,1.18128014949281,5.70086383653468));
#34134=CARTESIAN_POINT('Ctrl Pts',(-36.432861979191,-1.69643024063091,5.56932632487699));
#34135=CARTESIAN_POINT('Ctrl Pts',(-36.2936033351081,-4.15880662087851,
4.07426051749662));
#34136=CARTESIAN_POINT('Ctrl Pts',(-36.1543446910254,-5.60298974520627,
1.58170072687855));
#34137=CARTESIAN_POINT('Ctrl Pts',(-36.0150860469425,-5.67540281826104,
-1.29810405005511));
#34138=CARTESIAN_POINT('Ctrl Pts',(-35.8758274028596,-4.35831707567691,
-3.86009631254946));
#34139=CARTESIAN_POINT('Ctrl Pts',(-35.7365687587769,-1.97419228604106,
-5.47702803462159));
#34140=CARTESIAN_POINT('Ctrl Pts',(-35.597310114694,0.893270502876724,-5.75302868782914));
#34141=CARTESIAN_POINT('Ctrl Pts',(-35.4580514706112,3.54203545737847,-4.62052552129825));
#34142=CARTESIAN_POINT('Ctrl Pts',(-35.3187928265283,5.32361014705135,-2.35678727858641));
#34143=CARTESIAN_POINT('Ctrl Pts',(-35.1795341824455,5.80181479742939,0.483959017504846));
#34144=CARTESIAN_POINT('Ctrl Pts',(-35.0402755383626,4.85957141130056,3.20621848487671));
#34145=CARTESIAN_POINT('Ctrl Pts',(-34.9010168942798,2.72756776731154,5.14350516175671));
#34146=CARTESIAN_POINT('Ctrl Pts',(-34.7617582501969,-0.0722214601182912,
5.82151658376003));
#34147=CARTESIAN_POINT('Ctrl Pts',(-34.6224996061141,-2.85432883543797,
5.07425641581919));
#34148=CARTESIAN_POINT('Ctrl Pts',(-34.4832409620313,-4.93761593961783,
3.08467504076633));
#34149=CARTESIAN_POINT('Ctrl Pts',(-34.3439823179484,-5.81203528235817,
0.339878141277983));
#34150=CARTESIAN_POINT('Ctrl Pts',(-34.2047236738656,-5.26350432537642,
-2.48813052130279));
#34151=CARTESIAN_POINT('Ctrl Pts',(-34.0654650297828,-3.42631893091784,
-4.70697459711955));
#34152=CARTESIAN_POINT('Ctrl Pts',(-33.9262063856999,-0.750273943763396,
-5.77341842270285));
#34153=CARTESIAN_POINT('Ctrl Pts',(-33.7869477416171,2.10945928361774,-5.42636644588749));
#34154=CARTESIAN_POINT('Ctrl Pts',(-33.6476890975342,4.45273733238242,-3.75078678720913));
#34155=CARTESIAN_POINT('Ctrl Pts',(-33.5084304534514,5.70585958995129,-1.15690864550998));
#34156=CARTESIAN_POINT('Ctrl Pts',(-33.3691718093686,5.56202635443529,1.72021338992062));
#34157=CARTESIAN_POINT('Ctrl Pts',(-33.2299131652857,4.05645206202488,4.17617862917631));
#34158=CARTESIAN_POINT('Ctrl Pts',(-33.0906545212029,1.55774379897477,5.60969745450237));
#34159=CARTESIAN_POINT('Ctrl Pts',(-32.95139587712,-1.32234411818198,5.669803991974));
#34160=CARTESIAN_POINT('Ctrl Pts',(-32.8121372330372,-3.87868486797135,
4.34178246452594));
#34161=CARTESIAN_POINT('Ctrl Pts',(-32.6728785889544,-5.48541407425198,
1.95077002957627));
#34162=CARTESIAN_POINT('Ctrl Pts',(-32.5336199448715,-5.74915907244476,
-0.917845975107423));
#34163=CARTESIAN_POINT('Ctrl Pts',(-32.3943613007887,-4.60534764197699,
-3.5617473760546));
#34164=CARTESIAN_POINT('Ctrl Pts',(-32.2551026567059,-2.33401710862849,
-5.33363247805137));
#34165=CARTESIAN_POINT('Ctrl Pts',(-32.115844012623,0.508746697735507,-5.79969379121329));
#34166=CARTESIAN_POINT('Ctrl Pts',(-31.9765853685402,3.226954951551,-4.84582635006201));
#34167=CARTESIAN_POINT('Ctrl Pts',(-31.8373267244573,5.15511354248211,-2.70556383003843));
#34168=CARTESIAN_POINT('Ctrl Pts',(-31.6980680803746,5.82115481925269,0.0970970884525876));
#34169=CARTESIAN_POINT('Ctrl Pts',(-31.5588094362917,5.06201307624238,2.87598589882601));
#34170=CARTESIAN_POINT('Ctrl Pts',(-31.4195507922089,3.06354764125445,4.95075217760485));
#34171=CARTESIAN_POINT('Ctrl Pts',(-31.280292148126,0.31503926561749,5.81343457307417));
#34172=CARTESIAN_POINT('Ctrl Pts',(-31.1410335040432,-2.51059961519641,
5.25282408295484));
#34173=CARTESIAN_POINT('Ctrl Pts',(-31.0017748599603,-4.7215728408018,3.40617398018623));
#34174=CARTESIAN_POINT('Ctrl Pts',(-30.8625162158775,-5.77657175403985,
0.725596337314116));
#34175=CARTESIAN_POINT('Ctrl Pts',(-30.7232575717947,-5.4173028403555,-2.13262777112443));
#34176=CARTESIAN_POINT('Ctrl Pts',(-30.5839989277118,-3.7317252712905,-4.46872440120295));
#34177=CARTESIAN_POINT('Ctrl Pts',(-30.444740283629,-1.13251601637163,-5.71075115435407));
#34178=CARTESIAN_POINT('Ctrl Pts',(-30.3054816395461,1.7439651281085,-5.55462482137511));
#34179=CARTESIAN_POINT('Ctrl Pts',(-30.1662229954633,4.19347438043934,-4.03856953572594));
#34180=CARTESIAN_POINT('Ctrl Pts',(-30.0269643513805,5.61630273070555,-1.53375842666445));
#34181=CARTESIAN_POINT('Ctrl Pts',(-29.8877057072976,5.6641016350485,1.3465600403011));
#34182=CARTESIAN_POINT('Ctrl Pts',(-29.7484470632148,4.32516857241371,3.89720259859551));
#34183=CARTESIAN_POINT('Ctrl Pts',(-29.609188419132,1.92731215204464,5.49369995020442));
#34184=CARTESIAN_POINT('Ctrl Pts',(-29.4699297750491,-0.942404687467824,
5.74518447739786));
#34185=CARTESIAN_POINT('Ctrl Pts',(-29.3306711309663,-3.58139425721263,
4.59008566899347));
#34186=CARTESIAN_POINT('Ctrl Pts',(-29.1914124868835,-5.34355741690579,
2.31120431951092));
#34187=CARTESIAN_POINT('Ctrl Pts',(-29.0521538428006,-5.79746688257059,
-0.533525088249863));
#34188=CARTESIAN_POINT('Ctrl Pts',(-28.9128951987178,-4.83199280401928,
-3.24763249401785));
#34189=CARTESIAN_POINT('Ctrl Pts',(-28.7736365546349,-2.68351048916141,
-5.16662779081825));
#34190=CARTESIAN_POINT('Ctrl Pts',(-28.6343779105521,0.121970943793783,
-5.8206867604403));
#34191=CARTESIAN_POINT('Ctrl Pts',(-28.4951192664693,2.8975904467026,-5.0496773042911));
#34192=CARTESIAN_POINT('Ctrl Pts',(-28.3558606223864,4.96379801484174,-3.04236430135316));
#34193=CARTESIAN_POINT('Ctrl Pts',(-28.2166019783036,5.81472771045681,-0.290194637339041));
#34194=CARTESIAN_POINT('Ctrl Pts',(-28.0773433342207,5.24204792394922,2.5330228655333));
#34195=CARTESIAN_POINT('Ctrl Pts',(-27.9380846901379,3.38596683270716,4.73608486854933));
#34196=CARTESIAN_POINT('Ctrl Pts',(-27.7988260460551,0.700905481473475,
5.77961960515874));
#34197=CARTESIAN_POINT('Ctrl Pts',(-27.6595674019722,-2.15575731684136,
5.40814031485682));
#34198=CARTESIAN_POINT('Ctrl Pts',(-27.5203087578894,-4.48462987110196,
3.71259561405692));
#34199=CARTESIAN_POINT('Ctrl Pts',(-27.3810501138066,-5.71553844042309,
1.10810270748739));
#34200=CARTESIAN_POINT('Ctrl Pts',(-27.2417914697237,-5.54712186084846,
-1.76768502148767));
#34201=CARTESIAN_POINT('Ctrl Pts',(-27.1025328256409,-4.02061326513478,
-4.21069355884716));
#34202=CARTESIAN_POINT('Ctrl Pts',(-26.9632741815581,-1.50974504792053,
-5.62280545320343));
#34203=CARTESIAN_POINT('Ctrl Pts',(-26.8240155374752,1.37075137422973,-5.65829585160959));
#34204=CARTESIAN_POINT('Ctrl Pts',(-26.6847568933924,3.91564916628817,-4.30847570270991));
#34205=CARTESIAN_POINT('Ctrl Pts',(-26.5454982493095,5.50188551117867,-1.90381908178716));
#34206=CARTESIAN_POINT('Ctrl Pts',(-26.4062396052267,5.74110497526461,0.966946191515625));
#34207=CARTESIAN_POINT('Ctrl Pts',(-26.2669809611438,4.57473988103147,3.60097574210031));
#34208=CARTESIAN_POINT('Ctrl Pts',(-26.1277223170611,2.28834932779543,5.35338478238516));
#34209=CARTESIAN_POINT('Ctrl Pts',(-25.9884636729782,-0.55829373659443,
5.79513411216466));
#34210=CARTESIAN_POINT('Ctrl Pts',(-25.8492050288954,-3.26825073470533,
4.81807102577296));
#34211=CARTESIAN_POINT('Ctrl Pts',(-25.7099463848125,-5.17804769651491,
2.66140814737449));
#34212=CARTESIAN_POINT('Ctrl Pts',(-25.5706877407297,-5.82011241586959,
-0.146842571945131));
#34213=CARTESIAN_POINT('Ctrl Pts',(-25.4314290966468,-5.03724932521661,
-2.91914208456862));
#34214=CARTESIAN_POINT('Ctrl Pts',(-25.292170452564,-3.02112540787031,-4.97675321311146));
#34215=CARTESIAN_POINT('Ctrl Pts',(-25.1529118084812,-0.265344710105641,
-5.81591467089345));
#34216=CARTESIAN_POINT('Ctrl Pts',(-25.0136531643983,2.55539986286478,-5.23117604513226));
#34217=CARTESIAN_POINT('Ctrl Pts',(-24.8743945203155,4.75051041537242,-3.36569785746327));
#34218=CARTESIAN_POINT('Ctrl Pts',(-24.7351358762326,5.7825619204057,-0.676201827096679));
#34219=CARTESIAN_POINT('Ctrl Pts',(-24.5958772321498,5.39887903669928,2.17884749842298));
#34220=CARTESIAN_POINT('Ctrl Pts',(-24.456618588067,3.69339816481585,4.50045345164571));
#34221=CARTESIAN_POINT('Ctrl Pts',(-24.3173599439842,1.0836691646442,5.72022136074243));
#34222=CARTESIAN_POINT('Ctrl Pts',(-24.1781012999013,-1.79137263693289,
5.53951760985943));
#34223=CARTESIAN_POINT('Ctrl Pts',(-24.0388426558185,-4.22783584997752,
4.00258357813294));
#34224=CARTESIAN_POINT('Ctrl Pts',(-23.8995840117356,-5.6292055032563,1.48570410122738));
#34225=CARTESIAN_POINT('Ctrl Pts',(-23.7603253676528,-5.65238674767088,
-1.39491767823394));
#34226=CARTESIAN_POINT('Ctrl Pts',(-23.6210667235699,-4.29170416022648,
-3.93402423421483));
#34227=CARTESIAN_POINT('Ctrl Pts',(-23.4818080794871,-1.88029124778742,
-5.50997060770642));
#34228=CARTESIAN_POINT('Ctrl Pts',(-23.3425494354043,0.991470039123001,
-5.73692064053673));
#34229=CARTESIAN_POINT('Ctrl Pts',(-23.2032907913214,3.62049147315989,-4.55931055830499));
#34230=CARTESIAN_POINT('Ctrl Pts',(-23.0640321472386,5.36311439504185,-2.26545255081397));
#34231=CARTESIAN_POINT('Ctrl Pts',(-22.9247735031558,5.79269552259183,0.583052190493658));
#34232=CARTESIAN_POINT('Ctrl Pts',(-22.7855148590729,4.80406126953481,3.28880929712418));
#34233=CARTESIAN_POINT('Ctrl Pts',(-22.6462562149901,2.63925720826662,5.18937305104455));
#34234=CARTESIAN_POINT('Ctrl Pts',(-22.5069975709072,-0.171711518750607,
5.81943179602813));
#34235=CARTESIAN_POINT('Ctrl Pts',(-22.3677389268244,-2.94064041889114,
5.02472936595383));
#34236=CARTESIAN_POINT('Ctrl Pts',(-22.2284802827415,-4.98961753585213,
2.99983134862808));
#34237=CARTESIAN_POINT('Ctrl Pts',(-22.0892216386588,-5.81699543271016,
0.240489937676924));
#34238=CARTESIAN_POINT('Ctrl Pts',(-21.9499629945759,-5.22020864502445,
-2.57773019858685));
#34239=CARTESIAN_POINT('Ctrl Pts',(-21.8107043504931,-3.34536742456608,
-4.7648492178606));
#34240=CARTESIAN_POINT('Ctrl Pts',(-21.6714457064102,-0.651485825272392,
-5.78539864605405));
#34241=CARTESIAN_POINT('Ctrl Pts',(-21.5321870623274,2.20189789424249,-5.38951917499377));
#34242=CARTESIAN_POINT('Ctrl Pts',(-21.3929284182446,4.51619485389539,-3.67413327411291));
#34243=CARTESIAN_POINT('Ctrl Pts',(-21.2536697741617,5.72479982980199,-1.0592158339988));
#34244=CARTESIAN_POINT('Ctrl Pts',(-21.1144111300789,5.53181220726169,1.81502754190821));
#34245=CARTESIAN_POINT('Ctrl Pts',(-20.975152485996,3.98448080394246,4.24490094081229));
#34246=CARTESIAN_POINT('Ctrl Pts',(-20.8358938419132,1.46163602557251,5.63550276399928));
#34247=CARTESIAN_POINT('Ctrl Pts',(-20.6966351978304,-1.41905851103717,
5.64637443113256));
#34248=CARTESIAN_POINT('Ctrl Pts',(-20.5573765537475,-3.95232746684679,
4.27485425121175));
#34249=CARTESIAN_POINT('Ctrl Pts',(-20.4181179096647,-5.51795509215379,
1.85672907966367));
#34250=CARTESIAN_POINT('Ctrl Pts',(-20.2788592655818,-5.73263154962014,
-1.01597578248433));
#34251=CARTESIAN_POINT('Ctrl Pts',(-20.139600621499,-4.54379798255362,-3.6399410940339));
#34252=CARTESIAN_POINT('Ctrl Pts',(-20.0003419774162,-2.24251440666192,
-5.37274607721308));
#34253=CARTESIAN_POINT('Ctrl Pts',(-19.8610833333333,0.607799997858133,
-5.79015115838078));
#34254=CARTESIAN_POINT('Ctrl Pts',(-19.7218246892505,3.30930780587516,-4.78996379112292));
#34255=CARTESIAN_POINT('Ctrl Pts',(-19.5825660451677,5.20060364760623,-2.61705807631385));
#34256=CARTESIAN_POINT('Ctrl Pts',(-19.4433074010848,5.81864491334401,0.196577330103327));
#34257=CARTESIAN_POINT('Ctrl Pts',(-19.304048757002,5.01211765511721,2.96208505711049));
#34258=CARTESIAN_POINT('Ctrl Pts',(-19.1647901129191,2.97848251245621,5.00239074816106));
#34259=CARTESIAN_POINT('Ctrl Pts',(-19.0255314688363,0.215630773901309,
5.81796997617222));
#34260=CARTESIAN_POINT('Ctrl Pts',(-18.8862728247535,-2.60001346494751,
5.20914592389064));
#34261=CARTESIAN_POINT('Ctrl Pts',(-18.7470141806706,-4.77910101418741,
3.32497590524923));
#34262=CARTESIAN_POINT('Ctrl Pts',(-18.6077555365878,-5.7881297303052,0.62675792731469));
#34263=CARTESIAN_POINT('Ctrl Pts',(-18.468496892505,-5.38006090065132,-2.22490808339976));
#34264=CARTESIAN_POINT('Ctrl Pts',(-18.3292382484221,-3.65480129372495,
-4.53185379041305));
#34265=CARTESIAN_POINT('Ctrl Pts',(-18.1899796043393,-1.034743162069,-5.7292737639989));
#34266=CARTESIAN_POINT('Ctrl Pts',(-18.0507209602564,1.83864930447494,-5.52400579375589));
#34267=CARTESIAN_POINT('Ctrl Pts',(-17.9114623161736,4.26188851974257,-3.96630527312024));
#34268=CARTESIAN_POINT('Ctrl Pts',(-17.7722036720908,5.64169712044425,-1.4375412604395));
#34269=CARTESIAN_POINT('Ctrl Pts',(-17.6329450280079,5.64025901177969,1.44317343182744));
#34270=CARTESIAN_POINT('Ctrl Pts',(-17.4936863839251,4.25792628334514,3.97055852996697));
#34271=CARTESIAN_POINT('Ctrl Pts',(-17.3544277398422,1.83313300766102,5.52583881872415));
#34272=CARTESIAN_POINT('Ctrl Pts',(-17.2151690957594,-1.04046297412495,
5.72823778083364));
#34273=CARTESIAN_POINT('Ctrl Pts',(-17.0759104516766,-3.6593242495723,4.52820243703688));
#34274=CARTESIAN_POINT('Ctrl Pts',(-16.9366518075938,-5.38227965302423,
2.21953531418989));
#34275=CARTESIAN_POINT('Ctrl Pts',(-16.7973931635109,-5.78750106599166,
-0.632536706792661));
#34276=CARTESIAN_POINT('Ctrl Pts',(-16.6581345194281,-4.77577884795741,
-3.32974588665524));
#34277=CARTESIAN_POINT('Ctrl Pts',(-16.5188758753453,-2.59481115687255,
-5.21173928112917));
#34278=CARTESIAN_POINT('Ctrl Pts',(-16.3796172312624,0.221439551953394,
-5.81775178218575));
#34279=CARTESIAN_POINT('Ctrl Pts',(-16.2403585871796,2.98347560764755,-4.99941442299663));
#34280=CARTESIAN_POINT('Ctrl Pts',(-16.1010999430967,5.01507261679947,-2.95707928918434));
#34281=CARTESIAN_POINT('Ctrl Pts',(-15.9618412990139,5.81883828348449,-0.190767672706986));
#34282=CARTESIAN_POINT('Ctrl Pts',(-15.822582654931,5.19798808373605,2.62224925505428));
#34283=CARTESIAN_POINT('Ctrl Pts',(-15.6833240108482,3.3045236718621,4.79326554411477));
#34284=CARTESIAN_POINT('Ctrl Pts',(-15.5440653667654,0.602018584755516,
5.79075512328952));
#34285=CARTESIAN_POINT('Ctrl Pts',(-15.4048067226825,-2.24787764572838,
5.37050438638023));
#34286=CARTESIAN_POINT('Ctrl Pts',(-15.2655480785997,-4.54742997526647,
3.63540257665405));
#34287=CARTESIAN_POINT('Ctrl Pts',(-15.1262894345169,-5.73364308163917,
1.01025159572568));
#34288=CARTESIAN_POINT('Ctrl Pts',(-14.987030790434,-5.5160985118871,-1.86223749329987));
#34289=CARTESIAN_POINT('Ctrl Pts',(-14.8477721463512,-3.94805731755129,
-4.27879827657537));
#34290=CARTESIAN_POINT('Ctrl Pts',(-14.7085135022684,-1.41342024579856,
-5.64778845948229));
#34291=CARTESIAN_POINT('Ctrl Pts',(-14.5692548581855,1.46726200026636,-5.63404060127978));
#34292=CARTESIAN_POINT('Ctrl Pts',(-14.4299962141027,3.98871709067603,-4.24092056573142));
#34293=CARTESIAN_POINT('Ctrl Pts',(-14.2907375700198,5.53362164346046,-1.80950346264411));
#34294=CARTESIAN_POINT('Ctrl Pts',(-14.151478925937,5.72373941440754,1.06493116690821));
#34295=CARTESIAN_POINT('Ctrl Pts',(-14.0122202818542,4.51252420652974,3.67864058583845));
#34296=CARTESIAN_POINT('Ctrl Pts',(-13.8729616377713,2.19651569299616,5.39171494839225));
#34297=CARTESIAN_POINT('Ctrl Pts',(-13.7337029936885,-0.65726186560512,
5.78474529381513));
#34298=CARTESIAN_POINT('Ctrl Pts',(-13.5944443496056,-3.3501231662653,4.76150669905519));
#34299=CARTESIAN_POINT('Ctrl Pts',(-13.4551857055228,-5.22277974827667,
2.57251685617135));
#34300=CARTESIAN_POINT('Ctrl Pts',(-13.31592706144,-5.81675241886189,-0.246297730316495));
#34301=CARTESIAN_POINT('Ctrl Pts',(-13.1766684173571,-4.98661990155326,
-3.00481167991068));
#34302=CARTESIAN_POINT('Ctrl Pts',(-13.0374097732743,-2.93562206963557,
-5.02766291019628));
#34303=CARTESIAN_POINT('Ctrl Pts',(-12.8981511291915,-0.165901088094421,
-5.81960033879168));
#34304=CARTESIAN_POINT('Ctrl Pts',(-12.7588924851086,2.64443716288153,-5.18673532830294));
#34305=CARTESIAN_POINT('Ctrl Pts',(-12.6196338410258,4.80734254899847,-3.28401109786243));
#34306=CARTESIAN_POINT('Ctrl Pts',(-12.480375196943,5.79327477706733,-0.577268249335009));
#34307=CARTESIAN_POINT('Ctrl Pts',(-12.3411165528601,5.36084980668236,2.27080616180433));
#34308=CARTESIAN_POINT('Ctrl Pts',(-12.2018579087773,3.61593747712075,4.56292312403445));
#34309=CARTESIAN_POINT('Ctrl Pts',(-12.0625992646944,0.985741582185208,
5.73790770293893));
#34310=CARTESIAN_POINT('Ctrl Pts',(-11.9233406206116,-1.8857916776622,5.50809050604244));
#34311=CARTESIAN_POINT('Ctrl Pts',(-11.7840819765287,-4.29562990253827,
3.92973727044363));
#34312=CARTESIAN_POINT('Ctrl Pts',(-11.6448233324459,-5.6537766698856,1.38927342209956));
#34313=CARTESIAN_POINT('Ctrl Pts',(-11.5055646883631,-5.62771931318099,
-1.49132377649678));
#34314=CARTESIAN_POINT('Ctrl Pts',(-11.3663060442803,-4.22383740889487,
-4.00680281739882));
#34315=CARTESIAN_POINT('Ctrl Pts',(-11.2270474001974,-1.7858408760882,-5.54130342424841));
#34316=CARTESIAN_POINT('Ctrl Pts',(-11.0877887561146,1.08937991404511,-5.71913653248196));
#34317=CARTESIAN_POINT('Ctrl Pts',(-10.9485301120317,3.69788975011609,-4.49676357731658));
#34318=CARTESIAN_POINT('Ctrl Pts',(-10.8092714679489,5.40105179102856,-2.1734559634191));
#34319=CARTESIAN_POINT('Ctrl Pts',(-10.6700128238661,5.78188389217159,0.681975022813711));
#34320=CARTESIAN_POINT('Ctrl Pts',(-10.5307541797832,4.74714760502601,3.37043927261576));
#34321=CARTESIAN_POINT('Ctrl Pts',(-10.3914955357004,2.55017558130455,5.23372484744972));
#34322=CARTESIAN_POINT('Ctrl Pts',(-10.2522368916175,-0.271151411282281,
5.81564684162084));
#34323=CARTESIAN_POINT('Ctrl Pts',(-10.1129782475347,-3.02609288430336,
4.97373432441496));
#34324=CARTESIAN_POINT('Ctrl Pts',(-9.97371960345188,-5.0401613984529,2.91411124561851));
#34325=CARTESIAN_POINT('Ctrl Pts',(-9.83446095936901,-5.82025612817856,
0.141031474127366));
#34326=CARTESIAN_POINT('Ctrl Pts',(-9.69520231528622,-5.17538786306668,
-2.66657678327793));
#34327=CARTESIAN_POINT('Ctrl Pts',(-9.55594367120334,-3.26343855781002,
-4.82133177179226));
#34328=CARTESIAN_POINT('Ctrl Pts',(-9.41668502712053,-0.552507372994592,
-5.79568864562974));
#34329=CARTESIAN_POINT('Ctrl Pts',(-9.27742638303768,2.29369321295268,-5.35109733785042));
#34330=CARTESIAN_POINT('Ctrl Pts',(-9.13816773895486,4.57833295381206,-3.59640635055793));
#34331=CARTESIAN_POINT('Ctrl Pts',(-8.99890909487199,5.74206755002624,-0.961213569000321));
#34332=CARTESIAN_POINT('Ctrl Pts',(-8.85965045078918,5.49998192244803,1.90931142746273));
#34333=CARTESIAN_POINT('Ctrl Pts',(-8.72039180670633,3.91134546632114,4.31238309028591));
#34334=CARTESIAN_POINT('Ctrl Pts',(-8.58113316262349,1.3651012302635,5.65966164230935));
#34335=CARTESIAN_POINT('Ctrl Pts',(-8.44187451854066,-1.51535832115029,
5.62129526291009));
#34336=CARTESIAN_POINT('Ctrl Pts',(-8.30261587445782,-4.02481537988956,
4.20667712477429));
#34337=CARTESIAN_POINT('Ctrl Pts',(-8.16335723037498,-5.54888402081865,
1.76214568007252));
#34338=CARTESIAN_POINT('Ctrl Pts',(-8.02409858629214,-5.71442921910558,
-1.1138087691014));
#34339=CARTESIAN_POINT('Ctrl Pts',(-7.88483994220931,-4.48092083718648,
-3.71707139091558));
#34340=CARTESIAN_POINT('Ctrl Pts',(-7.74558129812645,-2.1503565465292,-5.4102900104425));
#34341=CARTESIAN_POINT('Ctrl Pts',(-7.60632265404363,0.706675727156433,
-5.77891691331019));
#34342=CARTESIAN_POINT('Ctrl Pts',(-7.4670640099608,3.39069383473469,-4.73270182806681));
#34343=CARTESIAN_POINT('Ctrl Pts',(-7.32780536587796,5.24457437879084,-2.52778774022372));
#34344=CARTESIAN_POINT('Ctrl Pts',(-7.18854672179512,5.81443507065043,0.296000141022397));
#34345=CARTESIAN_POINT('Ctrl Pts',(-7.04928807771229,4.96075792687253,3.04731883223044));
#34346=CARTESIAN_POINT('Ctrl Pts',(-6.91002943362943,2.89254720992126,5.05256785334662));
#34347=CARTESIAN_POINT('Ctrl Pts',(-6.77077078954661,0.116159284925314,
5.82080563967053));
#34348=CARTESIAN_POINT('Ctrl Pts',(-6.63151214546377,-2.688667711974,5.16394589523199));
#34349=CARTESIAN_POINT('Ctrl Pts',(-6.49225350138093,-4.83523295705307,
3.24280642735931));
#34350=CARTESIAN_POINT('Ctrl Pts',(-6.35299485729808,-5.79799668489952,
0.527736407867602));
#34351=CARTESIAN_POINT('Ctrl Pts',(-6.21373621321526,-5.34124715796441,
-2.31653838125593));
#34352=CARTESIAN_POINT('Ctrl Pts',(-6.07447756913242,-3.57680955360403,
-4.59365918321567));
#34353=CARTESIAN_POINT('Ctrl Pts',(-5.93521892504958,-0.936668004052796,
-5.74612254694228));
#34354=CARTESIAN_POINT('Ctrl Pts',(-5.79596028096675,1.93279631323058,-5.49177290916668));
#34355=CARTESIAN_POINT('Ctrl Pts',(-5.6567016368839,4.32905753390492,-3.89288224101835));
#34356=CARTESIAN_POINT('Ctrl Pts',(-5.51744299280107,5.66544326929399,-1.34090411167474));
#34357=CARTESIAN_POINT('Ctrl Pts',(-5.37818434871822,5.61476856777023,1.53936519535622));
#34358=CARTESIAN_POINT('Ctrl Pts',(-5.2389257046354,4.18944002671629,4.04275444923907));
#34359=CARTESIAN_POINT('Ctrl Pts',(-5.09966706055255,1.73841830727115,5.55636329474948));
#34360=CARTESIAN_POINT('Ctrl Pts',(-4.96040841646972,-1.13821728600617,
5.70961756023392));
#34361=CARTESIAN_POINT('Ctrl Pts',(-4.82114977238688,-3.73618515797981,
4.46499627542801));
#34362=CARTESIAN_POINT('Ctrl Pts',(-4.68189112830405,-5.419429437944,2.12721786412234));
#34363=CARTESIAN_POINT('Ctrl Pts',(-4.5426324842212,-5.77584441140805,-0.731363527598105));
#34364=CARTESIAN_POINT('Ctrl Pts',(-4.40337384013837,-4.71816963195763,
-3.41088648277354));
#34365=CARTESIAN_POINT('Ctrl Pts',(-4.26411519605553,-2.50535374173064,
-5.25532814418794));
#34366=CARTESIAN_POINT('Ctrl Pts',(-4.12485655197268,0.320843465798982,
-5.81311712807697));
#34367=CARTESIAN_POINT('Ctrl Pts',(-3.98559790788985,3.06848913610684,-4.94769094587604));
#34368=CARTESIAN_POINT('Ctrl Pts',(-3.84633926380702,5.06488204833466,-2.87093035630064));
#34369=CARTESIAN_POINT('Ctrl Pts',(-3.70708061972418,5.82124886323545,-0.0912849746588416));
#34370=CARTESIAN_POINT('Ctrl Pts',(-3.56782197564134,5.1524096337254,2.71070954559799));
#34371=CARTESIAN_POINT('Ctrl Pts',(-3.42856333155851,3.22211508326084,4.84904585092794));
#34372=CARTESIAN_POINT('Ctrl Pts',(-3.28930468747566,0.50295580625768,5.80019885276506));
#34373=CARTESIAN_POINT('Ctrl Pts',(-3.15004604339282,-2.3393412495323,5.33129944682399));
#34374=CARTESIAN_POINT('Ctrl Pts',(-3.01078739931,-4.60890153244437,3.55714744422309));
#34375=CARTESIAN_POINT('Ctrl Pts',(-2.87152875522714,-5.7500726195336,0.912105335297638));
#34376=CARTESIAN_POINT('Ctrl Pts',(-2.73227011114431,-5.48346361630806,
-1.95624590565041));
#34377=CARTESIAN_POINT('Ctrl Pts',(-2.59301146706147,-3.87434793125781,
-4.34565292985953));
#34378=CARTESIAN_POINT('Ctrl Pts',(-2.45375282297864,-1.31668250898415,
-5.6711214434338));
#34379=CARTESIAN_POINT('Ctrl Pts',(-2.3144941788958,1.56334396233179,-5.60813935051552));
#34380=CARTESIAN_POINT('Ctrl Pts',(-2.17523553481297,4.06061969479119,-4.17212642249236));
#34381=CARTESIAN_POINT('Ctrl Pts',(-2.03597689073013,5.56374111549523,-1.71465920456093));
#34382=CARTESIAN_POINT('Ctrl Pts',(-1.89671824664728,5.70470163197095,1.16260504562314));
#34383=CARTESIAN_POINT('Ctrl Pts',(-1.75745960256445,4.44899020576231,3.75523065046461));
#34384=CARTESIAN_POINT('Ctrl Pts',(-1.61820095848162,2.10404029395573,5.42847000776503));
#34385=CARTESIAN_POINT('Ctrl Pts',(-1.47894231439877,-0.756037886019822,
5.77266624528129));
#34386=CARTESIAN_POINT('Ctrl Pts',(-1.33968367031594,-3.43101701838151,
4.70355166697811));
#34387=CARTESIAN_POINT('Ctrl Pts',(-1.20042502623311,-5.26598561487944,
2.48287324446187));
#34388=CARTESIAN_POINT('Ctrl Pts',(-1.06116638215026,-5.81169368649649,
-0.345679466703461));
#34389=CARTESIAN_POINT('Ctrl Pts',(-0.921907738067424,-4.9345323547016,
-3.08960626820369));
#34390=CARTESIAN_POINT('Ctrl Pts',(-0.782649093984597,-2.84926354822401,
-5.0770981807467));
#34391=CARTESIAN_POINT('Ctrl Pts',(-0.643390449901746,-0.0664041808042648,
-5.82159667367763));
#34392=CARTESIAN_POINT('Ctrl Pts',(-0.504131805818908,2.73269248345949,
-5.140758053774));
#34393=CARTESIAN_POINT('Ctrl Pts',(-0.364873161736075,4.86278854237602,
-3.20140635770316));
#34394=CARTESIAN_POINT('Ctrl Pts',(-0.225614517653243,5.80225927534941,
-0.478084902857893));
#34395=CARTESIAN_POINT('Ctrl Pts',(-0.0863558735703991,5.32132481240374,
2.36194063957689));
#34396=CARTESIAN_POINT('Ctrl Pts',(0.0529027705124292,3.53727759009006,
4.62439958704637));
#34397=CARTESIAN_POINT('Ctrl Pts',(0.145741866567655,1.77099953538148,5.37678124514415));
#34398=CARTESIAN_POINT('Ctrl Pts',(0.192161414595269,0.851236939700787,
5.51865210108108));
#34399=CARTESIAN_POINT('Ctrl Pts',(-59.7754114145953,3.05041111877658,-4.27420965560363));
#34400=CARTESIAN_POINT('Ctrl Pts',(-59.7289918665677,3.76276951631921,-3.76581485246873));
#34401=CARTESIAN_POINT('Ctrl Pts',(-59.6361527705124,4.92764081706816,-2.38646903685034));
#34402=CARTESIAN_POINT('Ctrl Pts',(-59.4968941264296,5.46835202429936,0.268532173657807));
#34403=CARTESIAN_POINT('Ctrl Pts',(-59.3576354823467,4.67030006375477,2.85707072904638));
#34404=CARTESIAN_POINT('Ctrl Pts',(-59.2183768382639,2.7288083410323,4.74647128728181));
#34405=CARTESIAN_POINT('Ctrl Pts',(-59.0791181941811,0.119236398296101,
5.47362186748481));
#34406=CARTESIAN_POINT('Ctrl Pts',(-58.9398595500982,-2.5195326040976,4.86076733852051));
#34407=CARTESIAN_POINT('Ctrl Pts',(-58.8006009060154,-4.54144653710774,
3.05781259658032));
#34408=CARTESIAN_POINT('Ctrl Pts',(-58.6613422619325,-5.4514873740282,0.506243184157782));
#34409=CARTESIAN_POINT('Ctrl Pts',(-58.5220836178498,-5.02684959533072,
-2.16928123765479));
#34410=CARTESIAN_POINT('Ctrl Pts',(-58.3828249737669,-3.37149745588529,
-4.3136980286988));
#34411=CARTESIAN_POINT('Ctrl Pts',(-58.2435663296841,-0.890707405090836,
-5.40200302908979));
#34412=CARTESIAN_POINT('Ctrl Pts',(-58.1043076856012,1.80815287776022,-5.16774353188138));
#34413=CARTESIAN_POINT('Ctrl Pts',(-57.9650490415184,4.06432633833454,-3.6682753974527));
#34414=CARTESIAN_POINT('Ctrl Pts',(-57.8257903974356,5.32543796117294,-1.27070945920114));
#34415=CARTESIAN_POINT('Ctrl Pts',(-57.6865317533527,5.2827320554894,1.43796179978132));
#34416=CARTESIAN_POINT('Ctrl Pts',(-57.5472731092699,3.94666421546139,3.79457953437703));
#34417=CARTESIAN_POINT('Ctrl Pts',(-57.4080144651871,1.64434157169202,5.22217702626599));
#34418=CARTESIAN_POINT('Ctrl Pts',(-57.2687558211042,-1.06056230695092,
5.37123820032749));
#34419=CARTESIAN_POINT('Ctrl Pts',(-57.1294971770214,-3.50581059443648,
4.20526862770603));
#34420=CARTESIAN_POINT('Ctrl Pts',(-56.9902385329385,-5.09273748649819,
2.0097305963032));
#34421=CARTESIAN_POINT('Ctrl Pts',(-56.8509798888557,-5.43281848345632,
-0.677846219983215));
#34422=CARTESIAN_POINT('Ctrl Pts',(-56.7117212447728,-4.4427921577306,-3.19946714523332));
#34423=CARTESIAN_POINT('Ctrl Pts',(-56.5724626006901,-2.36504490024336,
-4.93776819958314));
#34424=CARTESIAN_POINT('Ctrl Pts',(-56.4332039566072,0.291732109474193,
-5.46716421440776));
#34425=CARTESIAN_POINT('Ctrl Pts',(-56.2939453125243,2.87708486376904,-4.65804410227385));
#34426=CARTESIAN_POINT('Ctrl Pts',(-56.1546866684415,4.75804602882236,-2.70850330611462));
#34427=CARTESIAN_POINT('Ctrl Pts',(-56.0154280243586,5.47410321551656,-0.0958444448425244));
#34428=CARTESIAN_POINT('Ctrl Pts',(-55.8761693802759,4.84994541162324,2.54027984206958));
#34429=CARTESIAN_POINT('Ctrl Pts',(-55.7369107361929,3.03838406631521,4.55447191639935));
#34430=CARTESIAN_POINT('Ctrl Pts',(-55.5976520921102,0.482940533822174,
5.45360070160385));
#34431=CARTESIAN_POINT('Ctrl Pts',(-55.4583934480273,-2.19074047383461,
5.01753409037006));
#34432=CARTESIAN_POINT('Ctrl Pts',(-55.3191348039445,-4.32806637309799,
3.35303349845926));
#34433=CARTESIAN_POINT('Ctrl Pts',(-55.1798761598616,-5.40575945122019,
0.867615656424194));
#34434=CARTESIAN_POINT('Ctrl Pts',(-55.0406175157789,-5.15997002146987,
-1.83021898942756));
#34435=CARTESIAN_POINT('Ctrl Pts',(-54.9013588716959,-3.65087427441368,
-4.07996436309852));
#34436=CARTESIAN_POINT('Ctrl Pts',(-54.7621002276132,-1.24794144780751,
-5.33081929111963));
#34437=CARTESIAN_POINT('Ctrl Pts',(-54.6228415835303,1.46052267221381,-5.27653917787774));
#34438=CARTESIAN_POINT('Ctrl Pts',(-54.4835829394475,3.81140961432537,-3.9304133273178));
#34439=CARTESIAN_POINT('Ctrl Pts',(-54.3443242953646,5.22915589407203,-1.622011346206));
#34440=CARTESIAN_POINT('Ctrl Pts',(-54.2050656512818,5.36665720191545,1.08350479872415));
#34441=CARTESIAN_POINT('Ctrl Pts',(-54.0658070071989,4.19024933629756,3.52374838366578));
#34442=CARTESIAN_POINT('Ctrl Pts',(-53.9265483631161,1.98795015045772,5.10127889563238));
#34443=CARTESIAN_POINT('Ctrl Pts',(-53.7872897190333,-0.701055348231372,
5.42987233463601));
#34444=CARTESIAN_POINT('Ctrl Pts',(-53.6480310749504,-3.2184227082265,4.42907975124644));
#34445=CARTESIAN_POINT('Ctrl Pts',(-53.5087724308676,-4.94782933935193,
2.34392342033126));
#34446=CARTESIAN_POINT('Ctrl Pts',(-53.3695137867847,-5.46586768047832,
-0.315091528340425));
#34447=CARTESIAN_POINT('Ctrl Pts',(-53.2302551427019,-4.64570732246977,
-2.8969631764453));
#34448=CARTESIAN_POINT('Ctrl Pts',(-53.0909964986191,-2.68814667251956,
-4.76957646324611));
#34449=CARTESIAN_POINT('Ctrl Pts',(-52.9517378545362,-0.0724518359154483,
-5.47446279585511));
#34450=CARTESIAN_POINT('Ctrl Pts',(-52.8124792104534,2.56098125529703,-4.83904610246136));
#34451=CARTESIAN_POINT('Ctrl Pts',(-52.6732205663706,4.56741384362734,-3.01889432620133));
#34452=CARTESIAN_POINT('Ctrl Pts',(-52.5339619222877,5.45561459371124,-0.459632001294636));
#34453=CARTESIAN_POINT('Ctrl Pts',(-52.3947032782049,5.00812688972579,2.21216121205818));
#34454=CARTESIAN_POINT('Ctrl Pts',(-52.2554446341221,3.33450835332562,4.34235491563401));
#34455=CARTESIAN_POINT('Ctrl Pts',(-52.1161859900392,0.844508045260551,
5.4094175595178));
#34456=CARTESIAN_POINT('Ctrl Pts',(-51.9769273459563,-1.85225167112555,
5.15210208735637));
#34457=CARTESIAN_POINT('Ctrl Pts',(-51.8376687018735,-4.09552789291051,
3.63340659025675));
#34458=CARTESIAN_POINT('Ctrl Pts',(-51.6984100577907,-5.33610327761922,
1.22515059576798));
#34459=CARTESIAN_POINT('Ctrl Pts',(-51.5591514137078,-5.27024995201298,
-1.48305684821466));
#34460=CARTESIAN_POINT('Ctrl Pts',(-51.419892769625,-3.91409066911317,-3.828170111906));
#34461=CARTESIAN_POINT('Ctrl Pts',(-51.2806341255422,-1.5996515031473,-5.23603927030803));
#34462=CARTESIAN_POINT('Ctrl Pts',(-51.1413754814594,1.1064275058807,-5.36197821199973));
#34463=CARTESIAN_POINT('Ctrl Pts',(-51.0021168373765,3.54162182914421,-4.1751535290404));
#34464=CARTESIAN_POINT('Ctrl Pts',(-50.8628581932937,5.10972715544653,-1.96613340560134));
#34465=CARTESIAN_POINT('Ctrl Pts',(-50.7235995492108,5.42682703630521,0.724251675701316));
#34466=CARTESIAN_POINT('Ctrl Pts',(-50.584340905128,4.41528646976498,3.23731950255755));
#34467=CARTESIAN_POINT('Ctrl Pts',(-50.4450822610451,2.32275914036367,4.95780013187161));
#34468=CARTESIAN_POINT('Ctrl Pts',(-50.3058236169624,-0.338445193631064,
5.46447133972146));
#34469=CARTESIAN_POINT('Ctrl Pts',(-50.1665649728795,-2.91678859056669,
4.6332857120697));
#34470=CARTESIAN_POINT('Ctrl Pts',(-50.0273063287967,-4.78101980518796,
2.66774095334042));
#34471=CARTESIAN_POINT('Ctrl Pts',(-49.8880476847138,-5.47472241248648,
0.0490579040265954));
#34472=CARTESIAN_POINT('Ctrl Pts',(-49.7487890406309,-4.8280584323024,-2.58163590500342));
#34473=CARTESIAN_POINT('Ctrl Pts',(-49.6095303965482,-2.99934946106781,
-4.58027236986203));
#34474=CARTESIAN_POINT('Ctrl Pts',(-49.4702717524653,-0.436315075885255,
-5.45752886628046));
#34475=CARTESIAN_POINT('Ctrl Pts',(-49.3310131083825,2.23354155621114,-4.99862824066834));
#34476=CARTESIAN_POINT('Ctrl Pts',(-49.1917544642996,4.35656416675584,-3.31592232005941));
#34477=CARTESIAN_POINT('Ctrl Pts',(-49.0524958202167,5.41297689183398,-0.821385013377194));
#34478=CARTESIAN_POINT('Ctrl Pts',(-48.913237176134,5.14414007584278,1.87425053070219));
#34479=CARTESIAN_POINT('Ctrl Pts',(-48.773978532051,3.61587256008425,4.11101663837049));
#34480=CARTESIAN_POINT('Ctrl Pts',(-48.6347198879684,1.20233737247478,5.34128982685639));
#34481=CARTESIAN_POINT('Ctrl Pts',(-48.4954612438854,-1.50556394359286,
5.26386449136776));
#34482=CARTESIAN_POINT('Ctrl Pts',(-48.3562025998026,-3.84486070708852,
3.89769653960079));
#34483=CARTESIAN_POINT('Ctrl Pts',(-48.2169439557197,-5.2428270364507,1.57726245044722));
#34484=CARTESIAN_POINT('Ctrl Pts',(-48.0776853116369,-5.35720131234524,
-1.12933000966752));
#34485=CARTESIAN_POINT('Ctrl Pts',(-47.9384266675541,-4.15998148346686,
-3.55943060459705));
#34486=CARTESIAN_POINT('Ctrl Pts',(-47.7991680234712,-1.94428075914289,
-5.11808211162696));
#34487=CARTESIAN_POINT('Ctrl Pts',(-47.6599093793885,0.747434778333361,
-5.42368264409589));
#34488=CARTESIAN_POINT('Ctrl Pts',(-47.5206507353055,3.25615718342438,-4.40141256513894));
#34489=CARTESIAN_POINT('Ctrl Pts',(-47.3813920912228,4.96768039494549,-2.30155244680704));
#34490=CARTESIAN_POINT('Ctrl Pts',(-47.2421334471398,5.46297521770101,0.361792678911387));
#34491=CARTESIAN_POINT('Ctrl Pts',(-47.1028748030571,4.62077949785816,2.93656074411938));
#34492=CARTESIAN_POINT('Ctrl Pts',(-46.9636161589742,2.64728652120321,4.79237584569334));
#34493=CARTESIAN_POINT('Ctrl Pts',(-46.8243575148914,0.0256630763402578,
5.47488206066962));
#34494=CARTESIAN_POINT('Ctrl Pts',(-46.6850988708086,-2.60224341403018,
4.81698260178151));
#34495=CARTESIAN_POINT('Ctrl Pts',(-46.5458402267257,-4.59304726030904,
2.97974982780383));
#34496=CARTESIAN_POINT('Ctrl Pts',(-46.4065815826429,-5.45934348435565,
0.41299018336124));
#34497=CARTESIAN_POINT('Ctrl Pts',(-46.26732293856,-4.98903831664372,-2.25488111588837));
#34498=CARTESIAN_POINT('Ctrl Pts',(-46.1280642944772,-3.29727573804136,
-4.37069386700247));
#34499=CARTESIAN_POINT('Ctrl Pts',(-45.9888056503943,-0.798246983000946,
-5.41643738317532));
#34500=CARTESIAN_POINT('Ctrl Pts',(-45.8495470063115,1.89621516645834,-5.13608413231546));
#34501=CARTESIAN_POINT('Ctrl Pts',(-45.7102883622287,4.12643031665392,-3.59827250406756));
#34502=CARTESIAN_POINT('Ctrl Pts',(-45.5710297181459,5.34637884412477,-1.17950219449742));
#34503=CARTESIAN_POINT('Ctrl Pts',(-45.431771074063,5.2573829125406,1.5280435473688));
#34504=CARTESIAN_POINT('Ctrl Pts',(-45.2925124299802,3.8812312381375,3.86148109510261));
#34505=CARTESIAN_POINT('Ctrl Pts',(-45.1532537858974,1.55484459692986,5.24951906855545));
#34506=CARTESIAN_POINT('Ctrl Pts',(-45.0139951418145,-1.1522118918849,5.35232659017816));
#34507=CARTESIAN_POINT('Ctrl Pts',(-44.8747364977316,-3.57717438483602,
4.14473347661853));
#34508=CARTESIAN_POINT('Ctrl Pts',(-44.7354778536489,-5.12634361161217,
1.92239261011174));
#34509=CARTESIAN_POINT('Ctrl Pts',(-44.5962192095659,-5.42043921542468,
-0.770604232804061));
#34510=CARTESIAN_POINT('Ctrl Pts',(-44.4569605654832,-4.38745829070579,
-3.27493540685099));
#34511=CARTESIAN_POINT('Ctrl Pts',(-44.3177019214003,-2.28030372689555,
-4.97746994815997));
#34512=CARTESIAN_POINT('Ctrl Pts',(-44.1784432773175,0.385133557856286,
-5.46137934173613));
#34513=CARTESIAN_POINT('Ctrl Pts',(-44.0391846332346,2.95627927606374,-4.60818890819867));
#34514=CARTESIAN_POINT('Ctrl Pts',(-43.8999259891518,4.8036443774009,-2.62678374960595));
#34515=CARTESIAN_POINT('Ctrl Pts',(-43.7606673450689,5.47494173748935,-0.00226778004610677));
#34516=CARTESIAN_POINT('Ctrl Pts',(-43.6214087009862,4.80581881314338,2.62280340608412));
#34517=CARTESIAN_POINT('Ctrl Pts',(-43.4821500569032,2.96009578429874,4.60573828169883));
#34518=CARTESIAN_POINT('Ctrl Pts',(-43.3428914128205,0.389657749635209,
5.46105841480188));
#34519=CARTESIAN_POINT('Ctrl Pts',(-43.2036327687376,-2.27617950142941,
4.97935729276398));
#34520=CARTESIAN_POINT('Ctrl Pts',(-43.0643741246547,-4.38474375836553,
3.27856894775812));
#34521=CARTESIAN_POINT('Ctrl Pts',(-42.925115480572,-5.41979897035326,0.775094376632309));
#34522=CARTESIAN_POINT('Ctrl Pts',(-42.7858568364891,-5.12793440387594,
-1.91814517731967));
#34523=CARTESIAN_POINT('Ctrl Pts',(-42.6465981924063,-3.58060674358378,
-4.14176864630699));
#34524=CARTESIAN_POINT('Ctrl Pts',(-42.5073395483234,-1.15664547880632,
-5.35137023649888));
#34525=CARTESIAN_POINT('Ctrl Pts',(-42.3680809042406,1.55049524906482,-5.25080533388515));
#34526=CARTESIAN_POINT('Ctrl Pts',(-42.2288222601577,3.87803097245991,-3.86469506537978));
#34527=CARTESIAN_POINT('Ctrl Pts',(-42.0895636160749,5.2561152444257,-1.53239835194539));
#34528=CARTESIAN_POINT('Ctrl Pts',(-41.9503049719921,5.34735413451096,1.17507273470952));
#34529=CARTESIAN_POINT('Ctrl Pts',(-41.8110463279092,4.12940978692406,3.59485284585963));
#34530=CARTESIAN_POINT('Ctrl Pts',(-41.6717876838264,1.90046935818554,5.13451150454715));
#34531=CARTESIAN_POINT('Ctrl Pts',(-41.5325290397435,-0.793759616039144,
5.41709680951658));
#34532=CARTESIAN_POINT('Ctrl Pts',(-41.3932703956607,-3.29365382994698,
4.37342390127059));
#34533=CARTESIAN_POINT('Ctrl Pts',(-41.2540117515779,-4.98716861275776,
2.25901336863089));
#34534=CARTESIAN_POINT('Ctrl Pts',(-41.114753107495,-5.45968374096753,-0.408467404261251));
#34535=CARTESIAN_POINT('Ctrl Pts',(-40.9754944634122,-4.59551417299541,
-2.9759438263394));
#34536=CARTESIAN_POINT('Ctrl Pts',(-40.8362358193294,-2.60623301292921,
-4.81482519454727));
#34537=CARTESIAN_POINT('Ctrl Pts',(-40.6969771752465,0.0211275576577767,
-5.47490144185597));
#34538=CARTESIAN_POINT('Ctrl Pts',(-40.5577185311637,2.64331550573975,-4.7945672702388));
#34539=CARTESIAN_POINT('Ctrl Pts',(-40.4184598870809,4.61834520229331,-2.94038768943546));
#34540=CARTESIAN_POINT('Ctrl Pts',(-40.279201242998,5.46267362630453,-0.366318200757423));
#34541=CARTESIAN_POINT('Ctrl Pts',(-40.1399425989152,4.9695853458046,2.29743632392573));
#34542=CARTESIAN_POINT('Ctrl Pts',(-40.0006839548323,3.25980229079568,4.39871358429398));
#34543=CARTESIAN_POINT('Ctrl Pts',(-39.8614253107496,0.75192761703796,5.42306159198518));
#34544=CARTESIAN_POINT('Ctrl Pts',(-39.7221666666666,-1.94004016284409,
5.11969103933832));
#34545=CARTESIAN_POINT('Ctrl Pts',(-39.5829080225839,-4.15703134725169,
3.56287560120978));
#34546=CARTESIAN_POINT('Ctrl Pts',(-39.443649378501,-5.35626391283587,1.13376764276522));
#34547=CARTESIAN_POINT('Ctrl Pts',(-39.3043907344182,-5.24413187550802,
-1.57291863871278));
#34548=CARTESIAN_POINT('Ctrl Pts',(-39.1651320903353,-3.84808832327816,
-3.89451003695966));
#34549=CARTESIAN_POINT('Ctrl Pts',(-39.0258734462525,-1.50992412536221,
-5.26261544361532));
#34550=CARTESIAN_POINT('Ctrl Pts',(-38.8866148021696,1.19791212070242,-5.34228403614066));
#34551=CARTESIAN_POINT('Ctrl Pts',(-38.7473561580868,3.61246566485912,-4.11401069419408));
#34552=CARTESIAN_POINT('Ctrl Pts',(-38.608097514004,5.14258564128613,-1.87851140368299));
#34553=CARTESIAN_POINT('Ctrl Pts',(-38.4688388699211,5.41365548740393,0.816900505221123));
#34554=CARTESIAN_POINT('Ctrl Pts',(-38.3295802258383,4.35930965310145,3.31231211091373));
#34555=CARTESIAN_POINT('Ctrl Pts',(-38.1903215817555,2.23768176077518,4.99677621164119));
#34556=CARTESIAN_POINT('Ctrl Pts',(-38.0510629376726,-0.43179379205009,
5.45788844635691));
#34557=CARTESIAN_POINT('Ctrl Pts',(-37.9118042935898,-2.99555403587155,
4.58275552368911));
#34558=CARTESIAN_POINT('Ctrl Pts',(-37.7725456495069,-4.82591809297065,
2.58563468642958));
#34559=CARTESIAN_POINT('Ctrl Pts',(-37.6332870054241,-5.4747611745053,-0.0445225095723984));
#34560=CARTESIAN_POINT('Ctrl Pts',(-37.4940283613413,-4.78322817852097,
-2.66377933844605));
#34561=CARTESIAN_POINT('Ctrl Pts',(-37.3547697172584,-2.92062590308386,
-4.63086779189008));
#34562=CARTESIAN_POINT('Ctrl Pts',(-37.2155110731756,-0.342971962908202,
-5.46418908936982));
#34563=CARTESIAN_POINT('Ctrl Pts',(-37.0762524290927,2.3186511952276,-4.95972265420142));
#34564=CARTESIAN_POINT('Ctrl Pts',(-36.9369937850099,4.41260308969872,-3.24097610983336));
#34565=CARTESIAN_POINT('Ctrl Pts',(-36.7977351409271,5.42622518849562,-0.728747127242984));
#34566=CARTESIAN_POINT('Ctrl Pts',(-36.6584764968442,5.11135418922643,1.96189972322917));
#34567=CARTESIAN_POINT('Ctrl Pts',(-36.5192178527614,3.54507940071622,4.17221814079114));
#34568=CARTESIAN_POINT('Ctrl Pts',(-36.3799592086785,1.1108691041234,5.3610597837772));
#34569=CARTESIAN_POINT('Ctrl Pts',(-36.2407005645957,-1.59531330686152,
5.23736265926658));
#34570=CARTESIAN_POINT('Ctrl Pts',(-36.1014419205129,-3.91091798769402,
3.83141131507184));
#34571=CARTESIAN_POINT('Ctrl Pts',(-35.9621832764301,-5.26901954743058,
1.48742232755986));
#34572=CARTESIAN_POINT('Ctrl Pts',(-35.8229246323472,-5.33711638764732,
-1.22072963281623));
#34573=CARTESIAN_POINT('Ctrl Pts',(-35.6836659882644,-4.09853647961605,
-3.63001252022438));
#34574=CARTESIAN_POINT('Ctrl Pts',(-35.5444073441815,-1.85651914755638,
-5.15056587439533));
#34575=CARTESIAN_POINT('Ctrl Pts',(-35.4051487000987,0.840026477797323,
-5.4101153119253));
#34576=CARTESIAN_POINT('Ctrl Pts',(-35.2658900560158,3.33090990905107,-4.34511580392452));
#34577=CARTESIAN_POINT('Ctrl Pts',(-35.1266314119331,5.0062925693755,-2.21630929284359));
#34578=CARTESIAN_POINT('Ctrl Pts',(-34.9873727678502,5.45599349068633,0.455112295282984));
#34579=CARTESIAN_POINT('Ctrl Pts',(-34.8481141237673,4.56991319325272,3.01510954657769));
#34580=CARTESIAN_POINT('Ctrl Pts',(-34.7088554796845,2.56498914623259,4.83692287011466));
#34581=CARTESIAN_POINT('Ctrl Pts',(-34.5695968356017,-0.0679166485057954,
5.47452093799858));
#34582=CARTESIAN_POINT('Ctrl Pts',(-34.4303381915189,-2.68419453053335,
4.77180174504182));
#34583=CARTESIAN_POINT('Ctrl Pts',(-34.291079547436,-4.6433058218266,2.90081078609419));
#34584=CARTESIAN_POINT('Ctrl Pts',(-34.1518209033532,-5.46560477632539,
0.319619462389833));
#34585=CARTESIAN_POINT('Ctrl Pts',(-34.0125622592703,-4.94976939804717,
-2.33982372795152));
#34586=CARTESIAN_POINT('Ctrl Pts',(-33.8733036151875,-3.22209074863717,
-4.42641202095737));
#34587=CARTESIAN_POINT('Ctrl Pts',(-33.7340449711047,-0.705553330523207,
-5.42928970211729));
#34588=CARTESIAN_POINT('Ctrl Pts',(-33.5947863270218,1.98372345931916,-5.1029240057712));
#34589=CARTESIAN_POINT('Ctrl Pts',(-33.455527682939,4.18732874961437,-3.52721846706185));
#34590=CARTESIAN_POINT('Ctrl Pts',(-33.3162690388561,5.36575776175026,-1.08795028100834));
#34591=CARTESIAN_POINT('Ctrl Pts',(-33.1770103947733,5.23049780876673,1.61767884458434));
#34592=CARTESIAN_POINT('Ctrl Pts',(-33.0377517506905,3.814664345283,3.92725452505383));
#34593=CARTESIAN_POINT('Ctrl Pts',(-32.8984931066076,1.46489336942115,5.2753274389326));
#34594=CARTESIAN_POINT('Ctrl Pts',(-32.7592344625248,-1.2435248544032,5.33185128339217));
#34595=CARTESIAN_POINT('Ctrl Pts',(-32.6199758184419,-3.64749309154975,
4.0829874257492));
#34596=CARTESIAN_POINT('Ctrl Pts',(-32.4807171743591,-5.15845205815569,
1.83449299138441));
#34597=CARTESIAN_POINT('Ctrl Pts',(-32.3414585302762,-5.4064763477243,-0.863137111487432));
#34598=CARTESIAN_POINT('Ctrl Pts',(-32.2021998861935,-4.33084261291954,
-3.34944688476314));
#34599=CARTESIAN_POINT('Ctrl Pts',(-32.0629412421106,-2.19489635509741,
-5.01571751219199));
#34600=CARTESIAN_POINT('Ctrl Pts',(-31.9236825980278,0.478422488163947,
-5.45399890855767));
#34601=CARTESIAN_POINT('Ctrl Pts',(-31.7844239539449,3.03461000137415,-4.55698741618728));
#34602=CARTESIAN_POINT('Ctrl Pts',(-31.6451653098621,4.84783932503205,-2.54429676932585));
#34603=CARTESIAN_POINT('Ctrl Pts',(-31.5059066657792,5.47418073672258,0.091309547280987));
#34604=CARTESIAN_POINT('Ctrl Pts',(-31.3666480216964,4.76028817844798,2.7045607092202));
#34605=CARTESIAN_POINT('Ctrl Pts',(-31.2273893776135,2.88094270029059,4.65565906498442));
#34606=CARTESIAN_POINT('Ctrl Pts',(-31.0881307335308,0.296261125619126,
5.46692066132079));
#34607=CARTESIAN_POINT('Ctrl Pts',(-30.9488720894479,-2.36095353548684,
4.93972575908839));
#34608=CARTESIAN_POINT('Ctrl Pts',(-30.809613445365,-4.44014012591879,3.20314655205396));
#34609=CARTESIAN_POINT('Ctrl Pts',(-30.6703548012823,-5.43225507689216,
0.682346650397424));
#34610=CARTESIAN_POINT('Ctrl Pts',(-30.5310961571993,-5.0944006429078,-2.00551097261269));
#34611=CARTESIAN_POINT('Ctrl Pts',(-30.3918375131166,-3.50929312638729,
-4.20236289780168));
#34612=CARTESIAN_POINT('Ctrl Pts',(-30.2525788690337,-1.06501159191773,
-5.37035776096993));
#34613=CARTESIAN_POINT('Ctrl Pts',(-30.1133202249509,1.64001484348643,-5.22353744936069));
#34614=CARTESIAN_POINT('Ctrl Pts',(-29.9740615808681,3.9435193507338,-3.79784771971142));
#34615=CARTESIAN_POINT('Ctrl Pts',(-29.8348029367852,5.2815390029392,-1.44233766232502));
#34616=CARTESIAN_POINT('Ctrl Pts',(-29.6955442927024,5.32648881951606,1.26629736922243));
#34617=CARTESIAN_POINT('Ctrl Pts',(-29.5562856486195,4.0673638165193,3.66490705963996));
#34618=CARTESIAN_POINT('Ctrl Pts',(-29.4170270045367,1.81243333736467,5.1662440485655));
#34619=CARTESIAN_POINT('Ctrl Pts',(-29.2777683604539,-0.886231984291257,
5.40273866124842));
#34620=CARTESIAN_POINT('Ctrl Pts',(-29.138509716371,-3.36792269956474,4.31649034071498));
#34621=CARTESIAN_POINT('Ctrl Pts',(-28.9992510722882,-5.02505086799114,
2.17344333853698));
#34622=CARTESIAN_POINT('Ctrl Pts',(-28.8599924282053,-5.45190473639203,
-0.501723945048768));
#34623=CARTESIAN_POINT('Ctrl Pts',(-28.7207337841225,-4.54397842851747,
-3.05405504418258));
#34624=CARTESIAN_POINT('Ctrl Pts',(-28.5814751400397,-2.52355793355221,
-4.85866725838835));
#34625=CARTESIAN_POINT('Ctrl Pts',(-28.4422164959568,0.114700778743591,
-5.47374057688935));
#34626=CARTESIAN_POINT('Ctrl Pts',(-28.302957851874,2.72487750262012,-4.74868768897724));
#34627=CARTESIAN_POINT('Ctrl Pts',(-28.1636992077911,4.66792729579326,-2.86102200846436));
#34628=CARTESIAN_POINT('Ctrl Pts',(-28.0244405637083,5.46813672032796,-0.272897379119357));
#34629=CARTESIAN_POINT('Ctrl Pts',(-27.8851819196255,4.92959192072193,2.38204023200329));
#34630=CARTESIAN_POINT('Ctrl Pts',(-27.7459232755426,3.18414386600476,4.45378715390773));
#34631=CARTESIAN_POINT('Ctrl Pts',(-27.6066646314598,0.659127510619695,
5.43512125867248));
#34632=CARTESIAN_POINT('Ctrl Pts',(-27.467405987377,-2.02726186526959,5.08578425627286));
#34633=CARTESIAN_POINT('Ctrl Pts',(-27.3281473432941,-4.21732031082938,
3.49130370600942));
#34634=CARTESIAN_POINT('Ctrl Pts',(-27.1888886992113,-5.37485969744026,
1.04205345571222));
#34635=CARTESIAN_POINT('Ctrl Pts',(-27.0496300551285,-5.21648170814461,
-1.66232089571234));
#34636=CARTESIAN_POINT('Ctrl Pts',(-26.9103714110456,-3.78096174542872,
-3.95971216773818));
#34637=CARTESIAN_POINT('Ctrl Pts',(-26.7711127669628,-1.41975561813873,
-5.28765412602722));
#34638=CARTESIAN_POINT('Ctrl Pts',(-26.6318541228799,1.2890467614478,-5.3210290939376));
#34639=CARTESIAN_POINT('Ctrl Pts',(-26.4925954787971,3.68225410651592,-4.05166593721347));
#34640=CARTESIAN_POINT('Ctrl Pts',(-26.3533368347143,5.17394170334293,-1.79034058830659));
#34641=CARTESIAN_POINT('Ctrl Pts',(-26.2140781906314,5.39890232074783,0.909310674496222));
#34642=CARTESIAN_POINT('Ctrl Pts',(-26.0748195465486,4.30205924938349,3.38633701608731));
#34643=CARTESIAN_POINT('Ctrl Pts',(-25.9355609024658,2.15195063489454,5.03429246634581));
#34644=CARTESIAN_POINT('Ctrl Pts',(-25.7963022583829,-0.525016240452773,
5.44971101242903));
#34645=CARTESIAN_POINT('Ctrl Pts',(-25.6570436143001,-3.07344431993646,
4.53088646778747));
#34646=CARTESIAN_POINT('Ctrl Pts',(-25.5177849702172,-4.86940647246544,
2.50277301760284));
#34647=CARTESIAN_POINT('Ctrl Pts',(-25.3785263261344,-5.4732004665362,-0.138089915769586));
#34648=CARTESIAN_POINT('Ctrl Pts',(-25.2392676820516,-4.73700048845459,
-2.74514453974834));
#34649=CARTESIAN_POINT('Ctrl Pts',(-25.1000090379687,-2.84104907436741,
-4.68011029023519));
#34650=CARTESIAN_POINT('Ctrl Pts',(-24.9607503938859,-0.249528649512625,
-5.46925293114166));
#34651=CARTESIAN_POINT('Ctrl Pts',(-24.821491749803,2.4030834324577,-4.91936806799172));
#34652=CARTESIAN_POINT('Ctrl Pts',(-24.6822331057202,4.46735285572938,-3.16508303747874));
#34653=CARTESIAN_POINT('Ctrl Pts',(-24.5429744616374,5.43788819512175,-0.635896335171685));
#34654=CARTESIAN_POINT('Ctrl Pts',(-24.4037158175546,5.07707500320166,2.04897574011852));
#34655=CARTESIAN_POINT('Ctrl Pts',(-24.2644571734717,3.473250534415,4.23220071557519));
#34656=CARTESIAN_POINT('Ctrl Pts',(-24.1251985293889,1.0190762916073,5.37926348895581));
#34657=CARTESIAN_POINT('Ctrl Pts',(-23.985939885306,-1.68459659395356,5.20933071395636));
#34658=CARTESIAN_POINT('Ctrl Pts',(-23.8466812412232,-3.97583268038608,
3.76400673077284));
#34659=CARTESIAN_POINT('Ctrl Pts',(-23.7074225971403,-5.2936726965345,1.39714764921047));
#34660=CARTESIAN_POINT('Ctrl Pts',(-23.5681639530575,-5.31547220635138,
-1.31177261567522));
#34661=CARTESIAN_POINT('Ctrl Pts',(-23.4289053089747,-4.03589407447513,
-3.6995339154204));
#34662=CARTESIAN_POINT('Ctrl Pts',(-23.2896466648919,-1.7682151476239,-5.1815448819288));
#34663=CARTESIAN_POINT('Ctrl Pts',(-23.150388020809,0.932372760685483,-5.39496739627414));
#34664=CARTESIAN_POINT('Ctrl Pts',(-23.0111293767262,3.40468949808556,-4.2875496024367));
#34665=CARTESIAN_POINT('Ctrl Pts',(-22.8718707326433,5.04344213850449,-2.13041863662671));
#34666=CARTESIAN_POINT('Ctrl Pts',(-22.7326120885605,5.44741777672601,0.548298949058622));
#34667=CARTESIAN_POINT('Ctrl Pts',(-22.5933534444776,4.51771177305655,3.09277747458744));
#34668=CARTESIAN_POINT('Ctrl Pts',(-22.4540948003948,2.48194240101049,4.88005677116521));
#34669=CARTESIAN_POINT('Ctrl Pts',(-22.314836156312,-0.161476531273241,
5.47256041552555));
#34670=CARTESIAN_POINT('Ctrl Pts',(-22.1755775122291,-2.76536145052879,
4.72522679028835));
#34671=CARTESIAN_POINT('Ctrl Pts',(-22.0363188681463,-4.69220782584875,
2.82102426270548));
#34672=CARTESIAN_POINT('Ctrl Pts',(-21.8970602240634,-5.47026927337987,
0.226155363511897));
#34673=CARTESIAN_POINT('Ctrl Pts',(-21.7578015799806,-4.90905438758531,
-2.42408275260119));
#34674=CARTESIAN_POINT('Ctrl Pts',(-21.6185429358978,-3.14596441452665,
-4.48083698367404));
#34675=CARTESIAN_POINT('Ctrl Pts',(-21.479284291815,-0.612653548254585,
-5.44055583571572));
#34676=CARTESIAN_POINT('Ctrl Pts',(-21.3400256477321,2.07065220066406,-5.06827304272516));
#34677=CARTESIAN_POINT('Ctrl Pts',(-21.2007670036493,4.24700384032274,-3.45513394125512));
#34678=CARTESIAN_POINT('Ctrl Pts',(-21.0615083595664,5.38356905510338,-0.99608051916624));
#34679=CARTESIAN_POINT('Ctrl Pts',(-20.9222497154836,5.20208459737315,1.70684153145577));
#34680=CARTESIAN_POINT('Ctrl Pts',(-20.7829910714008,3.74698298534229,3.99188059431702));
#34681=CARTESIAN_POINT('Ctrl Pts',(-20.6437324273179,1.3745141683616,5.29959460456198));
#34682=CARTESIAN_POINT('Ctrl Pts',(-20.5044737832351,-1.33447451693076,
5.30981825822612));
#34683=CARTESIAN_POINT('Ctrl Pts',(-20.3652151391523,-3.71674617082413,
4.02004851629844));
#34684=CARTESIAN_POINT('Ctrl Pts',(-20.2259564950694,-5.18905344548906,
1.74605741932713));
#34685=CARTESIAN_POINT('Ctrl Pts',(-20.0866978509866,-5.39093395967906,
-0.955417821745186));
#34686=CARTESIAN_POINT('Ctrl Pts',(-19.9474392069037,-4.27296166482091,
-3.42297981044299));
#34687=CARTESIAN_POINT('Ctrl Pts',(-19.8081805628209,-2.10884773690798,
-5.05249971739409));
#34688=CARTESIAN_POINT('Ctrl Pts',(-19.6689219187381,0.57157164572401,-5.44502507115747));
#34689=CARTESIAN_POINT('Ctrl Pts',(-19.5296632746552,3.11205415511225,-4.50445458489459));
#34690=CARTESIAN_POINT('Ctrl Pts',(-19.3904046305724,4.89061796001327,-2.4610664641421));
#34691=CARTESIAN_POINT('Ctrl Pts',(-19.2511459864896,5.47182043554474,0.184860198215039));
#34692=CARTESIAN_POINT('Ctrl Pts',(-19.1118873424067,4.71336680946623,2.78552786580056));
#34693=CARTESIAN_POINT('Ctrl Pts',(-18.9726286983239,2.80094793913186,4.7042196817328));
#34694=CARTESIAN_POINT('Ctrl Pts',(-18.833370054241,0.202777947913637,5.47118572848419));
#34695=CARTESIAN_POINT('Ctrl Pts',(-18.6941114101582,-2.44503780898611,
4.89865106783058));
#34696=CARTESIAN_POINT('Ctrl Pts',(-18.5548527660754,-4.4942392915216,3.12678834625449));
#34697=CARTESIAN_POINT('Ctrl Pts',(-18.4155941219925,-5.44312413174327,
0.589399574281588));
#34698=CARTESIAN_POINT('Ctrl Pts',(-18.2763354779097,-5.05937853556709,
-2.09229085109412));
#34699=CARTESIAN_POINT('Ctrl Pts',(-18.1370768338268,-3.43695425733871,
-4.26172941476702));
#34700=CARTESIAN_POINT('Ctrl Pts',(-17.997818189744,-0.973066558291814,
-5.3877763172633));
#34701=CARTESIAN_POINT('Ctrl Pts',(-17.8585595456612,1.72905530202626,-5.19474349070905));
#34702=CARTESIAN_POINT('Ctrl Pts',(-17.7193009015783,4.00785561649581,-3.7298908199909));
#34703=CARTESIAN_POINT('Ctrl Pts',(-17.5800422574955,5.30541974197549,-1.35185558887996));
#34704=CARTESIAN_POINT('Ctrl Pts',(-17.4407836134126,5.30406735280308,1.35715205067734));
#34705=CARTESIAN_POINT('Ctrl Pts',(-17.3015249693298,4.00412955202339,3.73389055843128));
#34706=CARTESIAN_POINT('Ctrl Pts',(-17.162266325247,1.72386780801632,5.19646725691738));
#34707=CARTESIAN_POINT('Ctrl Pts',(-17.0230076811642,-0.978445436872712,
5.38680208461312));
#34708=CARTESIAN_POINT('Ctrl Pts',(-16.8837490370813,-3.44120761917852,
4.25829570291177));
#34709=CARTESIAN_POINT('Ctrl Pts',(-16.7444903929985,-5.06146503762314,
2.08723832962307));
#34710=CARTESIAN_POINT('Ctrl Pts',(-16.6052317489156,-5.44253293941428,
-0.59483390548928));
#34711=CARTESIAN_POINT('Ctrl Pts',(-16.4659731048328,-4.491115145378,-3.13127400951843));
#34712=CARTESIAN_POINT('Ctrl Pts',(-16.3267144607499,-2.4401455881925,-4.90108984616219));
#34713=CARTESIAN_POINT('Ctrl Pts',(-16.1874558166671,0.208240489609049,
-5.47098054010582));
#34714=CARTESIAN_POINT('Ctrl Pts',(-16.0481971725843,2.8056434173249,-4.70142076255153));
#34715=CARTESIAN_POINT('Ctrl Pts',(-15.9089385285015,4.71614563855093,-2.78082047024009));
#34716=CARTESIAN_POINT('Ctrl Pts',(-15.7696798844186,5.47200227972015,-0.179396829589313));
#34717=CARTESIAN_POINT('Ctrl Pts',(-15.6304212403358,4.88815829869211,2.4659482189731));
#34718=CARTESIAN_POINT('Ctrl Pts',(-15.4911625962529,3.10755518281749,4.50755953454565));
#34719=CARTESIAN_POINT('Ctrl Pts',(-15.3519039521701,0.566134837870747,
5.44559303630728));
#34720=CARTESIAN_POINT('Ctrl Pts',(-15.2126453080873,-2.11389129628661,
5.05039164414136));
#34721=CARTESIAN_POINT('Ctrl Pts',(-15.0733866640044,-4.27637717001899,
3.41871181462692));
#34722=CARTESIAN_POINT('Ctrl Pts',(-14.9341280199216,-5.39188519861101,
0.950034829218862));
#34723=CARTESIAN_POINT('Ctrl Pts',(-14.7948693758387,-5.18730752801265,
-1.75123750004177));
#34724=CARTESIAN_POINT('Ctrl Pts',(-14.6556107317559,-3.71273054682144,
-4.02375745521871));
#34725=CARTESIAN_POINT('Ctrl Pts',(-14.5163520876731,-1.32917232451103,
-5.31114800240805));
#34726=CARTESIAN_POINT('Ctrl Pts',(-14.3770934435902,1.37980480282327,-5.29821959509371));
#34727=CARTESIAN_POINT('Ctrl Pts',(-14.2378347995074,3.7509667651852,-3.98813747233033));
#34728=CARTESIAN_POINT('Ctrl Pts',(-14.0985761554246,5.2037861808374,-1.70164671887413));
#34729=CARTESIAN_POINT('Ctrl Pts',(-13.9593175113417,5.38257184652445,1.00145518558331));
#34730=CARTESIAN_POINT('Ctrl Pts',(-13.8200588672589,4.24355198451,3.45937259145215));
#34731=CARTESIAN_POINT('Ctrl Pts',(-13.680800223176,2.0655908093598,5.07033793548493));
#34732=CARTESIAN_POINT('Ctrl Pts',(-13.5415415790932,-0.618085303585742,
5.43994142700276));
#34733=CARTESIAN_POINT('Ctrl Pts',(-13.4022829350104,-3.15043668685167,
4.47769369808479));
#34734=CARTESIAN_POINT('Ctrl Pts',(-13.2630242909275,-4.91147223839532,
2.41918015517678));
#34735=CARTESIAN_POINT('Ctrl Pts',(-13.1237656468447,-5.47004074454526,
-0.231616978531012));
#34736=CARTESIAN_POINT('Ctrl Pts',(-12.9845070027618,-4.68938886767918,
-2.82570773779167));
#34737=CARTESIAN_POINT('Ctrl Pts',(-12.845248358679,-2.760642223558,-4.72798547853501));
#34738=CARTESIAN_POINT('Ctrl Pts',(-12.7059897145962,-0.15601243547838,
-5.47271891217753));
#34739=CARTESIAN_POINT('Ctrl Pts',(-12.5667310705134,2.48681360073797,-4.87757627176797));
#34740=CARTESIAN_POINT('Ctrl Pts',(-12.4274724264305,4.52079746951866,-3.08826527541316));
#34741=CARTESIAN_POINT('Ctrl Pts',(-12.2882137823477,5.44796250432556,-0.54285976383591));
#34742=CARTESIAN_POINT('Ctrl Pts',(-12.1489551382648,5.04131253254851,2.13545314181759));
#34743=CARTESIAN_POINT('Ctrl Pts',(-12.009696494182,3.40040694622673,4.29094683861058));
#34744=CARTESIAN_POINT('Ctrl Pts',(-11.8704378500992,0.926985752507082,
5.39589562411822));
#34745=CARTESIAN_POINT('Ctrl Pts',(-11.7311792060163,-1.77338772045491,
5.17977684506475));
#34746=CARTESIAN_POINT('Ctrl Pts',(-11.5919205619335,-4.0395858201179,3.69550247918081));
#34747=CARTESIAN_POINT('Ctrl Pts',(-11.4526619178506,-5.31677928126165,
1.30646478945133));
#34748=CARTESIAN_POINT('Ctrl Pts',(-11.3134032737678,-5.2922750918781,-1.40243235972937));
#34749=CARTESIAN_POINT('Ctrl Pts',(-11.174144629685,-3.9720725692345,-3.76797447927451));
#34750=CARTESIAN_POINT('Ctrl Pts',(-11.0348859856021,-1.67939455765743,
-5.21101008360564));
#34751=CARTESIAN_POINT('Ctrl Pts',(-10.8956273415193,1.02444664771917,-5.37824332265714));
#34752=CARTESIAN_POINT('Ctrl Pts',(-10.7563686974365,3.47747439557152,-4.22873077883584));
#34753=CARTESIAN_POINT('Ctrl Pts',(-10.6171100533536,5.07911824896027,-2.04390557140199));
#34754=CARTESIAN_POINT('Ctrl Pts',(-10.4778514092708,5.43725058124388,0.641325415442486));
#34755=CARTESIAN_POINT('Ctrl Pts',(-10.3385927651879,4.46419048809091,3.16954183720107));
#34756=CARTESIAN_POINT('Ctrl Pts',(-10.1993341211051,2.39817054792408,4.92176494713011));
#34757=CARTESIAN_POINT('Ctrl Pts',(-10.0600754770223,-0.254989238126229,
5.46900106602376));
#34758=CARTESIAN_POINT('Ctrl Pts',(-9.92081683293943,-2.84572046082652,
4.67727134455151));
#34759=CARTESIAN_POINT('Ctrl Pts',(-9.78155818885659,-4.73973898548971,
2.74041356754016));
#34760=CARTESIAN_POINT('Ctrl Pts',(-9.64229954477374,-5.47333561277054,
0.132625192579784));
#34761=CARTESIAN_POINT('Ctrl Pts',(-9.50304090069093,-4.86690518028598,
-2.50763357327872));
#34762=CARTESIAN_POINT('Ctrl Pts',(-9.36378225660807,-3.06891897627543,
-4.53395285471581));
#34763=CARTESIAN_POINT('Ctrl Pts',(-9.22452361252525,-0.519574777180205,
-5.45023249253162));
#34764=CARTESIAN_POINT('Ctrl Pts',(-9.0852649684424,2.15697599396752,-5.0321413665732));
#34765=CARTESIAN_POINT('Ctrl Pts',(-8.94600632435957,4.30543815449961,-3.38203998638518));
#34766=CARTESIAN_POINT('Ctrl Pts',(-8.80674768027672,5.39980752055461,-0.903919749032533));
#34767=CARTESIAN_POINT('Ctrl Pts',(-8.66748903619389,5.17215157937558,1.79550555880287));
#34768=CARTESIAN_POINT('Ctrl Pts',(-8.52823039211106,3.67820693165339,4.05534042216757));
#34769=CARTESIAN_POINT('Ctrl Pts',(-8.38897174802822,1.28373339834046,5.32231347570908));
#34770=CARTESIAN_POINT('Ctrl Pts',(-8.24971310394538,-1.42503430821612,
5.28623395170288));
#34771=CARTESIAN_POINT('Ctrl Pts',(-8.11045445986255,-3.784913390138,3.9559351360814));
#34772=CARTESIAN_POINT('Ctrl Pts',(-7.9711958157797,-5.21813883331359,1.65711173069105));
#34773=CARTESIAN_POINT('Ctrl Pts',(-7.83193717169687,-5.3738165920501,-1.04741940345607));
#34774=CARTESIAN_POINT('Ctrl Pts',(-7.69267852761403,-4.21383235652447,
-3.49551270099778));
#34775=CARTESIAN_POINT('Ctrl Pts',(-7.55341988353118,-2.02218301172191,
-5.0878058177207));
#34776=CARTESIAN_POINT('Ctrl Pts',(-7.41416123944835,0.664553816695306,
-5.43446045127249));
#34777=CARTESIAN_POINT('Ctrl Pts',(-7.27490259536552,3.18858911170672,-4.45060576196482));
#34778=CARTESIAN_POINT('Ctrl Pts',(-7.13564395128268,4.93196778442169,-2.37711715006973));
#34779=CARTESIAN_POINT('Ctrl Pts',(-6.99638530719984,5.46786152352583,0.278356841617121));
#34780=CARTESIAN_POINT('Ctrl Pts',(-6.85712666311701,4.66506841443464,2.86568122099679));
#34781=CARTESIAN_POINT('Ctrl Pts',(-6.71786801903417,2.72013487156228,4.75140594479573));
#34782=CARTESIAN_POINT('Ctrl Pts',(-6.57860937495132,0.109235527944913,
5.47385237023832));
#34783=CARTESIAN_POINT('Ctrl Pts',(-6.43935073086849,-2.52840775642265,
4.85614521910033));
#34784=CARTESIAN_POINT('Ctrl Pts',(-6.30009208678566,-4.54702544991989,
3.04951663866756));
#34785=CARTESIAN_POINT('Ctrl Pts',(-6.1608334427028,-5.45240295947547,0.496280303087244));
#34786=CARTESIAN_POINT('Ctrl Pts',(-6.02157479861998,-5.02287831368086,
-2.17845945972919));
#34787=CARTESIAN_POINT('Ctrl Pts',(-5.88231615453714,-3.36361127048301,
-4.31985085307454));
#34788=CARTESIAN_POINT('Ctrl Pts',(-5.74305751045431,-0.880837239980666,
-5.40362081648892));
#34789=CARTESIAN_POINT('Ctrl Pts',(-5.60379886637147,1.81759061121365,-5.16443187018255));
#34790=CARTESIAN_POINT('Ctrl Pts',(-5.46454022228863,4.07102097368853,-3.66084422005602));
#34791=CARTESIAN_POINT('Ctrl Pts',(-5.32528157820578,5.32775048469594,-1.26097856625377));
#34792=CARTESIAN_POINT('Ctrl Pts',(-5.18602293412295,5.2800962848793,1.44761023557204));
#34793=CARTESIAN_POINT('Ctrl Pts',(-5.04676429004012,3.93972546754036,3.80178318847132));
#34794=CARTESIAN_POINT('Ctrl Pts',(-4.90750564595728,1.63479864485923,5.22517229979028));
#34795=CARTESIAN_POINT('Ctrl Pts',(-4.76824700187443,-1.07037303331147,
5.36929173553541));
#34796=CARTESIAN_POINT('Ctrl Pts',(-4.62898835779161,-3.51348717835118,
4.19885698962121));
#34797=CARTESIAN_POINT('Ctrl Pts',(-4.48972971370876,-5.09640048313106,
2.000423526974));
#34798=CARTESIAN_POINT('Ctrl Pts',(-4.35047106962593,-5.43157108803641,
-0.6877700831933));
#34799=CARTESIAN_POINT('Ctrl Pts',(-4.21121242554309,-4.43693976776381,
-3.20757816256517));
#34800=CARTESIAN_POINT('Ctrl Pts',(-4.07195378146025,-2.35602034604859,
-4.94208056396663));
#34801=CARTESIAN_POINT('Ctrl Pts',(-3.93269513737741,0.30171936231118,-5.46662213785894));
#34802=CARTESIAN_POINT('Ctrl Pts',(-3.79343649329457,2.88558965381968,-4.65278030015506));
#34803=CARTESIAN_POINT('Ctrl Pts',(-3.65417784921175,4.76298614341351,-2.69980650591098));
#34804=CARTESIAN_POINT('Ctrl Pts',(-3.5149192051289,5.47426917514671,-0.0858438686731754));
#34805=CARTESIAN_POINT('Ctrl Pts',(-3.37566056104607,4.8452965846843,2.54913577084127));
#34806=CARTESIAN_POINT('Ctrl Pts',(-3.23640191696323,3.03005861688361,4.56001501640902));
#34807=CARTESIAN_POINT('Ctrl Pts',(-3.09714327288038,0.47297676690079,5.45447386555561));
#34808=CARTESIAN_POINT('Ctrl Pts',(-2.95788462879755,-2.19990314678726,
5.01352354295405));
#34809=CARTESIAN_POINT('Ctrl Pts',(-2.81862598471472,-4.33418467121216,
3.34512113514759));
#34810=CARTESIAN_POINT('Ctrl Pts',(-2.67936734063187,-5.40733544218769,
0.857738646605811));
#34811=CARTESIAN_POINT('Ctrl Pts',(-2.54010869654903,-5.15661785864793,
-1.83964247396158));
#34812=CARTESIAN_POINT('Ctrl Pts',(-2.4008500524662,-3.64341466104068,-4.08662718923746));
#34813=CARTESIAN_POINT('Ctrl Pts',(-2.26159140838337,-1.23820070945758,
-5.33309020721854));
#34814=CARTESIAN_POINT('Ctrl Pts',(-2.12233276430052,1.4701597310491,-5.2738622068446));
#34815=CARTESIAN_POINT('Ctrl Pts',(-1.98307412021769,3.81858356332732,-3.92344385303797));
#34816=CARTESIAN_POINT('Ctrl Pts',(-1.84381547613485,5.2321103602713,-1.6124557204024));
#34817=CARTESIAN_POINT('Ctrl Pts',(-1.704556832052,5.36466882468081,1.09330714313199));
#34818=CARTESIAN_POINT('Ctrl Pts',(-1.56529818796917,4.18380497314764,3.53139745068011));
#34819=CARTESIAN_POINT('Ctrl Pts',(-1.42603954388634,1.97862747239897,5.10490218334346));
#34820=CARTESIAN_POINT('Ctrl Pts',(-1.28678089980349,-0.710973708892522,
5.42858235876716));
#34821=CARTESIAN_POINT('Ctrl Pts',(-1.14752225572066,-3.22650880324846,
4.42319311700711));
#34822=CARTESIAN_POINT('Ctrl Pts',(-1.00826361163783,-4.95210278852054,
2.33487981484443));
#34823=CARTESIAN_POINT('Ctrl Pts',(-0.869004967554984,-5.46528354152855,
-0.325074995677754));
#34824=CARTESIAN_POINT('Ctrl Pts',(-0.729746323472146,-4.64040603618749,
-2.90544808420485));
#34825=CARTESIAN_POINT('Ctrl Pts',(-0.59048767938932,-2.67943116337464,
-4.77447412454503));
#34826=CARTESIAN_POINT('Ctrl Pts',(-0.451229035306469,-0.0624461122722286,
-5.47459625409955));
#34827=CARTESIAN_POINT('Ctrl Pts',(-0.31197039122363,2.56980840002131,-4.83433950546158));
#34828=CARTESIAN_POINT('Ctrl Pts',(-0.172711747140798,4.57293856493704,
-3.01058424967472));
#34829=CARTESIAN_POINT('Ctrl Pts',(-0.0334531030579653,5.45641147518307,
-0.449588311427022));
#34830=CARTESIAN_POINT('Ctrl Pts',(0.105805541024878,5.0041434537287,2.22115548407858));
#34831=CARTESIAN_POINT('Ctrl Pts',(0.245064185107707,3.3264356378341,4.34875895322203));
#34832=CARTESIAN_POINT('Ctrl Pts',(0.337903281162932,1.66543784564298,5.05629436626422));
#34833=CARTESIAN_POINT('Ctrl Pts',(0.384322829190546,0.800498355117692,
5.18970890870239));
#34834=CARTESIAN_POINT('Ctrl Pts',(-59.58325,2.85706463458446,-4.00329423553987));
#34835=CARTESIAN_POINT('Ctrl Pts',(-59.5368304519724,3.52427108824591,-3.52712339958193));
#34836=CARTESIAN_POINT('Ctrl Pts',(-59.4439913559172,4.61530848209962,-2.23520568907806));
#34837=CARTESIAN_POINT('Ctrl Pts',(-59.3047327118343,5.12174738739822,0.251511598513074));
#34838=CARTESIAN_POINT('Ctrl Pts',(-59.1654740677515,4.3742789497841,2.67597888304926));
#34839=CARTESIAN_POINT('Ctrl Pts',(-59.0262154236687,2.55584624568566,4.44562215581043));
#34840=CARTESIAN_POINT('Ctrl Pts',(-58.8869567795858,0.111678748687467,
5.12668320818063));
#34841=CARTESIAN_POINT('Ctrl Pts',(-58.747698135503,-2.35983518894881,4.55267369514457));
#34842=CARTESIAN_POINT('Ctrl Pts',(-58.60843949142,-4.25359264236838,2.86399697899764));
#34843=CARTESIAN_POINT('Ctrl Pts',(-58.4691808473374,-5.10595168183977,
0.474155594652121));
#34844=CARTESIAN_POINT('Ctrl Pts',(-58.3299222032543,-4.70822903633895,
-2.03178406622669));
#34845=CARTESIAN_POINT('Ctrl Pts',(-58.1906635591718,-3.15779931679017,
-4.04027968761638));
#34846=CARTESIAN_POINT('Ctrl Pts',(-58.0514049150887,-0.834251032978302,
-5.05960384006236));
#34847=CARTESIAN_POINT('Ctrl Pts',(-57.9121462710061,1.69354537464531,-4.84019258737259));
#34848=CARTESIAN_POINT('Ctrl Pts',(-57.772887626923,3.8067141091864,-3.43576636062821));
#34849=CARTESIAN_POINT('Ctrl Pts',(-57.6336289828404,4.98789175297897,-1.19016713333119));
#34850=CARTESIAN_POINT('Ctrl Pts',(-57.4943703387573,4.94789270758304,1.34681839400263));
#34851=CARTESIAN_POINT('Ctrl Pts',(-57.3551116946747,3.69650985244822,3.55406486819218));
#34852=CARTESIAN_POINT('Ctrl Pts',(-57.2158530505917,1.54011704282762,4.89117588296368));
#34853=CARTESIAN_POINT('Ctrl Pts',(-57.076594406509,-0.993339894845993,
5.03078900139859));
#34854=CARTESIAN_POINT('Ctrl Pts',(-56.937335762426,-3.28359918545446,3.93872294825806));
#34855=CARTESIAN_POINT('Ctrl Pts',(-56.7980771183433,-4.76994070613421,
1.88234634223453));
#34856=CARTESIAN_POINT('Ctrl Pts',(-56.6588184742604,-5.08846609548997,
-0.634881787205557));
#34857=CARTESIAN_POINT('Ctrl Pts',(-56.5195598301776,-4.1611913471364,-2.99667293168903));
#34858=CARTESIAN_POINT('Ctrl Pts',(-56.3803011860948,-2.21513949450856,
-4.62479395317148));
#34859=CARTESIAN_POINT('Ctrl Pts',(-56.2410425420119,0.273241035485556,
-5.12063486534734));
#34860=CARTESIAN_POINT('Ctrl Pts',(-56.1017838979291,2.69472444693603,-4.36279981705527));
#34861=CARTESIAN_POINT('Ctrl Pts',(-55.9625252538462,4.45646324687071,-2.53682821994801));
#34862=CARTESIAN_POINT('Ctrl Pts',(-55.8232666097634,5.1271340465709,-0.089769464874975));
#34863=CARTESIAN_POINT('Ctrl Pts',(-55.6840079656806,4.54253770251526,2.37926738925458));
#34864=CARTESIAN_POINT('Ctrl Pts',(-55.5447493215977,2.84579990176412,4.26579242432466));
#34865=CARTESIAN_POINT('Ctrl Pts',(-55.4054906775149,0.452329953591429,
5.1079310587967));
#34866=CARTESIAN_POINT('Ctrl Pts',(-55.266232033432,-2.05188313562661,4.69950398298055));
#34867=CARTESIAN_POINT('Ctrl Pts',(-55.1269733893492,-4.0537373125207,3.14050567415567));
#34868=CARTESIAN_POINT('Ctrl Pts',(-54.9877147452663,-5.06312216608579,
0.812622925848719));
#34869=CARTESIAN_POINT('Ctrl Pts',(-54.8484561011836,-4.83291179117217,
-1.71421285349086));
#34870=CARTESIAN_POINT('Ctrl Pts',(-54.7091974571006,-3.41946818595568,
-3.82136093735749));
#34871=CARTESIAN_POINT('Ctrl Pts',(-54.5699388130178,-1.16884224379346,
-4.99293199407404));
#34872=CARTESIAN_POINT('Ctrl Pts',(-54.430680168935,1.36794927382256,-4.94209235775424));
#34873=CARTESIAN_POINT('Ctrl Pts',(-54.2914215248522,3.56982819462436,-3.68128900647443));
#34874=CARTESIAN_POINT('Ctrl Pts',(-54.1521628807693,4.89771240398387,-1.51920219068664));
#34875=CARTESIAN_POINT('Ctrl Pts',(-54.0129042366865,5.02649836382728,1.01482820554322));
#34876=CARTESIAN_POINT('Ctrl Pts',(-53.8736455926037,3.9246556358045,3.30040001040366));
#34877=CARTESIAN_POINT('Ctrl Pts',(-53.7343869485209,1.86194642264088,4.77794072875955));
#34878=CARTESIAN_POINT('Ctrl Pts',(-53.5951283044379,-0.656619833959052,
5.08570668461877));
#34879=CARTESIAN_POINT('Ctrl Pts',(-53.4558696603552,-3.01442702008815,
4.14834808434477));
#34880=CARTESIAN_POINT('Ctrl Pts',(-53.3166110162723,-4.63421738021059,
2.19535677311881));
#34881=CARTESIAN_POINT('Ctrl Pts',(-53.1773523721895,-5.11942051059543,
-0.295119846874734));
#34882=CARTESIAN_POINT('Ctrl Pts',(-53.0380937281066,-4.35124498857135,
-2.71334279768651));
#34883=CARTESIAN_POINT('Ctrl Pts',(-52.8988350840238,-2.51776186605044,
-4.46726283916524));
#34884=CARTESIAN_POINT('Ctrl Pts',(-52.759576439941,-0.0678595671353494,
-5.12747083536052));
#34885=CARTESIAN_POINT('Ctrl Pts',(-52.6203177958581,2.39865666935982,-4.53232923239918));
#34886=CARTESIAN_POINT('Ctrl Pts',(-52.4810591517753,4.27791404372175,-2.82754549439134));
#34887=CARTESIAN_POINT('Ctrl Pts',(-52.3418005076925,5.10981730287787,-0.430498803174167));
#34888=CARTESIAN_POINT('Ctrl Pts',(-52.2025418636096,4.69069304595447,2.07194614721496));
#34889=CARTESIAN_POINT('Ctrl Pts',(-52.0632832195268,3.12315472211971,4.06712019370289));
#34890=CARTESIAN_POINT('Ctrl Pts',(-51.924024575444,0.790979961646617,5.06654840977544));
#34891=CARTESIAN_POINT('Ctrl Pts',(-51.7847659313611,-1.73484902128376,
4.82554255619773));
#34892=CARTESIAN_POINT('Ctrl Pts',(-51.6455072872782,-3.83593799234573,
3.40310766905826));
#34893=CARTESIAN_POINT('Ctrl Pts',(-51.5062486431955,-4.99788106171436,
1.14749596133553));
#34894=CARTESIAN_POINT('Ctrl Pts',(-51.3669899991126,-4.93620176658556,
-1.3890551493307));
#34895=CARTESIAN_POINT('Ctrl Pts',(-51.2277313550298,-3.66600093949493,
-3.58552634907998));
#34896=CARTESIAN_POINT('Ctrl Pts',(-51.0884727109469,-1.49825959824569,
-4.90415948604745));
#34897=CARTESIAN_POINT('Ctrl Pts',(-50.9492140668641,1.03629798564688,-5.02211594582091));
#34898=CARTESIAN_POINT('Ctrl Pts',(-50.8099554227812,3.31714056994997,-3.91051665736339));
#34899=CARTESIAN_POINT('Ctrl Pts',(-50.6706967786984,4.78585350621771,-1.84151250480363));
#34900=CARTESIAN_POINT('Ctrl Pts',(-50.5314381346155,5.08285440870451,0.678345891295609));
#34901=CARTESIAN_POINT('Ctrl Pts',(-50.3921794905327,4.13542907271616,3.03212606480312));
#34902=CARTESIAN_POINT('Ctrl Pts',(-50.2529208464499,2.17553396450143,4.64355618654767));
#34903=CARTESIAN_POINT('Ctrl Pts',(-50.113662202367,-0.316993269371489,
5.11811267514673));
#34904=CARTESIAN_POINT('Ctrl Pts',(-49.9744035582842,-2.73191160279071,
4.33961070637241));
#34905=CARTESIAN_POINT('Ctrl Pts',(-49.8351449142014,-4.47798085922564,
2.49864953779702));
#34906=CARTESIAN_POINT('Ctrl Pts',(-49.6958862701186,-5.12771399651721,
0.0459484302882166));
#34907=CARTESIAN_POINT('Ctrl Pts',(-49.5566276260356,-4.52203800193704,
-2.41800214999114));
#34908=CARTESIAN_POINT('Ctrl Pts',(-49.4173689819529,-2.80923945602917,
-4.28995754839293));
#34909=CARTESIAN_POINT('Ctrl Pts',(-49.27811033787,-0.408659791847362,-5.11161024168038));
#34910=CARTESIAN_POINT('Ctrl Pts',(-49.1388516937872,2.09197132506023,-4.68179645685823));
#34911=CARTESIAN_POINT('Ctrl Pts',(-48.9995930497043,4.08042880925776,-3.10574674126912));
#34912=CARTESIAN_POINT('Ctrl Pts',(-48.8603344056215,5.06988213827541,-0.769322554147787));
#34913=CARTESIAN_POINT('Ctrl Pts',(-48.7210757615387,4.81808520680125,1.75545351072806));
#34914=CARTESIAN_POINT('Ctrl Pts',(-48.5818171174558,3.38668501140426,3.85044500309434));
#34915=CARTESIAN_POINT('Ctrl Pts',(-48.442558473373,1.12612872559781,5.00273886803099));
#34916=CARTESIAN_POINT('Ctrl Pts',(-48.3032998292901,-1.4101356606875,4.93022104035731));
#34917=CARTESIAN_POINT('Ctrl Pts',(-48.1640411852073,-3.60115903181333,
3.65064593132692));
#34918=CARTESIAN_POINT('Ctrl Pts',(-48.0247825411245,-4.91051701814359,
1.47728964757986));
#34919=CARTESIAN_POINT('Ctrl Pts',(-47.8855238970416,-5.0176418239618,-1.05774884294608));
#34920=CARTESIAN_POINT('Ctrl Pts',(-47.7462652529588,-3.89630627287599,
-3.33382055849918));
#34921=CARTESIAN_POINT('Ctrl Pts',(-47.607006608876,-1.82104496094234,-4.79367889397601));
#34922=CARTESIAN_POINT('Ctrl Pts',(-47.4677479647931,0.700059562034036,
-5.07990931985298));
#34923=CARTESIAN_POINT('Ctrl Pts',(-47.3284893207103,3.04976974288669,-4.12243454813989));
#34924=CARTESIAN_POINT('Ctrl Pts',(-47.1892306766275,4.65281020153438,-2.15567143062717));
#34925=CARTESIAN_POINT('Ctrl Pts',(-47.0499720325446,5.11671138294472,0.33886090357014));
#34926=CARTESIAN_POINT('Ctrl Pts',(-46.9107133884618,4.32789718286852,2.75043052318056));
#34927=CARTESIAN_POINT('Ctrl Pts',(-46.771454744379,2.47949158419529,4.48861711134167));
#34928=CARTESIAN_POINT('Ctrl Pts',(-46.6321961002961,0.0240364544226033,
5.12786352560043));
#34929=CARTESIAN_POINT('Ctrl Pts',(-46.4929374562133,-2.43730347789571,
4.51166419904695));
#34930=CARTESIAN_POINT('Ctrl Pts',(-46.3536788121304,-4.30192271842598,
2.79088212094582));
#34931=CARTESIAN_POINT('Ctrl Pts',(-46.2144201680476,-5.11330984246402,
0.386813318391489));
#34932=CARTESIAN_POINT('Ctrl Pts',(-46.0751615239648,-4.67281437814416,
-2.11195830350261));
#34933=CARTESIAN_POINT('Ctrl Pts',(-45.9359028798819,-3.0882820494734,-4.09366291616992));
#34934=CARTESIAN_POINT('Ctrl Pts',(-45.7966442357991,-0.747651098816729,
-5.07312329071181));
#34935=CARTESIAN_POINT('Ctrl Pts',(-45.6573855917162,1.77602594558582,-4.81053987915395));
#34936=CARTESIAN_POINT('Ctrl Pts',(-45.5181269476334,3.86488170470528,-3.37020051287143));
#34937=CARTESIAN_POINT('Ctrl Pts',(-45.3788683035506,5.00750532432036,-1.10474092674605));
#34938=CARTESIAN_POINT('Ctrl Pts',(-45.2396096594678,4.92415028827758,1.43119042296277));
#34939=CARTESIAN_POINT('Ctrl Pts',(-45.1003510153849,3.63522426235287,3.61672595737161));
#34940=CARTESIAN_POINT('Ctrl Pts',(-44.9610923713021,1.45629272160045,4.91678488418377));
#34941=CARTESIAN_POINT('Ctrl Pts',(-44.8218337272192,-1.07918038574816,
5.01307607994741));
#34942=CARTESIAN_POINT('Ctrl Pts',(-44.6825750831364,-3.35043967147466,
3.88202474182395));
#34943=CARTESIAN_POINT('Ctrl Pts',(-44.5433164390536,-4.80141674914282,
1.80054416479442));
#34944=CARTESIAN_POINT('Ctrl Pts',(-44.4040577949707,-5.07687147184152,
-0.721760449682717));
#34945=CARTESIAN_POINT('Ctrl Pts',(-44.2647991508879,-4.10936474789597,
-3.06735773216533));
#34946=CARTESIAN_POINT('Ctrl Pts',(-44.125540506805,-2.13576953418586,-4.66197925619238));
#34947=CARTESIAN_POINT('Ctrl Pts',(-43.9862818627222,0.360722350167653,
-5.11521665957699));
#34948=CARTESIAN_POINT('Ctrl Pts',(-43.8470232186393,2.7688992207005,-4.31610463194866));
#34949=CARTESIAN_POINT('Ctrl Pts',(-43.7077645745566,4.49917140129531,-2.46028835506957));
#34950=CARTESIAN_POINT('Ctrl Pts',(-43.5685059304736,5.12791941987977,-0.00212403965129634));
#34951=CARTESIAN_POINT('Ctrl Pts',(-43.4292472863909,4.50120801315461,2.4565603006312));
#34952=CARTESIAN_POINT('Ctrl Pts',(-43.289988642308,2.77247382434629,4.31380933533684));
#34953=CARTESIAN_POINT('Ctrl Pts',(-43.1507299982252,0.364959781723236,
5.11491607419408));
#34954=CARTESIAN_POINT('Ctrl Pts',(-43.0114713541423,-2.13190671757982,
4.66374697382507));
#34955=CARTESIAN_POINT('Ctrl Pts',(-42.8722127100594,-4.10682227278453,
3.0707609656379));
#34956=CARTESIAN_POINT('Ctrl Pts',(-42.7329540659767,-5.0762718079012,0.72596599137429));
#34957=CARTESIAN_POINT('Ctrl Pts',(-42.5936954218938,-4.80290671103353,
-1.79656595020431));
#34958=CARTESIAN_POINT('Ctrl Pts',(-42.454436777811,-3.35365447446679,-3.87924783356431));
#34959=CARTESIAN_POINT('Ctrl Pts',(-42.3151781337281,-1.08333295532153,
-5.01218034354698));
#34960=CARTESIAN_POINT('Ctrl Pts',(-42.1759194896453,1.45221905169649,-4.91798962119831));
#34961=CARTESIAN_POINT('Ctrl Pts',(-42.0366608455625,3.63222684150266,-3.61973621417252));
#34962=CARTESIAN_POINT('Ctrl Pts',(-41.8974022014796,4.9229629697167,-1.43526920371147));
#34963=CARTESIAN_POINT('Ctrl Pts',(-41.7581435573968,5.00841879714827,1.10059222271303));
#34964=CARTESIAN_POINT('Ctrl Pts',(-41.618884913314,3.8676723249881,3.36699760541134));
#34965=CARTESIAN_POINT('Ctrl Pts',(-41.4796262692311,1.78001049070443,4.80906693042493));
#34966=CARTESIAN_POINT('Ctrl Pts',(-41.3403676251483,-0.743448157983408,
5.07374092014123));
#34967=CARTESIAN_POINT('Ctrl Pts',(-41.2011089810654,-3.08488971148233,
4.09621991063895));
#34968=CARTESIAN_POINT('Ctrl Pts',(-41.0618503369826,-4.67106318309472,
2.11582863858619));
#34969=CARTESIAN_POINT('Ctrl Pts',(-40.9225916928997,-5.11362853233719,
-0.382577209973956));
#34970=CARTESIAN_POINT('Ctrl Pts',(-40.7833330488169,-4.30423326894481,
-2.78731735811214));
#34971=CARTESIAN_POINT('Ctrl Pts',(-40.6440744047341,-2.4410402010708,-4.50964353636523));
#34972=CARTESIAN_POINT('Ctrl Pts',(-40.5048157606512,0.0197884139050482,
-5.12788167833459));
#34973=CARTESIAN_POINT('Ctrl Pts',(-40.3655571165684,2.47577226656799,-4.49066963518998));
#34974=CARTESIAN_POINT('Ctrl Pts',(-40.2262984724856,4.32561718207586,-2.75401490236612));
#34975=CARTESIAN_POINT('Ctrl Pts',(-40.0870398284027,5.11642890754077,-0.343099580888201));
#34976=CARTESIAN_POINT('Ctrl Pts',(-39.94778118432,4.65459440947177,2.15181620303378));
#34977=CARTESIAN_POINT('Ctrl Pts',(-39.808522540237,3.0531838096976,4.11990663881172));
#34978=CARTESIAN_POINT('Ctrl Pts',(-39.6692638961543,0.704267627790603,
5.07932763235163));
#34979=CARTESIAN_POINT('Ctrl Pts',(-39.5300052520714,-1.81707314952296,
4.79518584182169));
#34980=CARTESIAN_POINT('Ctrl Pts',(-39.3907466079886,-3.89354312734584,
3.33704719832106));
#34981=CARTESIAN_POINT('Ctrl Pts',(-39.2514879639057,-5.01676384034499,
1.06190520223392));
#34982=CARTESIAN_POINT('Ctrl Pts',(-39.1122293198229,-4.91173915161331,
-1.47322116290581));
#34983=CARTESIAN_POINT('Ctrl Pts',(-38.9729706757401,-3.60418206959766,
-3.64766140116037));
#34984=CARTESIAN_POINT('Ctrl Pts',(-38.8337120316572,-1.41421947780232,
-4.92905116193056));
#34985=CARTESIAN_POINT('Ctrl Pts',(-38.6944533875743,1.12198396286053,-5.00367006060634));
#34986=CARTESIAN_POINT('Ctrl Pts',(-38.5551947434916,3.38349405796131,-3.85324928444358));
#34987=CARTESIAN_POINT('Ctrl Pts',(-38.4159360994086,4.81662929812997,-1.75944431361739));
#34988=CARTESIAN_POINT('Ctrl Pts',(-38.2766774553259,5.07051772191601,0.765122290918382));
#34989=CARTESIAN_POINT('Ctrl Pts',(-38.137418811243,4.08300027639372,3.10236536070355));
#34990=CARTESIAN_POINT('Ctrl Pts',(-37.9981601671602,2.09584910794909,4.68006181636883));
#34991=CARTESIAN_POINT('Ctrl Pts',(-37.8589015230773,-0.404425083919172,
5.11194703022454));
#34992=CARTESIAN_POINT('Ctrl Pts',(-37.7196428789945,-2.80568459910014,
4.29228331062813));
#34993=CARTESIAN_POINT('Ctrl Pts',(-37.5803842349116,-4.5200333253302,2.42174747367039));
#34994=CARTESIAN_POINT('Ctrl Pts',(-37.4411255908289,-5.12775030165407,
-0.041700506124886));
#34995=CARTESIAN_POINT('Ctrl Pts',(-37.3018669467459,-4.48004925758386,
-2.49493902489554));
#34996=CARTESIAN_POINT('Ctrl Pts',(-37.1626083026632,-2.7355056920653,-4.33734604303171));
#34997=CARTESIAN_POINT('Ctrl Pts',(-37.0233496585803,-0.321233115053798,
-5.11784831487974));
#34998=CARTESIAN_POINT('Ctrl Pts',(-36.8840910144975,2.17168639631715,-4.64535685221012));
#34999=CARTESIAN_POINT('Ctrl Pts',(-36.7448323704146,4.13291577533089,-3.03555090261152));
#35000=CARTESIAN_POINT('Ctrl Pts',(-36.6055737263318,5.08229070826373,-0.68255640427784));
#35001=CARTESIAN_POINT('Ctrl Pts',(-36.4663150822489,4.78737741250149,1.8375471690803));
#35002=CARTESIAN_POINT('Ctrl Pts',(-36.3270564381661,3.3203789876831,3.90776732501783));
#35003=CARTESIAN_POINT('Ctrl Pts',(-36.1877977940833,1.04045805875398,5.02125573101972));
#35004=CARTESIAN_POINT('Ctrl Pts',(-36.0485391500004,-1.49419637309213,
4.90539899365616));
#35005=CARTESIAN_POINT('Ctrl Pts',(-35.9092805059176,-3.66302935450954,
3.58856211264706));
#35006=CARTESIAN_POINT('Ctrl Pts',(-35.7700218618348,-4.9350493496549,1.39314392824117));
#35007=CARTESIAN_POINT('Ctrl Pts',(-35.6307632177519,-4.99882995703361,
-1.14335521557734));
#35008=CARTESIAN_POINT('Ctrl Pts',(-35.4915045736691,-3.8387558835552,-3.39992872789929));
#35009=CARTESIAN_POINT('Ctrl Pts',(-35.3522459295862,-1.73884600907171,
-4.82410371416908));
#35010=CARTESIAN_POINT('Ctrl Pts',(-35.2129872855035,0.786782452717923,
-5.06720193602146));
#35011=CARTESIAN_POINT('Ctrl Pts',(-35.0737286414205,3.11978436072366,-4.06970608655078));
#35012=CARTESIAN_POINT('Ctrl Pts',(-34.9344699973378,4.68897499169966,-2.07583130710078));
#35013=CARTESIAN_POINT('Ctrl Pts',(-34.7952113532549,5.11017218394326,0.426265573061127));
#35014=CARTESIAN_POINT('Ctrl Pts',(-34.6559527091721,4.28025497520489,2.82400060827867));
#35015=CARTESIAN_POINT('Ctrl Pts',(-34.5166940650892,2.40241052515365,4.53034057847261));
#35016=CARTESIAN_POINT('Ctrl Pts',(-34.3774354210064,-0.0636118368933031,
5.12752529223713));
#35017=CARTESIAN_POINT('Ctrl Pts',(-34.2381767769235,-2.51406022562872,
4.46934707426445));
#35018=CARTESIAN_POINT('Ctrl Pts',(-34.0989181328408,-4.34899570403538,
2.71694653142206));
#35019=CARTESIAN_POINT('Ctrl Pts',(-33.9596594887578,-5.11917427029261,
0.29936078350168));
#35020=CARTESIAN_POINT('Ctrl Pts',(-33.8204008446751,-4.63603447071792,
-2.19151693460024));
#35021=CARTESIAN_POINT('Ctrl Pts',(-33.6811422005921,-3.01786256635649,
-4.1458494447952));
#35022=CARTESIAN_POINT('Ctrl Pts',(-33.5418835565094,-0.660832717283021,
-5.08516098153175));
#35023=CARTESIAN_POINT('Ctrl Pts',(-33.4026249124265,1.85798763502059,-4.7794815656549));
#35024=CARTESIAN_POINT('Ctrl Pts',(-33.2633662683437,3.92192016684631,-3.30365014691457));
#35025=CARTESIAN_POINT('Ctrl Pts',(-33.1241076242608,5.02565593354922,-1.01899191650671));
#35026=CARTESIAN_POINT('Ctrl Pts',(-32.9848489801781,4.89896926309818,1.51514429924805));
#35027=CARTESIAN_POINT('Ctrl Pts',(-32.8455903360952,3.57287662854112,3.67833042093137));
#35028=CARTESIAN_POINT('Ctrl Pts',(-32.7063316920124,1.37204293986752,4.94095742336282));
#35029=CARTESIAN_POINT('Ctrl Pts',(-32.5670730479295,-1.16470559062442,
4.99389857481034));
#35030=CARTESIAN_POINT('Ctrl Pts',(-32.4278144038467,-3.41630131512815,
3.82419238697246));
#35031=CARTESIAN_POINT('Ctrl Pts',(-32.2885557597638,-4.8314900420594,1.71821595319255));
#35032=CARTESIAN_POINT('Ctrl Pts',(-32.149297115681,-5.06379362300385,-0.808428247867442));
#35033=CARTESIAN_POINT('Ctrl Pts',(-32.0100384715981,-4.0563375838621,-3.13714639347168));
#35034=CARTESIAN_POINT('Ctrl Pts',(-31.8707798275153,-2.05577560156633,
-4.69780254633261));
#35035=CARTESIAN_POINT('Ctrl Pts',(-31.7315211834325,0.448098278592388,
-5.10830402590205));
#35036=CARTESIAN_POINT('Ctrl Pts',(-31.5922625393496,2.84226505119731,-4.26814848231254));
#35037=CARTESIAN_POINT('Ctrl Pts',(-31.4530038952668,4.54056510758199,-2.38302970861326));
#35038=CARTESIAN_POINT('Ctrl Pts',(-31.313745251184,5.12720665419247,0.0855220061093843));
#35039=CARTESIAN_POINT('Ctrl Pts',(-31.1744866071012,4.45856328065359,2.5331355196144));
#35040=CARTESIAN_POINT('Ctrl Pts',(-31.0352279630183,2.69833775932673,4.360565952364));
#35041=CARTESIAN_POINT('Ctrl Pts',(-30.8959693189355,0.277482985620765,
5.12040674956741));
#35042=CARTESIAN_POINT('Ctrl Pts',(-30.7567106748526,-2.21130745577726,
4.62662743522194));
#35043=CARTESIAN_POINT('Ctrl Pts',(-30.6174520307698,-4.15870741103577,
3.00011912392169));
#35044=CARTESIAN_POINT('Ctrl Pts',(-30.478193386687,-5.08793839974446,0.639096963480733));
#35045=CARTESIAN_POINT('Ctrl Pts',(-30.3389347426041,-4.7714984454601,-1.87839417410094));
#35046=CARTESIAN_POINT('Ctrl Pts',(-30.1996760985213,-3.28686098148408,
-3.93600139440042));
#35047=CARTESIAN_POINT('Ctrl Pts',(-30.0604174544384,-0.997507167463827,
-5.02996436758579));
#35048=CARTESIAN_POINT('Ctrl Pts',(-29.9211588103556,1.53606455886436,-4.89245007734626));
#35049=CARTESIAN_POINT('Ctrl Pts',(-29.7819001662728,3.69356432102827,-3.55712590369689));
#35050=CARTESIAN_POINT('Ctrl Pts',(-29.6426415221899,4.94677527517285,-1.35091689798559));
#35051=CARTESIAN_POINT('Ctrl Pts',(-29.5033828781071,4.98887600398362,1.18603469814376));
#35052=CARTESIAN_POINT('Ctrl Pts',(-29.3641242340243,3.80955906062489,3.43261152068441));
#35053=CARTESIAN_POINT('Ctrl Pts',(-29.2248655899414,1.6975545226847,4.83878814692659));
#35054=CARTESIAN_POINT('Ctrl Pts',(-29.0856069458586,-0.83005928111469,
5.06029284509897));
#35055=CARTESIAN_POINT('Ctrl Pts',(-28.9463483017757,-3.15445114191686,
4.0428950124365));
#35056=CARTESIAN_POINT('Ctrl Pts',(-28.807089657693,-4.70654431907648,2.03568235756303));
#35057=CARTESIAN_POINT('Ctrl Pts',(-28.66783101361,-5.10634259021348,-0.469922801847675));
#35058=CARTESIAN_POINT('Ctrl Pts',(-28.5285723695273,-4.25596405301566,
-2.86047759434731));
#35059=CARTESIAN_POINT('Ctrl Pts',(-28.3893137254443,-2.36360537794301,
-4.55070672595844));
#35060=CARTESIAN_POINT('Ctrl Pts',(-28.2500550813616,0.107430613693398,
-5.12679439333839));
#35061=CARTESIAN_POINT('Ctrl Pts',(-28.1107964372787,2.55216455853763,-4.44769807366338));
#35062=CARTESIAN_POINT('Ctrl Pts',(-27.9715377931959,4.37205657674479,-2.67967971557556));
#35063=CARTESIAN_POINT('Ctrl Pts',(-27.832279149113,5.12154573019909,-0.255600120899675));
#35064=CARTESIAN_POINT('Ctrl Pts',(-27.6930205050302,4.61713591749465,2.23105759847328));
#35065=CARTESIAN_POINT('Ctrl Pts',(-27.5537618609474,2.98232089930236,4.17148943926614));
#35066=CARTESIAN_POINT('Ctrl Pts',(-27.4145032168645,0.617349539765915,
5.09062291218622));
#35067=CARTESIAN_POINT('Ctrl Pts',(-27.2752445727817,-1.89876641369781,
4.76342819768889));
#35068=CARTESIAN_POINT('Ctrl Pts',(-27.1359859286988,-3.9500107505568,3.27001179796192));
#35069=CARTESIAN_POINT('Ctrl Pts',(-26.996727284616,-5.03418095445742,0.97600420393705));
#35070=CARTESIAN_POINT('Ctrl Pts',(-26.8574686405332,-4.88584155544076,
-1.55695676993701));
#35071=CARTESIAN_POINT('Ctrl Pts',(-26.7182099964503,-3.54131022572266,
-3.7087307766292));
#35072=CARTESIAN_POINT('Ctrl Pts',(-26.5789513523675,-1.32976618835693,
-4.95250279885102));
#35073=CARTESIAN_POINT('Ctrl Pts',(-26.4396927082847,1.20734214866586,-4.9837623362656));
#35074=CARTESIAN_POINT('Ctrl Pts',(-26.3004340642018,3.44885904674366,-3.79485617171704));
#35075=CARTESIAN_POINT('Ctrl Pts',(-26.161175420119,4.84599789550719,-1.67686209482602));
#35076=CARTESIAN_POINT('Ctrl Pts',(-26.0219167760362,5.05669966623105,0.851675157476819));
#35077=CARTESIAN_POINT('Ctrl Pts',(-25.8826581319533,4.02937861773551,3.1716982900743));
#35078=CARTESIAN_POINT('Ctrl Pts',(-25.7433994878705,2.01555194199366,4.71520015030647));
#35079=CARTESIAN_POINT('Ctrl Pts',(-25.6041408437876,-0.491738744311117,
5.1042879126934));
#35080=CARTESIAN_POINT('Ctrl Pts',(-25.4648821997048,-2.87863790516758,
4.24370190980198));
#35081=CARTESIAN_POINT('Ctrl Pts',(-25.325623555622,-4.56076524841596,2.3441378878312));
#35082=CARTESIAN_POINT('Ctrl Pts',(-25.1863649115391,-5.12628851720279,
-0.129337259594039));
#35083=CARTESIAN_POINT('Ctrl Pts',(-25.0471062674563,-4.43675165169258,
-2.57114699492807));
#35084=CARTESIAN_POINT('Ctrl Pts',(-24.9078476233734,-2.6609727408645,-4.38346736735891));
#35085=CARTESIAN_POINT('Ctrl Pts',(-24.7685889792906,-0.233712588919614,
-5.12259119138986));
#35086=CARTESIAN_POINT('Ctrl Pts',(-24.6293303352077,2.25076700205062,-4.60756009085119));
#35087=CARTESIAN_POINT('Ctrl Pts',(-24.490071691125,4.18419529608634,-2.96446821749421));
#35088=CARTESIAN_POINT('Ctrl Pts',(-24.3508130470421,5.09321446983781,-0.595590843246681));
#35089=CARTESIAN_POINT('Ctrl Pts',(-24.2115544029592,4.75527096970404,1.91910398181406));
#35090=CARTESIAN_POINT('Ctrl Pts',(-24.0722957588764,3.25310290401414,3.96394797950469));
#35091=CARTESIAN_POINT('Ctrl Pts',(-23.9330371147936,0.954483418570409,
5.03830561716918));
#35092=CARTESIAN_POINT('Ctrl Pts',(-23.7937784707108,-1.57782055097424,
4.8791438180533));
#35093=CARTESIAN_POINT('Ctrl Pts',(-23.6545198266279,-3.72382951079462,
3.52542988341273));
#35094=CARTESIAN_POINT('Ctrl Pts',(-23.5152611825451,-4.95813988981271,
1.30859119719357));
#35095=CARTESIAN_POINT('Ctrl Pts',(-23.3760025384622,-4.97855766503187,
-1.22862755311651));
#35096=CARTESIAN_POINT('Ctrl Pts',(-23.2367438943794,-3.78008398872379,
-3.46504359662597));
#35097=CARTESIAN_POINT('Ctrl Pts',(-23.0974852502966,-1.65613904746037,
-4.85311915615117));
#35098=CARTESIAN_POINT('Ctrl Pts',(-22.9582266062137,0.873275482247959,
-5.05301415201156));
#35099=CARTESIAN_POINT('Ctrl Pts',(-22.8189679621309,3.18888752301124,-4.01578864656841));
#35100=CARTESIAN_POINT('Ctrl Pts',(-22.679709318048,4.72376988196712,-1.99538472243945));
#35101=CARTESIAN_POINT('Ctrl Pts',(-22.5404506739652,5.10214003086018,0.513545707623582));
#35102=CARTESIAN_POINT('Ctrl Pts',(-22.4011920298823,4.23136227657829,2.89674565205072));
#35103=CARTESIAN_POINT('Ctrl Pts',(-22.2619333857996,2.32462759375435,4.57074049128587));
#35104=CARTESIAN_POINT('Ctrl Pts',(-22.1226747417167,-0.151241543795875,
5.12568903502298));
#35105=CARTESIAN_POINT('Ctrl Pts',(-21.9834160976339,-2.59008248216644,
4.42572421462287));
#35106=CARTESIAN_POINT('Ctrl Pts',(-21.844157453551,-4.39479811584537,2.64221717678288));
#35107=CARTESIAN_POINT('Ctrl Pts',(-21.7048988094682,-5.12354311404958,
0.211820789346871));
#35108=CARTESIAN_POINT('Ctrl Pts',(-21.5656401653853,-4.59790013014616,
-2.27043530661552));
#35109=CARTESIAN_POINT('Ctrl Pts',(-21.4263815213025,-2.94656140448722,
-4.19682474948749));
#35110=CARTESIAN_POINT('Ctrl Pts',(-21.2871228772196,-0.573821271236779,
-5.09571302537738));
#35111=CARTESIAN_POINT('Ctrl Pts',(-21.1478642331369,1.93940650708562,-4.74702691045655));
#35112=CARTESIAN_POINT('Ctrl Pts',(-21.008605589054,3.97781282675011,-3.23613460839731));
#35113=CARTESIAN_POINT('Ctrl Pts',(-20.8693469449712,5.04233828040476,-0.932945204333682));
#35114=CARTESIAN_POINT('Ctrl Pts',(-20.7300883008883,4.87235698748461,1.59865552100332));
#35115=CARTESIAN_POINT('Ctrl Pts',(-20.5908296568055,3.50948516674211,3.73886024782176));
#35116=CARTESIAN_POINT('Ctrl Pts',(-20.4515710127226,1.28739231115071,4.96368644512469));
#35117=CARTESIAN_POINT('Ctrl Pts',(-20.3123123686398,-1.24989052282436,
4.97326208531968));
#35118=CARTESIAN_POINT('Ctrl Pts',(-20.173053724557,-3.48116487480147,3.76524278138513));
#35119=CARTESIAN_POINT('Ctrl Pts',(-20.0337950804741,-4.86015179882432,
1.63538575899058));
#35120=CARTESIAN_POINT('Ctrl Pts',(-19.8945364363913,-5.04923636973798,
-0.894859861006039));
#35121=CARTESIAN_POINT('Ctrl Pts',(-19.7552777923085,-4.00212534708821,
-3.20601852685208));
#35122=CARTESIAN_POINT('Ctrl Pts',(-19.6160191482256,-1.97518106715403,
-4.7322533575751));
#35123=CARTESIAN_POINT('Ctrl Pts',(-19.4767605041428,0.535343293589886,
-5.09989898393416));
#35124=CARTESIAN_POINT('Ctrl Pts',(-19.3375018600599,2.91480050434934,-4.21894537866626));
#35125=CARTESIAN_POINT('Ctrl Pts',(-19.1982432159771,4.5806322724203,-2.30507485197035));
#35126=CARTESIAN_POINT('Ctrl Pts',(-19.0589845718943,5.12499595774547,0.17314306632675));
#35127=CARTESIAN_POINT('Ctrl Pts',(-18.9197259278114,4.41461596381525,2.60897067449063));
#35128=CARTESIAN_POINT('Ctrl Pts',(-18.7804672837286,2.6234133658075,4.40604861530454));
#35129=CARTESIAN_POINT('Ctrl Pts',(-18.6412086396458,0.189925121925963,
5.12440148079616));
#35130=CARTESIAN_POINT('Ctrl Pts',(-18.5019499955629,-2.29006215302471,
4.58815621177052));
#35131=CARTESIAN_POINT('Ctrl Pts',(-18.3626913514801,-4.20937756885579,
2.92860078725975));
#35132=CARTESIAN_POINT('Ctrl Pts',(-18.2234327073973,-5.09811853318134,
0.552041221248485));
#35133=CARTESIAN_POINT('Ctrl Pts',(-18.0841740633144,-4.73869617048286,
-1.95967361878847));
#35134=CARTESIAN_POINT('Ctrl Pts',(-17.9449154192316,-3.21910722095246,
-3.99160503912099));
#35135=CARTESIAN_POINT('Ctrl Pts',(-17.8056567751488,-0.911389954514629,
-5.04627887052769));
#35136=CARTESIAN_POINT('Ctrl Pts',(-17.6663981310659,1.61946129957759,-4.86548118766222));
#35137=CARTESIAN_POINT('Ctrl Pts',(-17.5271394869831,3.75382271324905,-3.49347636686155));
#35138=CARTESIAN_POINT('Ctrl Pts',(-17.3878808429002,4.96914236350674,-1.26616991732043));
#35139=CARTESIAN_POINT('Ctrl Pts',(-17.2486221988174,4.96787569382644,1.27113066952724));
#35140=CARTESIAN_POINT('Ctrl Pts',(-17.1093635547345,3.75033282070164,3.49722258689558));
#35141=CARTESIAN_POINT('Ctrl Pts',(-16.9701049106517,1.61460260837161,4.86709569511061));
#35142=CARTESIAN_POINT('Ctrl Pts',(-16.8308462665689,-0.916427899620469,
5.0453663883926));
#35143=CARTESIAN_POINT('Ctrl Pts',(-16.691587622486,-3.22309098878473,3.98838896878665));
#35144=CARTESIAN_POINT('Ctrl Pts',(-16.5523289784032,-4.74065042222205,
1.95494134505625));
#35145=CARTESIAN_POINT('Ctrl Pts',(-16.4130703343204,-5.09756481283691,
-0.557131104185897));
#35146=CARTESIAN_POINT('Ctrl Pts',(-16.2738116902375,-4.20645144279858,
-2.93280213238163));
#35147=CARTESIAN_POINT('Ctrl Pts',(-16.1345530461547,-2.28548001951246,
-4.5904404111952));
#35148=CARTESIAN_POINT('Ctrl Pts',(-15.9952944020718,0.195041427264702,
-5.1242092980259));
#35149=CARTESIAN_POINT('Ctrl Pts',(-15.856035757989,2.62781122700226,-4.40342710210641));
#35150=CARTESIAN_POINT('Ctrl Pts',(-15.7167771139062,4.41721866030238,-2.60456165129585));
#35151=CARTESIAN_POINT('Ctrl Pts',(-15.5775184698233,5.12516627595581,-0.16802598647164));
#35152=CARTESIAN_POINT('Ctrl Pts',(-15.4382598257405,4.57832851364817,2.30964718289191));
#35153=CARTESIAN_POINT('Ctrl Pts',(-15.2990011816576,2.91058669377287,4.22185352497654));
#35154=CARTESIAN_POINT('Ctrl Pts',(-15.1597425375748,0.530251090985978,
5.10043094932504));
#35155=CARTESIAN_POINT('Ctrl Pts',(-15.020483893492,-1.97990494684484,4.73027890190248));
#35156=CARTESIAN_POINT('Ctrl Pts',(-14.8812252494091,-4.00532436477151,
3.20202105259979));
#35157=CARTESIAN_POINT('Ctrl Pts',(-14.7419666053263,-5.05012731558285,
0.889818062712039));
#35158=CARTESIAN_POINT('Ctrl Pts',(-14.6027079612435,-4.8585165441382,-1.64023750678368));
#35159=CARTESIAN_POINT('Ctrl Pts',(-14.4634493171606,-3.47740377609158,
-3.76871663386205));
#35160=CARTESIAN_POINT('Ctrl Pts',(-14.3241906730778,-1.2449244032235,-4.9745075453338));
#35161=CARTESIAN_POINT('Ctrl Pts',(-14.184932028995,1.29234760538017,-4.96239858890765));
#35162=CARTESIAN_POINT('Ctrl Pts',(-14.0456733849121,3.51321643969437,-3.73535437892922));
#35163=CARTESIAN_POINT('Ctrl Pts',(-13.9064147408293,4.87395071821435,-1.59378997510416));
#35164=CARTESIAN_POINT('Ctrl Pts',(-13.7671560967465,5.04140427864135,0.937979204258423));
#35165=CARTESIAN_POINT('Ctrl Pts',(-13.6278974526636,3.97457976249027,3.24010459706584));
#35166=CARTESIAN_POINT('Ctrl Pts',(-13.4886388085808,1.93466592572345,4.74896092257761));
#35167=CARTESIAN_POINT('Ctrl Pts',(-13.3493801644979,-0.57890874156636,
5.09513756019038));
#35168=CARTESIAN_POINT('Ctrl Pts',(-13.2101215204151,-2.95075020743805,
4.1938806971144));
#35169=CARTESIAN_POINT('Ctrl Pts',(-13.0708628763322,-4.60016472851397,
2.26584345418221));
#35170=CARTESIAN_POINT('Ctrl Pts',(-12.9316042322494,-5.12332907022864,
-0.216936226745527));
#35171=CARTESIAN_POINT('Ctrl Pts',(-12.7923455881666,-4.39215783380509,
-2.64660379567266));
#35172=CARTESIAN_POINT('Ctrl Pts',(-12.6530869440837,-2.58566237748044,
-4.42830804687374));
#35173=CARTESIAN_POINT('Ctrl Pts',(-12.5138283000009,-0.146123782862334,
-5.12583748556338));
#35174=CARTESIAN_POINT('Ctrl Pts',(-12.3745696559181,2.3291900385944,-4.56841721523299));
#35175=CARTESIAN_POINT('Ctrl Pts',(-12.2353110118352,4.23425239003886,-2.8925194529639));
#35176=CARTESIAN_POINT('Ctrl Pts',(-12.0960523677524,5.1026502315838,-0.50845127833681));
#35177=CARTESIAN_POINT('Ctrl Pts',(-11.9567937236695,4.72177525841466,2.00010012183084));
#35178=CARTESIAN_POINT('Ctrl Pts',(-11.8175350795867,3.18487641533271,4.01897055318671));
#35179=CARTESIAN_POINT('Ctrl Pts',(-11.6782764355039,0.868229922828961,
5.05388354529751));
#35180=CARTESIAN_POINT('Ctrl Pts',(-11.539017791421,-1.66098376324763,4.85146318408707));
#35181=CARTESIAN_POINT('Ctrl Pts',(-11.3997591473382,-3.78354173769753,
3.461267687918));
#35182=CARTESIAN_POINT('Ctrl Pts',(-11.2605005032553,-4.97978189263771,
1.2236561568031));
#35183=CARTESIAN_POINT('Ctrl Pts',(-11.1212418591726,-4.9568308705752,-1.31354094296196));
#35184=CARTESIAN_POINT('Ctrl Pts',(-10.9819832150897,-3.72030772957414,
-3.52914614115021));
#35185=CARTESIAN_POINT('Ctrl Pts',(-10.8427245710069,-1.57294823922665,
-4.88071674296288));
#35186=CARTESIAN_POINT('Ctrl Pts',(-10.703465926924,0.959513381393236,-5.03735011283231));
#35187=CARTESIAN_POINT('Ctrl Pts',(-10.5642072828412,3.25705904102695,-3.96069798035511));
#35188=CARTESIAN_POINT('Ctrl Pts',(-10.4249486387583,4.75718470689197,-1.91435517938488));
#35189=CARTESIAN_POINT('Ctrl Pts',(-10.2856899946755,5.09261727031618,0.60067580807126));
#35190=CARTESIAN_POINT('Ctrl Pts',(-10.1464313505927,4.18123337115581,2.96864440178638));
#35191=CARTESIAN_POINT('Ctrl Pts',(-10.0071727065098,2.24616551454361,4.60980504681049));
#35192=CARTESIAN_POINT('Ctrl Pts',(-9.86791406242699,-0.238827064970182,
5.12235529042668));
#35193=CARTESIAN_POINT('Ctrl Pts',(-9.72865541834415,-2.66534803734968,
4.38080836468806));
#35194=CARTESIAN_POINT('Ctrl Pts',(-9.58939677426131,-4.43931657252653,
2.56671588946183));
#35195=CARTESIAN_POINT('Ctrl Pts',(-9.45013813017847,-5.12641509736252,
0.124218911032201));
#35196=CARTESIAN_POINT('Ctrl Pts',(-9.31087948609565,-4.55842249750529,
-2.3486903632795));
#35197=CARTESIAN_POINT('Ctrl Pts',(-9.1716208420128,-2.87439939474084,-4.24657393763936));
#35198=CARTESIAN_POINT('Ctrl Pts',(-9.03236219792996,-0.486642181365819,
-5.1047763394335));
#35199=CARTESIAN_POINT('Ctrl Pts',(-8.89310355384714,2.02025877498237,-4.71318539529599));
#35200=CARTESIAN_POINT('Ctrl Pts',(-8.75384490976428,4.03254335518717,-3.16767362221242));
#35201=CARTESIAN_POINT('Ctrl Pts',(-8.61458626568145,5.05754749108297,-0.846625929064747));
#35202=CARTESIAN_POINT('Ctrl Pts',(-8.47532762159861,4.84432123630313,1.681699690143));
#35203=CARTESIAN_POINT('Ctrl Pts',(-8.33606897751578,3.44506839698563,3.79829775404922));
#35204=CARTESIAN_POINT('Ctrl Pts',(-8.19681033343293,1.20236556641743,4.98496530910879));
#35205=CARTESIAN_POINT('Ctrl Pts',(-8.0575516893501,-1.33471029528195,4.95117264049567));
#35206=CARTESIAN_POINT('Ctrl Pts',(-7.91829304526727,-3.54501140038643,
3.70519314738851));
#35207=CARTESIAN_POINT('Ctrl Pts',(-7.77903440118442,-4.88739364580853,
1.55207778130958));
#35208=CARTESIAN_POINT('Ctrl Pts',(-7.63977575710159,-5.03320396499462,
-0.98103003781074));
#35209=CARTESIAN_POINT('Ctrl Pts',(-7.50051711301875,-3.94674387586246,
-3.27395401108));
#35210=CARTESIAN_POINT('Ctrl Pts',(-7.36125846893591,-1.89400947691462,
-4.7653216249989));
#35211=CARTESIAN_POINT('Ctrl Pts',(-7.22199982485306,0.622431906234182,
-5.09000398923479));
#35212=CARTESIAN_POINT('Ctrl Pts',(-7.08274118077025,2.98648438867875,-4.16850969586284));
#35213=CARTESIAN_POINT('Ctrl Pts',(-6.94348253668739,4.61936119005255,-2.22644655991574));
#35214=CARTESIAN_POINT('Ctrl Pts',(-6.80422389260458,5.12128797640124,0.260713542211845));
#35215=CARTESIAN_POINT('Ctrl Pts',(-6.66496524852172,4.36937890199675,2.68404360976314));
#35216=CARTESIAN_POINT('Ctrl Pts',(-6.52570660443889,2.54772253320329,4.45024403624483));
#35217=CARTESIAN_POINT('Ctrl Pts',(-6.38644796035604,0.102311770964511,
5.12689910080611));
#35218=CARTESIAN_POINT('Ctrl Pts',(-6.24718931627322,-2.3681478008713,4.54834454296868));
#35219=CARTESIAN_POINT('Ctrl Pts',(-6.10793067219037,-4.25881794278671,
2.85622684997581));
#35220=CARTESIAN_POINT('Ctrl Pts',(-5.96867202810753,-5.10680923405142,
0.464824198306887));
#35221=CARTESIAN_POINT('Ctrl Pts',(-5.82941338402469,-4.70450946939732,
-2.04038053820247));
#35222=CARTESIAN_POINT('Ctrl Pts',(-5.69015473994187,-3.150412987362,-4.0460425229334));
#35223=CARTESIAN_POINT('Ctrl Pts',(-5.55089609585902,-0.825006475908536,
-5.06111908603556));
#35224=CARTESIAN_POINT('Ctrl Pts',(-5.41163745177619,1.70238490919671,-4.83709083119842));
#35225=CARTESIAN_POINT('Ctrl Pts',(-5.27237880769335,3.81298441347213,-3.42880619909369));
#35226=CARTESIAN_POINT('Ctrl Pts',(-5.13312016361051,4.99005770009789,-1.18105302083279));
#35227=CARTESIAN_POINT('Ctrl Pts',(-4.99386151952767,4.94542400198837,1.35585527578786));
#35228=CARTESIAN_POINT('Ctrl Pts',(-4.85460287544484,3.69001090836444,3.56081192770356));
#35229=CARTESIAN_POINT('Ctrl Pts',(-4.715344231362,1.53117898244731,4.89398130483108));
#35230=CARTESIAN_POINT('Ctrl Pts',(-4.57608558727916,-1.00252878061676,
5.0289659108369));
#35231=CARTESIAN_POINT('Ctrl Pts',(-4.43682694319632,-3.29078919872254,
3.93271770381442));
#35232=CARTESIAN_POINT('Ctrl Pts',(-4.29756829911349,-4.77337152831812,
1.87362918982565));
#35233=CARTESIAN_POINT('Ctrl Pts',(-4.15830965503064,-5.08729776466478,
-0.644176638788498));
#35234=CARTESIAN_POINT('Ctrl Pts',(-4.01905101094782,-4.15570990356999,
-3.0042698423568));
#35235=CARTESIAN_POINT('Ctrl Pts',(-3.87979236686497,-2.20668695036655,
-4.62883298374532));
#35236=CARTESIAN_POINT('Ctrl Pts',(-3.74053372278213,0.28259525882338,-5.12012714764091));
#35237=CARTESIAN_POINT('Ctrl Pts',(-3.60127507869929,2.70269017153252,-4.35786965443408));
#35238=CARTESIAN_POINT('Ctrl Pts',(-3.46201643461646,4.46109023849236,-2.52868265552132));
#35239=CARTESIAN_POINT('Ctrl Pts',(-3.32275779053363,5.12728948705797,-0.0804027626875136));
#35240=CARTESIAN_POINT('Ctrl Pts',(-3.18349914645079,4.53818353564321,2.38756199608455));
#35241=CARTESIAN_POINT('Ctrl Pts',(-3.04424050236796,2.83800215050638,4.27098418189009));
#35242=CARTESIAN_POINT('Ctrl Pts',(-2.90498185828511,0.442997727543895,
5.10874887834615));
#35243=CARTESIAN_POINT('Ctrl Pts',(-2.76572321420227,-2.06046504404221,
4.69574763908411));
#35244=CARTESIAN_POINT('Ctrl Pts',(-2.62646457011944,-4.05946780997995,
3.13309482607209));
#35245=CARTESIAN_POINT('Ctrl Pts',(-2.48720592603659,-5.06459826484176,
0.803371957913989));
#35246=CARTESIAN_POINT('Ctrl Pts',(-2.34794728195375,-4.8297721009878,-1.72303904227276));
#35247=CARTESIAN_POINT('Ctrl Pts',(-2.20868863787092,-3.41248139082355,
-3.82760144861539));
#35248=CARTESIAN_POINT('Ctrl Pts',(-2.06942999378809,-1.15971890993101,
-4.99505897100328));
#35249=CARTESIAN_POINT('Ctrl Pts',(-1.93017134970524,1.37697549976642,-4.93958506317368));
#35250=CARTESIAN_POINT('Ctrl Pts',(-1.79091270562242,3.57654743186344,-3.67476128358358));
#35251=CARTESIAN_POINT('Ctrl Pts',(-1.65165406153958,4.90047960504737,-1.51025223624387));
#35252=CARTESIAN_POINT('Ctrl Pts',(-1.51239541745672,5.02463601739066,1.02400924064084));
#35253=CARTESIAN_POINT('Ctrl Pts',(-1.3731367733739,3.91861974053298,3.3075642508956));
#35254=CARTESIAN_POINT('Ctrl Pts',(-1.23387812929106,1.85321465084221,4.7813343589219));
#35255=CARTESIAN_POINT('Ctrl Pts',(-1.09461948520821,-0.665909531765221,
5.08449847225302));
#35256=CARTESIAN_POINT('Ctrl Pts',(-0.955360841125384,-3.0220005881154,
4.1428345670361));
#35257=CARTESIAN_POINT('Ctrl Pts',(-0.816102197042551,-4.63821996216164,
2.186886385227));
#35258=CARTESIAN_POINT('Ctrl Pts',(-0.676843552959707,-5.11887339656061,
-0.30447052465205));
#35259=CARTESIAN_POINT('Ctrl Pts',(-0.537584908876869,-4.34627971767338,
-2.721289900206));
#35260=CARTESIAN_POINT('Ctrl Pts',(-0.398326264794041,-2.50959877852527,
-4.47185006834336));
#35261=CARTESIAN_POINT('Ctrl Pts',(-0.259067620711191,-0.0584880437401866,
-5.12759583452146));
#35262=CARTESIAN_POINT('Ctrl Pts',(-0.119808976628352,2.40692431658313,
-4.52792095714916));
#35263=CARTESIAN_POINT('Ctrl Pts',(0.0194496674544802,4.28308858749807,
-2.81976214164628));
#35264=CARTESIAN_POINT('Ctrl Pts',(0.158708311537312,5.11056367501673,-0.421091719996148));
#35265=CARTESIAN_POINT('Ctrl Pts',(0.297966955620156,4.68696209505367,2.08037032858027));
#35266=CARTESIAN_POINT('Ctrl Pts',(0.437225599702985,3.11559368557815,4.07311831939771));
#35267=CARTESIAN_POINT('Ctrl Pts',(0.53006469575821,1.55987615590447,4.73580748738429));
#35268=CARTESIAN_POINT('Ctrl Pts',(0.576484243785824,0.749759770534598,
4.86076571632371));
#35269=CARTESIAN_POINT('',(-8.88178419700125E-15,0.901975524284047,5.84759529345974));
#35270=CARTESIAN_POINT('Ctrl Pts',(-1.90958360235527E-14,3.90948457664364,
-2.98454410297303));
#35271=CARTESIAN_POINT('Ctrl Pts',(-1.91833507282437E-14,3.98829243888861,
-2.90007919033881));
#35272=CARTESIAN_POINT('Ctrl Pts',(-3.73580879594742E-14,4.06399823051801,
-2.81291231202011));
#35273=CARTESIAN_POINT('Ctrl Pts',(-3.49720252756924E-14,4.13644712233781,
-2.72320270054994));
#35274=CARTESIAN_POINT('Ctrl Pts',(-3.18638451300726E-14,4.22735285500253,
-2.61063896419842));
#35275=CARTESIAN_POINT('Ctrl Pts',(-1.94635529727361E-14,4.3131323964303,
-2.49407313917698));
#35276=CARTESIAN_POINT('Ctrl Pts',(-1.43218770176645E-14,4.39368586403212,
-2.37393105053264));
#35277=CARTESIAN_POINT('Ctrl Pts',(-1.10162867186718E-14,4.44547379531786,
-2.29669154221012));
#35278=CARTESIAN_POINT('Ctrl Pts',(-5.24917652412265E-15,4.4951010825493,
-2.21797295530272));
#35279=CARTESIAN_POINT('Ctrl Pts',(-3.44169137633799E-15,4.54253384538222,
-2.13787989953547));
#35280=CARTESIAN_POINT('Ctrl Pts',(-2.4768234675261E-15,4.5678543027812,
-2.09512479345715));
#35281=CARTESIAN_POINT('Ctrl Pts',(-9.30961986510496E-15,4.5925493020505,
-2.05197791192938));
#35282=CARTESIAN_POINT('Ctrl Pts',(-9.2148511043888E-15,4.61661294342695,
-2.00845450824052));
#35283=CARTESIAN_POINT('Ctrl Pts',(-9.15701027903361E-15,4.63129985995668,
-1.98189059020882));
#35284=CARTESIAN_POINT('Ctrl Pts',(-2.21079829589896E-14,4.645751578647,
-1.95518640516938));
#35285=CARTESIAN_POINT('Ctrl Pts',(-2.20934381900406E-14,4.6599666572219,
-1.92834534623301));
#35286=CARTESIAN_POINT('Ctrl Pts',(-2.20822060839698E-14,4.67094416198108,
-1.90761750778575));
#35287=CARTESIAN_POINT('Ctrl Pts',(-1.77421344277379E-14,4.68177804862746,
-1.88681267103478));
#35288=CARTESIAN_POINT('Ctrl Pts',(-1.75415237890775E-14,4.69246422230885,
-1.8659397413347));
#35289=CARTESIAN_POINT('Ctrl Pts',(-1.62668284098313E-14,4.76036498920956,
-1.73331154565338));
#35290=CARTESIAN_POINT('Ctrl Pts',(-3.47731085017832E-15,4.82235112178215,
-1.59785024042009));
#35291=CARTESIAN_POINT('Ctrl Pts',(-4.49640324973188E-15,4.87831618402814,
-1.46000130615661));
#35292=CARTESIAN_POINT('Ctrl Pts',(-5.52168602536538E-15,4.93462120051458,
-1.32131502216344));
#35293=CARTESIAN_POINT('Ctrl Pts',(-1.64490113575227E-14,4.98483221912858,
-1.18021136659838));
#35294=CARTESIAN_POINT('Ctrl Pts',(-2.18158824338843E-14,5.02880142240401,
-1.03710876150088));
#35295=CARTESIAN_POINT('Ctrl Pts',(-2.55685228577448E-14,5.05954570660026,
-0.937048109212461));
#35296=CARTESIAN_POINT('Ctrl Pts',(-6.915413085807E-15,5.08723747133457,
-0.836009395806493));
#35297=CARTESIAN_POINT('Ctrl Pts',(-7.43849426498855E-15,5.11181306297585,
-0.73412814542384));
#35298=CARTESIAN_POINT('Ctrl Pts',(-7.54805533896459E-15,5.1169605015016,
-0.712788782330314));
#35299=CARTESIAN_POINT('Ctrl Pts',(-1.50603780235338E-14,5.12197119102857,
-0.691412439291222));
#35300=CARTESIAN_POINT('Ctrl Pts',(-1.53765888910584E-14,5.12684448137593,
-0.670000335987038));
#35301=CARTESIAN_POINT('Ctrl Pts',(-1.57085190484981E-14,5.13196002988606,
-0.647523806712406));
#35302=CARTESIAN_POINT('Ctrl Pts',(-1.68377511556197E-14,5.13692242704591,
-0.62501543339186));
#35303=CARTESIAN_POINT('Ctrl Pts',(-1.62647673107585E-14,5.14172987403327,
-0.602483352090299));
#35304=CARTESIAN_POINT('Ctrl Pts',(-1.47775349171851E-14,5.15420804589469,
-0.543999257805867));
#35305=CARTESIAN_POINT('Ctrl Pts',(-2.94588731295145E-14,5.16564553352701,
-0.485341644951264));
#35306=CARTESIAN_POINT('Ctrl Pts',(-2.86992651865603E-14,5.1760363559108,
-0.426537904798046));
#35307=CARTESIAN_POINT('Ctrl Pts',(-2.68071769236455E-14,5.20198688412704,
-0.279678680214664));
#35308=CARTESIAN_POINT('Ctrl Pts',(-5.56602536354946E-15,5.22141246689856,
-0.131909892996859));
#35309=CARTESIAN_POINT('Ctrl Pts',(-7.71605002114484E-15,5.23446159560053,
0.0163413505315488));
#35310=CARTESIAN_POINT('Ctrl Pts',(-9.89977148514226E-15,5.24771524007957,
0.166916099250649));
#35311=CARTESIAN_POINT('Ctrl Pts',(-2.15550044527619E-14,5.25439114187506,
0.317989193576075));
#35312=CARTESIAN_POINT('Ctrl Pts',(-2.54796184151473E-14,5.25459601396279,
0.469135904779127));
#35313=CARTESIAN_POINT('Ctrl Pts',(-2.94411969011659E-14,5.25480281566683,
0.621706212349075));
#35314=CARTESIAN_POINT('Ctrl Pts',(-1.52795916454729E-14,5.24841622956477,
0.77435226947332));
#35315=CARTESIAN_POINT('Ctrl Pts',(-1.55986334959834E-14,5.23549467657462,
0.926649684258014));
#35316=CARTESIAN_POINT('Ctrl Pts',(-1.58261930992363E-14,5.2262782572643,
1.03527724904109));
#35317=CARTESIAN_POINT('Ctrl Pts',(-5.48374672990966E-15,5.21373617382266,
1.14372773684654));
#35318=CARTESIAN_POINT('Ctrl Pts',(-3.71924713249427E-15,5.19787343757021,
1.25184773611315));
#35319=CARTESIAN_POINT('Ctrl Pts',(-3.19499098604058E-15,5.19316040901973,
1.28397161659072));
#35320=CARTESIAN_POINT('Ctrl Pts',(-1.90671538789874E-14,5.18815415473348,
1.31606631618875));
#35321=CARTESIAN_POINT('Ctrl Pts',(-1.9373391779709E-14,5.1828545750351,
1.34812778544358));
#35322=CARTESIAN_POINT('Ctrl Pts',(-1.95571813998463E-14,5.17967401594245,
1.36736957505062));
#35323=CARTESIAN_POINT('Ctrl Pts',(-1.37749350569938E-14,5.17638788963684,
1.38659858233887));
#35324=CARTESIAN_POINT('Ctrl Pts',(-1.38777878078145E-14,5.17299861538347,
1.40580097511783));
#35325=CARTESIAN_POINT('Ctrl Pts',(-1.47043682530614E-14,5.14576057071216,
1.56012180996567));
#35326=CARTESIAN_POINT('Ctrl Pts',(-7.96362220616864E-15,5.11182907899611,
1.71294254845863));
#35327=CARTESIAN_POINT('Ctrl Pts',(-1.03805852802452E-14,5.07133602327383,
1.86381417395566));
#35328=CARTESIAN_POINT('Ctrl Pts',(-1.22216136978406E-14,5.0404919995899,
1.97873481669447));
#35329=CARTESIAN_POINT('Ctrl Pts',(-1.14125186604969E-14,5.00583989091105,
2.09252508158171));
#35330=CARTESIAN_POINT('Ctrl Pts',(-9.88098491916389E-15,4.96741807624543,
2.20499024943516));
#35331=CARTESIAN_POINT('Ctrl Pts',(-7.88224225419095E-15,4.9172753218514,
2.35176398562226));
#35332=CARTESIAN_POINT('Ctrl Pts',(-1.31674334524512E-15,4.86071404285811,
2.49628151547096));
#35333=CARTESIAN_POINT('Ctrl Pts',(-1.4432899320127E-15,4.79803186865836,
2.63821945379872));
#35334=CARTESIAN_POINT('Ctrl Pts',(-1.57089238570486E-15,4.73482669311825,
2.78134167989155));
#35335=CARTESIAN_POINT('Ctrl Pts',(-9.37532187212029E-16,4.665397799525,
2.92184176943859));
#35336=CARTESIAN_POINT('Ctrl Pts',(-2.66453525910038E-15,4.58999880867953,
3.05937585270003));
#35337=CARTESIAN_POINT('Ctrl Pts',(-3.51498131210545E-15,4.55286930080032,
3.12710318924464));
#35338=CARTESIAN_POINT('Ctrl Pts',(-1.51993577605973E-14,4.51429129789493,
3.19411102466394));
#35339=CARTESIAN_POINT('Ctrl Pts',(-1.48214773787458E-14,4.47429084970801,
3.26035642397394));
#35340=CARTESIAN_POINT('Ctrl Pts',(-1.46923288761638E-14,4.46061986218376,
3.28299717097943));
#35341=CARTESIAN_POINT('Ctrl Pts',(-3.01425676435767E-14,4.44678269964352,
3.3055488470762));
#35342=CARTESIAN_POINT('Ctrl Pts',(-3.05866443284231E-14,4.43278033145175,
3.32800969615114));
#35343=CARTESIAN_POINT('Ctrl Pts',(-3.09193787759791E-14,4.42228874203993,
3.34483899267496));
#35344=CARTESIAN_POINT('Ctrl Pts',(-1.22788573377448E-14,4.41170953178767,
3.36160906394854));
#35345=CARTESIAN_POINT('Ctrl Pts',(-1.22957199977236E-14,4.40104403199575,
3.37831829577569));
#35346=CARTESIAN_POINT('Ctrl Pts',(-1.24315705710625E-14,4.31511961298378,
3.51293280657181));
#35347=CARTESIAN_POINT('Ctrl Pts',(-6.54470196245199E-15,4.22358573877092,
3.64362044463653));
#35348=CARTESIAN_POINT('Ctrl Pts',(-9.29811783123569E-15,4.12678394837992,
3.7700546431706));
#35349=CARTESIAN_POINT('Ctrl Pts',(-1.21936673961834E-14,4.02498516628143,
3.90301548381599));
#35350=CARTESIAN_POINT('Ctrl Pts',(-1.35210479601085E-15,3.91736062357425,
4.031273317785));
#35351=CARTESIAN_POINT('Ctrl Pts',(-3.83026943495679E-15,3.80424802343179,
4.15443361376849));
#35352=CARTESIAN_POINT('Ctrl Pts',(-6.30843407390273E-15,3.69113542328933,
4.27759390975198));
#35353=CARTESIAN_POINT('Ctrl Pts',(-8.95192615878647E-15,3.57253430986338,
4.3956575217037));
#35354=CARTESIAN_POINT('Ctrl Pts',(-1.17961196366423E-14,3.44872813349398,
4.50820230933582));
#35355=CARTESIAN_POINT('Ctrl Pts',(-1.37944585530683E-14,3.35923703106024,
4.58955331631885));
#35356=CARTESIAN_POINT('Ctrl Pts',(1.94969968696725E-15,3.26702518967802,
4.66802026523585));
#35357=CARTESIAN_POINT('Ctrl Pts',(2.41473507855972E-15,3.17225699350504,
4.74353062519992));
#35358=CARTESIAN_POINT('Ctrl Pts',(2.61939892934227E-15,3.13054914865896,
4.77676302282734));
#35359=CARTESIAN_POINT('Ctrl Pts',(-4.91819235567617E-15,3.08834600239139,
4.80942259857627));
#35360=CARTESIAN_POINT('Ctrl Pts',(-4.74620343027254E-15,3.0456608739011,
4.8415023979526));
#35361=CARTESIAN_POINT('Ctrl Pts',(-4.638233594795E-15,3.01886434447562,
4.86164119847529));
#35362=CARTESIAN_POINT('Ctrl Pts',(-1.61449114338701E-14,2.99187785892113,
4.8815515007876));
#35363=CARTESIAN_POINT('Ctrl Pts',(-1.5779044737485E-14,2.96470463632097,
4.90123148272646));
#35364=CARTESIAN_POINT('Ctrl Pts',(-1.55471922837076E-14,2.94748476252777,
4.91370283403529));
#35365=CARTESIAN_POINT('Ctrl Pts',(-1.43437538502047E-14,2.93018925838119,
4.92608207797112));
#35366=CARTESIAN_POINT('Ctrl Pts',(-1.45161660469739E-14,2.91283233270296,
4.93835944710776));
#35367=CARTESIAN_POINT('Ctrl Pts',(-1.58262398775716E-14,2.78094575775771,
5.03164901893566));
#35368=CARTESIAN_POINT('Ctrl Pts',(-8.3751524115744E-15,2.64533737784887,
5.1191898859788));
#35369=CARTESIAN_POINT('Ctrl Pts',(-8.17401701880272E-15,2.50645976707215,
5.20087831118996));
#35370=CARTESIAN_POINT('Ctrl Pts',(-7.96868972380821E-15,2.36468778073431,
5.28426922091417));
#35371=CARTESIAN_POINT('Ctrl Pts',(-3.28750966826451E-14,2.21950841305984,
5.36156169934779));
#35372=CARTESIAN_POINT('Ctrl Pts',(-2.99482660892636E-14,2.07135972951188,
5.43261292336788));
#35373=CARTESIAN_POINT('Ctrl Pts',(-2.7010140735854E-14,1.92263933408113,
5.50393833699321));
#35374=CARTESIAN_POINT('Ctrl Pts',(-9.29007357318986E-15,1.77092604516859,
5.56897467112021));
#35375=CARTESIAN_POINT('Ctrl Pts',(-1.16365250768524E-14,1.61662808464398,
5.62753811018193));
#35376=CARTESIAN_POINT('Ctrl Pts',(-1.39647681338263E-14,1.46352747517648,
5.68564709738033));
#35377=CARTESIAN_POINT('Ctrl Pts',(-2.80861324317553E-15,1.3078814874935,
5.73738362050802));
#35378=CARTESIAN_POINT('Ctrl Pts',(-2.63331023653279E-15,1.15006424595524,
5.78252360898802));
#35379=CARTESIAN_POINT('Ctrl Pts',(-2.54208608144777E-15,1.06793933097009,
5.80601355013904));
#35380=CARTESIAN_POINT('Ctrl Pts',(-8.84559606733975E-15,0.985226104351652,
5.82771641374748));
#35381=CARTESIAN_POINT('Ctrl Pts',(-8.93729534823251E-15,0.901975524283881,
5.84759529345977));
#35382=CARTESIAN_POINT('Ctrl Pts',(-1.68094704822153E-14,0.901975524284047,
5.84759529345974));
#35383=CARTESIAN_POINT('Ctrl Pts',(-0.0464195480276284,1.8765612251201,
5.69726812402404));
#35384=CARTESIAN_POINT('Ctrl Pts',(-0.0928390960552399,2.81234038373308,
5.29865417244734));
#35385=CARTESIAN_POINT('Ctrl Pts',(-0.13925864408285,3.59529440116169,4.69979479235976));
#35386=CARTESIAN_POINT('Ctrl Pts',(-0.18567819211046,4.3782484185903,4.10093541227217));
#35387=CARTESIAN_POINT('Ctrl Pts',(-0.232097740138068,5.00837729483454,
3.30183060367369));
#35388=CARTESIAN_POINT('Ctrl Pts',(-0.27851728816568,5.40837521702949,2.40072698448045));
#35389=CARTESIAN_POINT('Ctrl Pts',(-0.324936836193292,5.80837313922444,
1.49962336528722));
#35390=CARTESIAN_POINT('Ctrl Pts',(-0.371356384220907,5.9782401073701,0.496520935499224));
#35391=CARTESIAN_POINT('Ctrl Pts',(-0.417775932248519,5.8972621654928,-0.485971441301911));
#35392=CARTESIAN_POINT('Ctrl Pts',(-0.464195480276132,5.8162842236155,-1.46846381810305));
#35393=CARTESIAN_POINT('Ctrl Pts',(-0.510615028303743,5.48446137171524,
-2.43034614191732));
#35394=CARTESIAN_POINT('Ctrl Pts',(-0.557034576331353,4.94237295361224,
-3.25377865988359));
#35395=CARTESIAN_POINT('Ctrl Pts',(-0.603454124358963,4.40028453550923,
-4.07721117784986));
#35396=CARTESIAN_POINT('Ctrl Pts',(-0.649873672386574,3.64793055120348,
-4.76219388996812));
#35397=CARTESIAN_POINT('Ctrl Pts',(-0.696293220414184,2.77743042301163,
-5.22492199455547));
#35398=CARTESIAN_POINT('Ctrl Pts',(-0.742712768441798,1.90693029481972,
-5.68765009914285));
#35399=CARTESIAN_POINT('Ctrl Pts',(-0.789132316469411,0.918284022741709,
-5.92812359619928));
#35400=CARTESIAN_POINT('Ctrl Pts',(-0.835551864497027,-0.0674947272534869,
-5.91688120200961));
#35401=CARTESIAN_POINT('Ctrl Pts',(-0.881971412524643,-1.05327347724868,
-5.90563880781993));
#35402=CARTESIAN_POINT('Ctrl Pts',(-0.928390960552261,-2.03618470516106,
-5.64268052238414));
#35403=CARTESIAN_POINT('Ctrl Pts',(-0.974810508579875,-2.89590077580765,
-5.16020841554193));
#35404=CARTESIAN_POINT('Ctrl Pts',(-1.02123005660749,-3.75561684645419,
-4.67773630869973));
#35405=CARTESIAN_POINT('Ctrl Pts',(-1.06764960463509,-4.49213775983495,
-3.97575038045114));
#35406=CARTESIAN_POINT('Ctrl Pts',(-1.1140691526627,-5.01530574290011,-3.14017733058129));
#35407=CARTESIAN_POINT('Ctrl Pts',(-1.16048870069031,-5.53847372596528,
-2.30460428071143));
#35408=CARTESIAN_POINT('Ctrl Pts',(-1.20690824871793,-5.84828877871485,
-1.33544410922033));
#35409=CARTESIAN_POINT('Ctrl Pts',(-1.25332779674554,-5.90682374005196,
-0.351338921506704));
#35410=CARTESIAN_POINT('Ctrl Pts',(-1.25884346709541,-5.91377898982057,
-0.234405430430919));
#35411=CARTESIAN_POINT('Ctrl Pts',(-1.26435913744529,-5.91718649071705,
-0.117260935116202));
#35412=CARTESIAN_POINT('Ctrl Pts',(-1.26987480779516,-5.91708582682028,
-0.000110601437552926));
#35413=CARTESIAN_POINT('Origin',(0.5,8.93855739141052,-1.42379484493389));
#35414=CARTESIAN_POINT('',(11.,8.88202841720304,-1.45243629670899));
#35415=CARTESIAN_POINT('',(0.500000000000002,8.88202841720304,-1.45243629670899));
#35416=CARTESIAN_POINT('',(5.75,8.88202841720304,-1.45243629670899));
#35417=CARTESIAN_POINT('',(11.,8.71554861415804,-1.53678637235233));
#35418=CARTESIAN_POINT('',(11.,8.93855739141052,-1.42379484493389));
#35419=CARTESIAN_POINT('',(0.5,8.71554861415804,-1.53678637235233));
#35420=CARTESIAN_POINT('',(0.5,8.71554861415804,-1.53678637235233));
#35421=CARTESIAN_POINT('',(0.5,8.93855739141052,-1.42379484493389));
#35422=CARTESIAN_POINT('Origin',(0.5,8.81402938945926,-1.55415119011903));
#35423=CARTESIAN_POINT('',(0.5,8.84313903162825,-1.67298896209539));
#35424=CARTESIAN_POINT('Origin',(0.5,0.,0.));
#35425=CARTESIAN_POINT('',(0.5,8.71554861415804,-1.53678637235233));
#35426=CARTESIAN_POINT('Origin',(0.5,8.71554861415804,-1.53678637235233));
#35427=CARTESIAN_POINT('',(11.,8.84313903162825,-1.67298896209539));
#35428=CARTESIAN_POINT('',(5.75,8.84313903162825,-1.67298896209539));
#35429=CARTESIAN_POINT('',(11.,8.71554861415804,-1.53678637235233));
#35430=CARTESIAN_POINT('Origin',(11.,8.81402938945926,-1.55415119011903));
#35431=CARTESIAN_POINT('Origin',(11.,0.,0.));
#35432=CARTESIAN_POINT('Origin',(0.5,8.55552123961132,-2.95432840397942));
#35433=CARTESIAN_POINT('',(11.,8.49487753163548,-2.97271857438856));
#35434=CARTESIAN_POINT('',(0.5,8.49487753163548,-2.97271857438856));
#35435=CARTESIAN_POINT('',(5.75,8.49487753163548,-2.97271857438856));
#35436=CARTESIAN_POINT('',(11.,8.31627969395529,-3.02687826843217));
#35437=CARTESIAN_POINT('',(11.,8.55552123961132,-2.95432840397942));
#35438=CARTESIAN_POINT('',(0.5,8.31627969395529,-3.02687826843217));
#35439=CARTESIAN_POINT('',(0.5,8.31627969395529,-3.02687826843217));
#35440=CARTESIAN_POINT('',(0.5,8.55552123961132,-2.95432840397942));
#35441=CARTESIAN_POINT('Origin',(0.5,8.41024895603388,-3.06108028276474));
#35442=CARTESIAN_POINT('',(0.5,8.41828039478761,-3.18316747827294));
#35443=CARTESIAN_POINT('Origin',(0.5,0.,0.));
#35444=CARTESIAN_POINT('',(0.5,8.31627969395529,-3.02687826843217));
#35445=CARTESIAN_POINT('Origin',(0.5,8.31627969395529,-3.02687826843217));
#35446=CARTESIAN_POINT('',(11.,8.41828039478761,-3.18316747827294));
#35447=CARTESIAN_POINT('',(5.75,8.41828039478761,-3.18316747827294));
#35448=CARTESIAN_POINT('',(11.,8.31627969395529,-3.02687826843217));
#35449=CARTESIAN_POINT('Origin',(11.,8.41024895603388,-3.06108028276474));
#35450=CARTESIAN_POINT('Origin',(11.,0.,0.));
#35451=CARTESIAN_POINT('Origin',(0.5,7.91252990424917,-4.39509618943234));
#35452=CARTESIAN_POINT('',(11.,7.84961409088462,-4.4026763024535));
#35453=CARTESIAN_POINT('',(0.5,7.84961409088462,-4.4026763024535));
#35454=CARTESIAN_POINT('',(5.75,7.84961409088462,-4.4026763024535));
#35455=CARTESIAN_POINT('',(11.,7.66432482349228,-4.425));
#35456=CARTESIAN_POINT('',(11.,7.91252990424917,-4.39509618943234));
#35457=CARTESIAN_POINT('',(0.5,7.66432482349228,-4.425));
#35458=CARTESIAN_POINT('',(0.5,7.66432482349228,-4.425));
#35459=CARTESIAN_POINT('',(0.5,7.91252990424917,-4.39509618943234));
#35460=CARTESIAN_POINT('Origin',(0.5,7.75092736387072,-4.475));
#35461=CARTESIAN_POINT('',(0.5,7.73763656800678,-4.59662706138363));
#35462=CARTESIAN_POINT('Origin',(0.5,0.,0.));
#35463=CARTESIAN_POINT('',(0.5,7.66432482349228,-4.425));
#35464=CARTESIAN_POINT('Origin',(0.5,7.66432482349228,-4.425));
#35465=CARTESIAN_POINT('',(11.,7.73763656800678,-4.59662706138363));
#35466=CARTESIAN_POINT('',(5.75,7.73763656800678,-4.59662706138363));
#35467=CARTESIAN_POINT('',(11.,7.66432482349228,-4.425));
#35468=CARTESIAN_POINT('Origin',(11.,7.75092736387072,-4.475));
#35469=CARTESIAN_POINT('Origin',(11.,0.,0.));
#35470=CARTESIAN_POINT('Origin',(0.5,7.02912035167973,-5.70232120119534));
#35471=CARTESIAN_POINT('',(11.,6.96584409807862,-5.6988609389301));
#35472=CARTESIAN_POINT('',(0.5,6.96584409807862,-5.6988609389301));
#35473=CARTESIAN_POINT('',(5.75,6.96584409807862,-5.6988609389301));
#35474=CARTESIAN_POINT('',(11.,6.77949332160295,-5.68867034572588));
#35475=CARTESIAN_POINT('',(11.,7.02912035167973,-5.70232120119534));
#35476=CARTESIAN_POINT('',(0.5,6.77949332160295,-5.68867034572588));
#35477=CARTESIAN_POINT('',(0.5,6.77949332160295,-5.68867034572588));
#35478=CARTESIAN_POINT('',(0.5,7.02912035167973,-5.70232120119534));
#35479=CARTESIAN_POINT('Origin',(0.5,6.85609776591485,-5.75294910669453));
#35480=CARTESIAN_POINT('',(0.5,6.82188856954008,-5.8704204572397));
#35481=CARTESIAN_POINT('Origin',(0.5,0.,0.));
#35482=CARTESIAN_POINT('',(0.5,6.77949332160295,-5.68867034572588));
#35483=CARTESIAN_POINT('Origin',(0.5,6.77949332160295,-5.68867034572588));
#35484=CARTESIAN_POINT('',(11.,6.82188856954008,-5.8704204572397));
#35485=CARTESIAN_POINT('',(5.75,6.82188856954008,-5.8704204572397));
#35486=CARTESIAN_POINT('',(11.,6.77949332160295,-5.68867034572588));
#35487=CARTESIAN_POINT('Origin',(11.,6.85609776591485,-5.75294910669453));
#35488=CARTESIAN_POINT('Origin',(11.,0.,0.));
#35489=CARTESIAN_POINT('Origin',(0.5,5.93213453413103,-6.83628406877377));
#35490=CARTESIAN_POINT('',(11.,5.87042045723969,-6.82188856954009));
#35491=CARTESIAN_POINT('',(0.5,5.87042045723969,-6.82188856954009));
#35492=CARTESIAN_POINT('',(5.75,5.87042045723969,-6.82188856954009));
#35493=CARTESIAN_POINT('',(11.,5.68867034572587,-6.77949332160296));
#35494=CARTESIAN_POINT('',(11.,5.93213453413103,-6.83628406877377));
#35495=CARTESIAN_POINT('',(0.5,5.68867034572587,-6.77949332160296));
#35496=CARTESIAN_POINT('',(0.5,5.68867034572587,-6.77949332160296));
#35497=CARTESIAN_POINT('',(0.5,5.93213453413103,-6.83628406877377));
#35498=CARTESIAN_POINT('Origin',(0.5,5.75294910669453,-6.85609776591486));
#35499=CARTESIAN_POINT('',(0.5,5.6988609389301,-6.96584409807862));
#35500=CARTESIAN_POINT('Origin',(0.5,0.,0.));
#35501=CARTESIAN_POINT('',(0.5,5.68867034572587,-6.77949332160296));
#35502=CARTESIAN_POINT('Origin',(0.5,5.68867034572587,-6.77949332160296));
#35503=CARTESIAN_POINT('',(11.,5.6988609389301,-6.96584409807862));
#35504=CARTESIAN_POINT('',(5.75,5.6988609389301,-6.96584409807862));
#35505=CARTESIAN_POINT('',(11.,5.68867034572587,-6.77949332160296));
#35506=CARTESIAN_POINT('Origin',(11.,5.75294910669453,-6.85609776591486));
#35507=CARTESIAN_POINT('Origin',(11.,0.,0.));
#35508=CARTESIAN_POINT('Origin',(0.5,4.65490381056767,-7.76252990424917));
#35509=CARTESIAN_POINT('',(11.,4.59662706138363,-7.73763656800678));
#35510=CARTESIAN_POINT('',(0.5,4.59662706138363,-7.73763656800678));
#35511=CARTESIAN_POINT('',(5.75,4.59662706138363,-7.73763656800678));
#35512=CARTESIAN_POINT('',(11.,4.425,-7.66432482349228));
#35513=CARTESIAN_POINT('',(11.,4.65490381056767,-7.76252990424917));
#35514=CARTESIAN_POINT('',(0.5,4.425,-7.66432482349228));
#35515=CARTESIAN_POINT('',(0.5,4.425,-7.66432482349228));
#35516=CARTESIAN_POINT('',(0.5,4.65490381056767,-7.76252990424917));
#35517=CARTESIAN_POINT('Origin',(0.5,4.475,-7.75092736387073));
#35518=CARTESIAN_POINT('',(0.5,4.4026763024535,-7.84961409088462));
#35519=CARTESIAN_POINT('Origin',(0.5,0.,0.));
#35520=CARTESIAN_POINT('',(0.5,4.425,-7.66432482349228));
#35521=CARTESIAN_POINT('Origin',(0.5,4.425,-7.66432482349228));
#35522=CARTESIAN_POINT('',(11.,4.4026763024535,-7.84961409088462));
#35523=CARTESIAN_POINT('',(5.75,4.4026763024535,-7.84961409088462));
#35524=CARTESIAN_POINT('',(11.,4.425,-7.66432482349228));
#35525=CARTESIAN_POINT('Origin',(11.,4.475,-7.75092736387073));
#35526=CARTESIAN_POINT('Origin',(11.,0.,0.));
#35527=CARTESIAN_POINT('Origin',(0.5,3.23623619021518,-8.45291519661362));
#35528=CARTESIAN_POINT('',(11.,3.18316747827293,-8.41828039478762));
#35529=CARTESIAN_POINT('',(0.5,3.18316747827293,-8.41828039478762));
#35530=CARTESIAN_POINT('',(5.75,3.18316747827293,-8.41828039478762));
#35531=CARTESIAN_POINT('',(11.,3.02687826843216,-8.31627969395529));
#35532=CARTESIAN_POINT('',(11.,3.23623619021518,-8.45291519661362));
#35533=CARTESIAN_POINT('',(0.5,3.02687826843216,-8.31627969395529));
#35534=CARTESIAN_POINT('',(0.5,3.02687826843216,-8.31627969395529));
#35535=CARTESIAN_POINT('',(0.5,3.23623619021518,-8.45291519661362));
#35536=CARTESIAN_POINT('Origin',(0.5,3.06108028276473,-8.41024895603388));
#35537=CARTESIAN_POINT('',(0.500000000000002,2.97271857438855,-8.49487753163548));
#35538=CARTESIAN_POINT('Origin',(0.5,0.,0.));
#35539=CARTESIAN_POINT('',(0.5,3.02687826843216,-8.31627969395529));
#35540=CARTESIAN_POINT('Origin',(0.5,3.02687826843216,-8.31627969395529));
#35541=CARTESIAN_POINT('',(11.,2.97271857438855,-8.49487753163548));
#35542=CARTESIAN_POINT('',(5.75,2.97271857438855,-8.49487753163548));
#35543=CARTESIAN_POINT('',(11.,3.02687826843216,-8.31627969395529));
#35544=CARTESIAN_POINT('Origin',(11.,3.06108028276473,-8.41024895603388));
#35545=CARTESIAN_POINT('Origin',(11.,0.,0.));
#35546=CARTESIAN_POINT('Origin',(0.5,1.71923717083755,-8.88646293811044));
#35547=CARTESIAN_POINT('',(11.,1.67298896209539,-8.84313903162825));
#35548=CARTESIAN_POINT('',(0.5,1.67298896209539,-8.84313903162825));
#35549=CARTESIAN_POINT('',(5.75,1.67298896209539,-8.84313903162825));
#35550=CARTESIAN_POINT('',(11.,1.53678637235233,-8.71554861415804));
#35551=CARTESIAN_POINT('',(11.,1.71923717083755,-8.88646293811044));
#35552=CARTESIAN_POINT('',(0.5,1.53678637235233,-8.71554861415804));
#35553=CARTESIAN_POINT('',(0.5,1.53678637235233,-8.71554861415804));
#35554=CARTESIAN_POINT('',(0.5,1.71923717083755,-8.88646293811044));
#35555=CARTESIAN_POINT('Origin',(0.5,1.55415119011902,-8.81402938945926));
#35556=CARTESIAN_POINT('',(0.5,1.45243629670899,-8.88202841720304));
#35557=CARTESIAN_POINT('Origin',(0.5,0.,0.));
#35558=CARTESIAN_POINT('',(0.5,1.53678637235233,-8.71554861415804));
#35559=CARTESIAN_POINT('Origin',(0.5,1.53678637235233,-8.71554861415804));
#35560=CARTESIAN_POINT('',(11.,1.45243629670899,-8.88202841720304));
#35561=CARTESIAN_POINT('',(5.75,1.45243629670899,-8.88202841720304));
#35562=CARTESIAN_POINT('',(11.,1.53678637235233,-8.71554861415804));
#35563=CARTESIAN_POINT('Origin',(11.,1.55415119011902,-8.81402938945926));
#35564=CARTESIAN_POINT('Origin',(11.,0.,0.));
#35565=CARTESIAN_POINT('Origin',(0.5,0.149999999999998,-9.05));
#35566=CARTESIAN_POINT('',(11.,0.111977522877841,-8.99930336383712));
#35567=CARTESIAN_POINT('',(0.5,0.111977522877841,-8.99930336383712));
#35568=CARTESIAN_POINT('',(5.75,0.11197752287784,-8.99930336383712));
#35569=CARTESIAN_POINT('',(11.,-1.62571862586811E-15,-8.85));
#35570=CARTESIAN_POINT('',(11.,0.149999999999998,-9.05));
#35571=CARTESIAN_POINT('',(0.5,-1.62571862586811E-15,-8.85));
#35572=CARTESIAN_POINT('',(0.5,-1.62571862586811E-15,-8.85));
#35573=CARTESIAN_POINT('',(0.5,0.149999999999998,-9.05));
#35574=CARTESIAN_POINT('Origin',(0.5,-1.64408832785532E-15,-8.95));
#35575=CARTESIAN_POINT('',(0.5,-0.111977522877842,-8.99930336383712));
#35576=CARTESIAN_POINT('Origin',(0.5,0.,0.));
#35577=CARTESIAN_POINT('',(0.5,-1.62571862586811E-15,-8.85));
#35578=CARTESIAN_POINT('Origin',(0.5,-1.62571862586811E-15,-8.85));
#35579=CARTESIAN_POINT('',(11.,-0.111977522877842,-8.99930336383712));
#35580=CARTESIAN_POINT('',(5.75,-0.111977522877842,-8.99930336383712));
#35581=CARTESIAN_POINT('',(11.,-1.62571862586811E-15,-8.85));
#35582=CARTESIAN_POINT('Origin',(11.,-1.64408832785532E-15,-8.95));
#35583=CARTESIAN_POINT('Origin',(11.,0.,0.));
#35584=CARTESIAN_POINT('Origin',(0.5,-1.42379484493389,-8.93855739141052));
#35585=CARTESIAN_POINT('',(11.,-1.45243629670899,-8.88202841720304));
#35586=CARTESIAN_POINT('',(0.5,-1.45243629670899,-8.88202841720304));
#35587=CARTESIAN_POINT('',(5.75,-1.45243629670899,-8.88202841720304));
#35588=CARTESIAN_POINT('',(11.,-1.53678637235233,-8.71554861415804));
#35589=CARTESIAN_POINT('',(11.,-1.42379484493389,-8.93855739141052));
#35590=CARTESIAN_POINT('',(0.5,-1.53678637235233,-8.71554861415804));
#35591=CARTESIAN_POINT('',(0.5,-1.53678637235233,-8.71554861415804));
#35592=CARTESIAN_POINT('',(0.5,-1.42379484493389,-8.93855739141052));
#35593=CARTESIAN_POINT('Origin',(0.5,-1.55415119011903,-8.81402938945926));
#35594=CARTESIAN_POINT('',(0.5,-1.67298896209539,-8.84313903162825));
#35595=CARTESIAN_POINT('Origin',(0.5,0.,0.));
#35596=CARTESIAN_POINT('',(0.5,-1.53678637235233,-8.71554861415804));
#35597=CARTESIAN_POINT('Origin',(0.5,-1.53678637235233,-8.71554861415804));
#35598=CARTESIAN_POINT('',(11.,-1.67298896209539,-8.84313903162825));
#35599=CARTESIAN_POINT('',(5.75,-1.67298896209539,-8.84313903162825));
#35600=CARTESIAN_POINT('',(11.,-1.53678637235233,-8.71554861415804));
#35601=CARTESIAN_POINT('Origin',(11.,-1.55415119011903,-8.81402938945926));
#35602=CARTESIAN_POINT('Origin',(11.,0.,0.));
#35603=CARTESIAN_POINT('Origin',(0.5,-2.95432840397942,-8.55552123961132));
#35604=CARTESIAN_POINT('',(11.,-2.97271857438856,-8.49487753163548));
#35605=CARTESIAN_POINT('',(0.5,-2.97271857438856,-8.49487753163548));
#35606=CARTESIAN_POINT('',(5.75,-2.97271857438856,-8.49487753163548));
#35607=CARTESIAN_POINT('',(11.,-3.02687826843217,-8.31627969395529));
#35608=CARTESIAN_POINT('',(11.,-2.95432840397942,-8.55552123961132));
#35609=CARTESIAN_POINT('',(0.5,-3.02687826843217,-8.31627969395529));
#35610=CARTESIAN_POINT('',(0.5,-3.02687826843217,-8.31627969395529));
#35611=CARTESIAN_POINT('',(0.5,-2.95432840397942,-8.55552123961132));
#35612=CARTESIAN_POINT('Origin',(0.5,-3.06108028276474,-8.41024895603388));
#35613=CARTESIAN_POINT('',(0.5,-3.18316747827294,-8.41828039478761));
#35614=CARTESIAN_POINT('Origin',(0.5,0.,0.));
#35615=CARTESIAN_POINT('',(0.5,-3.02687826843217,-8.31627969395529));
#35616=CARTESIAN_POINT('Origin',(0.5,-3.02687826843217,-8.31627969395529));
#35617=CARTESIAN_POINT('',(11.,-3.18316747827294,-8.41828039478761));
#35618=CARTESIAN_POINT('',(5.75,-3.18316747827294,-8.41828039478761));
#35619=CARTESIAN_POINT('',(11.,-3.02687826843217,-8.31627969395529));
#35620=CARTESIAN_POINT('Origin',(11.,-3.06108028276474,-8.41024895603388));
#35621=CARTESIAN_POINT('Origin',(11.,0.,0.));
#35622=CARTESIAN_POINT('Origin',(0.5,-4.39509618943234,-7.91252990424917));
#35623=CARTESIAN_POINT('',(11.,-4.4026763024535,-7.84961409088462));
#35624=CARTESIAN_POINT('',(0.5,-4.4026763024535,-7.84961409088462));
#35625=CARTESIAN_POINT('',(5.75,-4.4026763024535,-7.84961409088462));
#35626=CARTESIAN_POINT('',(11.,-4.425,-7.66432482349228));
#35627=CARTESIAN_POINT('',(11.,-4.39509618943234,-7.91252990424917));
#35628=CARTESIAN_POINT('',(0.5,-4.425,-7.66432482349228));
#35629=CARTESIAN_POINT('',(0.5,-4.425,-7.66432482349228));
#35630=CARTESIAN_POINT('',(0.5,-4.39509618943234,-7.91252990424917));
#35631=CARTESIAN_POINT('Origin',(0.5,-4.475,-7.75092736387072));
#35632=CARTESIAN_POINT('',(0.5,-4.59662706138363,-7.73763656800678));
#35633=CARTESIAN_POINT('Origin',(0.5,0.,0.));
#35634=CARTESIAN_POINT('',(0.5,-4.425,-7.66432482349228));
#35635=CARTESIAN_POINT('Origin',(0.5,-4.425,-7.66432482349228));
#35636=CARTESIAN_POINT('',(11.,-4.59662706138363,-7.73763656800678));
#35637=CARTESIAN_POINT('',(5.75,-4.59662706138363,-7.73763656800678));
#35638=CARTESIAN_POINT('',(11.,-4.425,-7.66432482349228));
#35639=CARTESIAN_POINT('Origin',(11.,-4.475,-7.75092736387072));
#35640=CARTESIAN_POINT('Origin',(11.,0.,0.));
#35641=CARTESIAN_POINT('Origin',(0.5,-5.70232120119534,-7.02912035167973));
#35642=CARTESIAN_POINT('',(11.,-5.6988609389301,-6.96584409807862));
#35643=CARTESIAN_POINT('',(0.5,-5.6988609389301,-6.96584409807862));
#35644=CARTESIAN_POINT('',(5.75,-5.6988609389301,-6.96584409807862));
#35645=CARTESIAN_POINT('',(11.,-5.68867034572587,-6.77949332160295));
#35646=CARTESIAN_POINT('',(11.,-5.70232120119534,-7.02912035167973));
#35647=CARTESIAN_POINT('',(0.5,-5.68867034572587,-6.77949332160295));
#35648=CARTESIAN_POINT('',(0.5,-5.68867034572587,-6.77949332160295));
#35649=CARTESIAN_POINT('',(0.5,-5.70232120119534,-7.02912035167973));
#35650=CARTESIAN_POINT('Origin',(0.5,-5.75294910669453,-6.85609776591485));
#35651=CARTESIAN_POINT('',(0.5,-5.8704204572397,-6.82188856954009));
#35652=CARTESIAN_POINT('Origin',(0.5,0.,0.));
#35653=CARTESIAN_POINT('',(0.5,-5.68867034572587,-6.77949332160295));
#35654=CARTESIAN_POINT('Origin',(0.5,-5.68867034572587,-6.77949332160295));
#35655=CARTESIAN_POINT('',(11.,-5.8704204572397,-6.82188856954009));
#35656=CARTESIAN_POINT('',(5.75,-5.8704204572397,-6.82188856954009));
#35657=CARTESIAN_POINT('',(11.,-5.68867034572587,-6.77949332160295));
#35658=CARTESIAN_POINT('Origin',(11.,-5.75294910669453,-6.85609776591485));
#35659=CARTESIAN_POINT('Origin',(11.,0.,0.));
#35660=CARTESIAN_POINT('Origin',(0.5,-6.83628406877377,-5.93213453413103));
#35661=CARTESIAN_POINT('',(11.,-6.82188856954009,-5.8704204572397));
#35662=CARTESIAN_POINT('',(0.500000000000002,-6.82188856954009,-5.8704204572397));
#35663=CARTESIAN_POINT('',(5.75,-6.82188856954009,-5.8704204572397));
#35664=CARTESIAN_POINT('',(11.,-6.77949332160296,-5.68867034572587));
#35665=CARTESIAN_POINT('',(11.,-6.83628406877377,-5.93213453413103));
#35666=CARTESIAN_POINT('',(0.5,-6.77949332160296,-5.68867034572587));
#35667=CARTESIAN_POINT('',(0.5,-6.77949332160296,-5.68867034572587));
#35668=CARTESIAN_POINT('',(0.5,-6.83628406877377,-5.93213453413103));
#35669=CARTESIAN_POINT('Origin',(0.5,-6.85609776591486,-5.75294910669453));
#35670=CARTESIAN_POINT('',(0.5,-6.96584409807862,-5.6988609389301));
#35671=CARTESIAN_POINT('Origin',(0.5,0.,0.));
#35672=CARTESIAN_POINT('',(0.5,-6.77949332160296,-5.68867034572587));
#35673=CARTESIAN_POINT('Origin',(0.5,-6.77949332160296,-5.68867034572587));
#35674=CARTESIAN_POINT('',(11.,-6.96584409807862,-5.6988609389301));
#35675=CARTESIAN_POINT('',(5.75,-6.96584409807862,-5.6988609389301));
#35676=CARTESIAN_POINT('',(11.,-6.77949332160296,-5.68867034572587));
#35677=CARTESIAN_POINT('Origin',(11.,-6.85609776591486,-5.75294910669453));
#35678=CARTESIAN_POINT('Origin',(11.,0.,0.));
#35679=CARTESIAN_POINT('Origin',(0.5,-7.76252990424917,-4.65490381056766));
#35680=CARTESIAN_POINT('',(11.,-7.73763656800678,-4.59662706138362));
#35681=CARTESIAN_POINT('',(0.5,-7.73763656800678,-4.59662706138362));
#35682=CARTESIAN_POINT('',(5.75,-7.73763656800678,-4.59662706138362));
#35683=CARTESIAN_POINT('',(11.,-7.66432482349228,-4.425));
#35684=CARTESIAN_POINT('',(11.,-7.76252990424917,-4.65490381056766));
#35685=CARTESIAN_POINT('',(0.5,-7.66432482349228,-4.425));
#35686=CARTESIAN_POINT('',(0.5,-7.66432482349228,-4.425));
#35687=CARTESIAN_POINT('',(0.5,-7.76252990424917,-4.65490381056766));
#35688=CARTESIAN_POINT('Origin',(0.5,-7.75092736387073,-4.475));
#35689=CARTESIAN_POINT('',(0.5,-7.84961409088462,-4.40267630245349));
#35690=CARTESIAN_POINT('Origin',(0.5,0.,0.));
#35691=CARTESIAN_POINT('',(0.5,-7.66432482349228,-4.425));
#35692=CARTESIAN_POINT('Origin',(0.5,-7.66432482349228,-4.425));
#35693=CARTESIAN_POINT('',(11.,-7.84961409088462,-4.40267630245349));
#35694=CARTESIAN_POINT('',(5.75,-7.84961409088462,-4.40267630245349));
#35695=CARTESIAN_POINT('',(11.,-7.66432482349228,-4.425));
#35696=CARTESIAN_POINT('Origin',(11.,-7.75092736387073,-4.475));
#35697=CARTESIAN_POINT('Origin',(11.,0.,0.));
#35698=CARTESIAN_POINT('Origin',(0.5,-8.45291519661362,-3.23623619021519));
#35699=CARTESIAN_POINT('',(11.,-8.41828039478761,-3.18316747827294));
#35700=CARTESIAN_POINT('',(0.5,-8.41828039478761,-3.18316747827294));
#35701=CARTESIAN_POINT('',(5.75,-8.41828039478761,-3.18316747827294));
#35702=CARTESIAN_POINT('',(11.,-8.31627969395529,-3.02687826843217));
#35703=CARTESIAN_POINT('',(11.,-8.45291519661362,-3.23623619021519));
#35704=CARTESIAN_POINT('',(0.5,-8.31627969395529,-3.02687826843217));
#35705=CARTESIAN_POINT('',(0.5,-8.31627969395529,-3.02687826843217));
#35706=CARTESIAN_POINT('',(0.5,-8.45291519661362,-3.23623619021519));
#35707=CARTESIAN_POINT('Origin',(0.5,-8.41024895603388,-3.06108028276473));
#35708=CARTESIAN_POINT('',(0.5,-8.49487753163548,-2.97271857438855));
#35709=CARTESIAN_POINT('Origin',(0.5,0.,0.));
#35710=CARTESIAN_POINT('',(0.5,-8.31627969395529,-3.02687826843217));
#35711=CARTESIAN_POINT('Origin',(0.5,-8.31627969395529,-3.02687826843217));
#35712=CARTESIAN_POINT('',(11.,-8.49487753163548,-2.97271857438855));
#35713=CARTESIAN_POINT('',(5.75,-8.49487753163548,-2.97271857438855));
#35714=CARTESIAN_POINT('',(11.,-8.31627969395529,-3.02687826843217));
#35715=CARTESIAN_POINT('Origin',(11.,-8.41024895603388,-3.06108028276473));
#35716=CARTESIAN_POINT('Origin',(11.,0.,0.));
#35717=CARTESIAN_POINT('Origin',(0.5,-8.88646293811044,-1.71923717083755));
#35718=CARTESIAN_POINT('',(11.,-8.84313903162825,-1.67298896209539));
#35719=CARTESIAN_POINT('',(0.5,-8.84313903162825,-1.67298896209539));
#35720=CARTESIAN_POINT('',(5.75,-8.84313903162825,-1.67298896209539));
#35721=CARTESIAN_POINT('',(11.,-8.71554861415804,-1.53678637235233));
#35722=CARTESIAN_POINT('',(11.,-8.88646293811044,-1.71923717083755));
#35723=CARTESIAN_POINT('',(0.5,-8.71554861415804,-1.53678637235233));
#35724=CARTESIAN_POINT('',(0.5,-8.71554861415804,-1.53678637235233));
#35725=CARTESIAN_POINT('',(0.5,-8.88646293811044,-1.71923717083755));
#35726=CARTESIAN_POINT('Origin',(0.5,-8.81402938945926,-1.55415119011902));
#35727=CARTESIAN_POINT('',(0.5,-8.88202841720304,-1.45243629670899));
#35728=CARTESIAN_POINT('Origin',(0.5,0.,0.));
#35729=CARTESIAN_POINT('',(0.5,-8.71554861415804,-1.53678637235233));
#35730=CARTESIAN_POINT('Origin',(0.5,-8.71554861415804,-1.53678637235233));
#35731=CARTESIAN_POINT('',(11.,-8.88202841720304,-1.45243629670899));
#35732=CARTESIAN_POINT('',(5.75,-8.88202841720304,-1.45243629670899));
#35733=CARTESIAN_POINT('',(11.,-8.71554861415804,-1.53678637235233));
#35734=CARTESIAN_POINT('Origin',(11.,-8.81402938945926,-1.55415119011902));
#35735=CARTESIAN_POINT('Origin',(11.,0.,0.));
#35736=CARTESIAN_POINT('Origin',(0.5,-9.05,-0.149999999999999));
#35737=CARTESIAN_POINT('',(11.,-8.99930336383712,-0.111977522877841));
#35738=CARTESIAN_POINT('',(0.5,-8.99930336383712,-0.111977522877841));
#35739=CARTESIAN_POINT('',(5.75,-8.99930336383712,-0.11197752287784));
#35740=CARTESIAN_POINT('',(11.,-8.85,1.08381241724541E-15));
#35741=CARTESIAN_POINT('',(11.,-9.05,-0.149999999999999));
#35742=CARTESIAN_POINT('',(0.5,-8.85,1.08381241724541E-15));
#35743=CARTESIAN_POINT('',(0.5,-8.85,1.08381241724541E-15));
#35744=CARTESIAN_POINT('',(0.5,-9.05,-0.149999999999999));
#35745=CARTESIAN_POINT('Origin',(0.5,-8.95,1.09605888523688E-15));
#35746=CARTESIAN_POINT('',(0.5,-9.,-1.10218211923262E-15));
#35747=CARTESIAN_POINT('Origin',(0.5,0.,0.));
#35748=CARTESIAN_POINT('',(0.5,-8.99930336383712,0.111977522877842));
#35749=CARTESIAN_POINT('',(0.5,-8.85,1.08381241724541E-15));
#35750=CARTESIAN_POINT('Origin',(0.5,0.,0.));
#35751=CARTESIAN_POINT('Origin',(0.5,-8.85,1.08381241724541E-15));
#35752=CARTESIAN_POINT('',(11.,-8.99930336383712,0.111977522877842));
#35753=CARTESIAN_POINT('',(5.75,-8.99930336383712,0.111977522877842));
#35754=CARTESIAN_POINT('',(11.,-8.85,1.08381241724541E-15));
#35755=CARTESIAN_POINT('Origin',(11.,-8.95,1.09605888523688E-15));
#35756=CARTESIAN_POINT('',(11.,-9.,-1.10218211923262E-15));
#35757=CARTESIAN_POINT('Origin',(11.,0.,0.));
#35758=CARTESIAN_POINT('Origin',(11.,0.,0.));
#35759=CARTESIAN_POINT('Origin',(0.5,-8.93855739141052,1.42379484493389));
#35760=CARTESIAN_POINT('',(11.,-8.88202841720304,1.45243629670899));
#35761=CARTESIAN_POINT('',(0.5,-8.88202841720304,1.45243629670899));
#35762=CARTESIAN_POINT('',(5.75,-8.88202841720304,1.45243629670899));
#35763=CARTESIAN_POINT('',(11.,-8.71554861415804,1.53678637235234));
#35764=CARTESIAN_POINT('',(11.,-8.93855739141052,1.42379484493389));
#35765=CARTESIAN_POINT('',(0.5,-8.71554861415804,1.53678637235234));
#35766=CARTESIAN_POINT('',(0.5,-8.71554861415804,1.53678637235234));
#35767=CARTESIAN_POINT('',(0.5,-8.93855739141052,1.42379484493389));
#35768=CARTESIAN_POINT('Origin',(0.5,-8.81402938945926,1.55415119011903));
#35769=CARTESIAN_POINT('',(0.5,-8.84313903162825,1.6729889620954));
#35770=CARTESIAN_POINT('Origin',(0.5,0.,0.));
#35771=CARTESIAN_POINT('',(0.5,-8.71554861415804,1.53678637235234));
#35772=CARTESIAN_POINT('Origin',(0.5,-8.71554861415804,1.53678637235234));
#35773=CARTESIAN_POINT('',(11.,-8.84313903162825,1.6729889620954));
#35774=CARTESIAN_POINT('',(5.75,-8.84313903162825,1.6729889620954));
#35775=CARTESIAN_POINT('',(11.,-8.71554861415804,1.53678637235234));
#35776=CARTESIAN_POINT('Origin',(11.,-8.81402938945926,1.55415119011903));
#35777=CARTESIAN_POINT('Origin',(11.,0.,0.));
#35778=CARTESIAN_POINT('Origin',(0.5,-8.55552123961132,2.95432840397942));
#35779=CARTESIAN_POINT('',(11.,-8.49487753163548,2.97271857438855));
#35780=CARTESIAN_POINT('',(0.5,-8.49487753163548,2.97271857438855));
#35781=CARTESIAN_POINT('',(5.75,-8.49487753163548,2.97271857438855));
#35782=CARTESIAN_POINT('',(11.,-8.31627969395529,3.02687826843217));
#35783=CARTESIAN_POINT('',(11.,-8.55552123961132,2.95432840397942));
#35784=CARTESIAN_POINT('',(0.5,-8.31627969395529,3.02687826843217));
#35785=CARTESIAN_POINT('',(0.5,-8.31627969395529,3.02687826843217));
#35786=CARTESIAN_POINT('',(0.5,-8.55552123961132,2.95432840397942));
#35787=CARTESIAN_POINT('Origin',(0.5,-8.41024895603388,3.06108028276474));
#35788=CARTESIAN_POINT('',(0.5,-8.41828039478761,3.18316747827294));
#35789=CARTESIAN_POINT('Origin',(0.5,0.,0.));
#35790=CARTESIAN_POINT('',(0.5,-8.31627969395529,3.02687826843217));
#35791=CARTESIAN_POINT('Origin',(0.5,-8.31627969395529,3.02687826843217));
#35792=CARTESIAN_POINT('',(11.,-8.41828039478761,3.18316747827294));
#35793=CARTESIAN_POINT('',(5.75,-8.41828039478761,3.18316747827294));
#35794=CARTESIAN_POINT('',(11.,-8.31627969395529,3.02687826843217));
#35795=CARTESIAN_POINT('Origin',(11.,-8.41024895603388,3.06108028276474));
#35796=CARTESIAN_POINT('Origin',(11.,0.,0.));
#35797=CARTESIAN_POINT('Origin',(0.5,-7.91252990424917,4.39509618943233));
#35798=CARTESIAN_POINT('',(11.,-7.84961409088462,4.4026763024535));
#35799=CARTESIAN_POINT('',(0.5,-7.84961409088462,4.4026763024535));
#35800=CARTESIAN_POINT('',(5.75,-7.84961409088462,4.4026763024535));
#35801=CARTESIAN_POINT('',(11.,-7.66432482349228,4.425));
#35802=CARTESIAN_POINT('',(11.,-7.91252990424917,4.39509618943233));
#35803=CARTESIAN_POINT('',(0.5,-7.66432482349228,4.425));
#35804=CARTESIAN_POINT('',(0.5,-7.66432482349228,4.425));
#35805=CARTESIAN_POINT('',(0.5,-7.91252990424917,4.39509618943233));
#35806=CARTESIAN_POINT('Origin',(0.5,-7.75092736387073,4.475));
#35807=CARTESIAN_POINT('',(0.5,-7.73763656800678,4.59662706138363));
#35808=CARTESIAN_POINT('Origin',(0.5,0.,0.));
#35809=CARTESIAN_POINT('',(0.5,-7.66432482349228,4.425));
#35810=CARTESIAN_POINT('Origin',(0.5,-7.66432482349228,4.425));
#35811=CARTESIAN_POINT('',(11.,-7.73763656800678,4.59662706138363));
#35812=CARTESIAN_POINT('',(5.75,-7.73763656800678,4.59662706138363));
#35813=CARTESIAN_POINT('',(11.,-7.66432482349228,4.425));
#35814=CARTESIAN_POINT('Origin',(11.,-7.75092736387073,4.475));
#35815=CARTESIAN_POINT('Origin',(11.,0.,0.));
#35816=CARTESIAN_POINT('Origin',(0.5,-7.02912035167973,5.70232120119534));
#35817=CARTESIAN_POINT('',(11.,-6.96584409807862,5.6988609389301));
#35818=CARTESIAN_POINT('',(0.5,-6.96584409807862,5.6988609389301));
#35819=CARTESIAN_POINT('',(5.75,-6.96584409807862,5.6988609389301));
#35820=CARTESIAN_POINT('',(11.,-6.77949332160295,5.68867034572587));
#35821=CARTESIAN_POINT('',(11.,-7.02912035167973,5.70232120119534));
#35822=CARTESIAN_POINT('',(0.5,-6.77949332160295,5.68867034572587));
#35823=CARTESIAN_POINT('',(0.5,-6.77949332160295,5.68867034572587));
#35824=CARTESIAN_POINT('',(0.5,-7.02912035167973,5.70232120119534));
#35825=CARTESIAN_POINT('Origin',(0.5,-6.85609776591485,5.75294910669453));
#35826=CARTESIAN_POINT('',(0.5,-6.82188856954009,5.8704204572397));
#35827=CARTESIAN_POINT('Origin',(0.5,0.,0.));
#35828=CARTESIAN_POINT('',(0.5,-6.77949332160295,5.68867034572587));
#35829=CARTESIAN_POINT('Origin',(0.5,-6.77949332160295,5.68867034572587));
#35830=CARTESIAN_POINT('',(11.,-6.82188856954009,5.8704204572397));
#35831=CARTESIAN_POINT('',(5.75,-6.82188856954009,5.8704204572397));
#35832=CARTESIAN_POINT('',(11.,-6.77949332160295,5.68867034572587));
#35833=CARTESIAN_POINT('Origin',(11.,-6.85609776591485,5.75294910669453));
#35834=CARTESIAN_POINT('Origin',(11.,0.,0.));
#35835=CARTESIAN_POINT('Origin',(0.5,-5.93213453413103,6.83628406877377));
#35836=CARTESIAN_POINT('',(11.,-5.8704204572397,6.82188856954009));
#35837=CARTESIAN_POINT('',(0.5,-5.8704204572397,6.82188856954009));
#35838=CARTESIAN_POINT('',(5.75,-5.8704204572397,6.82188856954009));
#35839=CARTESIAN_POINT('',(11.,-5.68867034572587,6.77949332160296));
#35840=CARTESIAN_POINT('',(11.,-5.93213453413103,6.83628406877377));
#35841=CARTESIAN_POINT('',(0.5,-5.68867034572587,6.77949332160296));
#35842=CARTESIAN_POINT('',(0.5,-5.68867034572587,6.77949332160296));
#35843=CARTESIAN_POINT('',(0.5,-5.93213453413103,6.83628406877377));
#35844=CARTESIAN_POINT('Origin',(0.5,-5.75294910669453,6.85609776591485));
#35845=CARTESIAN_POINT('',(0.5,-5.6988609389301,6.96584409807862));
#35846=CARTESIAN_POINT('Origin',(0.5,0.,0.));
#35847=CARTESIAN_POINT('',(0.5,-5.68867034572587,6.77949332160296));
#35848=CARTESIAN_POINT('Origin',(0.5,-5.68867034572587,6.77949332160296));
#35849=CARTESIAN_POINT('',(11.,-5.6988609389301,6.96584409807862));
#35850=CARTESIAN_POINT('',(5.75,-5.6988609389301,6.96584409807862));
#35851=CARTESIAN_POINT('',(11.,-5.68867034572587,6.77949332160296));
#35852=CARTESIAN_POINT('Origin',(11.,-5.75294910669453,6.85609776591485));
#35853=CARTESIAN_POINT('Origin',(11.,0.,0.));
#35854=CARTESIAN_POINT('Origin',(0.5,-4.65490381056766,7.76252990424917));
#35855=CARTESIAN_POINT('',(11.,-4.59662706138362,7.73763656800678));
#35856=CARTESIAN_POINT('',(0.5,-4.59662706138362,7.73763656800678));
#35857=CARTESIAN_POINT('',(5.75,-4.59662706138362,7.73763656800678));
#35858=CARTESIAN_POINT('',(11.,-4.425,7.66432482349228));
#35859=CARTESIAN_POINT('',(11.,-4.65490381056766,7.76252990424917));
#35860=CARTESIAN_POINT('',(0.5,-4.425,7.66432482349228));
#35861=CARTESIAN_POINT('',(0.5,-4.425,7.66432482349228));
#35862=CARTESIAN_POINT('',(0.5,-4.65490381056766,7.76252990424917));
#35863=CARTESIAN_POINT('Origin',(0.5,-4.475,7.75092736387073));
#35864=CARTESIAN_POINT('',(0.5,-4.4026763024535,7.84961409088462));
#35865=CARTESIAN_POINT('Origin',(0.5,0.,0.));
#35866=CARTESIAN_POINT('',(0.5,-4.425,7.66432482349228));
#35867=CARTESIAN_POINT('Origin',(0.5,-4.425,7.66432482349228));
#35868=CARTESIAN_POINT('',(11.,-4.4026763024535,7.84961409088462));
#35869=CARTESIAN_POINT('',(5.75,-4.4026763024535,7.84961409088462));
#35870=CARTESIAN_POINT('',(11.,-4.425,7.66432482349228));
#35871=CARTESIAN_POINT('Origin',(11.,-4.475,7.75092736387073));
#35872=CARTESIAN_POINT('Origin',(11.,0.,0.));
#35873=CARTESIAN_POINT('Origin',(0.5,-3.23623619021519,8.45291519661362));
#35874=CARTESIAN_POINT('',(11.,-3.18316747827294,8.41828039478761));
#35875=CARTESIAN_POINT('',(0.5,-3.18316747827294,8.41828039478761));
#35876=CARTESIAN_POINT('',(5.75,-3.18316747827294,8.41828039478761));
#35877=CARTESIAN_POINT('',(11.,-3.02687826843217,8.31627969395529));
#35878=CARTESIAN_POINT('',(11.,-3.23623619021519,8.45291519661362));
#35879=CARTESIAN_POINT('',(0.5,-3.02687826843217,8.31627969395529));
#35880=CARTESIAN_POINT('',(0.5,-3.02687826843217,8.31627969395529));
#35881=CARTESIAN_POINT('',(0.5,-3.23623619021519,8.45291519661362));
#35882=CARTESIAN_POINT('Origin',(0.5,-3.06108028276473,8.41024895603388));
#35883=CARTESIAN_POINT('',(0.5,-2.97271857438855,8.49487753163548));
#35884=CARTESIAN_POINT('Origin',(0.5,0.,0.));
#35885=CARTESIAN_POINT('',(0.5,-3.02687826843217,8.31627969395529));
#35886=CARTESIAN_POINT('Origin',(0.5,-3.02687826843217,8.31627969395529));
#35887=CARTESIAN_POINT('',(11.,-2.97271857438855,8.49487753163548));
#35888=CARTESIAN_POINT('',(5.75,-2.97271857438855,8.49487753163548));
#35889=CARTESIAN_POINT('',(11.,-3.02687826843217,8.31627969395529));
#35890=CARTESIAN_POINT('Origin',(11.,-3.06108028276473,8.41024895603388));
#35891=CARTESIAN_POINT('Origin',(11.,0.,0.));
#35892=CARTESIAN_POINT('Origin',(0.5,-1.71923717083755,8.88646293811044));
#35893=CARTESIAN_POINT('',(11.,-1.67298896209539,8.84313903162825));
#35894=CARTESIAN_POINT('',(0.5,-1.67298896209539,8.84313903162825));
#35895=CARTESIAN_POINT('',(5.75,-1.67298896209539,8.84313903162825));
#35896=CARTESIAN_POINT('',(11.,-1.53678637235233,8.71554861415804));
#35897=CARTESIAN_POINT('',(11.,-1.71923717083755,8.88646293811044));
#35898=CARTESIAN_POINT('',(0.5,-1.53678637235233,8.71554861415804));
#35899=CARTESIAN_POINT('',(0.5,-1.53678637235233,8.71554861415804));
#35900=CARTESIAN_POINT('',(0.5,-1.71923717083755,8.88646293811044));
#35901=CARTESIAN_POINT('Origin',(0.5,-1.55415119011903,8.81402938945926));
#35902=CARTESIAN_POINT('',(0.5,-1.45243629670899,8.88202841720304));
#35903=CARTESIAN_POINT('Origin',(0.5,0.,0.));
#35904=CARTESIAN_POINT('',(0.5,-1.53678637235233,8.71554861415804));
#35905=CARTESIAN_POINT('Origin',(0.5,-1.53678637235233,8.71554861415804));
#35906=CARTESIAN_POINT('',(11.,-1.45243629670899,8.88202841720304));
#35907=CARTESIAN_POINT('',(5.75,-1.45243629670899,8.88202841720304));
#35908=CARTESIAN_POINT('',(11.,-1.53678637235233,8.71554861415804));
#35909=CARTESIAN_POINT('Origin',(11.,-1.55415119011903,8.81402938945926));
#35910=CARTESIAN_POINT('Origin',(11.,0.,0.));
#35911=CARTESIAN_POINT('Origin',(0.5,-0.149999999999999,9.05));
#35912=CARTESIAN_POINT('',(11.,-0.111977522877842,8.99930336383712));
#35913=CARTESIAN_POINT('',(0.5,-0.111977522877842,8.99930336383712));
#35914=CARTESIAN_POINT('',(5.75,-0.111977522877842,8.99930336383712));
#35915=CARTESIAN_POINT('',(11.,5.41906208622704E-16,8.85));
#35916=CARTESIAN_POINT('',(11.,-0.149999999999999,9.05));
#35917=CARTESIAN_POINT('',(0.5,5.41906208622704E-16,8.85));
#35918=CARTESIAN_POINT('',(0.5,5.41906208622704E-16,8.85));
#35919=CARTESIAN_POINT('',(0.5,-0.149999999999999,9.05));
#35920=CARTESIAN_POINT('Origin',(0.5,5.48029442618441E-16,8.95));
#35921=CARTESIAN_POINT('',(0.5,0.111977522877842,8.99930336383712));
#35922=CARTESIAN_POINT('Origin',(0.5,0.,0.));
#35923=CARTESIAN_POINT('',(0.5,5.41906208622704E-16,8.85));
#35924=CARTESIAN_POINT('Origin',(0.5,5.41906208622704E-16,8.85));
#35925=CARTESIAN_POINT('',(11.,0.111977522877842,8.99930336383712));
#35926=CARTESIAN_POINT('',(5.75,0.111977522877842,8.99930336383712));
#35927=CARTESIAN_POINT('',(11.,5.41906208622704E-16,8.85));
#35928=CARTESIAN_POINT('Origin',(11.,5.48029442618441E-16,8.95));
#35929=CARTESIAN_POINT('Origin',(11.,0.,0.));
#35930=CARTESIAN_POINT('Origin',(0.5,1.42379484493389,8.93855739141052));
#35931=CARTESIAN_POINT('',(11.,1.45243629670899,8.88202841720304));
#35932=CARTESIAN_POINT('',(0.500000000000002,1.45243629670899,8.88202841720304));
#35933=CARTESIAN_POINT('',(5.75,1.45243629670899,8.88202841720304));
#35934=CARTESIAN_POINT('',(11.,1.53678637235233,8.71554861415804));
#35935=CARTESIAN_POINT('',(11.,1.42379484493389,8.93855739141052));
#35936=CARTESIAN_POINT('',(0.5,1.53678637235233,8.71554861415804));
#35937=CARTESIAN_POINT('',(0.5,1.53678637235233,8.71554861415804));
#35938=CARTESIAN_POINT('',(0.5,1.42379484493389,8.93855739141052));
#35939=CARTESIAN_POINT('Origin',(0.5,1.55415119011903,8.81402938945926));
#35940=CARTESIAN_POINT('',(0.5,1.67298896209539,8.84313903162825));
#35941=CARTESIAN_POINT('Origin',(0.5,0.,0.));
#35942=CARTESIAN_POINT('',(0.5,1.53678637235233,8.71554861415804));
#35943=CARTESIAN_POINT('Origin',(0.5,1.53678637235233,8.71554861415804));
#35944=CARTESIAN_POINT('',(11.,1.67298896209539,8.84313903162825));
#35945=CARTESIAN_POINT('',(5.75,1.67298896209539,8.84313903162825));
#35946=CARTESIAN_POINT('',(11.,1.53678637235233,8.71554861415804));
#35947=CARTESIAN_POINT('Origin',(11.,1.55415119011903,8.81402938945926));
#35948=CARTESIAN_POINT('Origin',(11.,0.,0.));
#35949=CARTESIAN_POINT('Origin',(0.5,2.95432840397942,8.55552123961132));
#35950=CARTESIAN_POINT('',(11.,2.97271857438855,8.49487753163548));
#35951=CARTESIAN_POINT('',(0.5,2.97271857438855,8.49487753163548));
#35952=CARTESIAN_POINT('',(5.75,2.97271857438855,8.49487753163548));
#35953=CARTESIAN_POINT('',(11.,3.02687826843217,8.31627969395529));
#35954=CARTESIAN_POINT('',(11.,2.95432840397942,8.55552123961132));
#35955=CARTESIAN_POINT('',(0.5,3.02687826843217,8.31627969395529));
#35956=CARTESIAN_POINT('',(0.5,3.02687826843217,8.31627969395529));
#35957=CARTESIAN_POINT('',(0.5,2.95432840397942,8.55552123961132));
#35958=CARTESIAN_POINT('Origin',(0.5,3.06108028276474,8.41024895603388));
#35959=CARTESIAN_POINT('',(0.5,3.18316747827294,8.41828039478761));
#35960=CARTESIAN_POINT('Origin',(0.5,0.,0.));
#35961=CARTESIAN_POINT('',(0.5,3.02687826843217,8.31627969395529));
#35962=CARTESIAN_POINT('Origin',(0.5,3.02687826843217,8.31627969395529));
#35963=CARTESIAN_POINT('',(11.,3.18316747827294,8.41828039478761));
#35964=CARTESIAN_POINT('',(5.75,3.18316747827294,8.41828039478761));
#35965=CARTESIAN_POINT('',(11.,3.02687826843217,8.31627969395529));
#35966=CARTESIAN_POINT('Origin',(11.,3.06108028276474,8.41024895603388));
#35967=CARTESIAN_POINT('Origin',(11.,0.,0.));
#35968=CARTESIAN_POINT('Origin',(0.5,4.39509618943234,7.91252990424917));
#35969=CARTESIAN_POINT('',(11.,4.4026763024535,7.84961409088462));
#35970=CARTESIAN_POINT('',(0.5,4.4026763024535,7.84961409088462));
#35971=CARTESIAN_POINT('',(5.75,4.4026763024535,7.84961409088462));
#35972=CARTESIAN_POINT('',(11.,4.425,7.66432482349228));
#35973=CARTESIAN_POINT('',(11.,4.39509618943234,7.91252990424917));
#35974=CARTESIAN_POINT('',(0.5,4.425,7.66432482349228));
#35975=CARTESIAN_POINT('',(0.5,4.425,7.66432482349228));
#35976=CARTESIAN_POINT('',(0.5,4.39509618943234,7.91252990424917));
#35977=CARTESIAN_POINT('Origin',(0.5,4.475,7.75092736387073));
#35978=CARTESIAN_POINT('',(0.5,4.59662706138363,7.73763656800678));
#35979=CARTESIAN_POINT('Origin',(0.5,0.,0.));
#35980=CARTESIAN_POINT('',(0.5,4.425,7.66432482349228));
#35981=CARTESIAN_POINT('Origin',(0.5,4.425,7.66432482349228));
#35982=CARTESIAN_POINT('',(11.,4.59662706138363,7.73763656800678));
#35983=CARTESIAN_POINT('',(5.75,4.59662706138363,7.73763656800678));
#35984=CARTESIAN_POINT('',(11.,4.425,7.66432482349228));
#35985=CARTESIAN_POINT('Origin',(11.,4.475,7.75092736387073));
#35986=CARTESIAN_POINT('Origin',(11.,0.,0.));
#35987=CARTESIAN_POINT('Origin',(0.5,5.70232120119534,7.02912035167973));
#35988=CARTESIAN_POINT('',(11.,5.6988609389301,6.96584409807862));
#35989=CARTESIAN_POINT('',(0.5,5.6988609389301,6.96584409807862));
#35990=CARTESIAN_POINT('',(5.75,5.6988609389301,6.96584409807862));
#35991=CARTESIAN_POINT('',(11.,5.68867034572587,6.77949332160296));
#35992=CARTESIAN_POINT('',(11.,5.70232120119534,7.02912035167973));
#35993=CARTESIAN_POINT('',(0.5,5.68867034572587,6.77949332160296));
#35994=CARTESIAN_POINT('',(0.5,5.68867034572587,6.77949332160296));
#35995=CARTESIAN_POINT('',(0.5,5.70232120119534,7.02912035167973));
#35996=CARTESIAN_POINT('Origin',(0.5,5.75294910669453,6.85609776591485));
#35997=CARTESIAN_POINT('',(0.5,5.8704204572397,6.82188856954009));
#35998=CARTESIAN_POINT('Origin',(0.5,0.,0.));
#35999=CARTESIAN_POINT('',(0.5,5.68867034572587,6.77949332160296));
#36000=CARTESIAN_POINT('Origin',(0.5,5.68867034572587,6.77949332160296));
#36001=CARTESIAN_POINT('',(11.,5.8704204572397,6.82188856954009));
#36002=CARTESIAN_POINT('',(5.75,5.8704204572397,6.82188856954009));
#36003=CARTESIAN_POINT('',(11.,5.68867034572587,6.77949332160296));
#36004=CARTESIAN_POINT('Origin',(11.,5.75294910669453,6.85609776591485));
#36005=CARTESIAN_POINT('Origin',(11.,0.,0.));
#36006=CARTESIAN_POINT('Origin',(0.5,6.83628406877377,5.93213453413103));
#36007=CARTESIAN_POINT('',(11.,6.82188856954009,5.8704204572397));
#36008=CARTESIAN_POINT('',(0.500000000000002,6.82188856954009,5.8704204572397));
#36009=CARTESIAN_POINT('',(5.75,6.82188856954009,5.8704204572397));
#36010=CARTESIAN_POINT('',(11.,6.77949332160296,5.68867034572587));
#36011=CARTESIAN_POINT('',(11.,6.83628406877377,5.93213453413103));
#36012=CARTESIAN_POINT('',(0.5,6.77949332160296,5.68867034572587));
#36013=CARTESIAN_POINT('',(0.5,6.77949332160296,5.68867034572587));
#36014=CARTESIAN_POINT('',(0.5,6.83628406877377,5.93213453413103));
#36015=CARTESIAN_POINT('Origin',(0.5,6.85609776591486,5.75294910669453));
#36016=CARTESIAN_POINT('',(0.5,6.96584409807862,5.6988609389301));
#36017=CARTESIAN_POINT('Origin',(0.5,0.,0.));
#36018=CARTESIAN_POINT('',(0.5,6.77949332160296,5.68867034572587));
#36019=CARTESIAN_POINT('Origin',(0.5,6.77949332160296,5.68867034572587));
#36020=CARTESIAN_POINT('',(11.,6.96584409807862,5.6988609389301));
#36021=CARTESIAN_POINT('',(5.75,6.96584409807862,5.6988609389301));
#36022=CARTESIAN_POINT('',(11.,6.77949332160296,5.68867034572587));
#36023=CARTESIAN_POINT('Origin',(11.,6.85609776591486,5.75294910669453));
#36024=CARTESIAN_POINT('Origin',(11.,0.,0.));
#36025=CARTESIAN_POINT('Origin',(0.5,7.76252990424917,4.65490381056767));
#36026=CARTESIAN_POINT('',(11.,7.73763656800678,4.59662706138362));
#36027=CARTESIAN_POINT('',(0.5,7.73763656800678,4.59662706138362));
#36028=CARTESIAN_POINT('',(5.75,7.73763656800678,4.59662706138362));
#36029=CARTESIAN_POINT('',(11.,7.66432482349228,4.425));
#36030=CARTESIAN_POINT('',(11.,7.76252990424917,4.65490381056767));
#36031=CARTESIAN_POINT('',(0.5,7.66432482349228,4.425));
#36032=CARTESIAN_POINT('',(0.5,7.66432482349228,4.425));
#36033=CARTESIAN_POINT('',(0.5,7.76252990424917,4.65490381056767));
#36034=CARTESIAN_POINT('Origin',(0.5,7.75092736387073,4.475));
#36035=CARTESIAN_POINT('',(0.5,7.84961409088462,4.4026763024535));
#36036=CARTESIAN_POINT('Origin',(0.5,0.,0.));
#36037=CARTESIAN_POINT('',(0.5,7.66432482349228,4.425));
#36038=CARTESIAN_POINT('Origin',(0.5,7.66432482349228,4.425));
#36039=CARTESIAN_POINT('',(11.,7.84961409088462,4.4026763024535));
#36040=CARTESIAN_POINT('',(5.75,7.84961409088462,4.4026763024535));
#36041=CARTESIAN_POINT('',(11.,7.66432482349228,4.425));
#36042=CARTESIAN_POINT('Origin',(11.,7.75092736387073,4.475));
#36043=CARTESIAN_POINT('Origin',(11.,0.,0.));
#36044=CARTESIAN_POINT('Origin',(0.5,8.45291519661362,3.23623619021519));
#36045=CARTESIAN_POINT('',(11.,8.41828039478761,3.18316747827294));
#36046=CARTESIAN_POINT('',(0.5,8.41828039478761,3.18316747827294));
#36047=CARTESIAN_POINT('',(5.75,8.41828039478761,3.18316747827294));
#36048=CARTESIAN_POINT('',(11.,8.31627969395529,3.02687826843217));
#36049=CARTESIAN_POINT('',(11.,8.45291519661362,3.23623619021519));
#36050=CARTESIAN_POINT('',(0.5,8.31627969395529,3.02687826843217));
#36051=CARTESIAN_POINT('',(0.5,8.31627969395529,3.02687826843217));
#36052=CARTESIAN_POINT('',(0.5,8.45291519661362,3.23623619021519));
#36053=CARTESIAN_POINT('Origin',(0.5,8.41024895603388,3.06108028276473));
#36054=CARTESIAN_POINT('',(0.5,8.49487753163548,2.97271857438855));
#36055=CARTESIAN_POINT('Origin',(0.5,0.,0.));
#36056=CARTESIAN_POINT('',(0.5,8.31627969395529,3.02687826843217));
#36057=CARTESIAN_POINT('Origin',(0.5,8.31627969395529,3.02687826843217));
#36058=CARTESIAN_POINT('',(11.,8.49487753163548,2.97271857438855));
#36059=CARTESIAN_POINT('',(5.75,8.49487753163548,2.97271857438855));
#36060=CARTESIAN_POINT('',(11.,8.31627969395529,3.02687826843217));
#36061=CARTESIAN_POINT('Origin',(11.,8.41024895603388,3.06108028276473));
#36062=CARTESIAN_POINT('Origin',(11.,0.,0.));
#36063=CARTESIAN_POINT('Origin',(0.5,8.88646293811044,1.71923717083755));
#36064=CARTESIAN_POINT('',(11.,8.84313903162825,1.67298896209539));
#36065=CARTESIAN_POINT('',(0.5,8.84313903162825,1.67298896209539));
#36066=CARTESIAN_POINT('',(5.75,8.84313903162825,1.67298896209539));
#36067=CARTESIAN_POINT('',(11.,8.71554861415804,1.53678637235233));
#36068=CARTESIAN_POINT('',(11.,8.88646293811044,1.71923717083755));
#36069=CARTESIAN_POINT('',(0.5,8.71554861415804,1.53678637235233));
#36070=CARTESIAN_POINT('',(0.5,8.71554861415804,1.53678637235233));
#36071=CARTESIAN_POINT('',(0.5,8.88646293811044,1.71923717083755));
#36072=CARTESIAN_POINT('Origin',(0.5,8.81402938945926,1.55415119011903));
#36073=CARTESIAN_POINT('',(0.5,8.88202841720304,1.45243629670899));
#36074=CARTESIAN_POINT('Origin',(0.5,0.,0.));
#36075=CARTESIAN_POINT('',(0.5,8.71554861415804,1.53678637235233));
#36076=CARTESIAN_POINT('Origin',(0.5,8.71554861415804,1.53678637235233));
#36077=CARTESIAN_POINT('',(11.,8.88202841720304,1.45243629670899));
#36078=CARTESIAN_POINT('',(5.75,8.88202841720304,1.45243629670899));
#36079=CARTESIAN_POINT('',(11.,8.71554861415804,1.53678637235233));
#36080=CARTESIAN_POINT('Origin',(11.,8.81402938945926,1.55415119011903));
#36081=CARTESIAN_POINT('Origin',(11.,0.,0.));
#36082=CARTESIAN_POINT('Origin',(0.5,9.05,0.15));
#36083=CARTESIAN_POINT('',(11.,8.99930336383712,0.111977522877842));
#36084=CARTESIAN_POINT('',(0.5,8.99930336383712,0.111977522877842));
#36085=CARTESIAN_POINT('',(5.75,8.99930336383712,0.111977522877842));
#36086=CARTESIAN_POINT('',(11.,8.85,0.));
#36087=CARTESIAN_POINT('',(11.,9.05,0.15));
#36088=CARTESIAN_POINT('',(0.5,8.85,0.));
#36089=CARTESIAN_POINT('',(0.5,8.85,0.));
#36090=CARTESIAN_POINT('',(0.5,9.05,0.15));
#36091=CARTESIAN_POINT('Origin',(0.5,8.95,0.));
#36092=CARTESIAN_POINT('',(0.5,8.99930336383712,-0.111977522877842));
#36093=CARTESIAN_POINT('Origin',(0.5,0.,0.));
#36094=CARTESIAN_POINT('',(0.5,8.85,0.));
#36095=CARTESIAN_POINT('Origin',(0.5,8.85,0.));
#36096=CARTESIAN_POINT('',(11.,8.99930336383712,-0.111977522877842));
#36097=CARTESIAN_POINT('',(5.75,8.99930336383712,-0.111977522877842));
#36098=CARTESIAN_POINT('',(11.,8.85,0.));
#36099=CARTESIAN_POINT('Origin',(11.,8.95,0.));
#36100=CARTESIAN_POINT('Origin',(11.,0.,0.));
#36101=CARTESIAN_POINT('Origin',(12.,0.,5.77350269189626));
#36102=CARTESIAN_POINT('',(12.,3.53525079574969E-16,5.77350269189626));
#36103=CARTESIAN_POINT('',(12.,5.,2.88675134594813));
#36104=CARTESIAN_POINT('',(12.,1.25,5.05181485540923));
#36105=CARTESIAN_POINT('',(6.,5.55111512312578E-16,5.77350269189626));
#36106=CARTESIAN_POINT('',(12.,3.53525079574969E-16,5.77350269189626));
#36107=CARTESIAN_POINT('',(6.,5.,2.88675134594813));
#36108=CARTESIAN_POINT('',(6.,5.,2.88675134594813));
#36109=CARTESIAN_POINT('',(12.,5.,2.88675134594813));
#36110=CARTESIAN_POINT('Origin',(12.,-5.,2.88675134594813));
#36111=CARTESIAN_POINT('',(12.,-5.,2.88675134594813));
#36112=CARTESIAN_POINT('',(12.,-3.75,3.60843918243516));
#36113=CARTESIAN_POINT('',(6.,-5.,2.88675134594813));
#36114=CARTESIAN_POINT('',(12.,-5.,2.88675134594813));
#36115=CARTESIAN_POINT('',(6.,3.53525079574969E-16,5.77350269189626));
#36116=CARTESIAN_POINT('Origin',(12.,-5.,-2.88675134594813));
#36117=CARTESIAN_POINT('',(12.,-5.,-2.88675134594813));
#36118=CARTESIAN_POINT('',(12.,-5.,-1.44337567297407));
#36119=CARTESIAN_POINT('',(6.,-5.,-2.88675134594813));
#36120=CARTESIAN_POINT('',(12.,-5.,-2.88675134594813));
#36121=CARTESIAN_POINT('',(6.,-5.,2.88675134594813));
#36122=CARTESIAN_POINT('Origin',(12.,-1.11022302462516E-15,-5.77350269189626));
#36123=CARTESIAN_POINT('',(12.,-1.06057523872491E-15,-5.77350269189626));
#36124=CARTESIAN_POINT('',(12.,-1.25,-5.05181485540923));
#36125=CARTESIAN_POINT('',(6.,-1.11022302462516E-15,-5.77350269189626));
#36126=CARTESIAN_POINT('',(12.,-1.06057523872491E-15,-5.77350269189626));
#36127=CARTESIAN_POINT('',(6.,-5.,-2.88675134594813));
#36128=CARTESIAN_POINT('Origin',(12.,5.,-2.88675134594813));
#36129=CARTESIAN_POINT('',(12.,5.,-2.88675134594813));
#36130=CARTESIAN_POINT('',(12.,3.75,-3.60843918243516));
#36131=CARTESIAN_POINT('',(6.,5.,-2.88675134594813));
#36132=CARTESIAN_POINT('',(12.,5.,-2.88675134594813));
#36133=CARTESIAN_POINT('',(6.,-1.06057523872491E-15,-5.77350269189626));
#36134=CARTESIAN_POINT('Origin',(12.,5.,2.88675134594813));
#36135=CARTESIAN_POINT('',(12.,5.,1.44337567297406));
#36136=CARTESIAN_POINT('',(6.,5.,-2.88675134594813));
#36137=CARTESIAN_POINT('Origin',(6.,0.,0.));
#36138=CARTESIAN_POINT('Origin',(-60.,5.5,0.));
#36139=CARTESIAN_POINT('',(-60.,-5.5,-6.73555739531044E-16));
#36140=CARTESIAN_POINT('Origin',(-60.,0.,0.));
#36141=CARTESIAN_POINT('Origin',(-59.75,0.,0.));
#36142=CARTESIAN_POINT('',(-59.75,-5.75,-7.04171909509728E-16));
#36143=CARTESIAN_POINT('Origin',(-29.75,0.,0.));
#36144=CARTESIAN_POINT('Origin',(0.,0.,0.));
#36145=CARTESIAN_POINT('Origin',(0.,9.,0.));
#36146=CARTESIAN_POINT('',(0.,-9.,-1.10218211923262E-15));
#36147=CARTESIAN_POINT('Origin',(0.,0.,0.));
#36148=CARTESIAN_POINT('Origin',(5.75,0.,0.));
#36149=CARTESIAN_POINT('',(11.5,-9.,-1.10218211923262E-15));
#36150=CARTESIAN_POINT('Origin',(11.5,0.,0.));
#36151=CARTESIAN_POINT('',(5.75,-9.,-1.10218211923262E-15));
#36152=CARTESIAN_POINT('',(5.75,-9.,-1.10218211923262E-15));
#36153=CARTESIAN_POINT('Origin',(11.75,0.,0.));
#36154=CARTESIAN_POINT('',(12.,-8.5,-1.04094977927525E-15));
#36155=CARTESIAN_POINT('Origin',(12.,0.,0.));
#36156=CARTESIAN_POINT('',(11.75,-8.75,-1.07156594925393E-15));
#36157=CARTESIAN_POINT('Origin',(12.,0.,0.));
#38488=UNCERTAINTY_MEASURE_WITH_UNIT(LENGTH_MEASURE(0.01),#38508,
'DISTANCE_ACCURACY_VALUE',
'Maximum model space distance between geometric entities at asserted c
onnectivities');
#38490=UNCERTAINTY_MEASURE_WITH_UNIT(LENGTH_MEASURE(0.01),#38508,
'DISTANCE_ACCURACY_VALUE',
'Maximum model space distance between geometric entities at asserted c
onnectivities');
#38505=(
GEOMETRIC_REPRESENTATION_CONTEXT(3)
GLOBAL_UNCERTAINTY_ASSIGNED_CONTEXT((#38488))
GLOBAL_UNIT_ASSIGNED_CONTEXT((#38508,#38510,#38511))
REPRESENTATION_CONTEXT('','3D')
);
#38507=(
GEOMETRIC_REPRESENTATION_CONTEXT(3)
GLOBAL_UNCERTAINTY_ASSIGNED_CONTEXT((#38490))
GLOBAL_UNIT_ASSIGNED_CONTEXT((#38508,#38510,#38511))
REPRESENTATION_CONTEXT('','3D')
);
#38508=(
LENGTH_UNIT()
NAMED_UNIT(*)
SI_UNIT(.MILLI.,.METRE.)
);
#38510=(
NAMED_UNIT(*)
PLANE_ANGLE_UNIT()
SI_UNIT($,.RADIAN.)
);
#38511=(
NAMED_UNIT(*)
SI_UNIT($,.STERADIAN.)
SOLID_ANGLE_UNIT()
);
#38526=SHAPE_DEFINITION_REPRESENTATION(#38542,#38588);
#38542=PRODUCT_DEFINITION_SHAPE('',$,#38605);
#38588=SHAPE_REPRESENTATION('',(#16357),#38505);
#38590=PRODUCT_DEFINITION_CONTEXT('part definition',#38640,'design');
#38605=PRODUCT_DEFINITION('2026-10-26-01-10-57-045',
'14_Cap_Screw_ISO_4762_M12x60',#38621,#38590);
#38621=PRODUCT_DEFINITION_FORMATION('',$,#38656);
#38640=APPLICATION_CONTEXT(
'Core Data for Automotive Mechanical Design Process');
#38641=PRODUCT_CONTEXT('part definition',#38640,'mechanical');
#38656=PRODUCT('2026-10-26-01-10-57-045','14_Cap_Screw_ISO_4762_M12x60',
$,(#38641));
#38721=COLOUR_RGB('Black',0.12,0.14,0.17);
#38722=FILL_AREA_STYLE_COLOUR('',#38721);
#38723=FILL_AREA_STYLE('',(#38722));
#38724=SURFACE_STYLE_FILL_AREA(#38723);
#38725=SURFACE_SIDE_STYLE('',(#38724));
#38726=SURFACE_STYLE_USAGE(.BOTH.,#38725);
#38727=PRESENTATION_STYLE_ASSIGNMENT((#38726));
ENDSEC;
END-ISO-10303-21;
